ISO-10303-21;
HEADER;
FILE_DESCRIPTION (('STEP AP214'),
    '1' );
FILE_NAME ('straight bevel gear_iso_ISO - Straight bevel gear 0.7M 36GT 12PT 20PA 5FW ---36O12H20MD8.0S1.step',
    '2026-10-09T15:17:24',
    ( '' ),
    ( '' ),
    'SwSTEP 2.0',
    'SolidWorks 2026',
    '' );
FILE_SCHEMA (( 'AUTOMOTIVE_DESIGN' ));
ENDSEC;

DATA;
#12=CARTESIAN_POINT ( 'NONE',  ( 2.251152103363648127, -7.636644423939545234, 0.1252683866804877588 ) ) ;
#20=CARTESIAN_POINT ( 'NONE',  ( 2.241509619876138171, 7.511759925807403704, 1.363398699156074922 ) ) ;
#25=CARTESIAN_POINT ( 'NONE',  ( 2.241528039335009215, 3.830846649711605600, -6.603755931420445258 ) ) ;
#28=CARTESIAN_POINT ( 'NONE',  ( 0.2671309869109511070, -12.08782215308010066, -1.966882337881812104 ) ) ;
#31=CARTESIAN_POINT ( 'NONE',  ( 0.2648978790185610999, -6.008231198269058382, 10.67083876753489946 ) ) ;
#33=B_SPLINE_CURVE_WITH_KNOTS ( 'NONE', 3,
 ( #58720, #44686, #34706, #18133, #9434, #8152, #55005, #39719, #13453, #43722, #8473, #64002, #3845, #49070, #3519, #23790 ),
 .UNSPECIFIED., .F., .F.,
 ( 4, 3, 3, 3, 3, 4 ),
 ( 0.000000000000000000, 0.0002999043160757348470, 0.0005998071753050991575, 0.0008997092107374514165, 0.001204458948195627314, 0.001510329163476480975 ),
 .UNSPECIFIED. ) ;
#46=CARTESIAN_POINT ( 'NONE',  ( 2.931247277082686509, 3.034789039497289842, -7.255238984871596131 ) ) ;
#51=CARTESIAN_POINT ( 'NONE',  ( 20.00005080000000035, 0.000000000000000000, 0.000000000000000000 ) ) ;
#53=CARTESIAN_POINT ( 'NONE',  ( 2.990245332647861964, -8.426135047918856813, 0.9653152459622899029 ) ) ;
#61=EDGE_CURVE ( 'NONE', #21447, #54893, #59089, .T. ) ;
#63=CARTESIAN_POINT ( 'NONE',  ( 1.719304012339869514, -10.22720798541492471, 7.581471372739622794 ) ) ;
#69=DIRECTION ( 'NONE',  ( 1.000000000000000000, 0.000000000000000000, 0.000000000000000000 ) ) ;
#75=CARTESIAN_POINT ( 'NONE',  ( 0.2833330754217384673, -3.999965385632516579, -11.58086621621911583 ) ) ;
#81=CARTESIAN_POINT ( 'NONE',  ( 2.305787727787084407, -3.971363876083918498, -6.545285700970570275 ) ) ;
#84=CARTESIAN_POINT ( 'NONE',  ( 3.047904605210419504, -5.772373816836783078, -5.398304302092596707 ) ) ;
#90=DIRECTION ( 'NONE',  ( 0.000000000000000000, 0.000000000000000000, -1.000000000000000000 ) ) ;
#103=CARTESIAN_POINT ( 'NONE',  ( 0.2652384529303130067, -7.922180393770610785, -9.338494547402472534 ) ) ;
#111=B_SPLINE_CURVE_WITH_KNOTS ( 'NONE', 3,
 ( #8141, #22114, #47410, #53377, #22445, #48713, #53707, #37074, #18119, #33412, #57373, #11799, #28412, #13126, #6844, #1847, #63323, #42709, #17792 ),
 .UNSPECIFIED., .F., .F.,
 ( 4, 3, 3, 3, 3, 3, 4 ),
 ( 0.000000000000000000, 2.831840207457774963E-05, 4.217266859783117455E-05, 5.602024318339443094E-05, 6.290810167912943239E-05, 9.120440630890260935E-05, 0.0001153103026480235913 ),
 .UNSPECIFIED. ) ;
#118=CARTESIAN_POINT ( 'NONE',  ( 2.827825597296804272, -9.007857251166447199, -0.5449445831287991204 ) ) ;
#162=CARTESIAN_POINT ( 'NONE',  ( 3.152665057734087117, 7.886634106564184954, -0.9030954876737516956 ) ) ;
#166=ORIENTED_EDGE ( 'NONE', *, *, #2823, .F. ) ;
#177=CARTESIAN_POINT ( 'NONE',  ( 0.6473888112830216146, -12.12394591856680570, 2.472751636945331732 ) ) ;
#183=ORIENTED_EDGE ( 'NONE', *, *, #61876, .T. ) ;
#193=VECTOR ( 'NONE', #7034, 1000.000000000000114 ) ;
#198=CARTESIAN_POINT ( 'NONE',  ( 0.4626703367448636306, 2.416235258140044362, -12.07256244737125961 ) ) ;
#208=CARTESIAN_POINT ( 'NONE',  ( 0.2655924914740778187, -12.05257978623652448, -2.169924872618184786 ) ) ;
#210=CARTESIAN_POINT ( 'NONE',  ( 3.092491956585784241, -7.275786042219372085, 3.124176487320387441 ) ) ;
#213=CARTESIAN_POINT ( 'NONE',  ( 0.2638984909335720941, -12.02508546958698332, 2.322601104020627805 ) ) ;
#216=B_SPLINE_CURVE_WITH_KNOTS ( 'NONE', 3,
 ( #1880, #63683, #38430, #58746, #6877, #27148, #47443, #64026, #15370, #54060, #44980, #50957, #45969, #34971, #50317, #55276, #15032, #5405, #30645 ),
 .UNSPECIFIED., .F., .F.,
 ( 4, 3, 3, 3, 3, 3, 4 ),
 ( 5.818439421673296370E-18, 2.825908398831187513E-05, 4.208813692483793747E-05, 5.591713746943596087E-05, 6.279584083231647704E-05, 9.105792820296370140E-05, 0.0001153131102488875055 ),
 .UNSPECIFIED. ) ;
#220=CARTESIAN_POINT ( 'NONE',  ( 0.2655924914740778742, -12.24627751708824341, 0.04405032194299108445 ) ) ;
#223=B_SPLINE_CURVE_WITH_KNOTS ( 'NONE', 3,
 ( #13246, #39149, #18241, #53499, #54134, #28212, #28523, #8905, #39480, #12909, #43480, #33190, #48831, #38166, #17904, #19206 ),
 .UNSPECIFIED., .F., .F.,
 ( 4, 3, 3, 3, 3, 4 ),
 ( 4.848699518061080308E-19, 0.0002176109881720241597, 0.0004352086762394590945, 0.0006528017811446864237, 0.0007615147961451705421, 0.0009453342004947242697 ),
 .UNSPECIFIED. ) ;
#224=CARTESIAN_POINT ( 'NONE',  ( 2.305787727787083519, 1.164987321564732392, 7.566723232958076473 ) ) ;
#225=ORIENTED_EDGE ( 'NONE', *, *, #59679, .F. ) ;
#227=EDGE_LOOP ( 'NONE', ( #64875, #62526, #21303, #60308, #50623, #6890 ) ) ;
#235=CARTESIAN_POINT ( 'NONE',  ( 0.3610902822527258804, 11.44530431865298681, -4.444884365376487345 ) ) ;
#239=VERTEX_POINT ( 'NONE', #11151 ) ;
#248=ORIENTED_EDGE ( 'NONE', *, *, #64139, .T. ) ;
#257=CARTESIAN_POINT ( 'NONE',  ( 5.536195898058073439, 0.008496323383586253108, 0.0002547682446687139432 ) ) ;
#264=EDGE_CURVE ( 'NONE', #36108, #56656, #5132, .T. ) ;
#268=CARTESIAN_POINT ( 'NONE',  ( 2.259025283528087069, 7.639069972920474072, -0.1366755880739947138 ) ) ;
#277=ORIENTED_EDGE ( 'NONE', *, *, #65294, .F. ) ;
#281=VERTEX_POINT ( 'NONE', #27095 ) ;
#289=FACE_OUTER_BOUND ( 'NONE', #43549, .T. ) ;
#292=CARTESIAN_POINT ( 'NONE',  ( 1.375507693218757543, -12.51366828189661895, 1.606074886185397510 ) ) ;
#295=CARTESIAN_POINT ( 'NONE',  ( 1.937114397841932290, 5.226660192101747704, -11.72279974487458354 ) ) ;
#297=CARTESIAN_POINT ( 'NONE',  ( 2.242418902651940105, 2.704708480794804082, 7.139616612143395713 ) ) ;
#300=ORIENTED_EDGE ( 'NONE', *, *, #9759, .F. ) ;
#303=B_SPLINE_CURVE_WITH_KNOTS ( 'NONE', 3,
 ( #44114, #19168, #39439, #59738, #4206, #61353, #15793, #39778, #54761, #14486, #10485, #24820, #45746, #4874, #9181, #29458 ),
 .UNSPECIFIED., .F., .F.,
 ( 4, 3, 3, 3, 3, 4 ),
 ( 0.000000000000000000, 0.0002176109881720250270, 0.0004352086762394614256, 0.0006528017811446909773, 0.0007615147961451746621, 0.0009453342004947338107 ),
 .UNSPECIFIED. ) ;
#306=CARTESIAN_POINT ( 'NONE',  ( 0.3675815128205912052, -11.62724744438068569, 3.951233083390429446 ) ) ;
#314=CARTESIAN_POINT ( 'NONE',  ( 2.903928887688428162, -8.044738195288756444, 3.491800274468522591 ) ) ;
#315=CARTESIAN_POINT ( 'NONE',  ( 0.3675815128205894289, 9.235491948680119023, -8.093875121225982738 ) ) ;
#323=EDGE_CURVE ( 'NONE', #38878, #54941, #51144, .T. ) ;
#328=CARTESIAN_POINT ( 'NONE',  ( 0.2648978790185584908, 0.1321385342564118659, -12.24533305150758089 ) ) ;
#335=ORIENTED_EDGE ( 'NONE', *, *, #60895, .T. ) ;
#336=CARTESIAN_POINT ( 'NONE',  ( 1.283627346226758892, -12.00363697230095994, -3.783098238613510578 ) ) ;
#343=EDGE_CURVE ( 'NONE', #56731, #58632, #17524, .T. ) ;
#344=CARTESIAN_POINT ( 'NONE',  ( 2.241352910868908754, -7.532448145350516988, 1.243507963608069700 ) ) ;
#346=CARTESIAN_POINT ( 'NONE',  ( 5.514624014163232779, 0.002216125254993209052, -0.003498325728817969996 ) ) ;
#357=CARTESIAN_POINT ( 'NONE',  ( 1.375507693220682448, -10.61839108744987925, -6.813306181536405326 ) ) ;
#366=AXIS2_PLACEMENT_3D ( 'NONE', #23570, #33544, #18606 ) ;
#367=CARTESIAN_POINT ( 'NONE',  ( 2.931247277082682068, 6.988361004535491361, -3.607110715259676859 ) ) ;
#370=ORIENTED_EDGE ( 'NONE', *, *, #43413, .T. ) ;
#378=CARTESIAN_POINT ( 'NONE',  ( 3.152665057734130638, -4.725420687650661478, -6.378477742800524375 ) ) ;
#394=CARTESIAN_POINT ( 'NONE',  ( 2.241449424704146320, 3.870245369721822648, 6.580749518451812108 ) ) ;
#401=VECTOR ( 'NONE', #10763, 1000.000000000000114 ) ;
#404=CARTESIAN_POINT ( 'NONE',  ( 2.903928887688316252, -0.5297564406061211484, -8.753847148606094919 ) ) ;
#407=ORIENTED_EDGE ( 'NONE', *, *, #56725, .T. ) ;
#409=CARTESIAN_POINT ( 'NONE',  ( 2.889800649504073782, 2.030191121417136646, 5.774917447013004690 ) ) ;
#410=( BOUNDED_SURFACE ( )  B_SPLINE_SURFACE ( 3, 1, ( 
 ( #23398, #43669 ),
 ( #12102, #63958 ),
 ( #38699, #23746 ),
 ( #28707, #49020 ) ),
 .UNSPECIFIED., .F., .F., .F. ) 
 B_SPLINE_SURFACE_WITH_KNOTS ( ( 4, 4 ),
 ( 2, 2 ),
 ( 0.000000000000000000, 1.000000000000000000 ),
 ( 0.000000000000000000, 1.000000000000000000 ),
 .UNSPECIFIED. ) 
 GEOMETRIC_REPRESENTATION_ITEM ( )  RATIONAL_B_SPLINE_SURFACE ( (
 ( 1.000000000000000000, 1.000000000000000000),
 ( 0.9942764183789327692, 0.8450855930916585379),
 ( 0.9942764183789327692, 0.8450855930916585379),
 ( 1.000000000000000000, 1.000000000000000000) ) ) 
 REPRESENTATION_ITEM ( '' )  SURFACE ( )  );
#413=CARTESIAN_POINT ( 'NONE',  ( 5.515539859299206427, 0.005618668168217187849, 0.002251761459665550975 ) ) ;
#414=ORIENTED_EDGE ( 'NONE', *, *, #15796, .T. ) ;
#424=CARTESIAN_POINT ( 'NONE',  ( 0.2671309869109501633, -12.24572650704445032, 0.1620273132355259660 ) ) ;
#436=ORIENTED_EDGE ( 'NONE', *, *, #2172, .F. ) ;
#439=CARTESIAN_POINT ( 'NONE',  ( 0.8375941296816026282, 11.81283813871928068, -3.890418817177600186 ) ) ;
#461=CARTESIAN_POINT ( 'NONE',  ( 0.2956976708475502202, -5.936640677855288040, -10.72256944221093811 ) ) ;
#466=CARTESIAN_POINT ( 'NONE',  ( 0.9296196016843265575, -3.871279966919617621, -11.85136013469065475 ) ) ;
#467=CIRCLE ( 'NONE', #37622, 12.73084802173761787 ) ;
#469=CARTESIAN_POINT ( 'NONE',  ( 0.2646305136544072623, 9.465888453932963742, 7.770320294339208900 ) ) ;
#472=CARTESIAN_POINT ( 'NONE',  ( 0.4626703367442831505, 10.51809671647419542, 6.399577980714641789 ) ) ;
#482=ORIENTED_EDGE ( 'NONE', *, *, #61735, .F. ) ;
#483=ORIENTED_EDGE ( 'NONE', *, *, #25990, .F. ) ;
#486=CARTESIAN_POINT ( 'NONE',  ( 2.655192694324243430, 8.589732161578094605, 4.290256727311597906 ) ) ;
#506=CARTESIAN_POINT ( 'NONE',  ( 0.3006302518452033112, -12.03044280705496050, 2.350739146140553792 ) ) ;
#507=EDGE_LOOP ( 'NONE', ( #54481, #11346, #34608, #56245 ) ) ;
#516=CARTESIAN_POINT ( 'NONE',  ( 2.259830038564999644, 7.639319632525575443, 0.1377140217659458543 ) ) ;
#532=EDGE_CURVE ( 'NONE', #49256, #59168, #43953, .T. ) ;
#538=CARTESIAN_POINT ( 'NONE',  ( 0.2653519890518156732, 10.60552241699067544, 6.123091032184181159 ) ) ;
#546=CARTESIAN_POINT ( 'NONE',  ( 1.937114397841932290, -12.80345148322678561, -0.9020203649533019563 ) ) ;
#559=CARTESIAN_POINT ( 'NONE',  ( 3.092491956585621260, -7.581757403488263769, -2.283527081234276057 ) ) ;
#569=LINE ( 'NONE', #20831, #8503 ) ;
#572=CARTESIAN_POINT ( 'NONE',  ( 2.284126774967664364, -5.036818232552930041, 5.756079777200394432 ) ) ;
#576=CARTESIAN_POINT ( 'NONE',  ( 0.2648321136542706178, 11.45826514585342970, 4.321267941897541043 ) ) ;
#591=CARTESIAN_POINT ( 'NONE',  ( 2.941278708680199916, -2.226055275041829429, 5.721889327162144490 ) ) ;
#594=CARTESIAN_POINT ( 'NONE',  ( 2.705197763288548884, -7.714317563576063463, 1.076142490489843784 ) ) ;
#597=( BOUNDED_SURFACE ( )  B_SPLINE_SURFACE ( 3, 1, ( 
 ( #49658, #4097 ),
 ( #23740, #28066 ),
 ( #48364, #8109 ),
 ( #8428, #29046 ) ),
 .UNSPECIFIED., .F., .F., .F. ) 
 B_SPLINE_SURFACE_WITH_KNOTS ( ( 4, 4 ),
 ( 2, 2 ),
 ( 0.000000000000000000, 1.000000000000000000 ),
 ( 0.000000000000000000, 1.000000000000000000 ),
 .UNSPECIFIED. ) 
 GEOMETRIC_REPRESENTATION_ITEM ( )  RATIONAL_B_SPLINE_SURFACE ( (
 ( 1.000000000000000000, 1.000000000000000000),
 ( 0.6933888150995267674, 0.9895912004443193632),
 ( 0.6933888150995267674, 0.9895912004443193632),
 ( 1.000000000000000000, 1.000000000000000000) ) ) 
 REPRESENTATION_ITEM ( '' )  SURFACE ( )  );
#603=CARTESIAN_POINT ( 'NONE',  ( 0.3109076770649076837, -10.73466383006817360, -5.925244271826556108 ) ) ;
#604=DIRECTION ( 'NONE',  ( -0.3865475372811021937, -0.6938894834606081918, 0.6075346789811139070 ) ) ;
#606=CARTESIAN_POINT ( 'NONE',  ( 0.3040950598368152291, 4.428852722102732287, 11.43390362554254480 ) ) ;
#608=ORIENTED_EDGE ( 'NONE', *, *, #47164, .F. ) ;
#613=CARTESIAN_POINT ( 'NONE',  ( 0.2652384770603640751, -12.07140968216695676, 2.061429379240443449 ) ) ;
#614=CARTESIAN_POINT ( 'NONE',  ( 2.251152103363440293, 2.494172441821923325, -7.218942724308278436 ) ) ;
#616=ORIENTED_EDGE ( 'NONE', *, *, #59826, .T. ) ;
#619=CARTESIAN_POINT ( 'NONE',  ( 1.014383007554947813, -1.731118468093999496, 12.37541872618881023 ) ) ;
#627=CARTESIAN_POINT ( 'NONE',  ( 0.2739690278137269508, -0.1830199730326568797, -12.24770428423990687 ) ) ;
#628=CARTESIAN_POINT ( 'NONE',  ( 0.3675815128205894289, -2.391755495700522705, -12.04510820461661780 ) ) ;
#629=CARTESIAN_POINT ( 'NONE',  ( 0.3665391374699472626, -9.237363111276819083, 8.095513416941198415 ) ) ;
#641=CARTESIAN_POINT ( 'NONE',  ( 1.549075743843502551, 9.261503792573927640, 8.652116335900316813 ) ) ;
#645=CARTESIAN_POINT ( 'NONE',  ( 1.198791140422372559, 12.44572864632920606, -1.670544840356793959 ) ) ;
#646=VERTEX_POINT ( 'NONE', #11962 ) ;
#647=CARTESIAN_POINT ( 'NONE',  ( 2.835339799623989965, -2.367573116406924694, -7.466040501142053643 ) ) ;
#655=CARTESIAN_POINT ( 'NONE',  ( 3.152665057735747567, 7.886634106564638813, 0.9030954876722160352 ) ) ;
#657=CARTESIAN_POINT ( 'NONE',  ( 2.524535260912605938, 2.850096701925833642, 7.184101064217893295 ) ) ;
#668=CARTESIAN_POINT ( 'NONE',  ( 0.9296196016816554719, 11.56707937094474126, 4.652334946094312862 ) ) ;
#670=CARTESIAN_POINT ( 'NONE',  ( 2.889800649504073782, 3.118861721612639748, -5.267262008933637496 ) ) ;
#671=CARTESIAN_POINT ( 'NONE',  ( 0.3665391374699467075, 5.911453292029604789, 10.76665847464314929 ) ) ;
#683=FACE_OUTER_BOUND ( 'NONE', #43289, .T. ) ;
#684=CARTESIAN_POINT ( 'NONE',  ( 1.634816307076842001, -10.62369813897163873, -6.964001572439102894 ) ) ;
#685=EDGE_CURVE ( 'NONE', #60037, #21790, #40763, .T. ) ;
#688=ORIENTED_EDGE ( 'NONE', *, *, #39482, .T. ) ;
#691=CARTESIAN_POINT ( 'NONE',  ( 2.440552418640496768, 6.024135401262435963, -4.797131306497506742 ) ) ;
#705=CARTESIAN_POINT ( 'NONE',  ( 5.520433897694421610, -0.01120198501134828974, -0.01006947824912434765 ) ) ;
#706=CARTESIAN_POINT ( 'NONE',  ( 5.520433897694421610, -0.01278034823631958410, -0.007971295965052542856 ) ) ;
#712=ORIENTED_EDGE ( 'NONE', *, *, #9742, .T. ) ;
#726=CARTESIAN_POINT ( 'NONE',  ( 2.256373768223944420, 4.807932997207285730, -5.936694589811832401 ) ) ;
#735=DIRECTION ( 'NONE',  ( -0.3939253465568944290, 0.1691689424289765653, 0.9034404741085558799 ) ) ;
#736=CARTESIAN_POINT ( 'NONE',  ( 2.244591118396558560, 3.910457279126710262, 6.558116599718180062 ) ) ;
#738=CARTESIAN_POINT ( 'NONE',  ( 3.152665057735260845, 4.377619405893435456, 6.622010822086191517 ) ) ;
#739=CARTESIAN_POINT ( 'NONE',  ( 2.241352910868908310, -7.503490710578242684, 1.407733736974842165 ) ) ;
#740=CARTESIAN_POINT ( 'NONE',  ( 1.719304012341582588, 7.017415949614099979, -10.62216384465570762 ) ) ;
#744=CARTESIAN_POINT ( 'NONE',  ( 1.948354844647729012, 11.46941405766174604, 3.407825014328282442 ) ) ;
#747=CARTESIAN_POINT ( 'NONE',  ( 0.2706063244538032264, -4.353289770698299144, 11.44820198696414160 ) ) ;
#750=CARTESIAN_POINT ( 'NONE',  ( 0.6473888112830223918, -12.36914475328378593, 0.3298838684458400006 ) ) ;
#751=CARTESIAN_POINT ( 'NONE',  ( 1.375507693220482608, 12.04466556545283140, -3.754650692912763876 ) ) ;
#755=CARTESIAN_POINT ( 'NONE',  ( 2.251152103361941936, 7.218942724306940839, 2.494172441824263231 ) ) ;
#761=CARTESIAN_POINT ( 'NONE',  ( 2.589278595512600756, 0.2408616556818840848, 7.746633201026948967 ) ) ;
#763=CARTESIAN_POINT ( 'NONE',  ( 2.241352910868908310, -2.689314586382304917, -7.145045428366603169 ) ) ;
#764=ADVANCED_FACE ( 'NONE', ( #2996 ), #41154, .F. ) ;
#766=CARTESIAN_POINT ( 'NONE',  ( 0.3654063281920738593, -4.446369912832434323, -11.44627072062583828 ) ) ;
#771=CARTESIAN_POINT ( 'NONE',  ( 0.3002738374340877536, -5.932527270856326140, -10.72659044316170096 ) ) ;
#778=CARTESIAN_POINT ( 'NONE',  ( 5.514970785353741078, 0.002093325033904021564, 0.004233694591582523939 ) ) ;
#780=CARTESIAN_POINT ( 'NONE',  ( 2.903928887688147054, -5.221047506681327555, 7.046356840276350120 ) ) ;
#782=DIRECTION ( 'NONE',  ( 0.3939253465568944290, -0.3234796780324422083, 0.8603393047164927809 ) ) ;
#784=CARTESIAN_POINT ( 'NONE',  ( 2.256373768223415510, -6.548448293197158598, 3.934258165100049442 ) ) ;
#794=CARTESIAN_POINT ( 'NONE',  ( 0.2638984909335720941, -7.718810690099123129, 9.508791614589169328 ) ) ;
#798=CARTESIAN_POINT ( 'NONE',  ( 1.719304012341585475, 10.62216384465587993, -7.017415949613843296 ) ) ;
#800=CARTESIAN_POINT ( 'NONE',  ( 20.00005080000000035, 5.400000000000000355, -1.000000000000000000 ) ) ;
#801=CARTESIAN_POINT ( 'NONE',  ( 3.152665057734045373, -6.378477742800418682, 4.725420687650736085 ) ) ;
#807=VERTEX_POINT ( 'NONE', #45172 ) ;
#810=CARTESIAN_POINT ( 'NONE',  ( 2.249013661412228249, -7.636012530783591323, -0.1200550008339948543 ) ) ;
#812=FACE_OUTER_BOUND ( 'NONE', #15918, .T. ) ;
#819=CARTESIAN_POINT ( 'NONE',  ( 0.2911222467163545602, 12.02952766044175625, 2.338869407810904910 ) ) ;
#822=B_SPLINE_CURVE_WITH_KNOTS ( 'NONE', 3,
 ( #26185, #46458, #55458, #61745, #16205, #36483, #51792, #31492, #30184, #50487, #32778, #57107, #2578, #36811, #1899, #52456 ),
 .UNSPECIFIED., .F., .F.,
 ( 4, 3, 3, 3, 3, 4 ),
 ( 0.000000000000000000, 0.0002176109881720274394, 0.0004352086762394653287, 0.0006528017811446958562, 0.0007615147961451794326, 0.0009453342004942210915 ),
 .UNSPECIFIED. ) ;
#830=CONICAL_SURFACE ( 'NONE', #22085, 7.938172270156617749, 1.280189991382167047 ) ;
#832=EDGE_CURVE ( 'NONE', #37322, #43331, #35952, .T. ) ;
#838=CARTESIAN_POINT ( 'NONE',  ( 2.266490820343223689, 7.500072841116514510, -1.470039317404083778 ) ) ;
#845=CARTESIAN_POINT ( 'NONE',  ( 1.020182472824350040, 2.608319446515835249, -12.22263240120574146 ) ) ;
#859=CARTESIAN_POINT ( 'NONE',  ( 0.3040950598368144520, -12.25911170648142523, -0.2511348647276926971 ) ) ;
#866=CARTESIAN_POINT ( 'NONE',  ( 2.717984159219664964, -7.415470774237006069, -2.397195612260698994 ) ) ;
#871=LINE ( 'NONE', #42385, #25569 ) ;
#874=CARTESIAN_POINT ( 'NONE',  ( 0.8320506296491582132, 0.3827056590416837434, 12.42924193558400958 ) ) ;
#875=ORIENTED_EDGE ( 'NONE', *, *, #40087, .T. ) ;
#883=CARTESIAN_POINT ( 'NONE',  ( 2.969415267404913017, 1.748187016698500740, 7.680649281077271517 ) ) ;
#892=ORIENTED_EDGE ( 'NONE', *, *, #1040, .T. ) ;
#893=CARTESIAN_POINT ( 'NONE',  ( 2.241317068080787234, -7.204761327832114759, -2.524952427345728445 ) ) ;
#897=CARTESIAN_POINT ( 'NONE',  ( 3.152665057733995191, 6.622010822086684456, 4.377619405892240856 ) ) ;
#904=CARTESIAN_POINT ( 'NONE',  ( 2.253265082352434501, 7.498995607278136966, 1.452519439326484640 ) ) ;
#914=B_SPLINE_CURVE_WITH_KNOTS ( 'NONE', 3,
 ( #2656, #63447, #32211, #32526, #47213, #6961, #22916, #43171, #6312, #52534, #21927, #52836, #26574, #46867, #1970, #1329, #62158, #21605, #7610 ),
 .UNSPECIFIED., .F., .F.,
 ( 4, 3, 3, 3, 3, 3, 4 ),
 ( 1.226634733346699349E-18, 2.831840207458639276E-05, 4.217266859784439504E-05, 5.602024318340332140E-05, 6.290810167913971876E-05, 9.120440630891354624E-05, 0.0001153103026480218702 ),
 .UNSPECIFIED. ) ;
#921=EDGE_CURVE ( 'NONE', #1325, #239, #15234, .T. ) ;
#929=CARTESIAN_POINT ( 'NONE',  ( 2.276198483117283455, 4.795748742147503130, 5.955030244776311932 ) ) ;
#930=CARTESIAN_POINT ( 'NONE',  ( 1.937114397841932290, -5.620553190832896284, -11.53912442307261088 ) ) ;
#932=CARTESIAN_POINT ( 'NONE',  ( 0.2638984909335720941, 9.508791614589194197, 7.718810690099093819 ) ) ;
#933=CARTESIAN_POINT ( 'NONE',  ( 2.241526690369557873, -0.01730530154271369553, -7.634439869182785721 ) ) ;
#934=CARTESIAN_POINT ( 'NONE',  ( 1.372161826076017777, -1.607409531431894134, 12.51237317864369558 ) ) ;
#936=CARTESIAN_POINT ( 'NONE',  ( 2.990245332647524901, 4.676740826319936595, -7.075286609974432039 ) ) ;
#937=CARTESIAN_POINT ( 'NONE',  ( 0.2648321136542694521, 6.245325033825879224, -10.53380804838491791 ) ) ;
#940=CARTESIAN_POINT ( 'NONE',  ( 5.516018279890452902, -0.002527316374434336339, 0.006286471671802434068 ) ) ;
#951=CARTESIAN_POINT ( 'NONE',  ( 5.514624014163232779, -0.001921576324372115032, 0.003668383633201685416 ) ) ;
#956=CARTESIAN_POINT ( 'NONE',  ( 1.719304012338201737, 9.242227816402087015, 8.755325027793320558 ) ) ;
#958=CARTESIAN_POINT ( 'NONE',  ( 0.5572780756287532000, -7.697784780878664357, -9.649189244958765954 ) ) ;
#959=CARTESIAN_POINT ( 'NONE',  ( 1.462291587751621380, 11.25382118863405623, -5.766456054323407798 ) ) ;
#970=ORIENTED_EDGE ( 'NONE', *, *, #59989, .T. ) ;
#981=CARTESIAN_POINT ( 'NONE',  ( 5.515188684475870851, -0.002983184900674883035, 0.004442604682416470725 ) ) ;
#984=CARTESIAN_POINT ( 'NONE',  ( 1.014383007554946481, -11.88680274101309564, -3.853787798429523459 ) ) ;
#989=CARTESIAN_POINT ( 'NONE',  ( 2.781367136451683653, -5.783466416658768594, 5.255136723410106292 ) ) ;
#992=DIRECTION ( 'NONE',  ( 0.000000000000000000, 0.000000000000000000, 1.000000000000000000 ) ) ;
#996=ORIENTED_EDGE ( 'NONE', *, *, #3434, .F. ) ;
#1001=ADVANCED_FACE ( 'NONE', ( #289 ), #9308, .F. ) ;
#1003=CARTESIAN_POINT ( 'NONE',  ( 2.034671305878333225, -5.218565780491386086, -10.44529075079083213 ) ) ;
#1007=ORIENTED_EDGE ( 'NONE', *, *, #42228, .T. ) ;
#1012=CARTESIAN_POINT ( 'NONE',  ( 20.00005080000000035, 0.000000000000000000, 4.000000000000000000 ) ) ;
#1015=EDGE_CURVE ( 'NONE', #35544, #27543, #32852, .T. ) ;
#1026=CARTESIAN_POINT ( 'NONE',  ( 0.2717059086739037066, 12.24704971877459592, -0.1760722388998280097 ) ) ;
#1027=CARTESIAN_POINT ( 'NONE',  ( 5.516018279890452902, -0.004180585980734566158, 0.005331956019561453694 ) ) ;
#1030=CARTESIAN_POINT ( 'NONE',  ( 2.259830038564998311, 0.1377140217660240973, -7.639319632525571002 ) ) ;
#1033=EDGE_CURVE ( 'NONE', #57362, #60006, #14589, .T. ) ;
#1035=CARTESIAN_POINT ( 'NONE',  ( 0.2652384770603646302, 2.061429379240482085, 12.07140968216694610 ) ) ;
#1040=EDGE_CURVE ( 'NONE', #59522, #20687, #26505, .T. ) ;
#1042=B_SPLINE_CURVE_WITH_KNOTS ( 'NONE', 3,
 ( #23940, #43878, #8628, #58879, #19266, #64468, #18938, #3676, #64162, #13293, #33579, #18636, #38895, #54528, #39203, #59496 ),
 .UNSPECIFIED., .F., .F.,
 ( 4, 3, 3, 3, 3, 4 ),
 ( 1.453652989256292427E-15, 0.0002126834539180066941, 0.0004253519300366991030, 0.0006380165497225274117, 0.0007442707582429557286, 0.0009453531351408830897 ),
 .UNSPECIFIED. ) ;
#1057=CARTESIAN_POINT ( 'NONE',  ( 0.2657645697724713152, 12.08564806881063980, -1.977350809428408906 ) ) ;
#1060=CARTESIAN_POINT ( 'NONE',  ( 1.104777566491141227, 7.679758239385275687, -9.895624035729994716 ) ) ;
#1062=EDGE_CURVE ( 'NONE', #33180, #57362, #50334, .T. ) ;
#1069=CARTESIAN_POINT ( 'NONE',  ( 0.2653519789438757992, 4.209148152332916837, 11.50012635727056853 ) ) ;
#1091=EDGE_CURVE ( 'NONE', #33895, #14308, #19679, .T. ) ;
#1092=FACE_OUTER_BOUND ( 'NONE', #61960, .T. ) ;
#1093=ORIENTED_EDGE ( 'NONE', *, *, #44532, .F. ) ;
#1101=CARTESIAN_POINT ( 'NONE',  ( 2.257661810676417691, -5.764872664104550459, 5.013319178751149963 ) ) ;
#1104=B_SPLINE_CURVE_WITH_KNOTS ( 'NONE', 3,
 ( #36509, #936, #65439, #25213, #45834, #40167, #46481 ),
 .UNSPECIFIED., .F., .F.,
 ( 4, 3, 4 ),
 ( 0.000000000000000000, 0.001700533616330591547, 0.005002426799371403193 ),
 .UNSPECIFIED. ) ;
#1110=ORIENTED_EDGE ( 'NONE', *, *, #38666, .T. ) ;
#1114=DIRECTION ( 'NONE',  ( -1.000000000000000000, -0.000000000000000000, -0.000000000000000000 ) ) ;
#1118=CARTESIAN_POINT ( 'NONE',  ( 3.152665057735843490, -3.546019893114926713, 7.102135024646879735 ) ) ;
#1123=DIRECTION ( 'NONE',  ( -1.000000000000000000, -0.000000000000000000, -0.000000000000000000 ) ) ;
#1124=DIRECTION ( 'NONE',  ( -1.000000000000000000, -0.000000000000000000, -0.000000000000000000 ) ) ;
#1127=CARTESIAN_POINT ( 'NONE',  ( 0.6473888112830232799, -0.3298838684457962023, -12.36914475328378060 ) ) ;
#1133=ORIENTED_EDGE ( 'NONE', *, *, #28308, .T. ) ;
#1139=ORIENTED_EDGE ( 'NONE', *, *, #35866, .T. ) ;
#1154=ORIENTED_EDGE ( 'NONE', *, *, #32074, .F. ) ;
#1157=CARTESIAN_POINT ( 'NONE',  ( 0.7400311444011731243, -10.56075429936772103, 6.506979270898144208 ) ) ;
#1158=CARTESIAN_POINT ( 'NONE',  ( 2.241537034860906275, -7.172440248506141813, -2.615577641485596239 ) ) ;
#1171=CARTESIAN_POINT ( 'NONE',  ( 5.515188684475870851, 0.001283816547384723609, -0.005194992164431485628 ) ) ;
#1178=CARTESIAN_POINT ( 'NONE',  ( 1.719304012341412724, 2.961219984259706450, -12.38166659046466300 ) ) ;
#1182=CARTESIAN_POINT ( 'NONE',  ( 3.152665057736233845, -4.725420687649230622, 6.378477742801980988 ) ) ;
#1183=CARTESIAN_POINT ( 'NONE',  ( 2.589278595513890391, 1.107986312493318248, -7.670769623692590855 ) ) ;
#1185=VECTOR ( 'NONE', #16056, 1000.000000000000000 ) ;
#1197=CARTESIAN_POINT ( 'NONE',  ( 1.719304012338199295, 12.64775761152512423, 1.452142814150486183 ) ) ;
#1205=EDGE_CURVE ( 'NONE', #54991, #48474, #10944, .T. ) ;
#1206=CARTESIAN_POINT ( 'NONE',  ( 5.514970785353741078, -0.001326349372336327673, 0.004532877335078707229 ) ) ;
#1207=VERTEX_POINT ( 'NONE', #1182 ) ;
#1209=CARTESIAN_POINT ( 'NONE',  ( 0.3675815128205894289, -9.574637318042015011, 7.689697408877242957 ) ) ;
#1210=FACE_OUTER_BOUND ( 'NONE', #31559, .T. ) ;
#1213=CARTESIAN_POINT ( 'NONE',  ( 0.2648978790185584908, -11.46165506714225479, -4.312320170909353045 ) ) ;
#1218=EDGE_CURVE ( 'NONE', #50940, #29095, #58539, .T. ) ;
#1246=CARTESIAN_POINT ( 'NONE',  ( 2.251139882113959878, 7.499076289418103336, 1.448366094935441550 ) ) ;
#1255=B_SPLINE_CURVE_WITH_KNOTS ( 'NONE', 3,
 ( #54171, #8611, #43196, #19252, #7638, #53852, #59483, #34200, #27923, #33230, #43864, #64455, #39518 ),
 .UNSPECIFIED., .F., .F.,
 ( 4, 3, 3, 3, 4 ),
 ( 2.453269466693398698E-18, 6.607593386745386026E-05, 0.0001321518677373480157, 0.0001982171734706193690, 0.0002642860854759500723 ),
 .UNSPECIFIED. ) ;
#1262=CARTESIAN_POINT ( 'NONE',  ( 1.452237505248555660, -10.65201107290472393, 6.833827325205280800 ) ) ;
#1268=CARTESIAN_POINT ( 'NONE',  ( 2.253265082352446935, 4.810902415501113971, 5.932955906470541052 ) ) ;
#1269=CARTESIAN_POINT ( 'NONE',  ( 2.258463476536644698, 1.460294809171041708, -7.499249607179725885 ) ) ;
#1274=CARTESIAN_POINT ( 'NONE',  ( 1.104777566491146112, -1.703053712365408368, 12.40974092093471448 ) ) ;
#1278=CIRCLE ( 'NONE', #10844, 7.938172270156617749 ) ;
#1281=EDGE_CURVE ( 'NONE', #41836, #46784, #10112, .T. ) ;
#1287=CARTESIAN_POINT ( 'NONE',  ( 3.152665057734040488, 0.000000000000000000, 0.000000000000000000 ) ) ;
#1288=CARTESIAN_POINT ( 'NONE',  ( 0.2646305136544065406, -9.296005949277276414, 7.972778379581520802 ) ) ;
#1300=CARTESIAN_POINT ( 'NONE',  ( 1.020182472820979624, 9.280950437305079959, 8.370187102468841900 ) ) ;
#1301=CARTESIAN_POINT ( 'NONE',  ( 2.907497136248777370, 7.848280798452265117, -0.3592423305246287835 ) ) ;
#1306=CARTESIAN_POINT ( 'NONE',  ( 0.7400311444011726802, -5.892391870929093223, 10.91558650018040844 ) ) ;
#1311=CIRCLE ( 'NONE', #12966, 7.938172270156617749 ) ;
#1312=EDGE_CURVE ( 'NONE', #11089, #62148, #17781, .T. ) ;
#1317=DIRECTION ( 'NONE',  ( -1.000000000000000000, -0.000000000000000000, -0.000000000000000000 ) ) ;
#1318=ORIENTED_EDGE ( 'NONE', *, *, #37285, .F. ) ;
#1324=CARTESIAN_POINT ( 'NONE',  ( 0.5547464869798220954, -11.69908463509554331, -3.933612953276354851 ) ) ;
#1325=VERTEX_POINT ( 'NONE', #7813 ) ;
#1328=CARTESIAN_POINT ( 'NONE',  ( 2.241537034860905386, -7.175668896091115023, 2.606707005150518341 ) ) ;
#1329=CARTESIAN_POINT ( 'NONE',  ( 2.284126774967179863, 5.036818232552660923, -5.756079777200417524 ) ) ;
#1340=CARTESIAN_POINT ( 'NONE',  ( 0.3675815128205912052, 9.574637318042068301, -7.689697408877177232 ) ) ;
#1341=CARTESIAN_POINT ( 'NONE',  ( 0.5572780756290729443, -10.53376864352709674, -6.434474476008335664 ) ) ;
#1351=CARTESIAN_POINT ( 'NONE',  ( 2.931247277082681180, 6.255823895767027132, -4.765826751677371576 ) ) ;
#1352=CARTESIAN_POINT ( 'NONE',  ( 2.177405672431261152, 6.668684901899884387, -8.997150696569983452 ) ) ;
#1359=CARTESIAN_POINT ( 'NONE',  ( 3.152665057734095555, 3.546019893116337141, 7.102135024645864547 ) ) ;
#1361=EDGE_CURVE ( 'NONE', #21752, #26538, #18835, .T. ) ;
#1366=CARTESIAN_POINT ( 'NONE',  ( 0.7446945582524626683, -5.891988114924091136, -10.91757157182818538 ) ) ;
#1375=CARTESIAN_POINT ( 'NONE',  ( 0.7400311444011752338, -7.698344902199155904, 9.726551103566787759 ) ) ;
#1377=CARTESIAN_POINT ( 'NONE',  ( 0.2671309869109468327, -1.966882337881771248, 12.08782215308011843 ) ) ;
#1379=EDGE_CURVE ( 'NONE', #26248, #26251, #21803, .T. ) ;
#1399=CARTESIAN_POINT ( 'NONE',  ( 0.2648978790185593790, 12.08224454301451445, -1.996248716311504801 ) ) ;
#1401=CARTESIAN_POINT ( 'NONE',  ( 1.633930747253263371, 7.601388527387222815, -10.17701904908809141 ) ) ;
#1405=AXIS2_PLACEMENT_3D ( 'NONE', #57150, #41841, #26543 ) ;
#1409=CARTESIAN_POINT ( 'NONE',  ( 1.109979610372474168, 6.674783385105688360, -10.60154531817214085 ) ) ;
#1416=CARTESIAN_POINT ( 'NONE',  ( 3.152665057733930798, -5.761241965769118067, -5.461013642405381674 ) ) ;
#1417=ORIENTED_EDGE ( 'NONE', *, *, #45658, .F. ) ;
#1418=CARTESIAN_POINT ( 'NONE',  ( 2.368238019615325651, 7.273245349264801263, 2.455958560214660746 ) ) ;
#1419=CARTESIAN_POINT ( 'NONE',  ( 1.452237505248555660, 10.06489946308202299, 7.672309600508729233 ) ) ;
#1422=VERTEX_POINT ( 'NONE', #54684 ) ;
#1423=CARTESIAN_POINT ( 'NONE',  ( 2.653899356900081941, -4.109946795501341121, -6.596318473603846044 ) ) ;
#1436=CARTESIAN_POINT ( 'NONE',  ( 0.3109076770649051857, -4.414555973477746420, -11.43910935267336804 ) ) ;
#1455=CARTESIAN_POINT ( 'NONE',  ( 1.549075743843518982, 10.62322497417013878, 6.912427991522386961 ) ) ;
#1456=CARTESIAN_POINT ( 'NONE',  ( 0.5572780756290133253, -9.256402261579143698, -8.165890079445691896 ) ) ;
#1457=CIRCLE ( 'NONE', #52440, 12.73084802173761787 ) ;
#1464=ADVANCED_FACE ( 'NONE', ( #54013 ), #21162, .F. ) ;
#1466=CARTESIAN_POINT ( 'NONE',  ( 2.297017764050093724, -7.133399178907334104, 2.771707546665567623 ) ) ;
#1475=CARTESIAN_POINT ( 'NONE',  ( 0.2650492433740077591, -6.027445608088923379, 10.66007796911767080 ) ) ;
#1486=B_SPLINE_CURVE_WITH_KNOTS ( 'NONE', 3,
 ( #50746, #210, #56740, #61051, #4875, #35747, #46729, #20148, #11164, #10486, #61686, #6183, #65677, #51738, #56043, #40418 ),
 .UNSPECIFIED., .F., .F.,
 ( 4, 3, 3, 3, 3, 4 ),
 ( 2.556437191840625382E-15, 0.0002126834539179719454, 0.0004253519300366298225, 0.0006380165497224222441, 0.0007442707582428313706, 0.0009453531351417650882 ),
 .UNSPECIFIED. ) ;
#1490=CARTESIAN_POINT ( 'NONE',  ( 2.298277635560269871, -7.651596582281746883, -0.1650558796844905085 ) ) ;
#1491=ORIENTED_EDGE ( 'NONE', *, *, #26515, .F. ) ;
#1495=CARTESIAN_POINT ( 'NONE',  ( 0.3654063281920717499, -12.04448018134537612, 2.391195511198612067 ) ) ;
#1499=CARTESIAN_POINT ( 'NONE',  ( 2.507146904658096531, 7.565123178000315640, 1.553587269793084369 ) ) ;
#1506=CARTESIAN_POINT ( 'NONE',  ( 2.665405856346786173, -7.981834391067681445, -5.274989403260977205 ) ) ;
#1519=AXIS2_PLACEMENT_3D ( 'NONE', #11060, #47303, #56621 ) ;
#1523=EDGE_CURVE ( 'NONE', #39184, #59129, #3827, .T. ) ;
#1529=CARTESIAN_POINT ( 'NONE',  ( 2.524535260913002954, 1.123794384998896723, -7.646662375930566746 ) ) ;
#1530=CARTESIAN_POINT ( 'NONE',  ( 2.653899356900512707, -1.606012885791721301, -7.604196386057654244 ) ) ;
#1534=CLOSED_SHELL ( 'NONE', ( #61097, #60293, #55039, #63809, #65692, #36548, #31545, #4048, #46722, #5916, #49794, #18381, #24153, #54881, #39764, #57160, #48204, #14423, #31819, #52918, #23674, #36072, #52484, #33996, #2388, #27711, #30410, #65420, #34631, #9670, #41058, #5324, #39090, #32330, #20790, #31553, #49718, #12763, #5443, #3476, #17652, #11291, #42458, #3290, #53534, #8291, #18824, #18027, #37065, #13983, #7474, #5343, #2011, #60008, #5837, #32345, #41997, #50663, #16888, #6344, #11148, #16828, #63038, #3194, #5981, #42443, #26756, #6094, #41656, #1001, #51727, #37752, #57889, #51260, #27088, #26537, #33506, #14084, #49706, #47692, #9016, #29626, #8784, #27764, #35173, #14851, #19005, #63559, #30435, #55708, #8623, #63017, #48062, #63044, #22083, #26074, #14451, #31023, #42961, #33246, #20326, #40141, #56157, #53157, #9000, #57877, #8318, #24540, #22751, #43204, #24087, #33581, #15983, #12791, #43599, #13639, #2157, #17263, #40787, #25448, #43334, #33495, #16627, #59249, #23082, #63319, #28888, #19325, #51959, #1464, #28257, #4273, #18577, #30908, #63121, #52092, #58110, #34611, #63148, #62236, #20008, #2469, #36392, #23464, #6164, #62123, #37365, #45048, #39120, #29510, #9505, #13049, #46742, #47214, #60429, #12676, #2515, #26231, #6264, #63857, #7817, #10864, #62386, #22559, #14257, #25422, #46622, #60118, #58678, #46459, #56758, #13518, #33462, #18825, #58588, #36167, #49217, #9341, #63347, #52697, #34562, #24565, #12292, #40397, #20582, #5259, #11251, #11162, #27328, #45183, #57079, #48542, #50182, #36994, #52097, #42520, #27918, #34127, #56808, #52127, #33866, #56491, #62991, #12737, #764, #54809, #34581, #1963, #19146, #55464, #21738, #34803, #48240, #25556, #62162, #42914, #50897, #19201, #2666, #51451, #11461, #45211, #36616, #33709, #23761, #29010, #16423, #46858, #60665, #26591, #6379 ) ) ;
#1536=CARTESIAN_POINT ( 'NONE',  ( 1.719304012341585253, 9.242227816401774376, -8.755325027795295867 ) ) ;
#1544=CARTESIAN_POINT ( 'NONE',  ( 0.2651627682582918810, -12.24583720278847210, 0.08809604936501859440 ) ) ;
#1553=CARTESIAN_POINT ( 'NONE',  ( 0.2653141334712548205, -7.837911425448844227, 9.409392642815717522 ) ) ;
#1557=CARTESIAN_POINT ( 'NONE',  ( 0.2676618633000453218, 5.983781707237607606, 10.68562420805844582 ) ) ;
#1558=CARTESIAN_POINT ( 'NONE',  ( 0.2648978790185619880, 11.46165506714233828, -4.312320170909121231 ) ) ;
#1565=CARTESIAN_POINT ( 'NONE',  ( 2.665405856346785285, 1.089747929268691351, 9.505137710817288976 ) ) ;
#1569=( BOUNDED_SURFACE ( )  B_SPLINE_SURFACE ( 3, 1, ( 
 ( #43414, #12496 ),
 ( #32770, #33121 ),
 ( #28148, #53752 ),
 ( #47453, #27812 ) ),
 .UNSPECIFIED., .F., .F., .F. ) 
 B_SPLINE_SURFACE_WITH_KNOTS ( ( 4, 4 ),
 ( 2, 2 ),
 ( 0.000000000000000000, 1.000000000000000000 ),
 ( 0.000000000000000000, 1.000000000000000000 ),
 .UNSPECIFIED. ) 
 GEOMETRIC_REPRESENTATION_ITEM ( )  RATIONAL_B_SPLINE_SURFACE ( (
 ( 1.000000000000000000, 1.000000000000000000),
 ( 0.6933888150995267674, 0.9895912004443193632),
 ( 0.6933888150995267674, 0.9895912004443193632),
 ( 1.000000000000000000, 1.000000000000000000) ) ) 
 REPRESENTATION_ITEM ( '' )  SURFACE ( )  );
#1574=CARTESIAN_POINT ( 'NONE',  ( 2.430348790457260488, 7.544199152379035489, -1.528169972228324625 ) ) ;
#1577=CARTESIAN_POINT ( 'NONE',  ( 2.241528039335008327, 1.341200777944249634, -7.515727438419993689 ) ) ;
#1578=CARTESIAN_POINT ( 'NONE',  ( 5.515188684475870851, -0.005140903460551598213, -0.001485678338381495175 ) ) ;
#1580=CARTESIAN_POINT ( 'NONE',  ( 1.283627346226319244, 12.47820286973601966, 1.641214790178025629 ) ) ;
#1583=CARTESIAN_POINT ( 'NONE',  ( 2.245754705088396808, 7.499730934370272273, 1.435454129948234625 ) ) ;
#1586=CARTESIAN_POINT ( 'NONE',  ( 0.8320506296491603226, 12.42924193558400070, -0.3827056590417270421 ) ) ;
#1592=CARTESIAN_POINT ( 'NONE',  ( 2.255723233588951437, -3.933511348457480405, 6.548644987607549872 ) ) ;
#1593=CARTESIAN_POINT ( 'NONE',  ( 0.2739690278137277835, -10.69833303470760377, -5.965352196073705926 ) ) ;
#1594=CARTESIAN_POINT ( 'NONE',  ( 0.2648978790185584908, -11.46165506714225479, -4.312320170909353045 ) ) ;
#1599=CARTESIAN_POINT ( 'NONE',  ( 5.514624014163232779, -0.003498325728817977369, -0.002216125254993196909 ) ) ;
#1604=CARTESIAN_POINT ( 'NONE',  ( 0.2651627682582914924, -0.08809604936497586469, -12.24583720278847565 ) ) ;
#1607=CARTESIAN_POINT ( 'NONE',  ( 3.100650473569745547, 2.280184661131199775, 7.585586315875747943 ) ) ;
#1609=CARTESIAN_POINT ( 'NONE',  ( 1.194176325881340039, -1.672143286119645245, 12.44396189284383958 ) ) ;
#1619=CARTESIAN_POINT ( 'NONE',  ( 2.903928887688454363, -8.528865300112075332, 2.041797854847293703 ) ) ;
#1624=CARTESIAN_POINT ( 'NONE',  ( 1.937114397841935398, -12.80345148322679982, 0.9020203649531247647 ) ) ;
#1631=CARTESIAN_POINT ( 'NONE',  ( 0.7446945582524635565, -7.698291984229281404, -9.728576129010285456 ) ) ;
#1633=CARTESIAN_POINT ( 'NONE',  ( 0.4626703367451678317, 12.17089897506954799, -1.858541096400990078 ) ) ;
#1634=ORIENTED_EDGE ( 'NONE', *, *, #57808, .T. ) ;
#1638=B_SPLINE_CURVE_WITH_KNOTS ( 'NONE', 3,
 ( #48811, #3262, #32499, #43138, #63417, #43461, #17887, #7925, #63741, #23535, #43809, #64089, #13532, #33812, #54111, #49149, #24840, #19532, #4896, #8888, #39459, #35111 ),
 .UNSPECIFIED., .F., .F.,
 ( 4, 3, 3, 3, 3, 3, 3, 4 ),
 ( 5.421010862427522170E-20, 4.449119708437005534E-05, 6.626296329540603137E-05, 8.803456484962761982E-05, 0.0001098060367612829541, 0.0001315774408628521560, 0.0001760698110411172115, 0.0001829697163287832666 ),
 .UNSPECIFIED. ) ;
#1642=EDGE_CURVE ( 'NONE', #14018, #19254, #4803, .T. ) ;
#1643=CARTESIAN_POINT ( 'NONE',  ( 5.516018279890452902, 0.005752102158674347356, 0.003580555109620895717 ) ) ;
#1649=ORIENTED_EDGE ( 'NONE', *, *, #26145, .F. ) ;
#1653=ORIENTED_EDGE ( 'NONE', *, *, #51338, .T. ) ;
#1655=B_SPLINE_CURVE_WITH_KNOTS ( 'NONE', 3,
 ( #51192, #41178, #5645, #4979, #20251, #35546, #10270, #41505, #647, #10592, #60484, #61460, #20904, #36186, #65464, #40532 ),
 .UNSPECIFIED., .F., .F.,
 ( 4, 3, 3, 3, 3, 4 ),
 ( 0.000000000000000000, 0.0002176109881720252981, 0.0004352086762394648950, 0.0006528017811446961815, 0.0007615147961451798663, 0.0009453342004946652891 ),
 .UNSPECIFIED. ) ;
#1666=EDGE_CURVE ( 'NONE', #31754, #32570, #1716, .T. ) ;
#1672=DIRECTION ( 'NONE',  ( 1.000000000000000000, -0.000000000000000000, -0.000000000000000000 ) ) ;
#1673=CARTESIAN_POINT ( 'NONE',  ( 0.2915757698887273541, -8.040595355212891704, -9.248369946372616113 ) ) ;
#1681=EDGE_CURVE ( 'NONE', #29318, #36377, #56899, .T. ) ;
#1684=CARTESIAN_POINT ( 'NONE',  ( 2.990245332647883725, 8.130497889782956733, -2.413832934171042055 ) ) ;
#1686=CARTESIAN_POINT ( 'NONE',  ( 2.251139882113957658, -6.675617500148627315, 3.710800524304805226 ) ) ;
#1691=CARTESIAN_POINT ( 'NONE',  ( 0.2648978790185610999, -2.256510822326061483, -12.03635331166814382 ) ) ;
#1694=CARTESIAN_POINT ( 'NONE',  ( 0.2647959493198550618, 12.24513905663510549, -0.1469673141001992533 ) ) ;
#1696=CARTESIAN_POINT ( 'NONE',  ( 2.368238019615076961, -0.1797502808084734671, -7.674602282635998307 ) ) ;
#1699=ORIENTED_EDGE ( 'NONE', *, *, #52657, .F. ) ;
#1701=CARTESIAN_POINT ( 'NONE',  ( 0.2638984909335716500, -2.322601104020747265, 12.02508546958696201 ) ) ;
#1704=CARTESIAN_POINT ( 'NONE',  ( 0.3654063281920745809, -1.872466061177166408, 12.13594617907221540 ) ) ;
#1707=ORIENTED_EDGE ( 'NONE', *, *, #343, .F. ) ;
#1711=ORIENTED_EDGE ( 'NONE', *, *, #56369, .F. ) ;
#1716=CIRCLE ( 'NONE', #7019, 12.73084802173761787 ) ;
#1717=CARTESIAN_POINT ( 'NONE',  ( 0.2648978790185619880, 11.46165506714233828, -4.312320170909121231 ) ) ;
#1719=CARTESIAN_POINT ( 'NONE',  ( 2.276198483118644145, 7.130755363255238066, 2.759333101208258476 ) ) ;
#1721=CARTESIAN_POINT ( 'NONE',  ( 0.2676618633000472092, 12.08777609394272368, -1.968216791520369657 ) ) ;
#1729=DIRECTION ( 'NONE',  ( -1.000000000000000000, -0.000000000000000000, -0.000000000000000000 ) ) ;
#1731=CARTESIAN_POINT ( 'NONE',  ( 0.2650492433740070375, 4.291726136518546397, 11.46945725111968706 ) ) ;
#1732=ORIENTED_EDGE ( 'NONE', *, *, #54686, .T. ) ;
#1741=CARTESIAN_POINT ( 'NONE',  ( 0.2647959493198567271, 6.249846955854266639, 10.53111783886892994 ) ) ;
#1745=EDGE_CURVE ( 'NONE', #21179, #58982, #25187, .T. ) ;
#1751=B_SPLINE_CURVE_WITH_KNOTS ( 'NONE', 3,
 ( #23981, #53906, #2734, #8675, #52911, #43248, #23312, #44241, #3382, #58579, #3721, #23652, #33288, #43575, #58921, #33618 ),
 .UNSPECIFIED., .F., .F.,
 ( 4, 3, 3, 3, 3, 4 ),
 ( 9.757819552369539906E-19, 0.0003017745587525238376, 0.0006035491769808721142, 0.0009053241094668146218, 0.001207275924541910319, 0.001510325902536801233 ),
 .UNSPECIFIED. ) ;
#1758=CARTESIAN_POINT ( 'NONE',  ( 0.2706063244538056134, -12.03021891034989466, -2.299194104693211393 ) ) ;
#1760=B_SPLINE_CURVE_WITH_KNOTS ( 'NONE', 3,
 ( #23699, #59589, #48325, #23035, #48636, #3091, #19025, #19359, #43968, #58959, #63909, #49314, #43290, #24326, #39624, #53633, #32983, #13370, #18042, #49617, #53947, #8388 ),
 .UNSPECIFIED., .F., .F.,
 ( 4, 3, 3, 3, 3, 3, 3, 4 ),
 ( 2.201357640472097428E-18, 4.449119708436821897E-05, 6.626296329540375455E-05, 8.803456484962473314E-05, 0.0001098060367612801081, 0.0001315774408628522915, 0.0001760698110411177265, 0.0001829697163287813150 ),
 .UNSPECIFIED. ) ;
#1767=CARTESIAN_POINT ( 'NONE',  ( 0.3160775863651090756, -5.922381034681523104, -10.73821170199162545 ) ) ;
#1768=CARTESIAN_POINT ( 'NONE',  ( 5.514624014163232779, -0.0005510299962886537617, -0.004104370840204212174 ) ) ;
#1772=CARTESIAN_POINT ( 'NONE',  ( 2.889800649504073782, -2.030191121417098898, -5.774917447013018901 ) ) ;
#1776=CARTESIAN_POINT ( 'NONE',  ( 3.152665057736204535, -4.377619405894248139, -6.622010822085805160 ) ) ;
#1777=ORIENTED_EDGE ( 'NONE', *, *, #54236, .F. ) ;
#1780=CARTESIAN_POINT ( 'NONE',  ( 0.3474126878361822324, -5.911350916722116544, 10.75620725594714422 ) ) ;
#1787=CARTESIAN_POINT ( 'NONE',  ( 1.634816307077031849, -11.67158647524064108, -5.013416918609148176 ) ) ;
#1791=CARTESIAN_POINT ( 'NONE',  ( 0.3610902822527190525, -7.689482111308914014, 9.572034936626860002 ) ) ;
#1793=CARTESIAN_POINT ( 'NONE',  ( 5.530133899448235191, -0.01437126147332077469, -0.006998616117864021532 ) ) ;
#1804=CARTESIAN_POINT ( 'NONE',  ( 1.719304012338831678, -5.066286238785654206, 11.67935079956403044 ) ) ;
#1824=ORIENTED_EDGE ( 'NONE', *, *, #38666, .F. ) ;
#1839=CARTESIAN_POINT ( 'NONE',  ( 2.368238019615420242, 1.155661230551846330, -7.589221137922761429 ) ) ;
#1847=CARTESIAN_POINT ( 'NONE',  ( 2.284126774967170093, -4.793997684221434241, -5.959830409747408630 ) ) ;
#1850=CARTESIAN_POINT ( 'NONE',  ( 0.2739690278137246748, 2.307031017960451624, 12.02985305092651735 ) ) ;
#1864=CARTESIAN_POINT ( 'NONE',  ( 0.2956976708475462234, 5.936640677855365311, 10.72256944221088837 ) ) ;
#1874=CARTESIAN_POINT ( 'NONE',  ( 0.3665391374699467075, -9.576575648339071378, 7.691255657244262522 ) ) ;
#1877=ORIENTED_EDGE ( 'NONE', *, *, #58799, .T. ) ;
#1879=CARTESIAN_POINT ( 'NONE',  ( 5.514624014163232779, -0.004104370840204217379, 0.0005510299962886126704 ) ) ;
#1880=CARTESIAN_POINT ( 'NONE',  ( 2.305787727787083519, 5.756228004061526349, -5.047606869482997638 ) ) ;
#1883=CARTESIAN_POINT ( 'NONE',  ( 2.247112776671467138, -7.214825360831402357, -2.501955819907554890 ) ) ;
#1890=CARTESIAN_POINT ( 'NONE',  ( 1.633930747250412319, 12.61425129500095643, 1.494486044210056708 ) ) ;
#1896=VERTEX_POINT ( 'NONE', #31 ) ;
#1899=CARTESIAN_POINT ( 'NONE',  ( 3.100650473569758869, 4.345221797103608452, -6.622643684997338909 ) ) ;
#1902=CARTESIAN_POINT ( 'NONE',  ( 2.969415267404317493, -3.055358878717488569, -7.260393470501798951 ) ) ;
#1903=CARTESIAN_POINT ( 'NONE',  ( 0.2652384770603659625, -11.48486213386623511, -4.250454630553679891 ) ) ;
#1913=CARTESIAN_POINT ( 'NONE',  ( 2.507146904658095199, 2.437115546363220808, 7.328382489803280997 ) ) ;
#1918=B_SPLINE_CURVE_WITH_KNOTS ( 'NONE', 3,
 ( #19464, #51029, #9791, #25101, #30408, #46047, #45370, #60670, #15107, #35386, #55693, #10130, #50705, #5151, #5491, #12086, #2117, #26400, #26090 ),
 .UNSPECIFIED., .F., .F.,
 ( 4, 3, 3, 3, 3, 3, 4 ),
 ( 8.883182750045175563E-18, 4.457896483013979952E-05, 6.639290541541090999E-05, 8.820687556477923707E-05, 0.0001100173248778835882, 0.0001545671401658055700, 0.0001830328308068600405 ),
 .UNSPECIFIED. ) ;
#1924=ORIENTED_EDGE ( 'NONE', *, *, #23729, .F. ) ;
#1934=CARTESIAN_POINT ( 'NONE',  ( 0.2833330754217391889, 1.928200609300473101, 12.09951353627561588 ) ) ;
#1936=EDGE_CURVE ( 'NONE', #29286, #11296, #27408, .T. ) ;
#1938=( BOUNDED_SURFACE ( )  B_SPLINE_SURFACE ( 3, 1, ( 
 ( #40206, #60495 ),
 ( #14927, #20915 ),
 ( #41189, #31237 ),
 ( #51543, #44882 ) ),
 .UNSPECIFIED., .F., .F., .F. ) 
 B_SPLINE_SURFACE_WITH_KNOTS ( ( 4, 4 ),
 ( 2, 2 ),
 ( 0.000000000000000000, 1.000000000000000000 ),
 ( 0.000000000000000000, 1.000000000000000000 ),
 .UNSPECIFIED. ) 
 GEOMETRIC_REPRESENTATION_ITEM ( )  RATIONAL_B_SPLINE_SURFACE ( (
 ( 1.000000000000000000, 1.000000000000000000),
 ( 0.6933888150995267674, 0.9895912004443193632),
 ( 0.6933888150995267674, 0.9895912004443193632),
 ( 1.000000000000000000, 1.000000000000000000) ) ) 
 REPRESENTATION_ITEM ( '' )  SURFACE ( )  );
#1941=CARTESIAN_POINT ( 'NONE',  ( 1.633930747253263149, 3.662223193115260234, -12.16309769563678067 ) ) ;
#1942=CARTESIAN_POINT ( 'NONE',  ( 1.549075743846073827, -7.618376504786843029, -10.12891450359553147 ) ) ;
#1943=CARTESIAN_POINT ( 'NONE',  ( 2.305787727787084407, 7.566723232958072032, 1.164987321564758371 ) ) ;
#1944=LINE ( 'NONE', #33818, #55213 ) ;
#1948=CARTESIAN_POINT ( 'NONE',  ( 1.372161826076364610, -5.789954543171384138, 11.20801830616777472 ) ) ;
#1955=CARTESIAN_POINT ( 'NONE',  ( 0.9232058338315058954, -0.3773051331667114372, -12.46548196349786508 ) ) ;
#1958=CARTESIAN_POINT ( 'NONE',  ( 3.152665057734126197, -1.848755561852092333, 7.719888720907804647 ) ) ;
#1961=FACE_OUTER_BOUND ( 'NONE', #62063, .T. ) ;
#1963=ADVANCED_FACE ( 'NONE', ( #30300 ), #64464, .F. ) ;
#1968=CARTESIAN_POINT ( 'NONE',  ( 2.241506898688420346, -7.160521809579514674, 2.648071636522706829 ) ) ;
#1970=CARTESIAN_POINT ( 'NONE',  ( 2.276198483116805615, 5.031786924855208731, -5.756970692722325644 ) ) ;
#1973=CARTESIAN_POINT ( 'NONE',  ( 5.516018279890452902, -0.006771744149385743039, -0.0002248006052446425063 ) ) ;
#1992=CARTESIAN_POINT ( 'NONE',  ( 2.249013661412227805, 5.926694833810679519, -4.816366775941289369 ) ) ;
#1993=CARTESIAN_POINT ( 'NONE',  ( 2.034671305879536263, 11.19279775165900226, -3.325478336154866099 ) ) ;
#1995=CARTESIAN_POINT ( 'NONE',  ( 2.835339799623984636, -4.778327228934542426, -6.206025468804415191 ) ) ;
#2006=CARTESIAN_POINT ( 'NONE',  ( 0.2655924914740778187, -9.409507842006076928, 7.838010948425017332 ) ) ;
#2011=ADVANCED_FACE ( 'NONE', ( #40934 ), #48387, .F. ) ;
#2013=CARTESIAN_POINT ( 'NONE',  ( 0.3040950598368144520, -2.376091969481297195, 12.02925914197704493 ) ) ;
#2017=CARTESIAN_POINT ( 'NONE',  ( 0.3341166715381319596, -1.881279064087924224, 12.12403120948088642 ) ) ;
#2022=VERTEX_POINT ( 'NONE', #36601 ) ;
#2023=CARTESIAN_POINT ( 'NONE',  ( 3.100650473568240084, 7.907988569971625026, 0.4517506188700623482 ) ) ;
#2028=CARTESIAN_POINT ( 'NONE',  ( 2.245754705088394587, -7.538396044169879850, 1.216173395688216807 ) ) ;
#2035=DIRECTION ( 'NONE',  ( -1.000000000000000000, -0.000000000000000000, -0.000000000000000000 ) ) ;
#2036=ORIENTED_EDGE ( 'NONE', *, *, #6051, .T. ) ;
#2042=CARTESIAN_POINT ( 'NONE',  ( 0.2646305136544065406, 9.296005949277333258, -7.972778379581457742 ) ) ;
#2044=CARTESIAN_POINT ( 'NONE',  ( 0.6511581176972717211, 6.471755598256907049, -10.54760823437315764 ) ) ;
#2046=EDGE_LOOP ( 'NONE', ( #35707, #36113, #6467, #52889 ) ) ;
#2049=ORIENTED_EDGE ( 'NONE', *, *, #24914, .F. ) ;
#2052=CARTESIAN_POINT ( 'NONE',  ( 2.269879328255101303, 6.692746930934405647, 3.692763753157670692 ) ) ;
#2054=CARTESIAN_POINT ( 'NONE',  ( 1.547277799338579118, -12.65564732076265209, 0.6737945300323602282 ) ) ;
#2055=CARTESIAN_POINT ( 'NONE',  ( 0.2834382757448004053, 12.02923522794685240, -2.326926314863185130 ) ) ;
#2068=B_SPLINE_CURVE_WITH_KNOTS ( 'NONE', 3,
 ( #49290, #3745, #24000, #39269, #34286, #24644, #10318, #51245, #15950, #56550, #14967, #30288, #19977, #56199, #25622, #50901 ),
 .UNSPECIFIED., .F., .F.,
 ( 4, 3, 3, 3, 3, 4 ),
 ( 3.074549376240319640E-15, 0.0002126834539179954726, 0.0004253519300366764974, 0.0006380165497224911993, 0.0007442707582429119268, 0.0009453531351411830885 ),
 .UNSPECIFIED. ) ;
#2070=DIRECTION ( 'NONE',  ( 0.000000000000000000, 0.000000000000000000, 1.000000000000000000 ) ) ;
#2077=CARTESIAN_POINT ( 'NONE',  ( 2.247112776671465806, -5.774169979601956548, 4.997244136394455083 ) ) ;
#2078=CARTESIAN_POINT ( 'NONE',  ( 2.373367633546872302, 5.072743978105314966, -5.764146204907413917 ) ) ;
#2094=EDGE_LOOP ( 'NONE', ( #25010, #16187, #63956, #48859 ) ) ;
#2104=CARTESIAN_POINT ( 'NONE',  ( 1.719304012341317467, -0.7661785589597189805, -12.70777170743969009 ) ) ;
#2109=CARTESIAN_POINT ( 'NONE',  ( 2.589278595513877512, -7.746633201027364635, 0.2408616556822583132 ) ) ;
#2110=CARTESIAN_POINT ( 'NONE',  ( 0.2651627682582904932, -12.07509313786331973, -2.039709641845705690 ) ) ;
#2117=CARTESIAN_POINT ( 'NONE',  ( 0.2657645697724712597, 9.477802844074149746, -7.755260067564052839 ) ) ;
#2121=CARTESIAN_POINT ( 'NONE',  ( 0.7400311444011720141, 8.241979373543657061, 9.270387619166349680 ) ) ;
#2122=DIRECTION ( 'NONE',  ( -1.000000000000000000, -0.000000000000000000, -0.000000000000000000 ) ) ;
#2128=CARTESIAN_POINT ( 'NONE',  ( 3.100650473569637189, 7.709402782713580038, 1.818095316078564005 ) ) ;
#2129=ORIENTED_EDGE ( 'NONE', *, *, #32713, .F. ) ;
#2135=DIRECTION ( 'NONE',  ( 0.000000000000000000, 0.000000000000000000, 1.000000000000000000 ) ) ;
#2136=CARTESIAN_POINT ( 'NONE',  ( 5.516018279890452902, -0.003191189039764480428, 0.005976902763918706153 ) ) ;
#2141=( BOUNDED_SURFACE ( )  B_SPLINE_SURFACE ( 3, 1, ( 
 ( #10981, #61837 ),
 ( #15307, #35583 ),
 ( #55877, #20636 ),
 ( #45902, #10309 ) ),
 .UNSPECIFIED., .F., .F., .F. ) 
 B_SPLINE_SURFACE_WITH_KNOTS ( ( 4, 4 ),
 ( 2, 2 ),
 ( 0.000000000000000000, 1.000000000000000000 ),
 ( 0.000000000000000000, 1.000000000000000000 ),
 .UNSPECIFIED. ) 
 GEOMETRIC_REPRESENTATION_ITEM ( )  RATIONAL_B_SPLINE_SURFACE ( (
 ( 1.000000000000000000, 1.000000000000000000),
 ( 0.6933888150995267674, 0.9895912004443193632),
 ( 0.6933888150995267674, 0.9895912004443193632),
 ( 1.000000000000000000, 1.000000000000000000) ) ) 
 REPRESENTATION_ITEM ( '' )  SURFACE ( )  );
#2147=CARTESIAN_POINT ( 'NONE',  ( 0.3278977287071224711, 4.427879319183047890, -11.44003061923226916 ) ) ;
#2150=CONICAL_SURFACE ( 'NONE', #3216, 7.938172270156617749, 1.280189991382167047 ) ;
#2156=CARTESIAN_POINT ( 'NONE',  ( 5.536195898058073439, -0.008071068258923201275, 0.002666509901869582554 ) ) ;
#2157=ADVANCED_FACE ( 'NONE', ( #19171 ), #20787, .F. ) ;
#2165=CARTESIAN_POINT ( 'NONE',  ( 1.452237505248552996, -1.611965288198645929, -12.55261342181977113 ) ) ;
#2166=CARTESIAN_POINT ( 'NONE',  ( 0.2648978790185593790, 9.295532325666449935, 7.972372351883061370 ) ) ;
#2172=EDGE_CURVE ( 'NONE', #43940, #7543, #5285, .T. ) ;
#2174=ORIENTED_EDGE ( 'NONE', *, *, #31651, .F. ) ;
#2182=CARTESIAN_POINT ( 'NONE',  ( 0.2676618633000428238, -9.484212776852388060, 7.748413788583189188 ) ) ;
#2184=CARTESIAN_POINT ( 'NONE',  ( 2.241526690369555652, 7.515450538999852270, -1.342748965918806769 ) ) ;
#2198=CARTESIAN_POINT ( 'NONE',  ( 0.4613984246114896104, -11.46927345719239710, 4.475519447653946159 ) ) ;
#2199=EDGE_CURVE ( 'NONE', #16200, #36996, #52042, .T. ) ;
#2209=CARTESIAN_POINT ( 'NONE',  ( 0.2646305136544072623, 11.55263159009964191, -4.064188116014436858 ) ) ;
#2210=CARTESIAN_POINT ( 'NONE',  ( 0.8320506296491601006, -3.891425424503382580, 11.81055997318802397 ) ) ;
#2214=EDGE_CURVE ( 'NONE', #62530, #44220, #34597, .T. ) ;
#2224=CARTESIAN_POINT ( 'NONE',  ( 2.253265082352434057, 3.929729351083079969, -6.549959928643395379 ) ) ;
#2230=CARTESIAN_POINT ( 'NONE',  ( 0.2652384770603659070, -6.180206054297680218, 10.57229757085620570 ) ) ;
#2244=CARTESIAN_POINT ( 'NONE',  ( 1.194176325881340039, -9.940715479868391213, -7.670099510969166978 ) ) ;
#2247=CARTESIAN_POINT ( 'NONE',  ( 0.3610902822527219946, 12.13436647668549639, 1.873269382026034657 ) ) ;
#2264=EDGE_CURVE ( 'NONE', #48793, #61407, #52467, .T. ) ;
#2268=CARTESIAN_POINT ( 'NONE',  ( 0.2739690278137258961, -11.44648082006009560, 4.360944092821414486 ) ) ;
#2270=ORIENTED_EDGE ( 'NONE', *, *, #57217, .F. ) ;
#2271=CARTESIAN_POINT ( 'NONE',  ( 5.516018279890452902, 0.003580555109620797271, 0.005752102158673854694 ) ) ;
#2275=CARTESIAN_POINT ( 'NONE',  ( 2.507146904658100084, 7.328382489803307642, -2.437115546363147534 ) ) ;
#2276=CARTESIAN_POINT ( 'NONE',  ( 3.152665057736161902, 7.719888720907650992, -1.848755561854025231 ) ) ;
#2277=CARTESIAN_POINT ( 'NONE',  ( 1.283627346226916766, 3.783098238613507913, -12.00363697230100968 ) ) ;
#2279=CARTESIAN_POINT ( 'NONE',  ( 2.305787727787084407, -1.164987321564783684, 7.566723232958066703 ) ) ;
#2289=VECTOR ( 'NONE', #8965, 1000.000000000000114 ) ;
#2298=VERTEX_POINT ( 'NONE', #62659 ) ;
#2300=CARTESIAN_POINT ( 'NONE',  ( 1.719304012338199517, 0.000000000000000000, 0.000000000000000000 ) ) ;
#2314=CIRCLE ( 'NONE', #22459, 6.000000000000000888 ) ;
#2316=EDGE_LOOP ( 'NONE', ( #32470, #31681, #2371, #436 ) ) ;
#2317=CARTESIAN_POINT ( 'NONE',  ( 2.941278708680199916, 1.198640839021388960, -6.021511413163950444 ) ) ;
#2320=CARTESIAN_POINT ( 'NONE',  ( 5.514970785353741078, 0.002619824551223220045, -0.003929719953530077733 ) ) ;
#2322=DIRECTION ( 'NONE',  ( -1.000000000000000000, 0.000000000000000000, -0.000000000000000000 ) ) ;
#2323=CARTESIAN_POINT ( 'NONE',  ( 0.3474126878361875614, -11.61929161290143675, -3.953748424960759067 ) ) ;
#2326=CARTESIAN_POINT ( 'NONE',  ( 2.963017218115622242, -7.259628195185911181, -3.051711603120605520 ) ) ;
#2330=CARTESIAN_POINT ( 'NONE',  ( 0.3654063281920728601, 10.76363796011285068, 5.910280591919091719 ) ) ;
#2331=CARTESIAN_POINT ( 'NONE',  ( 2.268878695253351729, 5.949442550447466616, -4.798796461777989464 ) ) ;
#2337=ORIENTED_EDGE ( 'NONE', *, *, #54609, .F. ) ;
#2339=DIRECTION ( 'NONE',  ( 0.000000000000000000, 0.000000000000000000, 1.000000000000000000 ) ) ;
#2346=( BOUNDED_SURFACE ( )  B_SPLINE_SURFACE ( 3, 1, ( 
 ( #940, #40508 ),
 ( #10571, #10248 ),
 ( #35180, #41828 ),
 ( #60805, #15243 ) ),
 .UNSPECIFIED., .F., .F., .F. ) 
 B_SPLINE_SURFACE_WITH_KNOTS ( ( 4, 4 ),
 ( 2, 2 ),
 ( 0.000000000000000000, 1.000000000000000000 ),
 ( 0.000000000000000000, 1.000000000000000000 ),
 .UNSPECIFIED. ) 
 GEOMETRIC_REPRESENTATION_ITEM ( )  RATIONAL_B_SPLINE_SURFACE ( (
 ( 1.000000000000000000, 1.000000000000000000),
 ( 0.6933888150995267674, 0.9895912004443193632),
 ( 0.6933888150995267674, 0.9895912004443193632),
 ( 1.000000000000000000, 1.000000000000000000) ) ) 
 REPRESENTATION_ITEM ( '' )  SURFACE ( )  );
#2347=ORIENTED_EDGE ( 'NONE', *, *, #1361, .T. ) ;
#2348=FACE_OUTER_BOUND ( 'NONE', #36031, .T. ) ;
#2351=B_SPLINE_CURVE_WITH_KNOTS ( 'NONE', 3,
 ( #16438, #52674, #32031, #11745, #52351, #6790, #27065, #47357, #22063, #42319, #17073, #37352, #23382 ),
 .UNSPECIFIED., .F., .F.,
 ( 4, 3, 3, 3, 4 ),
 ( 2.453269466693398313E-18, 6.607593386745693668E-05, 0.0001321518677373556864, 0.0001982171734706220795, 0.0002642860854759481208 ),
 .UNSPECIFIED. ) ;
#2359=FACE_OUTER_BOUND ( 'NONE', #61775, .T. ) ;
#2369=CARTESIAN_POINT ( 'NONE',  ( 2.249013661412228693, 7.216565855998295476, -2.498855301843012633 ) ) ;
#2371=ORIENTED_EDGE ( 'NONE', *, *, #33515, .F. ) ;
#2377=CARTESIAN_POINT ( 'NONE',  ( 2.260457164927187623, -2.742969430850472179, -7.131443009846826442 ) ) ;
#2378=CARTESIAN_POINT ( 'NONE',  ( 2.298277635560813881, 7.133696409974520591, 2.772101951899156536 ) ) ;
#2382=ORIENTED_EDGE ( 'NONE', *, *, #28629, .F. ) ;
#2386=CARTESIAN_POINT ( 'NONE',  ( 2.298277635560277421, 3.682855706290137032, 6.709004959608384944 ) ) ;
#2388=ADVANCED_FACE ( 'NONE', ( #16794 ), #54608, .T. ) ;
#2391=DIRECTION ( 'NONE',  ( -0.3939253465568943735, -0.6978179301705798032, 0.5982248387291173586 ) ) ;
#2392=CARTESIAN_POINT ( 'NONE',  ( 0.2638984909335716500, -6.295352574289060144, 10.50550771760518209 ) ) ;
#2395=CARTESIAN_POINT ( 'NONE',  ( 3.152665057734040488, 0.000000000000000000, 0.000000000000000000 ) ) ;
#2400=CARTESIAN_POINT ( 'NONE',  ( 2.524535260912720958, 7.335347545455701557, 2.434550409953099681 ) ) ;
#2401=CARTESIAN_POINT ( 'NONE',  ( 0.2801149460245138112, 12.02936836014266220, -2.320387321174041784 ) ) ;
#2414=EDGE_CURVE ( 'NONE', #8430, #7261, #43305, .T. ) ;
#2415=CARTESIAN_POINT ( 'NONE',  ( 2.350038591457886294, 10.55267716396152444, -1.210550722321003692 ) ) ;
#2434=CARTESIAN_POINT ( 'NONE',  ( 0.3002738374340838678, -12.25576345519757915, -0.2255758963752761692 ) ) ;
#2457=CARTESIAN_POINT ( 'NONE',  ( 2.491965175174684521, -7.715025372671061810, 0.2120508241299217667 ) ) ;
#2463=EDGE_CURVE ( 'NONE', #11727, #14210, #30140, .T. ) ;
#2465=CARTESIAN_POINT ( 'NONE',  ( 2.034671305879986125, 3.325478336154549019, 11.19279775165752788 ) ) ;
#2468=CARTESIAN_POINT ( 'NONE',  ( 0.2767916011545403787, -4.010899340181499184, 11.57477803659171478 ) ) ;
#2469=ADVANCED_FACE ( 'NONE', ( #65045 ), #16121, .F. ) ;
#2474=ORIENTED_EDGE ( 'NONE', *, *, #20938, .T. ) ;
#2476=CARTESIAN_POINT ( 'NONE',  ( 0.2759803524722195811, 12.02930579076649664, 2.313459762622579685 ) ) ;
#2498=VECTOR ( 'NONE', #5951, 1000.000000000000000 ) ;
#2500=CARTESIAN_POINT ( 'NONE',  ( 2.273267844204871047, -4.797225296800578853, 5.952585402747290644 ) ) ;
#2508=CARTESIAN_POINT ( 'NONE',  ( 0.2648978790185593790, -0.1321385342563263510, 12.24533305150758089 ) ) ;
#2513=CARTESIAN_POINT ( 'NONE',  ( 2.907497136251165237, -1.716624290781506135, -7.666666002096779842 ) ) ;
#2515=ADVANCED_FACE ( 'NONE', ( #41405 ), #23720, .F. ) ;
#2522=CARTESIAN_POINT ( 'NONE',  ( 2.305787727787083519, 1.164987321564732392, 7.566723232958076473 ) ) ;
#2537=CARTESIAN_POINT ( 'NONE',  ( 2.244591118396556340, -7.537402265771627086, -1.219892024449326762 ) ) ;
#2546=VECTOR ( 'NONE', #7137, 1000.000000000000000 ) ;
#2555=ORIENTED_EDGE ( 'NONE', *, *, #39920, .F. ) ;
#2575=DIRECTION ( 'NONE',  ( -1.000000000000000000, -0.000000000000000000, -0.000000000000000000 ) ) ;
#2578=CARTESIAN_POINT ( 'NONE',  ( 2.994568964204218808, 4.283796412555572530, -6.620406464816346315 ) ) ;
#2581=CARTESIAN_POINT ( 'NONE',  ( 2.524535260912187162, -2.850096701925626252, -7.184101064217829347 ) ) ;
#2593=CARTESIAN_POINT ( 'NONE',  ( 2.305787727787084407, 5.047606869483056258, 5.756228004061473946 ) ) ;
#2598=CARTESIAN_POINT ( 'NONE',  ( 0.2653519789438758547, -6.142177718873863768, -10.59450269107740183 ) ) ;
#2600=CARTESIAN_POINT ( 'NONE',  ( 0.2648978790185593790, -10.53870023327859151, -6.237101853238657512 ) ) ;
#2605=CARTESIAN_POINT ( 'NONE',  ( 2.781367136452101541, -3.637318098960572677, 6.916275212954527518 ) ) ;
#2606=DIRECTION ( 'NONE',  ( -0.3939253465568944290, 0.5982248387291196901, 0.6978179301705778048 ) ) ;
#2615=CARTESIAN_POINT ( 'NONE',  ( 1.634816307076110586, -8.702988562439410103, 9.253014110594328656 ) ) ;
#2617=CARTESIAN_POINT ( 'NONE',  ( 0.2833330754217406322, -11.58086621621910517, 3.999965385632548553 ) ) ;
#2618=CIRCLE ( 'NONE', #1519, 7.938172270156617749 ) ;
#2620=ORIENTED_EDGE ( 'NONE', *, *, #53045, .F. ) ;
#2621=CARTESIAN_POINT ( 'NONE',  ( 0.3053067050349203004, 1.901204202464671589, 12.11120005789971188 ) ) ;
#2624=CARTESIAN_POINT ( 'NONE',  ( 2.573738926104376379, 7.355212866432331076, -2.426778239006382343 ) ) ;
#2625=CARTESIAN_POINT ( 'NONE',  ( 2.406456491624914484, 10.14681500356570432, -2.427896847127299029 ) ) ;
#2627=CARTESIAN_POINT ( 'NONE',  ( 2.241537034860907163, -3.821322318518419969, 6.609284473755325351 ) ) ;
#2628=CARTESIAN_POINT ( 'NONE',  ( 2.280717697723836590, 7.556934756535390818, 1.173604464351628573 ) ) ;
#2629=DIRECTION ( 'NONE',  ( 1.000000000000000000, 0.000000000000000000, -0.000000000000000000 ) ) ;
#2634=CARTESIAN_POINT ( 'NONE',  ( 5.514624014163232779, 0.003060352188290547774, -0.002789935220458479061 ) ) ;
#2636=B_SPLINE_CURVE_WITH_KNOTS ( 'NONE', 3,
 ( #47547, #58180, #32879, #58864, #7636, #1992, #22608, #27575, #17288, #52859, #63469, #57867, #2679, #2331, #58517, #42523, #37218, #12281, #12946 ),
 .UNSPECIFIED., .F., .F.,
 ( 4, 3, 3, 3, 3, 3, 4 ),
 ( 0.000000000000000000, 2.831840207499475751E-05, 4.217266859840493434E-05, 5.602024318395896146E-05, 6.290810167969121175E-05, 9.120440630944927764E-05, 0.0001153103026479774721 ),
 .UNSPECIFIED. ) ;
#2645=CARTESIAN_POINT ( 'NONE',  ( 2.835339799623987300, -1.682641786445494336, 7.649567297875986327 ) ) ;
#2652=ORIENTED_EDGE ( 'NONE', *, *, #2214, .F. ) ;
#2653=ORIENTED_EDGE ( 'NONE', *, *, #12034, .T. ) ;
#2656=CARTESIAN_POINT ( 'NONE',  ( 2.241352910868908310, 4.970878533273838329, -5.794346703933798359 ) ) ;
#2658=CARTESIAN_POINT ( 'NONE',  ( 0.3106921474978480702, 8.060345844326409548, -9.239619355094065511 ) ) ;
#2661=CARTESIAN_POINT ( 'NONE',  ( 0.3006302518452008132, 11.59403866275566131, 3.979421585299158348 ) ) ;
#2663=DIRECTION ( 'NONE',  ( -1.000000000000000000, -0.000000000000000000, -0.000000000000000000 ) ) ;
#2666=ADVANCED_FACE ( 'NONE', ( #61694 ), #37287, .F. ) ;
#2668=DIRECTION ( 'NONE',  ( -0.3939253465568943735, 0.8008152550167566552, 0.4511294145502791619 ) ) ;
#2675=B_SPLINE_CURVE_WITH_KNOTS ( 'NONE', 3,
 ( #45573, #51251, #6031, #46900, #56896, #10013, #15326, #15637, #30294, #11320, #35264, #35907, #50591, #25628, #60541, #1359 ),
 .UNSPECIFIED., .F., .F.,
 ( 4, 3, 3, 3, 3, 4 ),
 ( 0.000000000000000000, 0.0002176109881720219913, 0.0004352086762394580103, 0.0006528017811446826290, 0.0007615147961451645790, 0.0009453342004946926110 ),
 .UNSPECIFIED. ) ;
#2679=CARTESIAN_POINT ( 'NONE',  ( 2.262775599886255762, 5.943524836196993455, -4.802882839669003978 ) ) ;
#2682=CARTESIAN_POINT ( 'NONE',  ( 3.152665057734130638, -4.725420687650661478, -6.378477742800524375 ) ) ;
#2685=CARTESIAN_POINT ( 'NONE',  ( 1.459561108994217093, 10.62073135189165285, -6.861308540878105156 ) ) ;
#2688=CARTESIAN_POINT ( 'NONE',  ( 0.2653519789438763543, -2.148225749114911487, -12.05632450344285012 ) ) ;
#2690=B_SPLINE_CURVE_WITH_KNOTS ( 'NONE', 3,
 ( #28970, #54248, #8687, #43938, #50247, #49278, #29599, #45240, #49589, #3393, #19966, #39916, #9643, #60200, #44561, #23663, #4706, #39594, #65497 ),
 .UNSPECIFIED., .F., .F.,
 ( 4, 3, 3, 3, 3, 3, 4 ),
 ( 1.164142361166801473E-17, 4.457896483014695525E-05, 6.639290541541897374E-05, 8.820687556478713819E-05, 0.0001100173248778907168, 0.0001545671401658091479, 0.0001830328308068564897 ),
 .UNSPECIFIED. ) ;
#2695=CARTESIAN_POINT ( 'NONE',  ( 3.092491956585210477, -0.4473002062004609036, -7.905533744258606887 ) ) ;
#2706=DIRECTION ( 'NONE',  ( 0.000000000000000000, 0.000000000000000000, 1.000000000000000000 ) ) ;
#2708=ORIENTED_EDGE ( 'NONE', *, *, #49696, .T. ) ;
#2715=ORIENTED_EDGE ( 'NONE', *, *, #55077, .F. ) ;
#2727=EDGE_LOOP ( 'NONE', ( #27679, #35001, #15455, #28749 ) ) ;
#2731=CARTESIAN_POINT ( 'NONE',  ( 2.305787727787083519, 3.682701754025512919, 6.711944854845837583 ) ) ;
#2734=CARTESIAN_POINT ( 'NONE',  ( 0.5547464869798248710, 11.49049644196208853, -4.506704303875337381 ) ) ;
#2735=CARTESIAN_POINT ( 'NONE',  ( 0.7446945582518830209, -0.3561743995936043627, 12.40088838629986157 ) ) ;
#2738=CARTESIAN_POINT ( 'NONE',  ( 0.5547464869798232057, 10.83828453080465160, 5.905377260991259369 ) ) ;
#2741=CARTESIAN_POINT ( 'NONE',  ( 2.249013661412229137, -2.724484898587339110, 7.134443398813868242 ) ) ;
#2742=CARTESIAN_POINT ( 'NONE',  ( 2.266490820341523715, 6.690312181903024680, 3.694838443753504453 ) ) ;
#2747=CARTESIAN_POINT ( 'NONE',  ( 0.3223008802179221921, 6.343104382804310326, 10.49760329338521458 ) ) ;
#2754=( BOUNDED_SURFACE ( )  B_SPLINE_SURFACE ( 3, 1, ( 
 ( #53795, #1624 ),
 ( #6930, #63103 ),
 ( #27515, #27862 ),
 ( #2271, #53128 ) ),
 .UNSPECIFIED., .F., .F., .F. ) 
 B_SPLINE_SURFACE_WITH_KNOTS ( ( 4, 4 ),
 ( 2, 2 ),
 ( 0.000000000000000000, 1.000000000000000000 ),
 ( 0.000000000000000000, 1.000000000000000000 ),
 .UNSPECIFIED. ) 
 GEOMETRIC_REPRESENTATION_ITEM ( )  RATIONAL_B_SPLINE_SURFACE ( (
 ( 1.000000000000000000, 1.000000000000000000),
 ( 0.6933888150995267674, 0.9895912004443193632),
 ( 0.6933888150995267674, 0.9895912004443193632),
 ( 1.000000000000000000, 1.000000000000000000) ) ) 
 REPRESENTATION_ITEM ( '' )  SURFACE ( )  );
#2756=CARTESIAN_POINT ( 'NONE',  ( 1.719304012341432264, 5.066286238787408358, -11.67935079956426847 ) ) ;
#2763=EDGE_CURVE ( 'NONE', #4753, #63287, #55915, .T. ) ;
#2768=CARTESIAN_POINT ( 'NONE',  ( 5.536195898058073439, 0.007485416011288106679, 0.004027525919832979431 ) ) ;
#2770=CARTESIAN_POINT ( 'NONE',  ( 0.4626703367447424498, -3.943760108616721549, -11.66326339726751016 ) ) ;
#2778=CARTESIAN_POINT ( 'NONE',  ( 1.719304012340734378, -7.017415949613340587, -10.62216384465587282 ) ) ;
#2787=CARTESIAN_POINT ( 'NONE',  ( 2.247112776671468026, -7.135103076758469776, 2.720990995225279985 ) ) ;
#2789=CARTESIAN_POINT ( 'NONE',  ( 2.373367633546871414, 5.764146204907464544, 5.072743978105256346 ) ) ;
#2805=CARTESIAN_POINT ( 'NONE',  ( 0.2834382757448014045, 3.999440312567370537, -11.58108645293227035 ) ) ;
#2809=CARTESIAN_POINT ( 'NONE',  ( 0.3057689695767511484, 9.538231270095108627, 7.702054583838497059 ) ) ;
#2810=DIRECTION ( 'NONE',  ( 0.9486832985018465170, 0.000000000000000000, -0.3162277646628396943 ) ) ;
#2811=CARTESIAN_POINT ( 'NONE',  ( 2.241526690369555652, -5.837196604699884439, 4.920579984890946612 ) ) ;
#2816=EDGE_LOOP ( 'NONE', ( #50574, #6694, #16683, #18126 ) ) ;
#2818=B_SPLINE_CURVE_WITH_KNOTS ( 'NONE', 3,
 ( #64753, #4927, #35147, #39830, #24876, #20200, #29212, #5248, #45807, #14227, #268, #44813, #19226, #10220, #65093, #35493, #60436, #19567, #55790 ),
 .UNSPECIFIED., .F., .F.,
 ( 4, 3, 3, 3, 3, 3, 4 ),
 ( 6.759600587344757484E-18, 2.825908398831393172E-05, 4.208813692484047856E-05, 5.591713746943926768E-05, 6.279584083231935017E-05, 9.105792820296614086E-05, 0.0001153131102488857165 ),
 .UNSPECIFIED. ) ;
#2821=CARTESIAN_POINT ( 'NONE',  ( 0.3675815128205894289, -10.50067073900656212, 6.367184624550128014 ) ) ;
#2822=FACE_OUTER_BOUND ( 'NONE', #45449, .T. ) ;
#2823=EDGE_CURVE ( 'NONE', #15607, #17370, #64856, .T. ) ;
#2824=CARTESIAN_POINT ( 'NONE',  ( 2.241536586108912932, -7.519576125149797896, -1.319514354261274391 ) ) ;
#2829=CARTESIAN_POINT ( 'NONE',  ( 0.2638984909335716500, 2.322601104020825868, -12.02508546958694602 ) ) ;
#2838=CARTESIAN_POINT ( 'NONE',  ( 5.516018279890452902, 0.006629829924290974764, 0.001397286410094337149 ) ) ;
#2840=CARTESIAN_POINT ( 'NONE',  ( 3.152665057733881504, -7.719888720907738922, -1.848755561851823881 ) ) ;
#2847=CARTESIAN_POINT ( 'NONE',  ( 0.000000000000000000, 0.000000000000000000, -6.000000000000000888 ) ) ;
#2851=ORIENTED_EDGE ( 'NONE', *, *, #5754, .T. ) ;
#2860=CARTESIAN_POINT ( 'NONE',  ( 2.242418902651938772, -7.535443599794972691, -1.227462051872218129 ) ) ;
#2863=EDGE_CURVE ( 'NONE', #13659, #64505, #45675, .T. ) ;
#2864=CARTESIAN_POINT ( 'NONE',  ( 0.3002738374340840899, 5.932527270856402524, 10.72659044316165300 ) ) ;
#2878=DIRECTION ( 'NONE',  ( -1.000000000000000000, -0.000000000000000000, -0.000000000000000000 ) ) ;
#2889=CARTESIAN_POINT ( 'NONE',  ( 0.2648978790185593790, -10.53870023327859151, -6.237101853238657512 ) ) ;
#2890=CARTESIAN_POINT ( 'NONE',  ( 0.3675815128205894289, 8.093875121226078662, 9.235491948680033758 ) ) ;
#2899=CARTESIAN_POINT ( 'NONE',  ( 1.634816307075117159, 3.661851000131278511, 12.16351623921463343 ) ) ;
#2906=CARTESIAN_POINT ( 'NONE',  ( 0.2739690278137238422, 7.732471127692722490, -9.499928778897034576 ) ) ;
#2908=CARTESIAN_POINT ( 'NONE',  ( 2.260457164927185847, 1.462935478981605586, 7.499412009325151729 ) ) ;
#2911=CARTESIAN_POINT ( 'NONE',  ( 2.994568964204198824, 2.317954327151229954, 7.537093683963799862 ) ) ;
#2913=CARTESIAN_POINT ( 'NONE',  ( 2.717984159220057538, -1.073093837952399321, 7.719081760284438154 ) ) ;
#2922=CARTESIAN_POINT ( 'NONE',  ( 5.516018279890452902, 0.003191189039764837348, 0.005976902763919047894 ) ) ;
#2928=CARTESIAN_POINT ( 'NONE',  ( 0.3223008802179222476, -11.43958962819736058, 4.423848692584651410 ) ) ;
#2934=CARTESIAN_POINT ( 'NONE',  ( 2.899286259009687061, 7.494390643303807664, -2.348384892629290732 ) ) ;
#2935=CARTESIAN_POINT ( 'NONE',  ( 2.781367136452742805, -4.783057651000458321, 6.179587792204651819 ) ) ;
#2939=EDGE_CURVE ( 'NONE', #44680, #17260, #17042, .T. ) ;
#2940=CARTESIAN_POINT ( 'NONE',  ( 2.266490820343221912, -1.183790889241783439, 7.550546162186916987 ) ) ;
#2941=CARTESIAN_POINT ( 'NONE',  ( 0.2638984909335716500, 7.718810690099061844, 9.508791614589220842 ) ) ;
#2945=SURFACE_STYLE_USAGE ( .BOTH. , #28849 ) ;
#2960=DIRECTION ( 'NONE',  ( -1.000000000000000000, -0.000000000000000000, -0.000000000000000000 ) ) ;
#2964=ORIENTED_EDGE ( 'NONE', *, *, #20451, .T. ) ;
#2966=CARTESIAN_POINT ( 'NONE',  ( 0.2646305136544072623, -6.008537389229345216, -10.67138229758235823 ) ) ;
#2977=CARTESIAN_POINT ( 'NONE',  ( 2.266490820343733947, 3.694838443752039403, -6.690312181904674915 ) ) ;
#2982=CARTESIAN_POINT ( 'NONE',  ( 0.3610902822527282119, -11.62472836966321132, -3.951920836718837649 ) ) ;
#2983=CARTESIAN_POINT ( 'NONE',  ( 0.6511581176955585359, 5.898618881004847658, 10.87850887236043818 ) ) ;
#2986=CARTESIAN_POINT ( 'NONE',  ( 2.835339799623981527, -7.241165502254423458, -2.985412098050572283 ) ) ;
#2987=B_SPLINE_CURVE_WITH_KNOTS ( 'NONE', 3,
 ( #25501, #64739, #49495, #40810, #61087, #15520, #19211, #39485, #59783, #14211, #34498, #32123, #6222, #57410, #1883, #5577, #47446, #893, #62704 ),
 .UNSPECIFIED., .F., .F.,
 ( 4, 3, 3, 3, 3, 3, 4 ),
 ( 5.587587132013241302E-18, 2.825908398831385041E-05, 4.208813692484114264E-05, 5.591713746944058905E-05, 6.279584083231968899E-05, 9.105792820296830926E-05, 0.0001153131102488871938 ),
 .UNSPECIFIED. ) ;
#2990=CARTESIAN_POINT ( 'NONE',  ( 0.3002738374340847005, -0.2255758963752309276, 12.25576345519757204 ) ) ;
#2995=VERTEX_POINT ( 'NONE', #41014 ) ;
#2996=FACE_OUTER_BOUND ( 'NONE', #31978, .T. ) ;
#2998=CARTESIAN_POINT ( 'NONE',  ( 3.152665057734040488, 0.000000000000000000, 0.000000000000000000 ) ) ;
#3004=ORIENTED_EDGE ( 'NONE', *, *, #26985, .F. ) ;
#3014=CARTESIAN_POINT ( 'NONE',  ( 5.514970785353741078, 0.001117786416802556615, 0.004588761610585030681 ) ) ;
#3015=CARTESIAN_POINT ( 'NONE',  ( 0.2648978790185584908, -10.67083876753496341, 6.008231198268946471 ) ) ;
#3024=CARTESIAN_POINT ( 'NONE',  ( 2.305787727787085295, 7.249469779319941409, -2.461236246750998724 ) ) ;
#3029=CARTESIAN_POINT ( 'NONE',  ( 2.990245332647884169, -7.587819667496408016, 3.789007530133533752 ) ) ;
#3032=CARTESIAN_POINT ( 'NONE',  ( 2.440552418640494992, 7.166505277347731351, 2.818488640081600938 ) ) ;
#3035=CARTESIAN_POINT ( 'NONE',  ( 1.719304012338401133, 5.690355757826538685, 11.38834240361399885 ) ) ;
#3038=CARTESIAN_POINT ( 'NONE',  ( 1.948354844646311479, 3.407825014329756819, -11.46941405766637345 ) ) ;
#3044=CARTESIAN_POINT ( 'NONE',  ( 2.245754705088395031, 3.721112460997019866, 6.667819336165956123 ) ) ;
#3046=CARTESIAN_POINT ( 'NONE',  ( 2.034671305877419734, -3.325478336156925341, -11.19279775166577551 ) ) ;
#3050=DIRECTION ( 'NONE',  ( -1.000000000000000000, -0.000000000000000000, -0.000000000000000000 ) ) ;
#3052=EDGE_CURVE ( 'NONE', #17260, #55082, #48040, .T. ) ;
#3056=CARTESIAN_POINT ( 'NONE',  ( 2.241352910868908310, 6.652881166698511706, 3.744764251557016532 ) ) ;
#3060=CARTESIAN_POINT ( 'NONE',  ( 0.2801149460245143108, 6.294737133725796241, 10.51028947658246260 ) ) ;
#3078=EDGE_CURVE ( 'NONE', #48048, #35612, #28132, .T. ) ;
#3081=CARTESIAN_POINT ( 'NONE',  ( 5.520433897694421610, 0.01329351892498004811, 0.007082458259338615496 ) ) ;
#3091=CARTESIAN_POINT ( 'NONE',  ( 0.2767916011545413779, 1.940025653809002826, -12.09541651105893756 ) ) ;
#3101=CARTESIAN_POINT ( 'NONE',  ( 0.2759803524722208579, -7.727919584673380804, -9.504501710971684503 ) ) ;
#3103=CARTESIAN_POINT ( 'NONE',  ( 2.259025283528085293, -7.131631878998414109, 2.741148848567739105 ) ) ;
#3105=VERTEX_POINT ( 'NONE', #8077 ) ;
#3107=CARTESIAN_POINT ( 'NONE',  ( 2.373367633546870969, -2.795365972209121974, 7.151506276328619016 ) ) ;
#3111=CARTESIAN_POINT ( 'NONE',  ( 3.152665057734040488, 0.000000000000000000, 0.000000000000000000 ) ) ;
#3121=CARTESIAN_POINT ( 'NONE',  ( 2.241528039335009215, 7.179411278563588183, -2.596349773934808702 ) ) ;
#3125=FACE_OUTER_BOUND ( 'NONE', #60137, .T. ) ;
#3132=( BOUNDED_SURFACE ( )  B_SPLINE_SURFACE ( 3, 1, ( 
 ( #55098, #30479 ),
 ( #20179, #44453 ),
 ( #24855, #14204 ),
 ( #50777, #54470 ) ),
 .UNSPECIFIED., .F., .F., .F. ) 
 B_SPLINE_SURFACE_WITH_KNOTS ( ( 4, 4 ),
 ( 2, 2 ),
 ( 0.000000000000000000, 1.000000000000000000 ),
 ( 0.000000000000000000, 1.000000000000000000 ),
 .UNSPECIFIED. ) 
 GEOMETRIC_REPRESENTATION_ITEM ( )  RATIONAL_B_SPLINE_SURFACE ( (
 ( 1.000000000000000000, 1.000000000000000000),
 ( 0.6933888150995267674, 0.9895912004443193632),
 ( 0.6933888150995267674, 0.9895912004443193632),
 ( 1.000000000000000000, 1.000000000000000000) ) ) 
 REPRESENTATION_ITEM ( '' )  SURFACE ( )  );
#3138=CARTESIAN_POINT ( 'NONE',  ( 5.514624014163232779, -0.001255375129357695543, 0.003946330869975248588 ) ) ;
#3140=DIRECTION ( 'NONE',  ( -1.000000000000000000, -0.000000000000000000, -0.000000000000000000 ) ) ;
#3141=CARTESIAN_POINT ( 'NONE',  ( 0.2834382757447979073, -10.50792790568173274, 6.300836243950126203 ) ) ;
#3142=CARTESIAN_POINT ( 'NONE',  ( 5.530133899448235191, -0.008946569461392248762, 0.01324661008606526670 ) ) ;
#3150=CARTESIAN_POINT ( 'NONE',  ( 2.244591118396560780, -4.825158615932929607, 5.917635828475974691 ) ) ;
#3158=CARTESIAN_POINT ( 'NONE',  ( 0.9232058338315048962, -3.908895078357443875, -11.84276737136204716 ) ) ;
#3160=CARTESIAN_POINT ( 'NONE',  ( 5.520433897694421610, -0.01006947824912430428, 0.01120198501134832270 ) ) ;
#3164=ORIENTED_EDGE ( 'NONE', *, *, #65294, .T. ) ;
#3166=CARTESIAN_POINT ( 'NONE',  ( 0.3106921474978498465, 9.239619355094145448, 8.060345844326317177 ) ) ;
#3169=CARTESIAN_POINT ( 'NONE',  ( 0.2915757698887287419, 2.339174865979285034, 12.02962099476164148 ) ) ;
#3174=B_SPLINE_CURVE_WITH_KNOTS ( 'NONE', 3,
 ( #46841, #26890, #63117, #32507, #1306, #21585, #16591, #22217, #31854, #17579, #36859, #1948, #52813, #57157, #37847, #27873 ),
 .UNSPECIFIED., .F., .F.,
 ( 4, 3, 3, 3, 3, 4 ),
 ( 0.000000000000000000, 0.0003017745587525276323, 0.0006035491769808768846, 0.0009053241094668227533, 0.001207275924539981740, 0.001510325902532936703 ),
 .UNSPECIFIED. ) ;
#3178=ORIENTED_EDGE ( 'NONE', *, *, #27782, .F. ) ;
#3182=DIRECTION ( 'NONE',  ( 0.3939253465568943180, -0.8669868725995597547, 0.3052156353794235888 ) ) ;
#3183=CARTESIAN_POINT ( 'NONE',  ( 1.194176325881342038, 11.96454551582842996, 3.807610977966959798 ) ) ;
#3184=CARTESIAN_POINT ( 'NONE',  ( 1.283627346226433819, 0.5505361391623041500, 12.57362488724968053 ) ) ;
#3185=EDGE_LOOP ( 'NONE', ( #13472, #483, #28093, #47344 ) ) ;
#3187=B_SPLINE_CURVE_WITH_KNOTS ( 'NONE', 3,
 ( #12074, #42994, #37346, #47350, #33354, #22731, #53317, #53652, #48000, #47659, #27366, #23053, #62602, #43313, #8091, #17064, #57657, #58647, #1791, #28359, #57315, #42310 ),
 .UNSPECIFIED., .F., .F.,
 ( 4, 3, 3, 3, 3, 3, 3, 4 ),
 ( 2.474737474518078493E-18, 4.449119708436613866E-05, 6.626296329540155904E-05, 8.803456484962335078E-05, 0.0001098060367612770858, 0.0001315774408628463013, 0.0001760698110411093511, 0.0001829697163287823721 ),
 .UNSPECIFIED. ) ;
#3189=CARTESIAN_POINT ( 'NONE',  ( 0.2648978790185602672, 10.53870023327872474, -6.237101853238436355 ) ) ;
#3194=ADVANCED_FACE ( 'NONE', ( #15576 ), #5459, .F. ) ;
#3203=CARTESIAN_POINT ( 'NONE',  ( 1.459561108992815992, -3.725588117663614973, 12.08294179906916810 ) ) ;
#3216=AXIS2_PLACEMENT_3D ( 'NONE', #7572, #37835, #52498 ) ;
#3227=ORIENTED_EDGE ( 'NONE', *, *, #61, .T. ) ;
#3230=CARTESIAN_POINT ( 'NONE',  ( 2.242418902651939216, 1.423836467585349652, 7.500817491983885255 ) ) ;
#3232=CARTESIAN_POINT ( 'NONE',  ( 2.717984159220022011, -5.223388265380124906, -5.783767685176870899 ) ) ;
#3243=CARTESIAN_POINT ( 'NONE',  ( 2.305787727787083519, -3.682701754025559993, 6.711944854845811825 ) ) ;
#3247=CARTESIAN_POINT ( 'NONE',  ( 1.452237505248555660, 11.24427360515642071, 5.807998527925930965 ) ) ;
#3250=CARTESIAN_POINT ( 'NONE',  ( 0.2655924914740778742, 12.06787830249865223, 2.083162675473652747 ) ) ;
#3251=CARTESIAN_POINT ( 'NONE',  ( 1.719304012338239485, 12.38166659046522788, 2.961219984258211202 ) ) ;
#3253=EDGE_CURVE ( 'NONE', #10208, #28435, #7584, .T. ) ;
#3257=CARTESIAN_POINT ( 'NONE',  ( 0.8320506296491568810, 12.17395768195220640, -2.535206712041328636 ) ) ;
#3262=CARTESIAN_POINT ( 'NONE',  ( 0.2647959493198559500, -9.474789498086940043, -7.758440170207265396 ) ) ;
#3263=CARTESIAN_POINT ( 'NONE',  ( 2.844750968616399422, -4.777247819183459754, 6.210802026112522078 ) ) ;
#3272=EDGE_LOOP ( 'NONE', ( #36581, #11343, #10174, #24060 ) ) ;
#3282=ORIENTED_EDGE ( 'NONE', *, *, #26792, .F. ) ;
#3283=CARTESIAN_POINT ( 'NONE',  ( 3.152665057734040488, 0.000000000000000000, 0.000000000000000000 ) ) ;
#3286=ORIENTED_EDGE ( 'NONE', *, *, #17301, .T. ) ;
#3290=ADVANCED_FACE ( 'NONE', ( #4656 ), #44732, .F. ) ;
#3291=CARTESIAN_POINT ( 'NONE',  ( 0.3341166715381344576, 10.49680960898235149, -6.352033667906496817 ) ) ;
#3298=CARTESIAN_POINT ( 'NONE',  ( 2.241352910868909643, -1.407733736974916772, 7.503490710578227585 ) ) ;
#3302=CARTESIAN_POINT ( 'NONE',  ( 2.241352910868908310, -2.689314586382399952, 7.145045428366567641 ) ) ;
#3303=CARTESIAN_POINT ( 'NONE',  ( 0.3474126878361817328, -8.085727498271713998, -9.233692382639453911 ) ) ;
#3318=CARTESIAN_POINT ( 'NONE',  ( 0.2706063244538033374, -0.1752385892652840171, 12.24670371972918304 ) ) ;
#3320=CIRCLE ( 'NONE', #26692, 12.73084802173761787 ) ;
#3323=CARTESIAN_POINT ( 'NONE',  ( 3.031336079629838753, 5.388626255827111855, 5.773872239512813032 ) ) ;
#3326=CARTESIAN_POINT ( 'NONE',  ( 2.273267844204863053, -3.690689057641665993, 6.695181685739943767 ) ) ;
#3330=B_SPLINE_CURVE_WITH_KNOTS ( 'NONE', 3,
 ( #42277, #46643, #6417, #11707, #16397, #26691, #37313 ),
 .UNSPECIFIED., .F., .F.,
 ( 4, 3, 4 ),
 ( 4.939146456270413598E-15, 0.002398160485434625965, 0.005002426799381625919 ),
 .UNSPECIFIED. ) ;
#3350=CARTESIAN_POINT ( 'NONE',  ( 0.2767916011545385468, 9.260929738915347542, -8.018602152763769197 ) ) ;
#3351=EDGE_CURVE ( 'NONE', #15607, #56731, #46385, .T. ) ;
#3352=CARTESIAN_POINT ( 'NONE',  ( 5.516018279890452902, -0.0009545156522404840260, 0.006707902355168859562 ) ) ;
#3356=CARTESIAN_POINT ( 'NONE',  ( 2.276198483117261251, 7.236140649716396922, -2.469789406312159041 ) ) ;
#3364=VERTEX_POINT ( 'NONE', #7237 ) ;
#3377=CARTESIAN_POINT ( 'NONE',  ( 2.249013661412228693, 3.714035584818222713, 6.673008335691879012 ) ) ;
#3382=CARTESIAN_POINT ( 'NONE',  ( 1.104777566491141672, 11.59867774809550589, -4.729982681549413925 ) ) ;
#3383=CARTESIAN_POINT ( 'NONE',  ( 0.3675815128205894289, -9.235491948680062180, 8.093875121226046687 ) ) ;
#3388=CARTESIAN_POINT ( 'NONE',  ( 2.284126774967660811, -2.764365694977838572, 7.131638985093299965 ) ) ;
#3391=EDGE_CURVE ( 'NONE', #45562, #42237, #62131, .T. ) ;
#3393=CARTESIAN_POINT ( 'NONE',  ( 0.2956976708475461679, 3.984495122852575566, 11.59055635407402463 ) ) ;
#3394=CARTESIAN_POINT ( 'NONE',  ( 0.3632410797595302943, -2.390576695689024866, -12.04386719438561926 ) ) ;
#3395=ORIENTED_EDGE ( 'NONE', *, *, #61859, .T. ) ;
#3408=CARTESIAN_POINT ( 'NONE',  ( 0.9232167919969156422, -9.278116382137428175, 8.324955738482442413 ) ) ;
#3417=CARTESIAN_POINT ( 'NONE',  ( 2.406456491626458138, -2.970787154400910346, 10.00134798414774373 ) ) ;
#3418=FACE_OUTER_BOUND ( 'NONE', #12804, .T. ) ;
#3420=CARTESIAN_POINT ( 'NONE',  ( 5.516018279890452902, 0.0009545156522407046611, 0.006707902355169304519 ) ) ;
#3425=ORIENTED_EDGE ( 'NONE', *, *, #58231, .F. ) ;
#3433=CARTESIAN_POINT ( 'NONE',  ( 0.2650492433740059273, 6.218175523534292815, 10.54996000109277432 ) ) ;
#3434=EDGE_CURVE ( 'NONE', #1207, #38878, #21788, .T. ) ;
#3435=CARTESIAN_POINT ( 'NONE',  ( 0.2652384770603680719, -12.24598129987881379, -0.06606665821610741007 ) ) ;
#3440=CARTESIAN_POINT ( 'NONE',  ( 0.3106921474978474040, -7.699584408545827152, -9.542334142800539709 ) ) ;
#3447=CARTESIAN_POINT ( 'NONE',  ( 3.100650473569514620, -3.129198107107880933, 7.276570693048374672 ) ) ;
#3448=CARTESIAN_POINT ( 'NONE',  ( 0.3106921474978470710, 10.49891314301085998, 6.333448016104091138 ) ) ;
#3449=CARTESIAN_POINT ( 'NONE',  ( 0.2646305136544072623, -11.46223899740603436, 4.312539723326094254 ) ) ;
#3450=ORIENTED_EDGE ( 'NONE', *, *, #20426, .T. ) ;
#3454=CARTESIAN_POINT ( 'NONE',  ( 0.3665391374699467075, 2.392238720110619443, -12.04754782681755110 ) ) ;
#3463=CARTESIAN_POINT ( 'NONE',  ( 0.2915757698887302407, 3.989025639548790192, -11.58754481235182432 ) ) ;
#3465=CARTESIAN_POINT ( 'NONE',  ( 0.2801149460245159206, -4.005169813315180072, 11.57793225195135278 ) ) ;
#3468=CARTESIAN_POINT ( 'NONE',  ( 0.2650492433740059828, -11.46945725111970660, 4.291726136518509094 ) ) ;
#3473=VERTEX_POINT ( 'NONE', #28505 ) ;
#3474=AXIS2_PLACEMENT_3D ( 'NONE', #54478, #2960, #48835 ) ;
#3476=ADVANCED_FACE ( 'NONE', ( #63418 ), #5417, .T. ) ;
#3487=CARTESIAN_POINT ( 'NONE',  ( 2.259830038565000532, -5.763537486834636070, -5.015955067335985618 ) ) ;
#3489=EDGE_CURVE ( 'NONE', #29012, #24593, #48949, .T. ) ;
#3490=VECTOR ( 'NONE', #18959, 1000.000000000000114 ) ;
#3496=ORIENTED_EDGE ( 'NONE', *, *, #19271, .T. ) ;
#3498=CARTESIAN_POINT ( 'NONE',  ( 2.889800649504073782, 3.118861721612566029, 5.267262008933680129 ) ) ;
#3500=EDGE_CURVE ( 'NONE', #27117, #18739, #9038, .T. ) ;
#3507=CARTESIAN_POINT ( 'NONE',  ( 0.2638984909335716500, -10.70468911391668243, 5.950360275955019596 ) ) ;
#3508=LINE ( 'NONE', #54693, #52319 ) ;
#3514=CARTESIAN_POINT ( 'NONE',  ( 0.2651627682582897716, -4.271106202749196612, -11.47719223137564803 ) ) ;
#3519=CARTESIAN_POINT ( 'NONE',  ( 0.4626703367445907378, -12.07256244737118145, -2.416235258139934672 ) ) ;
#3524=B_SPLINE_CURVE_WITH_KNOTS ( 'NONE', 3,
 ( #22726, #3107, #37995, #38982, #33985, #23049, #58973, #58643, #22372, #33669, #28676, #43309, #48989, #42638, #3447, #62943 ),
 .UNSPECIFIED., .F., .F.,
 ( 4, 3, 3, 3, 3, 4 ),
 ( 4.336808689942017736E-19, 0.0002176109881720242952, 0.0004352086762394619134, 0.0006528017811446884837, 0.0007615147961451716263, 0.0009453342004943081529 ),
 .UNSPECIFIED. ) ;
#3542=CARTESIAN_POINT ( 'NONE',  ( 2.288423627606496868, 5.962686897378696393, 4.792733268640499311 ) ) ;
#3554=CARTESIAN_POINT ( 'NONE',  ( 0.3106921474978440734, -10.49891314301081735, -6.333448016104161304 ) ) ;
#3559=CARTESIAN_POINT ( 'NONE',  ( 2.241311220309555097, 3.897297589552074282, -6.564680916077756834 ) ) ;
#3568=EDGE_CURVE ( 'NONE', #54893, #21752, #50276, .T. ) ;
#3573=CARTESIAN_POINT ( 'NONE',  ( 2.241528039335008327, 5.858435878248576145, -4.895273998033944807 ) ) ;
#3575=CARTESIAN_POINT ( 'NONE',  ( 2.288423627607476973, 1.486973602181149712, 7.504187945869062126 ) ) ;
#3576=CARTESIAN_POINT ( 'NONE',  ( 2.368238019615382495, -5.070835960312986224, -5.763545178420198312 ) ) ;
#3577=B_SPLINE_CURVE_WITH_KNOTS ( 'NONE', 3,
 ( #64189, #33914, #3032, #24270, #43906, #34246, #23297, #59526, #8986, #44536, #38590, #58906, #53891, #8328, #64816, #19294 ),
 .UNSPECIFIED., .F., .F.,
 ( 4, 3, 3, 3, 3, 4 ),
 ( 0.000000000000000000, 0.0002176109881720251354, 0.0004352086762394620219, 0.0006528017811446910857, 0.0007615147961451749874, 0.0009453342004947290402 ),
 .UNSPECIFIED. ) ;
#3588=CARTESIAN_POINT ( 'NONE',  ( 2.242418902651939216, -0.09970190380427686183, -7.634109827927233027 ) ) ;
#3589=CARTESIAN_POINT ( 'NONE',  ( 2.242819959140646358, -5.913965034148185751, 4.828731837260215265 ) ) ;
#3600=CARTESIAN_POINT ( 'NONE',  ( 0.3675815128205894289, -8.093875121226139058, 9.235491948679980467 ) ) ;
#3605=ORIENTED_EDGE ( 'NONE', *, *, #42483, .F. ) ;
#3611=LINE ( 'NONE', #44442, #49244 ) ;
#3624=CARTESIAN_POINT ( 'NONE',  ( 0.2739690278137255630, 5.965352196073746782, -10.69833303470758601 ) ) ;
#3626=CARTESIAN_POINT ( 'NONE',  ( 0.3665391374699465965, -11.62960183138724446, -3.952034409876413079 ) ) ;
#3640=CARTESIAN_POINT ( 'NONE',  ( 0.2648321136542728382, 7.979621084888234961, -9.289286523730330813 ) ) ;
#3648=CARTESIAN_POINT ( 'NONE',  ( 0.2653519890538384995, 1.477274386607676477E-15, 12.24619734961521189 ) ) ;
#3655=CARTESIAN_POINT ( 'NONE',  ( 1.549075743843706832, 5.743768701987367109, 11.29795072957420032 ) ) ;
#3662=AXIS2_PLACEMENT_3D ( 'NONE', #50150, #61098, #4605 ) ;
#3665=CARTESIAN_POINT ( 'NONE',  ( 2.305787727787084407, 5.047606869483056258, 5.756228004061473946 ) ) ;
#3676=CARTESIAN_POINT ( 'NONE',  ( 2.717984159218978402, 5.783767685176879780, -5.223388265379605322 ) ) ;
#3681=CARTESIAN_POINT ( 'NONE',  ( 1.719304012339819332, -7.581471372739574832, 10.22720798541442555 ) ) ;
#3686=CARTESIAN_POINT ( 'NONE',  ( 2.266490820343017631, 5.023127813992001478, 5.760233951938614538 ) ) ;
#3689=CARTESIAN_POINT ( 'NONE',  ( 0.2759803524722211909, 12.24828167798667522, 0.1894460813476448457 ) ) ;
#3690=CARTESIAN_POINT ( 'NONE',  ( 3.152665057735501097, 6.622010822086128456, -4.377619405893580229 ) ) ;
#3691=CARTESIAN_POINT ( 'NONE',  ( 5.536195898058073439, -0.007485416011287833460, 0.004027525919832407840 ) ) ;
#3694=ORIENTED_EDGE ( 'NONE', *, *, #19384, .F. ) ;
#3695=CARTESIAN_POINT ( 'NONE',  ( 2.268878695253353506, 7.231932316093202751, -2.474564429974424495 ) ) ;
#3710=CARTESIAN_POINT ( 'NONE',  ( 2.298277635560274756, 2.461898367585382719, 7.246601281227234459 ) ) ;
#3720=DIRECTION ( 'NONE',  ( -0.3865475372811021937, 0.5778504531711138315, -0.7187975063895625238 ) ) ;
#3721=CARTESIAN_POINT ( 'NONE',  ( 1.283627346227174337, 11.62704807385648209, -4.817767733507369421 ) ) ;
#3723=CARTESIAN_POINT ( 'NONE',  ( 0.9296196016834723519, -0.4155906739599753430, 12.46069139398446168 ) ) ;
#3725=CARTESIAN_POINT ( 'NONE',  ( 2.268878695253353062, -7.130600918714364411, -2.752970156154558978 ) ) ;
#3726=( BOUNDED_SURFACE ( )  B_SPLINE_SURFACE ( 3, 1, ( 
 ( #47380, #28076 ),
 ( #37376, #43342 ),
 ( #47694, #7437 ),
 ( #27727, #58680 ) ),
 .UNSPECIFIED., .F., .F., .F. ) 
 B_SPLINE_SURFACE_WITH_KNOTS ( ( 4, 4 ),
 ( 2, 2 ),
 ( 0.000000000000000000, 1.000000000000000000 ),
 ( 0.000000000000000000, 1.000000000000000000 ),
 .UNSPECIFIED. ) 
 GEOMETRIC_REPRESENTATION_ITEM ( )  RATIONAL_B_SPLINE_SURFACE ( (
 ( 1.000000000000000000, 1.000000000000000000),
 ( 0.6933888150995267674, 0.9895912004443193632),
 ( 0.6933888150995267674, 0.9895912004443193632),
 ( 1.000000000000000000, 1.000000000000000000) ) ) 
 REPRESENTATION_ITEM ( '' )  SURFACE ( )  );
#3735=CARTESIAN_POINT ( 'NONE',  ( 0.2651627682582899381, -9.437482589529922805, -7.803986935114110679 ) ) ;
#3738=CARTESIAN_POINT ( 'NONE',  ( 0.9232167919969059833, 6.587352952801155404, 10.58277433962383718 ) ) ;
#3739=EDGE_CURVE ( 'NONE', #43940, #42272, #871, .T. ) ;
#3744=CARTESIAN_POINT ( 'NONE',  ( 5.514970785353741078, 0.004694330894494709236, 0.0005190732562555246078 ) ) ;
#3745=CARTESIAN_POINT ( 'NONE',  ( 3.092491956585309953, 4.340140213817062609, 6.622742949902756138 ) ) ;
#3749=CARTESIAN_POINT ( 'NONE',  ( 2.177405672431837136, -10.01846874164949774, -5.005033771131442322 ) ) ;
#3753=CARTESIAN_POINT ( 'NONE',  ( 0.2650492433740060938, 7.955688793816089621, 9.309907554970001442 ) ) ;
#3764=CARTESIAN_POINT ( 'NONE',  ( 0.2651627682582916035, 6.199212018117441936, 10.56115808354085317 ) ) ;
#3772=ORIENTED_EDGE ( 'NONE', *, *, #53219, .T. ) ;
#3775=CARTESIAN_POINT ( 'NONE',  ( 0.2834382757447981294, -9.254160138069011055, 8.029794915379529385 ) ) ;
#3776=CARTESIAN_POINT ( 'NONE',  ( 5.514624014163232779, 0.004104370840204214776, -0.0005510299962886395586 ) ) ;
#3783=CARTESIAN_POINT ( 'NONE',  ( 0.9232058338315048962, 2.536181247095527613, -12.21058493388770927 ) ) ;
#3785=CARTESIAN_POINT ( 'NONE',  ( 0.3665391374699464300, -12.13918562134719714, 1.872534962004759551 ) ) ;
#3791=CARTESIAN_POINT ( 'NONE',  ( 0.3654063281920744699, 3.951404032559424184, -11.62642356802257559 ) ) ;
#3795=CARTESIAN_POINT ( 'NONE',  ( 0.2958664285830430174, 9.529149585189953697, 7.708042451272207884 ) ) ;
#3798=CARTESIAN_POINT ( 'NONE',  ( 0.2869720083484345041, -3.994435966589990450, -11.58405933820305300 ) ) ;
#3799=CARTESIAN_POINT ( 'NONE',  ( 0.2648978790185584908, -12.08224454301450201, 1.996248716311589400 ) ) ;
#3804=EDGE_CURVE ( 'NONE', #46970, #28685, #22131, .T. ) ;
#3805=EDGE_LOOP ( 'NONE', ( #45295, #41670, #183, #28266 ) ) ;
#3806=CARTESIAN_POINT ( 'NONE',  ( 0.2655924914740778187, 6.161287456391830730, -10.58356227062103017 ) ) ;
#3807=FACE_OUTER_BOUND ( 'NONE', #34565, .T. ) ;
#3809=DIRECTION ( 'NONE',  ( -0.3865475372811021937, 0.01937500237528418795, 0.9220659470476462172 ) ) ;
#3811=CARTESIAN_POINT ( 'NONE',  ( 0.2655924914740778187, -7.838010948424984470, -9.409507842006103573 ) ) ;
#3812=CARTESIAN_POINT ( 'NONE',  ( 0.2706063244538042811, 10.69357582853954902, -5.971590789837406987 ) ) ;
#3819=CARTESIAN_POINT ( 'NONE',  ( 2.290907136833253421, -5.755317856506250607, -5.041121061899964673 ) ) ;
#3821=VERTEX_POINT ( 'NONE', #29102 ) ;
#3827=LINE ( 'NONE', #3498, #18715 ) ;
#3836=ORIENTED_EDGE ( 'NONE', *, *, #6757, .F. ) ;
#3837=CARTESIAN_POINT ( 'NONE',  ( 0.000000000000000000, 0.000000000000000000, 0.000000000000000000 ) ) ;
#3838=CARTESIAN_POINT ( 'NONE',  ( 0.2653141617321015944, -4.147035654172644747, -11.52265685897333647 ) ) ;
#3839=ORIENTED_EDGE ( 'NONE', *, *, #20406, .F. ) ;
#3840=EDGE_CURVE ( 'NONE', #3821, #38649, #55802, .T. ) ;
#3843=EDGE_CURVE ( 'NONE', #61427, #9266, #48729, .T. ) ;
#3845=CARTESIAN_POINT ( 'NONE',  ( 0.6511581176963612272, -12.12498040206541994, -2.473966499148246179 ) ) ;
#3847=CARTESIAN_POINT ( 'NONE',  ( 0.2956976708475438365, -6.317697191869704021, 10.50256636126824361 ) ) ;
#3851=ORIENTED_EDGE ( 'NONE', *, *, #17190, .T. ) ;
#3864=CARTESIAN_POINT ( 'NONE',  ( 2.273267844203308741, 5.952585402746135124, 4.797225296801178374 ) ) ;
#3865=VERTEX_POINT ( 'NONE', #18489 ) ;
#3880=CARTESIAN_POINT ( 'NONE',  ( 0.9296196016823239372, 3.871279966920111448, 11.85136013468979144 ) ) ;
#3883=ORIENTED_EDGE ( 'NONE', *, *, #40939, .F. ) ;
#3891=CARTESIAN_POINT ( 'NONE',  ( 0.2646305136544065406, -12.03696649559613263, -2.256625640822439216 ) ) ;
#3893=B_SPLINE_CURVE_WITH_KNOTS ( 'NONE', 3,
 ( #8354, #28971, #63873, #12348, #18010, #38947, #37951, #33941, #32951, #53261, #28313, #54250, #18689, #58595, #33301, #57935 ),
 .UNSPECIFIED., .F., .F.,
 ( 4, 3, 3, 3, 3, 4 ),
 ( 2.799023667439389453E-15, 0.0002126834539180046070, 0.0004253519300366957962, 0.0006380165497225226412, 0.0007442707582429485729, 0.0009453531351410136277 ),
 .UNSPECIFIED. ) ;
#3896=CARTESIAN_POINT ( 'NONE',  ( 2.368238019615179990, -3.681632831800436101, 6.736275681109117563 ) ) ;
#3898=CARTESIAN_POINT ( 'NONE',  ( 2.268878695253352618, -5.949442550447433753, 4.798796461778030320 ) ) ;
#3901=CARTESIAN_POINT ( 'NONE',  ( 5.516018279890452902, -0.005752102158674371642, -0.003580555109620855384 ) ) ;
#3903=VERTEX_POINT ( 'NONE', #8155 ) ;
#3904=CARTESIAN_POINT ( 'NONE',  ( 0.4626703367443995019, -6.399577980714719061, 10.51809671647419364 ) ) ;
#3912=CARTESIAN_POINT ( 'NONE',  ( 2.290907136833250313, -7.243397831411269472, 2.463690939638650601 ) ) ;
#3913=CARTESIAN_POINT ( 'NONE',  ( 0.9232058338315048962, -2.536181247095447677, 12.21058493388772881 ) ) ;
#3915=CARTESIAN_POINT ( 'NONE',  ( 1.719304012339869514, -10.22720798541492471, 7.581471372739622794 ) ) ;
#3916=CARTESIAN_POINT ( 'NONE',  ( 2.241352910868909643, 7.532448145350525870, -1.243507963608017075 ) ) ;
#3927=LINE ( 'NONE', #34490, #17099 ) ;
#3929=CARTESIAN_POINT ( 'NONE',  ( 2.276905613633646297, 6.543460433228703188, -3.955794200962136298 ) ) ;
#3942=CARTESIAN_POINT ( 'NONE',  ( 2.705197763288542667, -4.134294772209968549, 6.601241161176667482 ) ) ;
#3945=EDGE_CURVE ( 'NONE', #56656, #42237, #49456, .T. ) ;
#3946=CARTESIAN_POINT ( 'NONE',  ( 0.2767916011545359933, 11.57477803659173254, 4.010899340181466322 ) ) ;
#3948=CARTESIAN_POINT ( 'NONE',  ( 2.268878695253353506, -1.472930498387327480, 7.500319319173580190 ) ) ;
#3953=CARTESIAN_POINT ( 'NONE',  ( 2.241352910868908310, -7.503490710578242684, 1.407733736974842165 ) ) ;
#3961=CARTESIAN_POINT ( 'NONE',  ( 2.305787727787083519, -7.566723232958080914, 1.164987321564707967 ) ) ;
#3963=CARTESIAN_POINT ( 'NONE',  ( 2.241528039335008327, -4.919377664485136137, 5.838210500619361198 ) ) ;
#3975=CARTESIAN_POINT ( 'NONE',  ( 0.2655924914740778742, -6.084990060696584102, 10.62761259256415158 ) ) ;
#3988=CARTESIAN_POINT ( 'NONE',  ( 0.3401186441510245517, 12.26845925752607158, 0.2556125181570270688 ) ) ;
#3998=CARTESIAN_POINT ( 'NONE',  ( 2.655192694324852720, 9.584054627284606553, -0.5793947661800037396 ) ) ;
#4007=CARTESIAN_POINT ( 'NONE',  ( 2.268878695253353506, 2.474564429974497326, 7.231932316093173441 ) ) ;
#4008=B_SPLINE_CURVE_WITH_KNOTS ( 'NONE', 3,
 ( #63960, #8116, #14068, #28709, #59638, #53991, #28387, #3141, #44323, #12749, #34356, #38021, #18438, #23400, #28073, #33035, #43671, #17767, #48371, #38701, #39013, #2821 ),
 .UNSPECIFIED., .F., .F.,
 ( 4, 3, 3, 3, 3, 3, 3, 4 ),
 ( 3.157244383156456744E-18, 4.449119708436542037E-05, 6.626296329539970234E-05, 8.803456484962158895E-05, 0.0001098060367612736842, 0.0001315774408628445666, 0.0001760698110411097305, 0.0001829697163287816945 ),
 .UNSPECIFIED. ) ;
#4011=EDGE_LOOP ( 'NONE', ( #8472, #41353 ) ) ;
#4014=ORIENTED_EDGE ( 'NONE', *, *, #18863, .F. ) ;
#4019=DIRECTION ( 'NONE',  ( -1.000000000000000000, -0.000000000000000000, -0.000000000000000000 ) ) ;
#4020=ORIENTED_EDGE ( 'NONE', *, *, #9691, .F. ) ;
#4023=ORIENTED_EDGE ( 'NONE', *, *, #50393, .F. ) ;
#4029=CARTESIAN_POINT ( 'NONE',  ( 2.297017764050090172, -6.708511771223851561, -3.682881532880156072 ) ) ;
#4035=CARTESIAN_POINT ( 'NONE',  ( 0.8320506296491532172, 6.546053790694177366, 10.57268643647776862 ) ) ;
#4039=CARTESIAN_POINT ( 'NONE',  ( 2.899286259009685285, 6.972741252562111747, -3.614094927251865208 ) ) ;
#4043=CARTESIAN_POINT ( 'NONE',  ( 2.241451721903216399, 3.869794645251212195, -6.581017239736924651 ) ) ;
#4044=CARTESIAN_POINT ( 'NONE',  ( 0.5572780756282654790, 1.841882550626922299, 12.20533540249701510 ) ) ;
#4048=ADVANCED_FACE ( 'NONE', ( #42640 ), #21408, .F. ) ;
#4049=CARTESIAN_POINT ( 'NONE',  ( 2.297017764050091948, -5.967068736727081379, -4.791851130936033876 ) ) ;
#4054=ORIENTED_EDGE ( 'NONE', *, *, #44399, .F. ) ;
#4057=VERTEX_POINT ( 'NONE', #5814 ) ;
#4060=CARTESIAN_POINT ( 'NONE',  ( 2.373367633546871414, -7.275198254387427177, 2.455525055524864886 ) ) ;
#4076=DIRECTION ( 'NONE',  ( 0.3939253465568944290, -0.9190910618577644575, -0.009718094113436328077 ) ) ;
#4080=ORIENTED_EDGE ( 'NONE', *, *, #16052, .T. ) ;
#4082=ORIENTED_EDGE ( 'NONE', *, *, #36041, .F. ) ;
#4083=CARTESIAN_POINT ( 'NONE',  ( 1.109979610370815939, -9.898186741522138732, 7.679283534372324027 ) ) ;
#4090=CARTESIAN_POINT ( 'NONE',  ( 0.2648978790185619880, 9.465406350830608773, 7.769924372105235122 ) ) ;
#4091=DIRECTION ( 'NONE',  ( -0.3939253465568944290, 0.009718094113433240269, 0.9190910618577644575 ) ) ;
#4092=CARTESIAN_POINT ( 'NONE',  ( 1.719304012338831678, -5.066286238785654206, 11.67935079956403044 ) ) ;
#4097=CARTESIAN_POINT ( 'NONE',  ( 0.3665391374699467075, -12.13918562134719892, 1.872534962004761327 ) ) ;
#4099=ORIENTED_EDGE ( 'NONE', *, *, #12002, .T. ) ;
#4100=CARTESIAN_POINT ( 'NONE',  ( 0.7400311444011717921, 1.803686700615571459, -12.27261279799596316 ) ) ;
#4102=B_SPLINE_CURVE_WITH_KNOTS ( 'NONE', 3,
 ( #19561, #45147, #65405, #15203, #14852, #65723, #20534, #14529, #20195, #25507, #50479, #40817, #9887, #25183, #39824, #5586, #4922, #40468, #19873 ),
 .UNSPECIFIED., .F., .F.,
 ( 4, 3, 3, 3, 3, 3, 4 ),
 ( 6.269651592512720910E-18, 2.825908398831185141E-05, 4.208813692483835759E-05, 5.591713746943659783E-05, 6.279584083231569099E-05, 9.105792820296166852E-05, 0.0001153131102488848627 ),
 .UNSPECIFIED. ) ;
#4113=CARTESIAN_POINT ( 'NONE',  ( 2.889800649504073782, 5.774917447012996696, 2.030191121417155742 ) ) ;
#4115=CARTESIAN_POINT ( 'NONE',  ( 0.2650492433740058718, -7.955688793816027449, -9.309907554970058285 ) ) ;
#4119=B_SPLINE_CURVE_WITH_KNOTS ( 'NONE', 3,
 ( #43937, #13986, #18687, #40233, #45554, #25954, #25275, #15306, #9642, #54889, #60522, #35582, #45901, #55876, #10308, #19965, #45239, #40570, #34593 ),
 .UNSPECIFIED., .F., .F.,
 ( 4, 3, 3, 3, 3, 3, 4 ),
 ( 8.282800797427508197E-18, 4.457896483015377895E-05, 6.639290541542518080E-05, 8.820687556479407708E-05, 0.0001100173248779025482, 0.0001545671401658153549, 0.0001830328308068586039 ),
 .UNSPECIFIED. ) ;
#4125=LINE ( 'NONE', #49680, #61662 ) ;
#4130=EDGE_CURVE ( 'NONE', #13640, #12912, #27284, .T. ) ;
#4137=CARTESIAN_POINT ( 'NONE',  ( 0.2657645697724686507, -12.08564806881063092, 1.977350809428493505 ) ) ;
#4144=ORIENTED_EDGE ( 'NONE', *, *, #11926, .T. ) ;
#4156=CARTESIAN_POINT ( 'NONE',  ( 2.241506898688418126, 0.03933068055390912671, 7.634383346098562839 ) ) ;
#4157=CARTESIAN_POINT ( 'NONE',  ( 1.109979610369143277, 7.679283534372506992, 9.898186741521291410 ) ) ;
#4164=ORIENTED_EDGE ( 'NONE', *, *, #21724, .F. ) ;
#4168=CARTESIAN_POINT ( 'NONE',  ( 5.514970785353741078, 0.003415090918276138688, -0.003262412238248723392 ) ) ;
#4171=CARTESIAN_POINT ( 'NONE',  ( 2.259025283526323147, 5.939720477911452967, 4.805599953369094735 ) ) ;
#4174=DIRECTION ( 'NONE',  ( -1.000000000000000000, -0.000000000000000000, -0.000000000000000000 ) ) ;
#4176=CARTESIAN_POINT ( 'NONE',  ( 2.244591118396558116, -7.500068934084582750, 1.431619869711830084 ) ) ;
#4177=CARTESIAN_POINT ( 'NONE',  ( 0.3160775863651117401, 0.2401734240704574974, -12.26075464248083158 ) ) ;
#4198=CARTESIAN_POINT ( 'NONE',  ( 2.241352910868908310, -5.794346703933879184, 4.970878533273742406 ) ) ;
#4201=ORIENTED_EDGE ( 'NONE', *, *, #37915, .F. ) ;
#4202=CARTESIAN_POINT ( 'NONE',  ( 2.556980015512952065, -6.074557383032423985, -4.795979673457674508 ) ) ;
#4203=CARTESIAN_POINT ( 'NONE',  ( 0.3675815128205894289, 10.76447900494940235, 5.910255304480483751 ) ) ;
#4205=VECTOR ( 'NONE', #59552, 1000.000000000000227 ) ;
#4206=CARTESIAN_POINT ( 'NONE',  ( 2.573738926104376379, -6.586859681822632595, -4.074516960797446963 ) ) ;
#4210=CARTESIAN_POINT ( 'NONE',  ( 5.520433897694421610, 0.002108682515300482584, -0.01491416502703863875 ) ) ;
#4224=CARTESIAN_POINT ( 'NONE',  ( 1.633930747255852411, 12.36466318969160127, -2.909970528253460031 ) ) ;
#4227=CARTESIAN_POINT ( 'NONE',  ( 2.259830038564997867, -7.225713255971560223, 2.483392345594741979 ) ) ;
#4230=CARTESIAN_POINT ( 'NONE',  ( 2.491965175174677416, -4.796682362486693663, 6.046355957631128319 ) ) ;
#4245=VERTEX_POINT ( 'NONE', #17738 ) ;
#4246=CARTESIAN_POINT ( 'NONE',  ( 0.2671309869109493862, 5.982543484153372226, -10.68612389951470831 ) ) ;
#4252=CARTESIAN_POINT ( 'NONE',  ( 2.994568964204211703, 0.3996732855055812328, -7.875338388187465455 ) ) ;
#4268=LINE ( 'NONE', #58852, #30621 ) ;
#4273=ADVANCED_FACE ( 'NONE', ( #28679 ), #9700, .F. ) ;
#4276=EDGE_LOOP ( 'NONE', ( #47308, #10753, #9120, #57788 ) ) ;
#4277=CARTESIAN_POINT ( 'NONE',  ( 0.3654063281920718054, 0.2633658439603340229, 12.27672420655578911 ) ) ;
#4278=( BOUNDED_SURFACE ( )  B_SPLINE_SURFACE ( 3, 1, ( 
 ( #40634, #20994 ),
 ( #60928, #45965 ),
 ( #30340, #51621 ),
 ( #11040, #21333 ) ),
 .UNSPECIFIED., .F., .F., .F. ) 
 B_SPLINE_SURFACE_WITH_KNOTS ( ( 4, 4 ),
 ( 2, 2 ),
 ( 0.000000000000000000, 1.000000000000000000 ),
 ( 0.000000000000000000, 1.000000000000000000 ),
 .UNSPECIFIED. ) 
 GEOMETRIC_REPRESENTATION_ITEM ( )  RATIONAL_B_SPLINE_SURFACE ( (
 ( 1.000000000000000000, 1.000000000000000000),
 ( 0.9856612449720755231, 0.9999558406602322425),
 ( 0.9856612449720755231, 0.9999558406602322425),
 ( 1.000000000000000000, 1.000000000000000000) ) ) 
 REPRESENTATION_ITEM ( '' )  SURFACE ( )  );
#4280=CARTESIAN_POINT ( 'NONE',  ( 5.514970785353741078, 0.004324946436530184915, 0.001897634820904495461 ) ) ;
#4281=CARTESIAN_POINT ( 'NONE',  ( 2.258463476536642478, -7.499249607179731214, -1.460294809171017727 ) ) ;
#4282=CARTESIAN_POINT ( 'NONE',  ( 5.516018279890452902, -0.005331956019561682678, 0.004180585980735035401 ) ) ;
#4284=CARTESIAN_POINT ( 'NONE',  ( 2.524535260912991852, 5.135322114976021979, 5.776056274541075730 ) ) ;
#4298=CARTESIAN_POINT ( 'NONE',  ( 0.2872850955227758685, -0.2089153415334024932, -12.25172867346922878 ) ) ;
#4308=ORIENTED_EDGE ( 'NONE', *, *, #8547, .F. ) ;
#4310=CARTESIAN_POINT ( 'NONE',  ( 0.3040950598368144520, 4.428852722102886830, -11.43390362554248618 ) ) ;
#4314=CARTESIAN_POINT ( 'NONE',  ( 0.2648978790185610999, 9.295532325666560070, -7.972372351882934360 ) ) ;
#4315=EDGE_CURVE ( 'NONE', #47209, #43940, #31185, .T. ) ;
#4319=VECTOR ( 'NONE', #3182, 1000.000000000000114 ) ;
#4321=EDGE_LOOP ( 'NONE', ( #19942, #277, #21052, #65669 ) ) ;
#4322=CARTESIAN_POINT ( 'NONE',  ( 1.547277799339514370, -2.861188171559366111, -12.34637640861339314 ) ) ;
#4324=CARTESIAN_POINT ( 'NONE',  ( 0.2655924914740778187, -2.169924872618142153, 12.05257978623653159 ) ) ;
#4333=CARTESIAN_POINT ( 'NONE',  ( 0.2655924914740778187, 2.169924872618221201, -12.05257978623651560 ) ) ;
#4337=CARTESIAN_POINT ( 'NONE',  ( 2.835339799623981083, -6.941489812670547543, 3.628068688271650188 ) ) ;
#4343=VECTOR ( 'NONE', #29342, 1000.000000000000114 ) ;
#4351=CARTESIAN_POINT ( 'NONE',  ( 2.255723233588633470, -2.488140745366235418, -7.222632368701038530 ) ) ;
#4359=CARTESIAN_POINT ( 'NONE',  ( 1.937114397841932290, 7.182898292393913309, -10.63710405811926307 ) ) ;
#4364=ORIENTED_EDGE ( 'NONE', *, *, #22030, .F. ) ;
#4371=CARTESIAN_POINT ( 'NONE',  ( 2.241352910868908310, -3.744764251556946366, -6.652881166698550786 ) ) ;
#4383=CIRCLE ( 'NONE', #50029, 12.73084802173761787 ) ;
#4387=CARTESIAN_POINT ( 'NONE',  ( 2.305787727787084407, -5.970480882365190034, -4.792270232040956479 ) ) ;
#4400=CARTESIAN_POINT ( 'NONE',  ( 2.268878695254622713, -1.181158368265835090, -7.551766617933176384 ) ) ;
#4405=CARTESIAN_POINT ( 'NONE',  ( 5.514970785353741078, -0.0005190732562555365340, 0.004694330894494709236 ) ) ;
#4406=EDGE_CURVE ( 'NONE', #2022, #32570, #24005, .T. ) ;
#4409=DIRECTION ( 'NONE',  ( -1.000000000000000000, 0.000000000000000000, 0.000000000000000000 ) ) ;
#4411=CARTESIAN_POINT ( 'NONE',  ( 0.2872850955227767566, -9.251080475901400035, 8.035297825011330275 ) ) ;
#4431=CARTESIAN_POINT ( 'NONE',  ( 5.514624014163232779, 0.0005510299962886269819, 0.004104370840204215644 ) ) ;
#4433=CARTESIAN_POINT ( 'NONE',  ( 0.2657645697724695943, -4.045961170622937253, -11.55867655367625346 ) ) ;
#4451=CONICAL_SURFACE ( 'NONE', #39438, 7.938172270156617749, 1.280189991382167047 ) ;
#4467=CARTESIAN_POINT ( 'NONE',  ( 2.290907136833252977, 6.705538900522879153, -3.684064771923190484 ) ) ;
#4471=VECTOR ( 'NONE', #15929, 1000.000000000000114 ) ;
#4475=( BOUNDED_SURFACE ( )  B_SPLINE_SURFACE ( 3, 1, ( 
 ( #48389, #7809 ),
 ( #43035, #38038 ),
 ( #58345, #7132 ),
 ( #28401, #12767 ) ),
 .UNSPECIFIED., .F., .F., .F. ) 
 B_SPLINE_SURFACE_WITH_KNOTS ( ( 4, 4 ),
 ( 2, 2 ),
 ( 0.000000000000000000, 1.000000000000000000 ),
 ( 0.000000000000000000, 1.000000000000000000 ),
 .UNSPECIFIED. ) 
 GEOMETRIC_REPRESENTATION_ITEM ( )  RATIONAL_B_SPLINE_SURFACE ( (
 ( 1.000000000000000000, 1.000000000000000000),
 ( 0.6933888150995267674, 0.9895912004443193632),
 ( 0.6933888150995267674, 0.9895912004443193632),
 ( 1.000000000000000000, 1.000000000000000000) ) ) 
 REPRESENTATION_ITEM ( '' )  SURFACE ( )  );
#4477=CARTESIAN_POINT ( 'NONE',  ( 2.256373768223415510, 0.1329433694244317177, 7.638251659827612450 ) ) ;
#4480=EDGE_LOOP ( 'NONE', ( #3883, #34523, #31116, #17431 ) ) ;
#4522=CARTESIAN_POINT ( 'NONE',  ( 0.2706063244538030599, 0.1752385892653718358, -12.24670371972918126 ) ) ;
#4529=CARTESIAN_POINT ( 'NONE',  ( 1.719304012341412724, 1.452142814149018690, -12.64775761152637301 ) ) ;
#4548=CARTESIAN_POINT ( 'NONE',  ( 2.368238019614961054, -5.994627685102860148, -4.795442552788027335 ) ) ;
#4553=CARTESIAN_POINT ( 'NONE',  ( 0.9232167919969166414, -4.649596781010333579, -11.56588005394303131 ) ) ;
#4556=CARTESIAN_POINT ( 'NONE',  ( 2.373367633546856759, 6.557448619657638034, 3.994744114396107104 ) ) ;
#4563=CARTESIAN_POINT ( 'NONE',  ( 0.3002738374340793714, -8.050654058169927296, 9.243462099800803244 ) ) ;
#4571=DIRECTION ( 'NONE',  ( 0.000000000000000000, 0.000000000000000000, 1.000000000000000000 ) ) ;
#4573=CARTESIAN_POINT ( 'NONE',  ( 1.375507693220225480, -1.606074886184773787, -12.51366828189718738 ) ) ;
#4579=CARTESIAN_POINT ( 'NONE',  ( 2.245754705088395031, -4.993005209687621182, 5.777230445738523734 ) ) ;
#4591=B_SPLINE_CURVE_WITH_KNOTS ( 'NONE', 3,
 ( #40856, #5280, #55490, #20232, #627, #25550, #35828, #20889, #4298, #14263, #29877, #55154, #24907, #14568, #15565, #40175, #45184, #9938, #34543, #45844, #50834, #40512 ),
 .UNSPECIFIED., .F., .F.,
 ( 4, 3, 3, 3, 3, 3, 3, 4 ),
 ( 1.230521702633870283E-18, 4.449119708436919475E-05, 6.626296329540433730E-05, 8.803456484962549208E-05, 0.0001098060367612784546, 0.0001315774408628484155, 0.0001760698110411127392, 0.0001829697163287819926 ),
 .UNSPECIFIED. ) ;
#4602=CARTESIAN_POINT ( 'NONE',  ( 2.835339799623977086, -4.197472173747748059, 6.612744557053419570 ) ) ;
#4605=DIRECTION ( 'NONE',  ( 0.000000000000000000, 0.000000000000000000, 1.000000000000000000 ) ) ;
#4607=CARTESIAN_POINT ( 'NONE',  ( 1.462291587749944943, -12.08418494300879509, 3.724645088506750135 ) ) ;
#4614=CARTESIAN_POINT ( 'NONE',  ( 2.241451721903215066, -7.528807736569459230, 1.265761656830178161 ) ) ;
#4615=CARTESIAN_POINT ( 'NONE',  ( 0.6511581176971041884, 0.3309006379880005677, -12.37037447926147138 ) ) ;
#4618=AXIS2_PLACEMENT_3D ( 'NONE', #44377, #64655, #19124 ) ;
#4620=EDGE_CURVE ( 'NONE', #45757, #57898, #27170, .T. ) ;
#4624=CARTESIAN_POINT ( 'NONE',  ( 0.2834382757447986845, 0.2027202995056993362, 12.25055062943085282 ) ) ;
#4625=EDGE_CURVE ( 'NONE', #35019, #34453, #21652, .T. ) ;
#4629=CARTESIAN_POINT ( 'NONE',  ( 5.530133899448235191, -0.01550764871776214027, -0.003876417824003597183 ) ) ;
#4633=CARTESIAN_POINT ( 'NONE',  ( 3.152665057734130638, 7.609997527621177760, -2.258875078502145861 ) ) ;
#4636=CARTESIAN_POINT ( 'NONE',  ( 3.031336079628980329, 2.306006909710660580, -7.553623348802083193 ) ) ;
#4642=DIRECTION ( 'NONE',  ( -1.000000000000000000, -0.000000000000000000, -0.000000000000000000 ) ) ;
#4656=FACE_OUTER_BOUND ( 'NONE', #14761, .T. ) ;
#4658=CARTESIAN_POINT ( 'NONE',  ( 2.524535260912970536, 6.580044328001175558, -4.054303386867658787 ) ) ;
#4665=CARTESIAN_POINT ( 'NONE',  ( 0.3002738374340858107, -12.03040002643110284, -2.350339881555072008 ) ) ;
#4680=CARTESIAN_POINT ( 'NONE',  ( 2.556980015513660831, 7.190718924764508913, -2.862731173723810141 ) ) ;
#4687=CARTESIAN_POINT ( 'NONE',  ( 0.3218525148189846363, 11.60666749448229496, -3.964374483810531924 ) ) ;
#4706=CARTESIAN_POINT ( 'NONE',  ( 0.2657645697724702050, 4.045961170623010972, 11.55867655367622326 ) ) ;
#4707=CARTESIAN_POINT ( 'NONE',  ( 2.269879328256726669, -6.692746930935540739, -3.692763753156722561 ) ) ;
#4709=CIRCLE ( 'NONE', #24853, 12.73084802173761787 ) ;
#4714=DIRECTION ( 'NONE',  ( -1.000000000000000000, -0.000000000000000000, -0.000000000000000000 ) ) ;
#4716=CARTESIAN_POINT ( 'NONE',  ( 2.770579946183333142, 6.910873157406283163, -3.639932028439744727 ) ) ;
#4718=CARTESIAN_POINT ( 'NONE',  ( 2.247206125382658737, -3.717496781928407046, -6.670391186503415781 ) ) ;
#4723=CARTESIAN_POINT ( 'NONE',  ( 2.241317068080775243, -4.836852665784620697, 5.906676463196279592 ) ) ;
#4727=CARTESIAN_POINT ( 'NONE',  ( 0.2739690278137274504, -12.09341522051407836, -1.946552041163031488 ) ) ;
#4729=CARTESIAN_POINT ( 'NONE',  ( 2.260457164927183182, -5.941202713844071504, -4.804526096743075847 ) ) ;
#4732=CIRCLE ( 'NONE', #13199, 7.938172270156617749 ) ;
#4736=CARTESIAN_POINT ( 'NONE',  ( 1.719304012339893051, -12.70777170743898310, 0.7661785589588769874 ) ) ;
#4738=ORIENTED_EDGE ( 'NONE', *, *, #37842, .F. ) ;
#4748=CARTESIAN_POINT ( 'NONE',  ( 3.152665057735807075, 3.546019893115007537, -7.102135024646828221 ) ) ;
#4750=CARTESIAN_POINT ( 'NONE',  ( 1.719304012341317467, -0.7661785589597189805, -12.70777170743969009 ) ) ;
#4752=CARTESIAN_POINT ( 'NONE',  ( 2.717984159219611673, -2.397195612260686559, 7.415470774236992746 ) ) ;
#4753=VERTEX_POINT ( 'NONE', #22819 ) ;
#4764=CARTESIAN_POINT ( 'NONE',  ( 0.3057689695767505378, -6.328747727191121442, -10.49983108339466398 ) ) ;
#4765=ORIENTED_EDGE ( 'NONE', *, *, #22860, .F. ) ;
#4769=CARTESIAN_POINT ( 'NONE',  ( 0.3665391374699467075, -8.095513416941292562, 9.237363111276739147 ) ) ;
#4770=CARTESIAN_POINT ( 'NONE',  ( 0.3675815128205894289, -6.367184624550092487, -10.50067073900658521 ) ) ;
#4772=CARTESIAN_POINT ( 'NONE',  ( 0.2739690278137261736, -12.24770428423990687, 0.1830199730326978469 ) ) ;
#4786=EDGE_CURVE ( 'NONE', #33447, #31123, #51200, .T. ) ;
#4792=CARTESIAN_POINT ( 'NONE',  ( 2.440552418640494547, -6.024135401262400435, 4.797131306497546710 ) ) ;
#4795=ORIENTED_EDGE ( 'NONE', *, *, #24188, .T. ) ;
#4801=CARTESIAN_POINT ( 'NONE',  ( 2.251139882113960766, 6.675617500148649519, -3.710800524304753267 ) ) ;
#4803=LINE ( 'NONE', #26054, #64349 ) ;
#4806=CARTESIAN_POINT ( 'NONE',  ( 0.3040950598368152291, -10.74226959800787284, -5.912066680610724489 ) ) ;
#4810=CARTESIAN_POINT ( 'NONE',  ( 0.3218525148189859131, -12.11874253990390038, 1.888670068297610971 ) ) ;
#4811=CARTESIAN_POINT ( 'NONE',  ( 1.937114397841935398, 5.620553190833136092, -11.53912442307249542 ) ) ;
#4814=CARTESIAN_POINT ( 'NONE',  ( 2.241352910868908310, 6.652881166698511706, 3.744764251557016532 ) ) ;
#4817=ORIENTED_EDGE ( 'NONE', *, *, #49370, .T. ) ;
#4830=EDGE_CURVE ( 'NONE', #12988, #46103, #24206, .T. ) ;
#4842=CARTESIAN_POINT ( 'NONE',  ( 2.241317068080790342, 5.906676463195350557, 4.836852665785724703 ) ) ;
#4849=CARTESIAN_POINT ( 'NONE',  ( 0.3474126878361829540, 10.49748369253940972, -6.359473273659596693 ) ) ;
#4859=CARTESIAN_POINT ( 'NONE',  ( 2.242418902651939216, 7.500817491983897689, -1.423836467585266385 ) ) ;
#4865=( BOUNDED_SURFACE ( )  B_SPLINE_SURFACE ( 3, 1, ( 
 ( #30447, #61050 ),
 ( #50745, #25462 ),
 ( #15480, #208 ),
 ( #51424, #11163 ) ),
 .UNSPECIFIED., .F., .F., .F. ) 
 B_SPLINE_SURFACE_WITH_KNOTS ( ( 4, 4 ),
 ( 2, 2 ),
 ( 0.000000000000000000, 1.000000000000000000 ),
 ( 0.000000000000000000, 1.000000000000000000 ),
 .UNSPECIFIED. ) 
 GEOMETRIC_REPRESENTATION_ITEM ( )  RATIONAL_B_SPLINE_SURFACE ( (
 ( 1.000000000000000000, 1.000000000000000000),
 ( 0.9856612449720755231, 0.9999558406602322425),
 ( 0.9856612449720755231, 0.9999558406602322425),
 ( 1.000000000000000000, 1.000000000000000000) ) ) 
 REPRESENTATION_ITEM ( '' )  SURFACE ( )  );
#4870=CARTESIAN_POINT ( 'NONE',  ( 2.705197763288548440, -0.2797837188786904128, 7.783989928191465957 ) ) ;
#4874=CARTESIAN_POINT ( 'NONE',  ( 3.047904605210419948, -6.622084192655463220, -4.313929735713934122 ) ) ;
#4875=CARTESIAN_POINT ( 'NONE',  ( 2.907497136250919656, -7.252103438786975609, 3.021847490615727327 ) ) ;
#4879=CARTESIAN_POINT ( 'NONE',  ( 5.530133899448235191, -0.001124651387254880456, -0.01594518557925637958 ) ) ;
#4885=CARTESIAN_POINT ( 'NONE',  ( 5.514970785353741078, 0.003929719953530069060, 0.002619824551223233922 ) ) ;
#4889=B_SPLINE_CURVE_WITH_KNOTS ( 'NONE', 3,
 ( #27521, #47185, #12891, #22557, #58131, #12237, #21903 ),
 .UNSPECIFIED., .F., .F.,
 ( 4, 3, 4 ),
 ( 8.338150981373126328E-05, 9.911389841680512771E-05, 0.0001667630577588621215 ),
 .UNSPECIFIED. ) ;
#4896=CARTESIAN_POINT ( 'NONE',  ( 0.3610902822527236600, -9.572034936626840462, -7.689482111308950429 ) ) ;
#4903=ORIENTED_EDGE ( 'NONE', *, *, #47319, .F. ) ;
#4908=CARTESIAN_POINT ( 'NONE',  ( 0.3218525148189780305, 11.43947393562877046, 4.423735011438867382 ) ) ;
#4917=CARTESIAN_POINT ( 'NONE',  ( -14.47334165536100059, 0.000000000000000000, 0.000000000000000000 ) ) ;
#4922=CARTESIAN_POINT ( 'NONE',  ( 2.242418902651940993, 7.139616612143419694, -2.704708480794735248 ) ) ;
#4923=CARTESIAN_POINT ( 'NONE',  ( 3.100650473569748211, -4.345221797103555161, 6.622643684997368219 ) ) ;
#4925=CARTESIAN_POINT ( 'NONE',  ( 0.3474126878361755710, 11.61929161290146162, 3.953748424960682240 ) ) ;
#4927=CARTESIAN_POINT ( 'NONE',  ( 2.297017764050091948, 7.651182381906872720, -0.1647869190092008940 ) ) ;
#4929=CARTESIAN_POINT ( 'NONE',  ( 2.241449424704146320, 5.887589908049645437, 4.860179885671820799 ) ) ;
#4938=CARTESIAN_POINT ( 'NONE',  ( 5.520433897694421610, 0.009283255140285181714, 0.01186170453199828639 ) ) ;
#4943=CARTESIAN_POINT ( 'NONE',  ( 2.245754705088395475, -7.499730934370265167, -1.435454129948283031 ) ) ;
#4949=CARTESIAN_POINT ( 'NONE',  ( 2.844750968615495257, 2.364925124214210861, -7.470159816919067275 ) ) ;
#4953=CARTESIAN_POINT ( 'NONE',  ( 1.452237505248552996, 4.880303821311168022, -11.67686475128074797 ) ) ;
#4955=VERTEX_POINT ( 'NONE', #46686 ) ;
#4959=EDGE_CURVE ( 'NONE', #35685, #7749, #51099, .T. ) ;
#4970=CARTESIAN_POINT ( 'NONE',  ( 2.245754705088392811, -6.556487589645213276, -3.913944702466338299 ) ) ;
#4972=CARTESIAN_POINT ( 'NONE',  ( 5.536195898058073439, -0.001224473329857922455, 0.008411485181669254088 ) ) ;
#4977=CARTESIAN_POINT ( 'NONE',  ( 1.634816307076184971, -12.68239325670201900, -0.7191532042400472502 ) ) ;
#4979=CARTESIAN_POINT ( 'NONE',  ( 2.507146904658101416, -2.437115546363171958, -7.328382489803296984 ) ) ;
#4980=ORIENTED_EDGE ( 'NONE', *, *, #3434, .T. ) ;
#4983=EDGE_CURVE ( 'NONE', #42237, #25922, #17018, .T. ) ;
#5000=VERTEX_POINT ( 'NONE', #23732 ) ;
#5003=CARTESIAN_POINT ( 'NONE',  ( 2.524535260911856316, -5.776056274541021551, 5.135322114975514829 ) ) ;
#5005=CARTESIAN_POINT ( 'NONE',  ( 2.931247277082685621, -0.9994150891045774365, -7.800615791174665858 ) ) ;
#5009=CARTESIAN_POINT ( 'NONE',  ( 2.268878695252931621, -2.474564429974762891, -7.231932316092929192 ) ) ;
#5014=CARTESIAN_POINT ( 'NONE',  ( 1.719304012341584365, 10.22720798541559439, -7.581471372738991299 ) ) ;
#5015=CARTESIAN_POINT ( 'NONE',  ( 2.259025283528079076, -6.683966451873007308, -3.701170455111045587 ) ) ;
#5019=CARTESIAN_POINT ( 'NONE',  ( 2.257661810676421688, -7.638648121130933610, 0.1348365785570732611 ) ) ;
#5021=ORIENTED_EDGE ( 'NONE', *, *, #53336, .F. ) ;
#5022=CARTESIAN_POINT ( 'NONE',  ( 0.2801149460245124789, 10.70654700624303324, 5.954809120985752102 ) ) ;
#5025=CARTESIAN_POINT ( 'NONE',  ( 2.276198483116797622, -3.688810392808719030, -6.697332984100004438 ) ) ;
#5036=CARTESIAN_POINT ( 'NONE',  ( 0.2647959493198560055, -12.08462848595693373, -1.981611532097670381 ) ) ;
#5040=CARTESIAN_POINT ( 'NONE',  ( 2.268878695253351285, 0.1481365927654600123, -7.642144312464377087 ) ) ;
#5048=CARTESIAN_POINT ( 'NONE',  ( 5.514970785353741078, -0.002619824551223732222, -0.003929719953530097683 ) ) ;
#5055=B_SPLINE_CURVE_WITH_KNOTS ( 'NONE', 3,
 ( #60558, #394, #34310, #30617, #9045, #50929, #44594, #34625, #20669, #24669 ),
 .UNSPECIFIED., .F., .F.,
 ( 4, 3, 3, 4 ),
 ( 1.226634733346699349E-18, 6.607638129004437383E-05, 9.911389841680539876E-05, 0.0001667630577588623112 ),
 .UNSPECIFIED. ) ;
#5062=CARTESIAN_POINT ( 'NONE',  ( 2.969415267404556413, -2.326350273511729849, 7.525730903320692278 ) ) ;
#5064=VERTEX_POINT ( 'NONE', #14683 ) ;
#5071=ORIENTED_EDGE ( 'NONE', *, *, #11926, .F. ) ;
#5072=CARTESIAN_POINT ( 'NONE',  ( 1.549075743845332420, -10.12891450359508916, 7.618376504787018888 ) ) ;
#5086=EDGE_LOOP ( 'NONE', ( #24967, #20366, #22670, #24591 ) ) ;
#5087=CARTESIAN_POINT ( 'NONE',  ( 3.152665057736252940, 7.609997527622067715, 2.258875078500286016 ) ) ;
#5092=CARTESIAN_POINT ( 'NONE',  ( 0.3164563675027597944, 8.065346584422250942, 9.237806174449792351 ) ) ;
#5094=CARTESIAN_POINT ( 'NONE',  ( 0.2646305136544065406, -11.46223899740597219, -4.312539723326248797 ) ) ;
#5097=EDGE_CURVE ( 'NONE', #15837, #7744, #9711, .T. ) ;
#5103=CARTESIAN_POINT ( 'NONE',  ( 1.287602823385394668, 12.28793447239681136, 2.727479899219913850 ) ) ;
#5122=CARTESIAN_POINT ( 'NONE',  ( 2.297017764050092392, 0.1647869190091743041, 7.651182381906873609 ) ) ;
#5125=ORIENTED_EDGE ( 'NONE', *, *, #9814, .T. ) ;
#5132=B_SPLINE_CURVE_WITH_KNOTS ( 'NONE', 3,
 ( #41725, #21796, #32062, #2147, #16470, #6488, #42044, #37049, #31729, #36741, #7128, #16778, #31425, #47392, #58019, #42348, #57355, #26429, #47062 ),
 .UNSPECIFIED., .F., .F.,
 ( 4, 3, 3, 3, 3, 3, 4 ),
 ( 8.619918672207806447E-18, 4.457896483014664354E-05, 6.639290541541868914E-05, 8.820687556478665030E-05, 0.0001100173248778875862, 0.0001545671401658071692, 0.0001830328308068590647 ),
 .UNSPECIFIED. ) ;
#5139=CARTESIAN_POINT ( 'NONE',  ( 5.516018279890452902, -0.006629829924290984305, -0.001397286410094293998 ) ) ;
#5143=CARTESIAN_POINT ( 'NONE',  ( 0.2653519890518156732, -12.06015162724940737, -2.126521162241181706 ) ) ;
#5145=EDGE_CURVE ( 'NONE', #44559, #34363, #9963, .T. ) ;
#5149=ORIENTED_EDGE ( 'NONE', *, *, #55234, .F. ) ;
#5151=CARTESIAN_POINT ( 'NONE',  ( 0.2759803524722280188, 9.504501710971712924, -7.727919584673335507 ) ) ;
#5159=ORIENTED_EDGE ( 'NONE', *, *, #685, .F. ) ;
#5162=VERTEX_POINT ( 'NONE', #7027 ) ;
#5164=ORIENTED_EDGE ( 'NONE', *, *, #19774, .T. ) ;
#5183=DIRECTION ( 'NONE',  ( 0.3865475372811021382, -0.8082200352954679312, 0.4442537292684300421 ) ) ;
#5198=CARTESIAN_POINT ( 'NONE',  ( 3.047904605210279616, 6.622084192655491641, 4.313929735713805336 ) ) ;
#5205=AXIS2_PLACEMENT_3D ( 'NONE', #65015, #12844, #53438 ) ;
#5210=CARTESIAN_POINT ( 'NONE',  ( 3.152665057735657861, -7.609997527621795932, -2.258875078500884204 ) ) ;
#5211=ORIENTED_EDGE ( 'NONE', *, *, #62630, .F. ) ;
#5220=CARTESIAN_POINT ( 'NONE',  ( 2.258463476536645587, -5.014277205346500565, 5.764393264552618135 ) ) ;
#5224=CARTESIAN_POINT ( 'NONE',  ( 3.152665057735980714, 1.848755561853925533, 7.719888720907654545 ) ) ;
#5245=EDGE_CURVE ( 'NONE', #31059, #17057, #39276, .T. ) ;
#5247=( BOUNDED_SURFACE ( )  B_SPLINE_SURFACE ( 3, 1, ( 
 ( #35037, #65627 ),
 ( #35705, #56002 ),
 ( #9788, #30072 ),
 ( #51026, #50385 ) ),
 .UNSPECIFIED., .F., .F., .F. ) 
 B_SPLINE_SURFACE_WITH_KNOTS ( ( 4, 4 ),
 ( 2, 2 ),
 ( 0.000000000000000000, 1.000000000000000000 ),
 ( 0.000000000000000000, 1.000000000000000000 ),
 .UNSPECIFIED. ) 
 GEOMETRIC_REPRESENTATION_ITEM ( )  RATIONAL_B_SPLINE_SURFACE ( (
 ( 1.000000000000000000, 1.000000000000000000),
 ( 0.9942764183789327692, 0.8450855930916585379),
 ( 0.9942764183789327692, 0.8450855930916585379),
 ( 1.000000000000000000, 1.000000000000000000) ) ) 
 REPRESENTATION_ITEM ( '' )  SURFACE ( )  );
#5248=CARTESIAN_POINT ( 'NONE',  ( 2.266490820343223245, 7.641399530653804284, -0.1453321357832998706 ) ) ;
#5251=CARTESIAN_POINT ( 'NONE',  ( 1.937114397841932290, -10.63710405811928794, -7.182898292393876893 ) ) ;
#5259=ADVANCED_FACE ( 'NONE', ( #12999 ), #64091, .F. ) ;
#5263=CARTESIAN_POINT ( 'NONE',  ( 5.515539859299206427, -0.003740028639278314155, 0.004759416711442216591 ) ) ;
#5264=CARTESIAN_POINT ( 'NONE',  ( 1.452237505248555660, 1.611965288198897506, -12.55261342181973738 ) ) ;
#5267=EDGE_CURVE ( 'NONE', #41256, #28847, #36919, .T. ) ;
#5268=ORIENTED_EDGE ( 'NONE', *, *, #4983, .T. ) ;
#5275=CARTESIAN_POINT ( 'NONE',  ( 2.269879328256730666, 2.753278809616109157, 7.130835954829854550 ) ) ;
#5276=VERTEX_POINT ( 'NONE', #8340 ) ;
#5280=CARTESIAN_POINT ( 'NONE',  ( 0.2647959493198550618, -0.1469673141000716610, -12.24513905663510904 ) ) ;
#5283=CARTESIAN_POINT ( 'NONE',  ( 0.3106921474978494579, -11.60027394202201378, 3.971572160646712479 ) ) ;
#5285=B_SPLINE_CURVE_WITH_KNOTS ( 'NONE', 3,
 ( #28824, #39442, #54441, #18554, #34123, #54765, #60383, #59105, #8872, #65039, #34764, #33797, #40091, #59743, #35092, #64072, #49461, #43793, #24157 ),
 .UNSPECIFIED., .F., .F.,
 ( 4, 3, 3, 3, 3, 3, 4 ),
 ( 5.962126228860470552E-18, 2.825908398831331847E-05, 4.208813692484108843E-05, 5.591713746944027057E-05, 6.279584083232090871E-05, 9.105792820296878360E-05, 0.0001153131102488872209 ),
 .UNSPECIFIED. ) ;
#5295=CARTESIAN_POINT ( 'NONE',  ( 1.633930747253262705, 9.253127167384784357, -8.702439996575780157 ) ) ;
#5296=CARTESIAN_POINT ( 'NONE',  ( 0.3665391374699464300, -7.691255657244227883, -9.576575648339098024 ) ) ;
#5297=B_SPLINE_CURVE_WITH_KNOTS ( 'NONE', 3,
 ( #19094, #23775, #8797, #19434, #9111, #58704, #28737 ),
 .UNSPECIFIED., .F., .F.,
 ( 4, 3, 4 ),
 ( 0.000000000000000000, 0.001700533616330726855, 0.005002426799376749611 ),
 .UNSPECIFIED. ) ;
#5300=CARTESIAN_POINT ( 'NONE',  ( 1.109979610370654735, -11.08130463534499910, 5.843815872356589836 ) ) ;
#5304=EDGE_CURVE ( 'NONE', #5000, #22716, #18703, .T. ) ;
#5307=CARTESIAN_POINT ( 'NONE',  ( 2.350038591457611847, -6.324706260080944276, -8.533611140766819148 ) ) ;
#5308=VERTEX_POINT ( 'NONE', #52491 ) ;
#5311=CARTESIAN_POINT ( 'NONE',  ( 3.031336079629501690, 3.088871717871464639, 7.268683861177206218 ) ) ;
#5313=ORIENTED_EDGE ( 'NONE', *, *, #57217, .T. ) ;
#5319=ORIENTED_EDGE ( 'NONE', *, *, #60575, .F. ) ;
#5324=ADVANCED_FACE ( 'NONE', ( #6924 ), #29803, .T. ) ;
#5330=CARTESIAN_POINT ( 'NONE',  ( 2.241311220309522234, -2.523702734785425061, -7.205198716057754638 ) ) ;
#5341=AXIS2_PLACEMENT_3D ( 'NONE', #32504, #53138, #2629 ) ;
#5342=ORIENTED_EDGE ( 'NONE', *, *, #61876, .F. ) ;
#5343=ADVANCED_FACE ( 'NONE', ( #32490 ), #59425, .F. ) ;
#5352=CARTESIAN_POINT ( 'NONE',  ( 2.241528039335008327, 7.515727438420007900, 1.341200777944175027 ) ) ;
#5355=CARTESIAN_POINT ( 'NONE',  ( 1.633930747253262261, 5.718685543473208455, -11.34237452761398757 ) ) ;
#5360=CARTESIAN_POINT ( 'NONE',  ( 0.2801149460245135892, 12.24954625471156255, -0.1962575296605837960 ) ) ;
#5361=CARTESIAN_POINT ( 'NONE',  ( 2.241449424704146320, 2.668712484599962131, 7.152834201978770068 ) ) ;
#5362=CARTESIAN_POINT ( 'NONE',  ( 0.2653519991613847440, -2.148211862902992486, 12.05632699103097139 ) ) ;
#5369=VERTEX_POINT ( 'NONE', #52151 ) ;
#5372=DIRECTION ( 'NONE',  ( -1.000000000000000000, -0.000000000000000000, -0.000000000000000000 ) ) ;
#5373=CARTESIAN_POINT ( 'NONE',  ( 2.259830038566062793, -1.190932096468327650, -7.547174990768978020 ) ) ;
#5376=EDGE_LOOP ( 'NONE', ( #57279, #57840, #46225, #61713, #12806, #30994, #19463, #65482, #2347, #39806, #46203, #10129, #14736, #61394, #45973, #8508, #15397, #43632, #39988, #9520, #26057, #892, #51937, #22174, #49693, #32674, #1732, #24673, #5667, #22562, #17321, #33439, #23956, #45238, #2474, #22871, #875, #13979, #31224, #21692, #1653, #16822, #65304, #53043, #61555, #30576, #43178, #59131, #43652, #3164, #30861, #9813, #7442, #40855, #64714, #46141, #10389, #56317, #41397, #47915, #8913, #31584, #14679, #32001, #1133, #11489, #62606, #37301, #17912, #40627, #10640, #14770, #49210, #22658, #61141, #43679, #60172, #2851, #17419, #8160, #63061, #20158, #19354, #54482, #45603, #64549, #63230, #47257, #58445, #38656, #38678, #49185, #10903, #39271, #24580, #10437, #58646, #32682, #58413, #28703, #18069, #34789, #30047, #9065, #59694, #3496, #64925, #27643, #58910, #4795, #8637, #32656 ) ) ;
#5377=B_SPLINE_CURVE_WITH_KNOTS ( 'NONE', 3,
 ( #64901, #28683, #8093, #53967, #8407, #38989, #13074, #59284, #49335, #13708, #14038, #49638, #43989, #38676, #24040, #28046, #44611, #48347, #7764 ),
 .UNSPECIFIED., .F., .F.,
 ( 4, 3, 3, 3, 3, 3, 4 ),
 ( 6.447129612864634281E-18, 2.825908398830911041E-05, 4.208813692483603334E-05, 5.591713746943527646E-05, 6.279584083231498626E-05, 9.105792820296256299E-05, 0.0001153131102488861502 ),
 .UNSPECIFIED. ) ;
#5378=CARTESIAN_POINT ( 'NONE',  ( 0.3665391374699464300, 8.095513416941352958, -9.237363111276685856 ) ) ;
#5387=CARTESIAN_POINT ( 'NONE',  ( 2.491965175174155167, -2.439431489055726932, 7.322278065136082148 ) ) ;
#5390=EDGE_CURVE ( 'NONE', #7766, #4955, #27384, .T. ) ;
#5403=CARTESIAN_POINT ( 'NONE',  ( 0.2647959493198550618, -12.24513905663510727, 0.1469673141001137107 ) ) ;
#5405=CARTESIAN_POINT ( 'NONE',  ( 2.241317068080775687, 5.789053609344685825, -4.977030124433445835 ) ) ;
#5409=VERTEX_POINT ( 'NONE', #6273 ) ;
#5412=CARTESIAN_POINT ( 'NONE',  ( 0.3160775863651066331, -4.419114254409969966, 11.43919651388224068 ) ) ;
#5415=B_SPLINE_CURVE_WITH_KNOTS ( 'NONE', 3,
 ( #5224, #25491, #45782, #883, #20518, #40801, #15509, #56077, #30792, #7499, #52749, #63037, #27792, #31471, #48095, #57081 ),
 .UNSPECIFIED., .F., .F.,
 ( 4, 3, 3, 3, 3, 4 ),
 ( 2.855882139221416949E-15, 0.0002126834539179672833, 0.0004253519300366195768, 0.0006380165497224064147, 0.0007442707582428126139, 0.0009453531351418871694 ),
 .UNSPECIFIED. ) ;
#5417=CONICAL_SURFACE ( 'NONE', #15963, 7.938172270156617749, 1.280189991382167047 ) ;
#5420=CARTESIAN_POINT ( 'NONE',  ( 0.3632410797595235774, 8.092233745354631580, 9.235006602299375089 ) ) ;
#5421=CARTESIAN_POINT ( 'NONE',  ( 1.109979610372407999, 11.92772269523445772, -3.830786822172277617 ) ) ;
#5443=ADVANCED_FACE ( 'NONE', ( #18859 ), #22355, .T. ) ;
#5449=CARTESIAN_POINT ( 'NONE',  ( 2.889800649504073782, 4.732281052280366218, -3.882893708501999885 ) ) ;
#5452=DIRECTION ( 'NONE',  ( 0.3865475372811021937, 0.6075346789811209014, -0.6938894834606021966 ) ) ;
#5453=CARTESIAN_POINT ( 'NONE',  ( 1.719304012339893051, -12.70777170743897422, -0.7661785589590540679 ) ) ;
#5459=( BOUNDED_SURFACE ( )  B_SPLINE_SURFACE ( 3, 1, ( 
 ( #24923, #35842 ),
 ( #55166, #20592 ),
 ( #10263, #65774 ),
 ( #4972, #40868 ) ),
 .UNSPECIFIED., .F., .F., .F. ) 
 B_SPLINE_SURFACE_WITH_KNOTS ( ( 4, 4 ),
 ( 2, 2 ),
 ( 0.000000000000000000, 1.000000000000000000 ),
 ( 0.000000000000000000, 1.000000000000000000 ),
 .UNSPECIFIED. ) 
 GEOMETRIC_REPRESENTATION_ITEM ( )  RATIONAL_B_SPLINE_SURFACE ( (
 ( 1.000000000000000000, 1.000000000000000000),
 ( 0.6933888150995267674, 0.9895912004443193632),
 ( 0.6933888150995267674, 0.9895912004443193632),
 ( 1.000000000000000000, 1.000000000000000000) ) ) 
 REPRESENTATION_ITEM ( '' )  SURFACE ( )  );
#5460=LINE ( 'NONE', #63251, #16223 ) ;
#5463=VERTEX_POINT ( 'NONE', #18561 ) ;
#5464=CARTESIAN_POINT ( 'NONE',  ( 2.263328370261531663, -6.545781832005213907, 3.943189046766310213 ) ) ;
#5475=CARTESIAN_POINT ( 'NONE',  ( 1.948354844647347983, 10.70340528294774529, 5.347695345040441417 ) ) ;
#5476=CARTESIAN_POINT ( 'NONE',  ( 0.2652384529303112304, 6.065769141714355328, -10.63836770010960109 ) ) ;
#5478=CARTESIAN_POINT ( 'NONE',  ( 0.2653141334712560417, 4.147025708564583191, -11.52266042163702942 ) ) ;
#5482=CARTESIAN_POINT ( 'NONE',  ( 0.3665391374699472626, 8.095513416941232165, 9.237363111276792438 ) ) ;
#5484=CARTESIAN_POINT ( 'NONE',  ( 0.3675815128205912052, -11.44679196252406506, -4.447030445008294919 ) ) ;
#5491=CARTESIAN_POINT ( 'NONE',  ( 0.2706063244538075008, 9.494160524941802848, -7.737788863017200924 ) ) ;
#5500=CARTESIAN_POINT ( 'NONE',  ( 0.3401186441510237191, 12.03768714635924830, 2.382124782498401316 ) ) ;
#5506=CARTESIAN_POINT ( 'NONE',  ( 5.516018279890452902, 0.006629829924290471695, -0.001397286410094441449 ) ) ;
#5507=CARTESIAN_POINT ( 'NONE',  ( 1.459561108993335354, -10.62073135189157291, 6.861308540877669060 ) ) ;
#5509=CARTESIAN_POINT ( 'NONE',  ( 1.372161826076379043, -12.30755118281447658, 2.769012792636629250 ) ) ;
#5510=FACE_OUTER_BOUND ( 'NONE', #15434, .T. ) ;
#5525=EDGE_CURVE ( 'NONE', #24280, #25736, #8542, .T. ) ;
#5527=CARTESIAN_POINT ( 'NONE',  ( 1.109979610372296310, 2.646302643133297217, -12.24510427445534511 ) ) ;
#5531=CARTESIAN_POINT ( 'NONE',  ( 0.2648978790185584908, 10.53870023327863770, 6.237101853238585569 ) ) ;
#5538=VERTEX_POINT ( 'NONE', #32813 ) ;
#5543=EDGE_LOOP ( 'NONE', ( #63570, #57890, #34012, #51648 ) ) ;
#5553=ORIENTED_EDGE ( 'NONE', *, *, #54999, .F. ) ;
#5557=CARTESIAN_POINT ( 'NONE',  ( 0.2650492433740052611, -7.786978278830034128, 9.451472485870532125 ) ) ;
#5560=CARTESIAN_POINT ( 'NONE',  ( 2.241536586108912488, 2.605228657247447899, -7.176205604390183623 ) ) ;
#5567=VECTOR ( 'NONE', #17027, 999.9999999999998863 ) ;
#5568=CARTESIAN_POINT ( 'NONE',  ( 0.3537226245948361103, 11.44347094181051894, 4.442821955543838186 ) ) ;
#5569=VECTOR ( 'NONE', #49516, 1000.000000000000114 ) ;
#5576=EDGE_LOOP ( 'NONE', ( #56015, #24769, #57051, #49544 ) ) ;
#5577=CARTESIAN_POINT ( 'NONE',  ( 2.244591118396556784, -7.211060161907631105, -2.510215291309289665 ) ) ;
#5585=EDGE_CURVE ( 'NONE', #27385, #33979, #64391, .T. ) ;
#5586=CARTESIAN_POINT ( 'NONE',  ( 2.244591118396559448, 7.137527852925285465, -2.712243649838633530 ) ) ;
#5589=CARTESIAN_POINT ( 'NONE',  ( 0.2650492594609250019, -10.66007682546621282, 6.027447650185331796 ) ) ;
#5591=ORIENTED_EDGE ( 'NONE', *, *, #3804, .T. ) ;
#5597=FACE_OUTER_BOUND ( 'NONE', #12326, .T. ) ;
#5599=CARTESIAN_POINT ( 'NONE',  ( 0.2958664285830420737, -10.72286791615085022, -5.936220506376345796 ) ) ;
#5609=CARTESIAN_POINT ( 'NONE',  ( 0.2646305136544072623, -0.1321451301296985015, -12.24595685781654808 ) ) ;
#5610=CARTESIAN_POINT ( 'NONE',  ( 0.2653141617320999290, -12.06772699408310423, 2.083144498805234335 ) ) ;
#5611=CARTESIAN_POINT ( 'NONE',  ( 2.305787727787084407, 2.461236246751170142, -7.249469779319884566 ) ) ;
#5617=CARTESIAN_POINT ( 'NONE',  ( 3.092491956585937452, -0.9322768171840393192, 7.863103788722447973 ) ) ;
#5621=DIRECTION ( 'NONE',  ( 0.000000000000000000, -1.000000000000000000, 0.000000000000000000 ) ) ;
#5630=VECTOR ( 'NONE', #35538, 1000.000000000000114 ) ;
#5631=ORIENTED_EDGE ( 'NONE', *, *, #34760, .T. ) ;
#5636=CARTESIAN_POINT ( 'NONE',  ( 2.251139882113958546, -6.551456272498873190, -3.925854078924290391 ) ) ;
#5641=AXIS2_PLACEMENT_3D ( 'NONE', #30010, #20365, #56260 ) ;
#5642=CARTESIAN_POINT ( 'NONE',  ( 1.549075743846936026, 11.29795072957594648, -5.743768701986331493 ) ) ;
#5645=CARTESIAN_POINT ( 'NONE',  ( 2.440552418640498988, -2.447453236303777313, -7.301551120181787979 ) ) ;
#5648=CARTESIAN_POINT ( 'NONE',  ( 0.3218525148189825269, 10.49750909897053042, 6.342972338926835540 ) ) ;
#5652=CARTESIAN_POINT ( 'NONE',  ( 2.990245332647884613, -5.049055049623163427, -6.814589384235021363 ) ) ;
#5660=ORIENTED_EDGE ( 'NONE', *, *, #57551, .T. ) ;
#5664=ORIENTED_EDGE ( 'NONE', *, *, #32779, .F. ) ;
#5667=ORIENTED_EDGE ( 'NONE', *, *, #56920, .T. ) ;
#5669=LINE ( 'NONE', #35232, #29870 ) ;
#5670=CARTESIAN_POINT ( 'NONE',  ( 1.462291587748162813, 11.65117843858566893, 4.914320681884643882 ) ) ;
#5672=CARTESIAN_POINT ( 'NONE',  ( 5.514970785353741078, -0.001117786416802585238, -0.004588761610585022008 ) ) ;
#5673=CARTESIAN_POINT ( 'NONE',  ( 2.290907136833252089, 2.768669624188787814, -7.132394668149358630 ) ) ;
#5676=CARTESIAN_POINT ( 'NONE',  ( 2.253265082352140514, -2.491579069691978621, -7.220580418433788061 ) ) ;
#5677=ORIENTED_EDGE ( 'NONE', *, *, #9156, .T. ) ;
#5679=B_SPLINE_CURVE_WITH_KNOTS ( 'NONE', 3,
 ( #37249, #43220, #52578, #47568, #1375, #36608, #22281, #42548, #62852, #57896, #56912, #12304, #52881, #7313, #22634, #33902 ),
 .UNSPECIFIED., .F., .F.,
 ( 4, 3, 3, 3, 3, 4 ),
 ( 5.963111948670274387E-19, 0.0003017745587525298007, 0.0006035491769808827393, 0.0009053241094668298006, 0.001207275924539980873, 0.001510325902532946895 ),
 .UNSPECIFIED. ) ;
#5689=ORIENTED_EDGE ( 'NONE', *, *, #53219, .F. ) ;
#5695=CARTESIAN_POINT ( 'NONE',  ( 2.255723233588630805, -3.704537245405363777, -6.680843247642031635 ) ) ;
#5698=CARTESIAN_POINT ( 'NONE',  ( 1.719304012341582588, 5.690355757825640737, -11.38834240361563488 ) ) ;
#5704=FACE_OUTER_BOUND ( 'NONE', #6821, .T. ) ;
#5707=CARTESIAN_POINT ( 'NONE',  ( 1.452237505248555660, 12.55261342181975515, 1.611965288198772717 ) ) ;
#5708=CARTESIAN_POINT ( 'NONE',  ( 2.241311220309554209, 0.09281826062106607322, -7.633829235838274663 ) ) ;
#5714=CARTESIAN_POINT ( 'NONE',  ( 5.514970785353741078, -0.001897634820904983786, -0.004324946436530298539 ) ) ;
#5718=CARTESIAN_POINT ( 'NONE',  ( 0.2648978790185619880, -1.996248716311710414, 12.08224454301447892 ) ) ;
#5733=CARTESIAN_POINT ( 'NONE',  ( 2.247112776671929879, 4.818685025479959805, -5.923998863713823226 ) ) ;
#5736=CARTESIAN_POINT ( 'NONE',  ( 5.514970785353741078, 0.004713149585127261558, 0.0003039746380524470729 ) ) ;
#5745=CARTESIAN_POINT ( 'NONE',  ( 2.251152103363644574, 3.926807817126193090, 6.550893877460167047 ) ) ;
#5748=CARTESIAN_POINT ( 'NONE',  ( 0.2872850955227750913, -12.25172867346922878, 0.2089153415334442931 ) ) ;
#5754=EDGE_CURVE ( 'NONE', #25736, #49400, #58252, .T. ) ;
#5758=CARTESIAN_POINT ( 'NONE',  ( 2.770579946183337583, -5.784075095088754281, -5.249166435139423825 ) ) ;
#5759=AXIS2_PLACEMENT_3D ( 'NONE', #27581, #62831, #2339 ) ;
#5761=CARTESIAN_POINT ( 'NONE',  ( 0.3341166715381256869, 8.078283863465498982, 9.234320413907830982 ) ) ;
#5763=CARTESIAN_POINT ( 'NONE',  ( 0.4626703367448859461, 11.66326339726757766, -3.943760108616669591 ) ) ;
#5764=CARTESIAN_POINT ( 'NONE',  ( 0.2653141617321022605, -9.352766656400001821, -7.905395731875590748 ) ) ;
#5766=CIRCLE ( 'NONE', #39573, 7.938172270156617749 ) ;
#5772=CARTESIAN_POINT ( 'NONE',  ( 2.653899356899243944, 0.2611590963044465585, 7.767552767343915754 ) ) ;
#5781=VECTOR ( 'NONE', #34944, 1000.000000000000114 ) ;
#5784=CARTESIAN_POINT ( 'NONE',  ( 0.2652384529303124516, 2.061422456317187457, -12.07141085622970955 ) ) ;
#5787=B_SPLINE_CURVE_WITH_KNOTS ( 'NONE', 3,
 ( #60018, #55346, #14113, #54710, #64331, #9131, #55011, #24420, #64983, #14436 ),
 .UNSPECIFIED., .F., .F.,
 ( 4, 3, 3, 4 ),
 ( 9.351243737687475743E-19, 6.607638129004469909E-05, 9.911389841680516837E-05, 0.0001667630577588622570 ),
 .UNSPECIFIED. ) ;
#5790=ORIENTED_EDGE ( 'NONE', *, *, #44875, .F. ) ;
#5795=CARTESIAN_POINT ( 'NONE',  ( 0.6511581176954559513, 10.54760823437294803, 6.471755598256069497 ) ) ;
#5799=CARTESIAN_POINT ( 'NONE',  ( 0.3040950598368144520, 10.49113473328030821, 6.347045025870802881 ) ) ;
#5806=ORIENTED_EDGE ( 'NONE', *, *, #50812, .T. ) ;
#5807=B_SPLINE_CURVE_WITH_KNOTS ( 'NONE', 3,
 ( #59902, #49288, #45565, #35255, #14632, #54257, #39926, #14965, #55562, #54898, #29608, #9021, #19668, #60210, #24642, #9322 ),
 .UNSPECIFIED., .F., .F.,
 ( 4, 3, 3, 3, 3, 4 ),
 ( 1.463672932855430986E-18, 0.0003017745587525266565, 0.0006035491769808764510, 0.0009053241094668187418, 0.001207275924539138231, 0.001510325902531263996 ),
 .UNSPECIFIED. ) ;
#5814=CARTESIAN_POINT ( 'NONE',  ( 3.152665057736049103, -0.4801242025610908959, -7.923639299008895520 ) ) ;
#5823=CARTESIAN_POINT ( 'NONE',  ( 2.241451721903216399, -2.668222118333498205, 7.153019588493063630 ) ) ;
#5826=ORIENTED_EDGE ( 'NONE', *, *, #60895, .F. ) ;
#5832=CARTESIAN_POINT ( 'NONE',  ( 2.261269890822070749, -7.639767381742377239, -0.1394916642590645905 ) ) ;
#5834=CARTESIAN_POINT ( 'NONE',  ( 2.639814597422740938, 7.689608172406201092, -1.095525832903406327 ) ) ;
#5835=CARTESIAN_POINT ( 'NONE',  ( 1.719304012338836563, -2.961219984258077087, 12.38166659046417095 ) ) ;
#5836=CARTESIAN_POINT ( 'NONE',  ( 0.2958664285830415741, -12.02992237133199893, 2.345117904768581063 ) ) ;
#5837=ADVANCED_FACE ( 'NONE', ( #48681 ), #410, .F. ) ;
#5848=CARTESIAN_POINT ( 'NONE',  ( 0.3665391374699472626, -6.368473106897056368, -10.50279796150443268 ) ) ;
#5852=( BOUNDED_SURFACE ( )  B_SPLINE_SURFACE ( 3, 1, ( 
 ( #10771, #21069 ),
 ( #16088, #31391 ),
 ( #22382, #57987 ),
 ( #46680, #32667 ) ),
 .UNSPECIFIED., .F., .F., .F. ) 
 B_SPLINE_SURFACE_WITH_KNOTS ( ( 4, 4 ),
 ( 2, 2 ),
 ( 0.000000000000000000, 1.000000000000000000 ),
 ( 0.000000000000000000, 1.000000000000000000 ),
 .UNSPECIFIED. ) 
 GEOMETRIC_REPRESENTATION_ITEM ( )  RATIONAL_B_SPLINE_SURFACE ( (
 ( 1.000000000000000000, 1.000000000000000000),
 ( 0.6933888150995267674, 0.9895912004443193632),
 ( 0.6933888150995267674, 0.9895912004443193632),
 ( 1.000000000000000000, 1.000000000000000000) ) ) 
 REPRESENTATION_ITEM ( '' )  SURFACE ( )  );
#5857=CARTESIAN_POINT ( 'NONE',  ( 2.990245332647840204, 8.426135047918846155, -0.9653152459622572623 ) ) ;
#5860=EDGE_CURVE ( 'NONE', #39632, #33098, #15043, .T. ) ;
#5864=CARTESIAN_POINT ( 'NONE',  ( 0.9296196016850440946, 2.573053270831450856, -12.19921892950026532 ) ) ;
#5865=FACE_BOUND ( 'NONE', #14078, .T. ) ;
#5885=ORIENTED_EDGE ( 'NONE', *, *, #55911, .F. ) ;
#5893=CARTESIAN_POINT ( 'NONE',  ( 0.4626703367448379844, -1.858541096401079340, -12.17089897506941831 ) ) ;
#5895=EDGE_CURVE ( 'NONE', #7261, #5463, #65502, .T. ) ;
#5901=CARTESIAN_POINT ( 'NONE',  ( 2.261269890822072082, -5.017604628138437661, 5.762737836065097596 ) ) ;
#5916=ADVANCED_FACE ( 'NONE', ( #44993 ), #48552, .T. ) ;
#5921=CARTESIAN_POINT ( 'NONE',  ( 0.2646305136544065406, -7.972778379581612285, 9.296005949277198255 ) ) ;
#5922=VECTOR ( 'NONE', #58220, 1000.000000000000000 ) ;
#5926=CARTESIAN_POINT ( 'NONE',  ( 2.258463476536645587, 7.499249607179738319, 1.460294809170969099 ) ) ;
#5944=DIRECTION ( 'NONE',  ( -1.000000000000000000, -0.000000000000000000, -0.000000000000000000 ) ) ;
#5945=CARTESIAN_POINT ( 'NONE',  ( 1.104777566491146557, -9.895624035730012480, -7.679758239385240159 ) ) ;
#5946=CARTESIAN_POINT ( 'NONE',  ( 2.241352910868908310, 2.532612177304540246, -7.202080440908716241 ) ) ;
#5951=DIRECTION ( 'NONE',  ( -0.3865475372811022492, -0.7187975063895643002, -0.5778504531711118331 ) ) ;
#5952=CARTESIAN_POINT ( 'NONE',  ( -14.47334165536099881, 3.872983346207417021, -1.000000000000000000 ) ) ;
#5954=CARTESIAN_POINT ( 'NONE',  ( 2.259025283528086181, 2.741148848567763086, 7.131631878998401675 ) ) ;
#5966=ORIENTED_EDGE ( 'NONE', *, *, #45821, .T. ) ;
#5968=CARTESIAN_POINT ( 'NONE',  ( 5.515539859299206427, 0.005336559634876942085, 0.002856745161749560304 ) ) ;
#5973=CARTESIAN_POINT ( 'NONE',  ( 1.198791140417294843, 9.279671759317841051, 8.460175745277314974 ) ) ;
#5976=CARTESIAN_POINT ( 'NONE',  ( 0.8375941296829887417, 12.30893872205359152, -1.780036797757713174 ) ) ;
#5979=CARTESIAN_POINT ( 'NONE',  ( 1.462291587749844135, -11.25382118863310765, 5.766456054323949587 ) ) ;
#5981=ADVANCED_FACE ( 'NONE', ( #3807 ), #50117, .F. ) ;
#6003=CARTESIAN_POINT ( 'NONE',  ( 2.770579946183334030, -1.056759439485520424, -7.739026583264751125 ) ) ;
#6010=EDGE_LOOP ( 'NONE', ( #61169, #33056, #53639, #57174 ) ) ;
#6015=CARTESIAN_POINT ( 'NONE',  ( 0.2767916011545391020, -8.018602152763797619, -9.260929738915313791 ) ) ;
#6017=CARTESIAN_POINT ( 'NONE',  ( 3.152665057734129306, -7.923639299008720549, -0.4801242025592799556 ) ) ;
#6018=ORIENTED_EDGE ( 'NONE', *, *, #38040, .F. ) ;
#6022=CARTESIAN_POINT ( 'NONE',  ( 0.2646305136544065406, -4.312539723326210606, 11.46223899740598640 ) ) ;
#6024=CARTESIAN_POINT ( 'NONE',  ( 2.899286259009683953, 6.239228647238633130, -4.769992516330172627 ) ) ;
#6031=CARTESIAN_POINT ( 'NONE',  ( 2.440552418640495880, 3.678171968408328940, 6.765628357760791189 ) ) ;
#6032=CARTESIAN_POINT ( 'NONE',  ( 0.3654063281920718054, 12.27672420655579089, -0.2633658439603773216 ) ) ;
#6036=CARTESIAN_POINT ( 'NONE',  ( 0.3665391374699465965, 12.13918562134718826, 1.872534962004841708 ) ) ;
#6041=ORIENTED_EDGE ( 'NONE', *, *, #34661, .F. ) ;
#6042=( BOUNDED_SURFACE ( )  B_SPLINE_SURFACE ( 3, 1, ( 
 ( #21892, #629 ),
 ( #31840, #20890 ),
 ( #30856, #46822 ),
 ( #41833, #1288 ) ),
 .UNSPECIFIED., .F., .F., .F. ) 
 B_SPLINE_SURFACE_WITH_KNOTS ( ( 4, 4 ),
 ( 2, 2 ),
 ( 0.000000000000000000, 1.000000000000000000 ),
 ( 0.000000000000000000, 1.000000000000000000 ),
 .UNSPECIFIED. ) 
 GEOMETRIC_REPRESENTATION_ITEM ( )  RATIONAL_B_SPLINE_SURFACE ( (
 ( 1.000000000000000000, 1.000000000000000000),
 ( 0.9942764183789327692, 0.8450855930916585379),
 ( 0.9942764183789327692, 0.8450855930916585379),
 ( 1.000000000000000000, 1.000000000000000000) ) ) 
 REPRESENTATION_ITEM ( '' )  SURFACE ( )  );
#6047=ORIENTED_EDGE ( 'NONE', *, *, #9426, .T. ) ;
#6051=EDGE_CURVE ( 'NONE', #17370, #11727, #51902, .T. ) ;
#6055=CARTESIAN_POINT ( 'NONE',  ( 1.719304012339844867, -12.64775761152577971, 1.452142814149586902 ) ) ;
#6059=CARTESIAN_POINT ( 'NONE',  ( 2.247206125383335085, 7.135412558555234597, 2.720255231379262728 ) ) ;
#6061=CARTESIAN_POINT ( 'NONE',  ( 0.3401186441510234415, 12.12646044229293274, -1.878666403202209567 ) ) ;
#6064=ORIENTED_EDGE ( 'NONE', *, *, #17607, .T. ) ;
#6073=CARTESIAN_POINT ( 'NONE',  ( 0.2653519991613826345, 4.167757449530418157, 11.51519138201631876 ) ) ;
#6075=VERTEX_POINT ( 'NONE', #52291 ) ;
#6078=CARTESIAN_POINT ( 'NONE',  ( 0.2676618633000457659, -4.339362305359514949, 11.45242956837285853 ) ) ;
#6079=CARTESIAN_POINT ( 'NONE',  ( 2.573738926104378599, -5.779258037546978422, -5.156412073069344792 ) ) ;
#6080=EDGE_LOOP ( 'NONE', ( #13156, #15115, #17283, #21192, #48982, #9686 ) ) ;
#6081=CARTESIAN_POINT ( 'NONE',  ( 2.907497136250910774, 7.497839665536955245, 2.346692756478168995 ) ) ;
#6082=CARTESIAN_POINT ( 'NONE',  ( 0.2638984909335720941, 10.70468911391664157, 5.950360275955092426 ) ) ;
#6083=CARTESIAN_POINT ( 'NONE',  ( 0.2651627923886325511, -9.324231535593057174, -7.938954356958184633 ) ) ;
#6086=CARTESIAN_POINT ( 'NONE',  ( 0.2646305136544072623, 10.53923716745255490, -6.237419468586968385 ) ) ;
#6092=CARTESIAN_POINT ( 'NONE',  ( 0.2648978790185593790, 12.08224454301448958, 1.996248716311670446 ) ) ;
#6094=ADVANCED_FACE ( 'NONE', ( #57264 ), #25061, .F. ) ;
#6098=EDGE_CURVE ( 'NONE', #59129, #60647, #17733, .T. ) ;
#6102=CARTESIAN_POINT ( 'NONE',  ( 0.2653519890538384995, 1.477274386607676477E-15, 12.24619734961521189 ) ) ;
#6103=FACE_OUTER_BOUND ( 'NONE', #44197, .T. ) ;
#6105=CARTESIAN_POINT ( 'NONE',  ( 1.547277799337858584, 4.961646058323314179, 11.66196709685579158 ) ) ;
#6111=CARTESIAN_POINT ( 'NONE',  ( 1.634816307074488995, 10.62369813896843418, 6.964001572434787235 ) ) ;
#6115=CARTESIAN_POINT ( 'NONE',  ( 2.273267844204867494, -6.543821324256909655, 3.952852893982274907 ) ) ;
#6118=CARTESIAN_POINT ( 'NONE',  ( 0.2834382757448042356, -5.949714385480707080, 10.71064820518740213 ) ) ;
#6119=ORIENTED_EDGE ( 'NONE', *, *, #33503, .F. ) ;
#6132=CARTESIAN_POINT ( 'NONE',  ( 5.515539859299206427, 0.001241880655086591853, -0.005924322247674741922 ) ) ;
#6134=CARTESIAN_POINT ( 'NONE',  ( 2.241509619876139059, -2.647089031563618633, 7.160887714159610340 ) ) ;
#6135=ORIENTED_EDGE ( 'NONE', *, *, #323, .T. ) ;
#6136=CARTESIAN_POINT ( 'NONE',  ( 0.2646305136544072623, 6.008537389229419823, 10.67138229758231738 ) ) ;
#6143=ORIENTED_EDGE ( 'NONE', *, *, #51371, .T. ) ;
#6145=CARTESIAN_POINT ( 'NONE',  ( 0.3675815128205912052, -2.391755495700685241, 12.04510820461658582 ) ) ;
#6150=ORIENTED_EDGE ( 'NONE', *, *, #47830, .T. ) ;
#6155=CARTESIAN_POINT ( 'NONE',  ( 0.3665391374699465965, 6.368473106897129199, 10.50279796150439005 ) ) ;
#6162=EDGE_CURVE ( 'NONE', #64295, #10376, #56609, .T. ) ;
#6164=ADVANCED_FACE ( 'NONE', ( #58931 ), #15340, .F. ) ;
#6169=CARTESIAN_POINT ( 'NONE',  ( 2.305787727787083519, 3.682701754025512919, 6.711944854845837583 ) ) ;
#6183=CARTESIAN_POINT ( 'NONE',  ( 2.524535260912731616, -7.184101064217925270, 2.850096701925854514 ) ) ;
#6185=CARTESIAN_POINT ( 'NONE',  ( 2.241352910868908310, -3.744764251556946366, -6.652881166698550786 ) ) ;
#6190=CARTESIAN_POINT ( 'NONE',  ( 2.969415267404726499, 7.007431655063608211, 3.597837242549700942 ) ) ;
#6192=CARTESIAN_POINT ( 'NONE',  ( 0.9232058338315048962, 11.84276737136206137, -3.908895078357403019 ) ) ;
#6205=CARTESIAN_POINT ( 'NONE',  ( 0.2872850955227771452, 11.44140577127598668, -4.386654201695032285 ) ) ;
#6208=VERTEX_POINT ( 'NONE', #24296 ) ;
#6210=ORIENTED_EDGE ( 'NONE', *, *, #60031, .F. ) ;
#6213=EDGE_CURVE ( 'NONE', #64826, #22962, #34274, .T. ) ;
#6215=VERTEX_POINT ( 'NONE', #33940 ) ;
#6218=CARTESIAN_POINT ( 'NONE',  ( 0.2646305136544065406, 1.996350543473153216, -12.08286001766533602 ) ) ;
#6222=CARTESIAN_POINT ( 'NONE',  ( 2.256373768223412846, -7.223078030710452069, -2.487510024221244009 ) ) ;
#6223=EDGE_CURVE ( 'NONE', #60104, #28065, #2690, .T. ) ;
#6226=CARTESIAN_POINT ( 'NONE',  ( 0.3040950598368144520, 5.912066680610613467, 10.74226959800793679 ) ) ;
#6253=CARTESIAN_POINT ( 'NONE',  ( 5.516018279890452902, 0.006629829924290974764, 0.001397286410094337149 ) ) ;
#6257=CARTESIAN_POINT ( 'NONE',  ( 2.889800649504073782, -5.774917447013012683, 2.030191121417117106 ) ) ;
#6259=CARTESIAN_POINT ( 'NONE',  ( 1.020182472822701358, -12.37761526492762876, 1.729367949134579918 ) ) ;
#6264=ADVANCED_FACE ( 'NONE', ( #683 ), #2141, .F. ) ;
#6266=CARTESIAN_POINT ( 'NONE',  ( 2.251152103363646351, 2.729599998984407083, 7.133254101175193540 ) ) ;
#6270=VERTEX_POINT ( 'NONE', #45555 ) ;
#6273=CARTESIAN_POINT ( 'NONE',  ( 0.3675815128205894289, -9.574637318042015011, 7.689697408877242957 ) ) ;
#6282=FACE_OUTER_BOUND ( 'NONE', #29358, .T. ) ;
#6284=CARTESIAN_POINT ( 'NONE',  ( 1.719304012339844867, -11.67935079956417610, 5.066286238786176455 ) ) ;
#6285=CARTESIAN_POINT ( 'NONE',  ( 0.9296196016843308874, -7.691217109781701033, -9.812579935705461054 ) ) ;
#6286=CARTESIAN_POINT ( 'NONE',  ( 1.020182472824531450, 11.03967505355455714, -5.858468047365605003 ) ) ;
#6287=DIRECTION ( 'NONE',  ( -1.000000000000000000, -0.000000000000000000, -0.000000000000000000 ) ) ;
#6289=CARTESIAN_POINT ( 'NONE',  ( 5.514970785353741078, 0.002093325033903813397, -0.004233694591582959355 ) ) ;
#6294=ORIENTED_EDGE ( 'NONE', *, *, #12088, .T. ) ;
#6303=CARTESIAN_POINT ( 'NONE',  ( 0.2646305136544065406, -2.256625640822235379, -12.03696649559616993 ) ) ;
#6311=CARTESIAN_POINT ( 'NONE',  ( 2.907497136250123848, -5.781215374755555025, 5.319973245618085045 ) ) ;
#6312=CARTESIAN_POINT ( 'NONE',  ( 2.255723233588638355, 5.010912740807773602, -5.766109278028810792 ) ) ;
#6323=CARTESIAN_POINT ( 'NONE',  ( 0.3053067050349149714, -2.355726819985503262, 12.03105545708856106 ) ) ;
#6324=FACE_OUTER_BOUND ( 'NONE', #62203, .T. ) ;
#6325=CARTESIAN_POINT ( 'NONE',  ( 0.6511581176972880414, -10.54760823437317008, -6.471755598256867081 ) ) ;
#6326=EDGE_CURVE ( 'NONE', #54096, #44256, #34319, .T. ) ;
#6328=VERTEX_POINT ( 'NONE', #21271 ) ;
#6331=CARTESIAN_POINT ( 'NONE',  ( 0.3341166715381310159, 10.74942732659231837, 5.914486946113945542 ) ) ;
#6333=CARTESIAN_POINT ( 'NONE',  ( 2.770579946183330478, 6.173813901927609926, -4.784693811915826878 ) ) ;
#6338=DIRECTION ( 'NONE',  ( 1.000000000000000000, -0.000000000000000000, -0.000000000000000000 ) ) ;
#6339=CARTESIAN_POINT ( 'NONE',  ( 3.152665057735980714, 1.848755561853925533, 7.719888720907654545 ) ) ;
#6341=B_SPLINE_CURVE_WITH_KNOTS ( 'NONE', 3,
 ( #2279, #47187, #42151, #7930, #23206, #43465, #17574, #2940, #18224, #6618, #32182, #52506, #37514, #58463, #38495, #57819, #37843, #63745, #62438 ),
 .UNSPECIFIED., .F., .F.,
 ( 4, 3, 3, 3, 3, 3, 4 ),
 ( 6.508826038821074665E-18, 2.825908398831552076E-05, 4.208813692484427327E-05, 5.591713746944529178E-05, 6.279584083232600446E-05, 9.105792820297518039E-05, 0.0001153131102488865703 ),
 .UNSPECIFIED. ) ;
#6344=ADVANCED_FACE ( 'NONE', ( #6324 ), #58684, .F. ) ;
#6355=CARTESIAN_POINT ( 'NONE',  ( 2.430348790457504293, -6.566563360302382080, 4.016278121583770400 ) ) ;
#6362=FACE_OUTER_BOUND ( 'NONE', #16068, .T. ) ;
#6376=CARTESIAN_POINT ( 'NONE',  ( 0.2706063244538051693, 12.09107863371559866, -1.954041462022295450 ) ) ;
#6379=ADVANCED_FACE ( 'NONE', ( #47227 ), #21942, .T. ) ;
#6383=FACE_OUTER_BOUND ( 'NONE', #16647, .T. ) ;
#6385=CARTESIAN_POINT ( 'NONE',  ( 0.3675815128205912052, 6.367184624550311867, -10.50067073900645198 ) ) ;
#6391=CARTESIAN_POINT ( 'NONE',  ( 2.899286259009692390, -5.780956296532483663, -5.316140236670832131 ) ) ;
#6395=CARTESIAN_POINT ( 'NONE',  ( 3.152665057736252940, 7.609997527622067715, 2.258875078500286016 ) ) ;
#6396=CARTESIAN_POINT ( 'NONE',  ( 5.536195898058073439, 0.007485416011287806572, -0.004027525919832459014 ) ) ;
#6401=CARTESIAN_POINT ( 'NONE',  ( 2.241317068080788122, 7.204761327831662676, 2.524952427347059825 ) ) ;
#6411=B_SPLINE_CURVE_WITH_KNOTS ( 'NONE', 3,
 ( #15175, #20165, #30148, #35107, #55419, #45766, #25479, #46115, #10502, #25157, #56062, #35455, #11180, #26461, #10185, #25822, #30465, #61067, #45428 ),
 .UNSPECIFIED., .F., .F.,
 ( 4, 3, 3, 3, 3, 3, 4 ),
 ( 1.099757308482672315E-17, 4.457896483014753801E-05, 6.639290541542144030E-05, 8.820687556479127171E-05, 0.0001100173248778949181, 0.0001545671401658163307, 0.0001830328308068594713 ),
 .UNSPECIFIED. ) ;
#6416=( BOUNDED_SURFACE ( )  B_SPLINE_SURFACE ( 3, 1, ( 
 ( #28535, #24526 ),
 ( #39823, #23228 ),
 ( #53827, #49178 ),
 ( #59147, #2966 ) ),
 .UNSPECIFIED., .F., .F., .F. ) 
 B_SPLINE_SURFACE_WITH_KNOTS ( ( 4, 4 ),
 ( 2, 2 ),
 ( 0.000000000000000000, 1.000000000000000000 ),
 ( 0.000000000000000000, 1.000000000000000000 ),
 .UNSPECIFIED. ) 
 GEOMETRIC_REPRESENTATION_ITEM ( )  RATIONAL_B_SPLINE_SURFACE ( (
 ( 1.000000000000000000, 1.000000000000000000),
 ( 0.9856612449720755231, 0.9999558406602322425),
 ( 0.9856612449720755231, 0.9999558406602322425),
 ( 1.000000000000000000, 1.000000000000000000) ) ) 
 REPRESENTATION_ITEM ( '' )  SURFACE ( )  );
#6417=CARTESIAN_POINT ( 'NONE',  ( 2.177405672432018324, 0.6747479782259074854, 11.17876532285389146 ) ) ;
#6421=CARTESIAN_POINT ( 'NONE',  ( 1.719304012338833676, 5.066286238785588480, 11.67935079956406597 ) ) ;
#6435=CARTESIAN_POINT ( 'NONE',  ( 0.2767916011545419885, -5.959903879715655606, 10.70244578860293139 ) ) ;
#6448=CARTESIAN_POINT ( 'NONE',  ( 5.516018279890452902, -0.003191189039764880282, -0.005976902763919027944 ) ) ;
#6453=ORIENTED_EDGE ( 'NONE', *, *, #8010, .T. ) ;
#6454=CARTESIAN_POINT ( 'NONE',  ( 2.990245332647846421, 3.789007530133591484, 7.587819667496370712 ) ) ;
#6455=ORIENTED_EDGE ( 'NONE', *, *, #33540, .T. ) ;
#6458=CARTESIAN_POINT ( 'NONE',  ( 2.247206125382827047, -7.635476611656036638, -0.1157489416152311518 ) ) ;
#6462=CARTESIAN_POINT ( 'NONE',  ( 1.194176325881339595, 8.457794872459121649, 9.279760592562121602 ) ) ;
#6464=CARTESIAN_POINT ( 'NONE',  ( 0.2638984909335720941, 12.02508546958700109, -2.322601104020543872 ) ) ;
#6465=CARTESIAN_POINT ( 'NONE',  ( 0.2671309869109492752, -12.03155065772886623, 2.286013846429986618 ) ) ;
#6467=ORIENTED_EDGE ( 'NONE', *, *, #45658, .T. ) ;
#6488=CARTESIAN_POINT ( 'NONE',  ( 0.3160775863651120177, 4.419114254410051679, -11.43919651388221226 ) ) ;
#6489=CARTESIAN_POINT ( 'NONE',  ( 2.241449424704145876, 3.763973574060632377, -6.642105568284066841 ) ) ;
#6491=CARTESIAN_POINT ( 'NONE',  ( 0.2648978790185619880, 12.03635331166815270, -2.256510822326019738 ) ) ;
#6498=CARTESIAN_POINT ( 'NONE',  ( 2.653899356900514039, 1.091629880170411848, -7.694895988366599937 ) ) ;
#6506=DIRECTION ( 'NONE',  ( 0.000000000000000000, 0.000000000000000000, 1.000000000000000000 ) ) ;
#6509=ORIENTED_EDGE ( 'NONE', *, *, #40319, .F. ) ;
#6512=CARTESIAN_POINT ( 'NONE',  ( 0.2655924914740778187, -10.58356227062105148, -6.161287456391793427 ) ) ;
#6513=CARTESIAN_POINT ( 'NONE',  ( 0.2648978790185584908, -12.24533305150758089, -0.1321385342563691223 ) ) ;
#6524=EDGE_CURVE ( 'NONE', #43331, #60300, #40683, .T. ) ;
#6527=CIRCLE ( 'NONE', #35166, 7.938172270156617749 ) ;
#6529=CARTESIAN_POINT ( 'NONE',  ( 0.2647959493198570047, 11.45640103018464195, -4.326188315749620372 ) ) ;
#6536=CARTESIAN_POINT ( 'NONE',  ( 0.6473888112830247232, -11.51036712212683355, 4.540486098228939227 ) ) ;
#6539=B_SPLINE_CURVE_WITH_KNOTS ( 'NONE', 3,
 ( #13492, #54420, #60051, #38450, #33776, #64678, #49111, #58767, #53762, #13188, #55048, #33471, #23835, #43423, #44098, #59387 ),
 .UNSPECIFIED., .F., .F.,
 ( 4, 3, 3, 3, 3, 4 ),
 ( 3.104202383059129028E-15, 0.0002126834539179675815, 0.0004253519300366209862, 0.0006380165497224082579, 0.0007442707582428152160, 0.0009453531351418435844 ),
 .UNSPECIFIED. ) ;
#6543=CARTESIAN_POINT ( 'NONE',  ( 5.520433897694421610, 0.01006947824912450551, 0.01120198501134887781 ) ) ;
#6552=EDGE_LOOP ( 'NONE', ( #14356, #18879, #14618, #36187 ) ) ;
#6555=B_SPLINE_CURVE_WITH_KNOTS ( 'NONE', 3,
 ( #60285, #25367, #4792, #50980, #14711, #34990, #25054, #45325, #20057, #40321, #42598, #36658, #51964, #47953, #27323, #57275 ),
 .UNSPECIFIED., .F., .F.,
 ( 4, 3, 3, 3, 3, 4 ),
 ( 0.000000000000000000, 0.0002176109881720194434, 0.0004352086762394498788, 0.0006528017811446724375, 0.0007615147961451543875, 0.0009453342004946168253 ),
 .UNSPECIFIED. ) ;
#6557=CARTESIAN_POINT ( 'NONE',  ( 1.194176325881336043, 12.44396189284385024, 1.672143286119605055 ) ) ;
#6561=CARTESIAN_POINT ( 'NONE',  ( 2.994568964204214812, -7.825096839971885210, 0.9739368093814469995 ) ) ;
#6566=CARTESIAN_POINT ( 'NONE',  ( 1.372161826075799507, 12.60140585080784703, -0.5897614319401539573 ) ) ;
#6568=CARTESIAN_POINT ( 'NONE',  ( 0.2648978790185584908, 2.256510822326303956, -12.03635331166809941 ) ) ;
#6572=CARTESIAN_POINT ( 'NONE',  ( 0.3665391374699467075, 7.691255657244293609, 9.576575648339046509 ) ) ;
#6585=CARTESIAN_POINT ( 'NONE',  ( 2.249013661412228693, 1.444210756221647518, -7.499157010299421167 ) ) ;
#6587=CARTESIAN_POINT ( 'NONE',  ( 0.2650492433740075926, -6.218175523534217319, -10.54996000109281340 ) ) ;
#6590=CARTESIAN_POINT ( 'NONE',  ( 0.4626703367445803017, -12.17089897506931528, 1.858541096401158832 ) ) ;
#6593=CARTESIAN_POINT ( 'NONE',  ( 0.3675815128205912052, 6.367184624550311867, -10.50067073900645198 ) ) ;
#6609=ORIENTED_EDGE ( 'NONE', *, *, #20480, .T. ) ;
#6613=( BOUNDED_SURFACE ( )  B_SPLINE_SURFACE ( 3, 1, ( 
 ( #8118, #48684 ),
 ( #3142, #63961 ),
 ( #18440, #13415 ),
 ( #53992, #8436 ) ),
 .UNSPECIFIED., .F., .F., .F. ) 
 B_SPLINE_SURFACE_WITH_KNOTS ( ( 4, 4 ),
 ( 2, 2 ),
 ( 0.000000000000000000, 1.000000000000000000 ),
 ( 0.000000000000000000, 1.000000000000000000 ),
 .UNSPECIFIED. ) 
 GEOMETRIC_REPRESENTATION_ITEM ( )  RATIONAL_B_SPLINE_SURFACE ( (
 ( 1.000000000000000000, 1.000000000000000000),
 ( 0.6933888150995267674, 0.9895912004443193632),
 ( 0.6933888150995267674, 0.9895912004443193632),
 ( 1.000000000000000000, 1.000000000000000000) ) ) 
 REPRESENTATION_ITEM ( '' )  SURFACE ( )  );
#6616=CARTESIAN_POINT ( 'NONE',  ( 2.368238019614553824, 7.674602282635826001, -0.1797502808084445181 ) ) ;
#6618=CARTESIAN_POINT ( 'NONE',  ( 2.260457164927183626, -1.190240296002724740, 7.547495527593548914 ) ) ;
#6627=CARTESIAN_POINT ( 'NONE',  ( 1.937114397841932290, 0.9020203649533465873, -12.80345148322678384 ) ) ;
#6628=CARTESIAN_POINT ( 'NONE',  ( 3.152665057733930798, -5.761241965769118067, -5.461013642405381674 ) ) ;
#6636=CARTESIAN_POINT ( 'NONE',  ( 5.515539859299206427, -0.004037661319610856558, 0.004509673239148324041 ) ) ;
#6643=CARTESIAN_POINT ( 'NONE',  ( 2.241528039335007438, -7.179411278563573973, 2.596349773934855332 ) ) ;
#6648=ORIENTED_EDGE ( 'NONE', *, *, #28327, .F. ) ;
#6655=CARTESIAN_POINT ( 'NONE',  ( 2.305787727787083519, 4.792270232040894307, 5.970480882365237996 ) ) ;
#6656=CARTESIAN_POINT ( 'NONE',  ( 0.2872850955227730929, -8.035297825011307182, -9.251080475901439115 ) ) ;
#6658=CARTESIAN_POINT ( 'NONE',  ( 0.3675815128205912052, -10.50067073900647330, -6.367184624550275451 ) ) ;
#6666=CARTESIAN_POINT ( 'NONE',  ( 3.152665057736253829, 5.761241965767907480, -5.461013642407265500 ) ) ;
#6669=CARTESIAN_POINT ( 'NONE',  ( 2.969415267403817005, 7.815364626283781924, 0.9841783286033500833 ) ) ;
#6679=EDGE_LOOP ( 'NONE', ( #8469, #60130, #2270, #45789 ) ) ;
#6681=CARTESIAN_POINT ( 'NONE',  ( 0.2646305136544072623, 7.972778379581551889, 9.296005949277251545 ) ) ;
#6687=CARTESIAN_POINT ( 'NONE',  ( 0.2653519890518162283, 2.126538543978078177, 12.06014856238021693 ) ) ;
#6690=CARTESIAN_POINT ( 'NONE',  ( 0.3109076770649050747, -1.896437056876546512, 12.11383728282219074 ) ) ;
#6694=ORIENTED_EDGE ( 'NONE', *, *, #23821, .T. ) ;
#6696=CARTESIAN_POINT ( 'NONE',  ( 2.889800649504073782, -5.334644486274173758, -3.002151847318972777 ) ) ;
#6715=B_SPLINE_CURVE_WITH_KNOTS ( 'NONE', 3,
 ( #224, #35756, #25472, #26455, #36439, #35450, #46109, #31122, #10838, #51749, #16494, #57059, #15490, #30771, #20495, #11174 ),
 .UNSPECIFIED., .F., .F.,
 ( 4, 3, 3, 3, 3, 4 ),
 ( 0.000000000000000000, 0.0002176109881720219370, 0.0004352086762394582272, 0.0006528017811446855563, 0.0007615147961451689158, 0.0009453342004945030925 ),
 .UNSPECIFIED. ) ;
#6717=AXIS2_PLACEMENT_3D ( 'NONE', #59122, #28840, #37838 ) ;
#6729=EDGE_CURVE ( 'NONE', #48474, #58225, #54927, .T. ) ;
#6731=CARTESIAN_POINT ( 'NONE',  ( 2.589278595513614611, 7.361833592938543447, 2.423168677231871460 ) ) ;
#6732=CARTESIAN_POINT ( 'NONE',  ( 0.3665391374699465965, 9.576575648339021640, 7.691255657244325583 ) ) ;
#6733=DIRECTION ( 'NONE',  ( -1.000000000000000000, -0.000000000000000000, -0.000000000000000000 ) ) ;
#6734=ORIENTED_EDGE ( 'NONE', *, *, #27332, .T. ) ;
#6735=VECTOR ( 'NONE', #30967, 1000.000000000000114 ) ;
#6739=CARTESIAN_POINT ( 'NONE',  ( 1.719304012340733934, -12.20344780066092305, -3.626341562669774365 ) ) ;
#6741=CARTESIAN_POINT ( 'NONE',  ( 1.937114397841935398, 0.9020203649531696177, 12.80345148322679627 ) ) ;
#6744=DIRECTION ( 'NONE',  ( -1.000000000000000000, -0.000000000000000000, -0.000000000000000000 ) ) ;
#6757=EDGE_CURVE ( 'NONE', #16846, #44289, #21627, .T. ) ;
#6759=B_SPLINE_CURVE_WITH_KNOTS ( 'NONE', 3,
 ( #47750, #2198, #57078, #6536, #26810, #32111, #63035, #17498, #12477, #47110, #36459, #52431, #27141, #37770, #47436, #57747 ),
 .UNSPECIFIED., .F., .F.,
 ( 4, 3, 3, 3, 3, 4 ),
 ( 2.710505431213761085E-19, 0.0003017745587525258975, 0.0006035491769808751499, 0.0009053241094668185249, 0.001207275924539989763, 0.001510325902532974216 ),
 .UNSPECIFIED. ) ;
#6761=CARTESIAN_POINT ( 'NONE',  ( 5.514970785353741078, -0.001326349372336609999, -0.004532877335078314314 ) ) ;
#6762=CARTESIAN_POINT ( 'NONE',  ( 0.2657645697724698719, -12.24540328300721548, -0.1513403555226850161 ) ) ;
#6765=CARTESIAN_POINT ( 'NONE',  ( 2.655192694323065705, -5.293797899977148447, -8.010337395401304406 ) ) ;
#6778=CARTESIAN_POINT ( 'NONE',  ( 1.462291587750749633, -11.65117843858596558, -4.914320681886166220 ) ) ;
#6784=CARTESIAN_POINT ( 'NONE',  ( 2.907497136251154579, -7.848280798453004081, 0.3592423305256113863 ) ) ;
#6788=ORIENTED_EDGE ( 'NONE', *, *, #55545, .F. ) ;
#6790=CARTESIAN_POINT ( 'NONE',  ( 0.2653519991613815243, 9.395283368383282152, -7.854838327448875113 ) ) ;
#6796=CARTESIAN_POINT ( 'NONE',  ( 1.020182472821632214, -4.691131056022166845, 11.58401323226448909 ) ) ;
#6799=CARTESIAN_POINT ( 'NONE',  ( 3.152665057734040488, 0.000000000000000000, 0.000000000000000000 ) ) ;
#6806=CARTESIAN_POINT ( 'NONE',  ( 2.305787727787084407, 7.508843116234155346, 1.493241775258449255 ) ) ;
#6820=( BOUNDED_SURFACE ( )  B_SPLINE_SURFACE ( 3, 1, ( 
 ( #16866, #5609 ),
 ( #35812, #37139 ),
 ( #26849, #10554 ),
 ( #40840, #30834 ) ),
 .UNSPECIFIED., .F., .F., .F. ) 
 B_SPLINE_SURFACE_WITH_KNOTS ( ( 4, 4 ),
 ( 2, 2 ),
 ( 0.000000000000000000, 1.000000000000000000 ),
 ( 0.000000000000000000, 1.000000000000000000 ),
 .UNSPECIFIED. ) 
 GEOMETRIC_REPRESENTATION_ITEM ( )  RATIONAL_B_SPLINE_SURFACE ( (
 ( 1.000000000000000000, 1.000000000000000000),
 ( 0.9856612449720755231, 0.9999558406602322425),
 ( 0.9856612449720755231, 0.9999558406602322425),
 ( 1.000000000000000000, 1.000000000000000000) ) ) 
 REPRESENTATION_ITEM ( '' )  SURFACE ( )  );
#6821=EDGE_LOOP ( 'NONE', ( #18142, #20252, #30407, #1699 ) ) ;
#6827=CARTESIAN_POINT ( 'NONE',  ( 5.536195898058073439, 0.002666509901869610743, 0.008071068258923192601 ) ) ;
#6834=DIRECTION ( 'NONE',  ( -0.3865475372811021937, 0.8082200352954617140, 0.4442537292684412553 ) ) ;
#6844=CARTESIAN_POINT ( 'NONE',  ( 2.276198483116796734, -4.795748742147632804, -5.955030244776002846 ) ) ;
#6855=CARTESIAN_POINT ( 'NONE',  ( 0.2717059086739065932, -4.354191483751194802, -11.44824199474646420 ) ) ;
#6856=EDGE_LOOP ( 'NONE', ( #46673, #17653, #40172, #45748 ) ) ;
#6859=CARTESIAN_POINT ( 'NONE',  ( 0.2648978790185602672, -7.769924372105269761, 9.465406350830582127 ) ) ;
#6874=CARTESIAN_POINT ( 'NONE',  ( 5.514624014163232779, -0.002216125254993232471, 0.003498325728817954818 ) ) ;
#6877=CARTESIAN_POINT ( 'NONE',  ( 2.276905613633652070, 5.757134111949752331, -5.031956778294075505 ) ) ;
#6885=CARTESIAN_POINT ( 'NONE',  ( 1.547277799337430038, 12.58038279313686481, 1.534072017333138360 ) ) ;
#6886=EDGE_CURVE ( 'NONE', #46786, #9459, #6539, .T. ) ;
#6890=ORIENTED_EDGE ( 'NONE', *, *, #61859, .F. ) ;
#6891=CARTESIAN_POINT ( 'NONE',  ( 1.014383007554949589, 12.48801387563329257, -0.4441500209063513616 ) ) ;
#6904=ORIENTED_EDGE ( 'NONE', *, *, #22612, .F. ) ;
#6911=CARTESIAN_POINT ( 'NONE',  ( 3.152665057734040488, 0.000000000000000000, 0.000000000000000000 ) ) ;
#6912=CARTESIAN_POINT ( 'NONE',  ( 2.844750968616352793, -1.031816958530431316, 7.767336242081023912 ) ) ;
#6914=B_SPLINE_CURVE_WITH_KNOTS ( 'NONE', 3,
 ( #52597, #41606, #15996, #12325, #6059, #57911, #31311, #21324, #37611, #61550, #32589, #26642, #52266, #62529, #1719, #27615, #22653, #2378, #11669 ),
 .UNSPECIFIED., .F., .F.,
 ( 4, 3, 3, 3, 3, 3, 4 ),
 ( 4.336808689942017255E-19, 2.831840207625097852E-05, 4.217266860012006086E-05, 5.602024318565493148E-05, 6.290810168137762047E-05, 9.120440631110077504E-05, 0.0001153103026478315791 ),
 .UNSPECIFIED. ) ;
#6919=EDGE_LOOP ( 'NONE', ( #20085, #57270, #25579, #17902 ) ) ;
#6921=EDGE_LOOP ( 'NONE', ( #11908, #28823, #2653, #2652 ) ) ;
#6923=CARTESIAN_POINT ( 'NONE',  ( 2.241526690369556984, 7.179945570618761153, 2.594870554108865246 ) ) ;
#6924=FACE_OUTER_BOUND ( 'NONE', #22998, .T. ) ;
#6925=AXIS2_PLACEMENT_3D ( 'NONE', #51, #4409, #49949 ) ;
#6926=CARTESIAN_POINT ( 'NONE',  ( 1.634816307074478114, 12.68239325670150386, 0.7191532042390553769 ) ) ;
#6927=DIRECTION ( 'NONE',  ( 1.000000000000000000, 0.000000000000000000, 0.000000000000000000 ) ) ;
#6928=ORIENTED_EDGE ( 'NONE', *, *, #55416, .F. ) ;
#6930=CARTESIAN_POINT ( 'NONE',  ( 5.530133899448235191, -0.001124651387255098814, 0.01594518557925581753 ) ) ;
#6937=CARTESIAN_POINT ( 'NONE',  ( 0.2648978790185619880, 12.03635331166815270, -2.256510822326019738 ) ) ;
#6939=CARTESIAN_POINT ( 'NONE',  ( 2.241352910868909643, 5.794346703933845433, 4.970878533273779709 ) ) ;
#6943=CARTESIAN_POINT ( 'NONE',  ( 2.080613030138688480, 0.000000000000000000, 0.000000000000000000 ) ) ;
#6944=EDGE_LOOP ( 'NONE', ( #53725, #35649, #47603, #61882 ) ) ;
#6950=CARTESIAN_POINT ( 'NONE',  ( 5.530133899448235191, -0.01594518557925581406, -0.001124651387255154325 ) ) ;
#6952=CARTESIAN_POINT ( 'NONE',  ( 2.440552418640497656, -1.531218882877344534, 7.547055375260057097 ) ) ;
#6955=CARTESIAN_POINT ( 'NONE',  ( 0.2638984909335720941, -2.322601104020586060, -12.02508546958699398 ) ) ;
#6960=CARTESIAN_POINT ( 'NONE',  ( 2.241451721903216843, -7.194631024842657929, 2.553895636571910988 ) ) ;
#6961=CARTESIAN_POINT ( 'NONE',  ( 2.249013661412018195, 5.000301708455996419, -5.772355099776886433 ) ) ;
#6965=CARTESIAN_POINT ( 'NONE',  ( 2.259830038564998311, 2.742210045659281725, -7.131511317046831167 ) ) ;
#6971=CARTESIAN_POINT ( 'NONE',  ( 2.247112776671923662, 3.716786765231635759, -6.670755883246408224 ) ) ;
#6972=COLOUR_RGB ( '', 0.40784314, 0.44705882, 0.49803922) ;
#6975=CARTESIAN_POINT ( 'NONE',  ( 0.3057689695767539795, -11.59726335252430829, -3.975296631252078772 ) ) ;
#6978=CARTESIAN_POINT ( 'NONE',  ( 5.514970785353741078, -0.003415090918276162540, 0.003262412238248699973 ) ) ;
#6987=CARTESIAN_POINT ( 'NONE',  ( 3.047904605210434603, -4.747272783555597009, -6.318654123925961485 ) ) ;
#6989=CARTESIAN_POINT ( 'NONE',  ( 1.633930747253265814, 10.62371422070961557, -6.963441708414618070 ) ) ;
#6999=CARTESIAN_POINT ( 'NONE',  ( 0.2646305136544072623, 7.770320294339177813, 9.465888453932986835 ) ) ;
#7000=CARTESIAN_POINT ( 'NONE',  ( 1.375507693219674588, -5.789143338281887985, -11.20969178069651484 ) ) ;
#7002=EDGE_CURVE ( 'NONE', #20463, #29440, #26431, .T. ) ;
#7003=ORIENTED_EDGE ( 'NONE', *, *, #51131, .T. ) ;
#7008=CARTESIAN_POINT ( 'NONE',  ( 0.2872850955227743142, -1.921748909352239298, 12.10187515377843503 ) ) ;
#7011=ORIENTED_EDGE ( 'NONE', *, *, #27856, .T. ) ;
#7019=AXIS2_PLACEMENT_3D ( 'NONE', #61284, #15714, #56291 ) ;
#7025=EDGE_LOOP ( 'NONE', ( #7508, #3286, #19631, #43735 ) ) ;
#7026=CARTESIAN_POINT ( 'NONE',  ( 1.547277799339723758, 7.618736734813467137, -10.12789507952378898 ) ) ;
#7027=CARTESIAN_POINT ( 'NONE',  ( 0.2648978790185602672, 7.769924372105329269, -9.465406350830530613 ) ) ;
#7034=DIRECTION ( 'NONE',  ( -0.3865475372811021937, 0.8730852074079739067, 0.2971585806051880718 ) ) ;
#7038=CARTESIAN_POINT ( 'NONE',  ( 0.2833330754217368019, -4.379886056890972768, 11.44258640049859821 ) ) ;
#7039=CARTESIAN_POINT ( 'NONE',  ( 2.297017764049617661, 6.708511771223625964, 3.682881532880238673 ) ) ;
#7043=CARTESIAN_POINT ( 'NONE',  ( 0.2717059086739041507, 12.03041489115254414, -2.300075171420108422 ) ) ;
#7044=CARTESIAN_POINT ( 'NONE',  ( 0.2652384770603665731, -9.338499095996370514, -7.922175044417074652 ) ) ;
#7048=ORIENTED_EDGE ( 'NONE', *, *, #39665, .F. ) ;
#7049=DIRECTION ( 'NONE',  ( -0.3865475372811021937, -0.01937500237527774866, -0.9220659470476463282 ) ) ;
#7057=CARTESIAN_POINT ( 'NONE',  ( 0.3040950598368144520, 12.02925914197705204, 2.376091969481256783 ) ) ;
#7063=CARTESIAN_POINT ( 'NONE',  ( 0.3675815128205894289, 10.50067073900651771, 6.367184624550202621 ) ) ;
#7086=B_SPLINE_CURVE_WITH_KNOTS ( 'NONE', 3,
 ( #58380, #12160, #37763, #53053, #25917, #42730, #22137, #7847, #27781, #22471, #43069, #48085, #63029, #15907, #43388, #28122 ),
 .UNSPECIFIED., .F., .F.,
 ( 4, 3, 3, 3, 3, 4 ),
 ( 0.000000000000000000, 0.0002999043160757463937, 0.0005998071753051251783, 0.0008997092107374914235, 0.001204458948196565800, 0.001510329163478326504 ),
 .UNSPECIFIED. ) ;
#7098=CARTESIAN_POINT ( 'NONE',  ( 2.350038591458107451, 4.746773736939504218, 9.502240128958677090 ) ) ;
#7099=ORIENTED_EDGE ( 'NONE', *, *, #6223, .F. ) ;
#7104=EDGE_LOOP ( 'NONE', ( #58177, #45034, #28856, #23703 ) ) ;
#7107=CARTESIAN_POINT ( 'NONE',  ( 5.515539859299206427, -0.004509673239148311030, -0.004037661319610873038 ) ) ;
#7108=CARTESIAN_POINT ( 'NONE',  ( 2.241536586108912044, -5.844297002038577382, 4.912162027558472310 ) ) ;
#7124=CARTESIAN_POINT ( 'NONE',  ( 1.719304012338199295, 11.67935079956398958, 5.066286238785226992 ) ) ;
#7127=EDGE_CURVE ( 'NONE', #35179, #3105, #5807, .T. ) ;
#7128=CARTESIAN_POINT ( 'NONE',  ( 0.2911222467163570027, 4.392242282525022468, -11.44063169461051288 ) ) ;
#7132=CARTESIAN_POINT ( 'NONE',  ( 0.9232058338315058954, 12.21058493388777144, -2.536181247095240288 ) ) ;
#7135=CARTESIAN_POINT ( 'NONE',  ( 0.3106921474978482922, -1.896868624982982920, -12.11369598333778796 ) ) ;
#7137=DIRECTION ( 'NONE',  ( 0.3865475372811021382, 0.9220659470476459951, 0.01937500237529380179 ) ) ;
#7146=CARTESIAN_POINT ( 'NONE',  ( 2.406456491625610372, 7.573451137023644364, -7.176027849161648930 ) ) ;
#7160=CARTESIAN_POINT ( 'NONE',  ( 0.3675815128205894289, 4.447030445008180344, 11.44679196252410946 ) ) ;
#7162=CARTESIAN_POINT ( 'NONE',  ( 0.2657645697724702050, -11.45515365350258818, -4.330388001246531893 ) ) ;
#7163=CARTESIAN_POINT ( 'NONE',  ( 1.014383007554950478, 11.88680274101312406, 3.853787798429443079 ) ) ;
#7173=CARTESIAN_POINT ( 'NONE',  ( 1.719304012338820131, 1.452142814150020556, 12.64775761152757561 ) ) ;
#7185=VECTOR ( 'NONE', #62977, 1000.000000000000000 ) ;
#7188=CARTESIAN_POINT ( 'NONE',  ( 0.5547464869798257592, 12.20441397277155993, 1.842327806480188235 ) ) ;
#7190=CARTESIAN_POINT ( 'NONE',  ( 2.507146904658099196, -7.640248566386908635, 1.127530020444472703 ) ) ;
#7192=CARTESIAN_POINT ( 'NONE',  ( 2.247206125382830155, 7.499376972323892332, 1.439877054338129847 ) ) ;
#7199=CARTESIAN_POINT ( 'NONE',  ( 2.298277635560275645, -3.968740875991601413, 6.543949079923926604 ) ) ;
#7206=CARTESIAN_POINT ( 'NONE',  ( 0.2671309869109482760, 7.747281147400671308, -9.484919892054740842 ) ) ;
#7208=CARTESIAN_POINT ( 'NONE',  ( 0.3040950598368144520, -3.956873563689455420, -11.60568999039898941 ) ) ;
#7209=CARTESIAN_POINT ( 'NONE',  ( 3.092491956585914359, -5.424230976134662541, -5.768471164322597211 ) ) ;
#7211=CARTESIAN_POINT ( 'NONE',  ( 0.2915757698887290750, 12.10419100255479385, 1.916267336493217233 ) ) ;
#7217=CARTESIAN_POINT ( 'NONE',  ( 0.3160775863651085205, 6.338373607799337783, -10.49803827792115740 ) ) ;
#7225=CARTESIAN_POINT ( 'NONE',  ( 1.719304012339819332, -8.755325027794356174, 9.242227816401850760 ) ) ;
#7237=CARTESIAN_POINT ( 'NONE',  ( 0.3675815128205894289, -1.872154644482166397, 12.13672785388549613 ) ) ;
#7239=CARTESIAN_POINT ( 'NONE',  ( 1.109979610371589320, -7.679283534372219222, -9.898186741522541965 ) ) ;
#7261=VERTEX_POINT ( 'NONE', #6666 ) ;
#7263=CARTESIAN_POINT ( 'NONE',  ( 2.269879328256730222, 3.949706986712200329, 6.544400685875841894 ) ) ;
#7280=DIRECTION ( 'NONE',  ( 0.000000000000000000, 0.000000000000000000, 1.000000000000000000 ) ) ;
#7282=CARTESIAN_POINT ( 'NONE',  ( 0.3218525148189819718, -2.370084734146296501, 12.03385614540603221 ) ) ;
#7288=ORIENTED_EDGE ( 'NONE', *, *, #5145, .F. ) ;
#7292=CARTESIAN_POINT ( 'NONE',  ( 2.903928887688274063, 5.221047506681124162, -7.046356840275977973 ) ) ;
#7296=CARTESIAN_POINT ( 'NONE',  ( 0.2833330754217374681, 2.326361469893388545, -12.02930703389097467 ) ) ;
#7313=CARTESIAN_POINT ( 'NONE',  ( 1.547277799338532933, -7.618736734813612799, 10.12789507952316725 ) ) ;
#7314=CONICAL_SURFACE ( 'NONE', #44335, 7.938172270156617749, 1.280189991382167047 ) ;
#7317=VERTEX_POINT ( 'NONE', #33228 ) ;
#7325=CARTESIAN_POINT ( 'NONE',  ( 2.276198483117262139, -7.555081843354695792, 1.175725118478829545 ) ) ;
#7329=EDGE_CURVE ( 'NONE', #36221, #31314, #2636, .T. ) ;
#7336=ORIENTED_EDGE ( 'NONE', *, *, #20445, .T. ) ;
#7339=CARTESIAN_POINT ( 'NONE',  ( 2.241311220309555097, 3.736531646286262998, 6.657499176698799204 ) ) ;
#7346=CARTESIAN_POINT ( 'NONE',  ( 1.549075743846935138, 6.912427991524520365, -10.62322497417011569 ) ) ;
#7348=ORIENTED_EDGE ( 'NONE', *, *, #63306, .F. ) ;
#7352=EDGE_CURVE ( 'NONE', #49132, #36604, #42261, .T. ) ;
#7354=ORIENTED_EDGE ( 'NONE', *, *, #63549, .F. ) ;
#7356=CARTESIAN_POINT ( 'NONE',  ( 0.3474126878361767923, 6.359473273659701498, 10.49748369253934044 ) ) ;
#7365=ORIENTED_EDGE ( 'NONE', *, *, #52132, .T. ) ;
#7366=CARTESIAN_POINT ( 'NONE',  ( 2.655192694323943670, -9.204230091442310524, -2.733486750964531087 ) ) ;
#7370=VERTEX_POINT ( 'NONE', #9246 ) ;
#7371=CONICAL_SURFACE ( 'NONE', #24371, 7.938172270156617749, 1.280189991382167047 ) ;
#7375=DIRECTION ( 'NONE',  ( -0.3939253465568944290, 0.9068155327749432004, 0.1500280335741505655 ) ) ;
#7378=CARTESIAN_POINT ( 'NONE',  ( 2.280717697723834370, -5.756537207046726223, 5.034569468898537181 ) ) ;
#7379=CARTESIAN_POINT ( 'NONE',  ( 0.3675815128205912052, -3.951233083390393030, -11.62724744438069635 ) ) ;
#7383=VERTEX_POINT ( 'NONE', #35164 ) ;
#7384=CARTESIAN_POINT ( 'NONE',  ( 2.255723233588950549, -0.1321982600347777204, 7.638048593862504454 ) ) ;
#7389=CARTESIAN_POINT ( 'NONE',  ( 2.406456491625053928, -5.751891873093266661, -8.704497555695612121 ) ) ;
#7397=EDGE_CURVE ( 'NONE', #26297, #7370, #26380, .T. ) ;
#7404=ORIENTED_EDGE ( 'NONE', *, *, #8010, .F. ) ;
#7414=ORIENTED_EDGE ( 'NONE', *, *, #64284, .T. ) ;
#7417=CARTESIAN_POINT ( 'NONE',  ( 2.665405856346780400, 2.723742051529458585, 9.171500569027783101 ) ) ;
#7421=CARTESIAN_POINT ( 'NONE',  ( 1.014383007554947369, 8.367379244277135086, 9.280879504740973118 ) ) ;
#7422=CARTESIAN_POINT ( 'NONE',  ( 1.719304012339826659, -12.64775761152879596, -1.452142814149639305 ) ) ;
#7423=CARTESIAN_POINT ( 'NONE',  ( 2.241506898688417682, -5.822995664778295222, 4.937416071751822066 ) ) ;
#7427=EDGE_LOOP ( 'NONE', ( #59635, #58194, #50398, #41105 ) ) ;
#7434=CARTESIAN_POINT ( 'NONE',  ( 0.9232058338315058954, 6.559496812049661507, 10.60677148422246674 ) ) ;
#7437=CARTESIAN_POINT ( 'NONE',  ( 0.9232058338315058954, 11.84276737136200452, 3.908895078357559782 ) ) ;
#7442=ORIENTED_EDGE ( 'NONE', *, *, #59189, .T. ) ;
#7452=CARTESIAN_POINT ( 'NONE',  ( 2.305787727787083519, -3.682701754025559993, 6.711944854845811825 ) ) ;
#7459=B_SPLINE_CURVE_WITH_KNOTS ( 'NONE', 3,
 ( #9842, #4556, #29783, #15155, #14490, #56047, #55070, #24824, #14173, #45106, #24481, #65040, #30452, #5198, #40770, #25466 ),
 .UNSPECIFIED., .F., .F.,
 ( 4, 3, 3, 3, 3, 4 ),
 ( 0.000000000000000000, 0.0002176109881719783250, 0.0004352086762393702441, 0.0006528017811445535005, 0.0007615147961450135497, 0.0009453342004945436416 ),
 .UNSPECIFIED. ) ;
#7460=EDGE_CURVE ( 'NONE', #33098, #55547, #39096, .T. ) ;
#7464=EDGE_LOOP ( 'NONE', ( #32008, #40340, #2382, #5885 ) ) ;
#7466=CARTESIAN_POINT ( 'NONE',  ( 0.3665391374699464300, -10.76665847464317061, 5.911453292029563933 ) ) ;
#7474=ADVANCED_FACE ( 'NONE', ( #56810 ), #31831, .F. ) ;
#7475=EDGE_LOOP ( 'NONE', ( #50570, #31479, #6509, #40691 ) ) ;
#7479=CARTESIAN_POINT ( 'NONE',  ( 0.2648978790185593790, -4.312320170909161199, -11.46165506714232762 ) ) ;
#7486=CARTESIAN_POINT ( 'NONE',  ( 0.2759803524722231893, 5.960075719898836333, 10.70204612651777865 ) ) ;
#7488=EDGE_LOOP ( 'NONE', ( #1491, #17728, #50811, #42667 ) ) ;
#7499=CARTESIAN_POINT ( 'NONE',  ( 2.589278595513750503, 1.582391164331769406, 7.587119248534422766 ) ) ;
#7507=CARTESIAN_POINT ( 'NONE',  ( 1.194176325881334710, -11.96454551582841042, -3.807610977967044175 ) ) ;
#7508=ORIENTED_EDGE ( 'NONE', *, *, #59154, .F. ) ;
#7536=CARTESIAN_POINT ( 'NONE',  ( 2.889800649504073782, 3.986129653162709285, -4.645655809191325147 ) ) ;
#7543=VERTEX_POINT ( 'NONE', #51804 ) ;
#7544=CARTESIAN_POINT ( 'NONE',  ( 0.2653519890518161728, -6.123106317427082779, -10.60551359205156707 ) ) ;
#7556=( BOUNDED_SURFACE ( )  B_SPLINE_SURFACE ( 3, 1, ( 
 ( #4405, #64889 ),
 ( #40615, #60908 ),
 ( #30623, #15348 ),
 ( #30318, #5378 ) ),
 .UNSPECIFIED., .F., .F., .F. ) 
 B_SPLINE_SURFACE_WITH_KNOTS ( ( 4, 4 ),
 ( 2, 2 ),
 ( 0.000000000000000000, 1.000000000000000000 ),
 ( 0.000000000000000000, 1.000000000000000000 ),
 .UNSPECIFIED. ) 
 GEOMETRIC_REPRESENTATION_ITEM ( )  RATIONAL_B_SPLINE_SURFACE ( (
 ( 1.000000000000000000, 1.000000000000000000),
 ( 0.9942764183789327692, 0.8450855930916580938),
 ( 0.9942764183789327692, 0.8450855930916580938),
 ( 1.000000000000000000, 1.000000000000000000) ) ) 
 REPRESENTATION_ITEM ( '' )  SURFACE ( )  );
#7563=FACE_OUTER_BOUND ( 'NONE', #18649, .T. ) ;
#7565=DIRECTION ( 'NONE',  ( 0.000000000000000000, 0.000000000000000000, 1.000000000000000000 ) ) ;
#7569=CARTESIAN_POINT ( 'NONE',  ( 0.2657645697724703715, -11.55867655367624280, 4.045961170622970116 ) ) ;
#7572=CARTESIAN_POINT ( 'NONE',  ( 3.152665057734040488, 0.000000000000000000, 0.000000000000000000 ) ) ;
#7580=CARTESIAN_POINT ( 'NONE',  ( 0.6511581176968144202, -7.698038847496639470, -9.688955459274998461 ) ) ;
#7581=CARTESIAN_POINT ( 'NONE',  ( 2.298277635560815657, 5.755367168478065842, 5.044791616847147608 ) ) ;
#7584=CIRCLE ( 'NONE', #52226, 12.73084802173761787 ) ;
#7589=ORIENTED_EDGE ( 'NONE', *, *, #39255, .T. ) ;
#7591=DIRECTION ( 'NONE',  ( -1.000000000000000000, -0.000000000000000000, -0.000000000000000000 ) ) ;
#7593=CARTESIAN_POINT ( 'NONE',  ( 1.462291587751940014, 8.602888600422827992, -9.267729738231986758 ) ) ;
#7598=CARTESIAN_POINT ( 'NONE',  ( 1.937114397841935398, -12.33981801388255306, -3.531416430611418633 ) ) ;
#7604=CARTESIAN_POINT ( 'NONE',  ( 2.266490820343224577, 3.946561086901473558, 6.544980046121041006 ) ) ;
#7609=EDGE_CURVE ( 'NONE', #5162, #6270, #27214, .T. ) ;
#7610=CARTESIAN_POINT ( 'NONE',  ( 2.305787727787083519, 5.047606869483132641, -5.756228004061408221 ) ) ;
#7614=CARTESIAN_POINT ( 'NONE',  ( 0.3537226245948361103, 8.088784578751420540, -9.233810598191700691 ) ) ;
#7615=CARTESIAN_POINT ( 'NONE',  ( 0.2646305136544072623, -1.996350543472915184, -12.08286001766537687 ) ) ;
#7618=DIRECTION ( 'NONE',  ( 0.000000000000000000, 0.000000000000000000, 1.000000000000000000 ) ) ;
#7628=CARTESIAN_POINT ( 'NONE',  ( 2.589278595513451631, -4.081908913131900185, -6.588350318048493470 ) ) ;
#7630=CARTESIAN_POINT ( 'NONE',  ( 0.9296196016818686347, 5.870433615767222335, 10.99907063288793729 ) ) ;
#7634=ORIENTED_EDGE ( 'NONE', *, *, #57033, .T. ) ;
#7636=CARTESIAN_POINT ( 'NONE',  ( 2.247206125382827935, 5.923516414428655175, -4.819320926502576263 ) ) ;
#7638=CARTESIAN_POINT ( 'NONE',  ( 0.2653141617321012058, 9.352766656400060441, 7.905395731875527687 ) ) ;
#7644=CARTESIAN_POINT ( 'NONE',  ( 0.2650492594609232255, -2.017987075343877557, -12.07870403910583690 ) ) ;
#7651=CARTESIAN_POINT ( 'NONE',  ( 5.514970785353741078, 0.001326349372336295580, -0.004532877335078716770 ) ) ;
#7652=CARTESIAN_POINT ( 'NONE',  ( 1.372161826076671254, -8.551811013234788206, -9.274145586376244310 ) ) ;
#7660=ORIENTED_EDGE ( 'NONE', *, *, #44038, .F. ) ;
#7661=CARTESIAN_POINT ( 'NONE',  ( 2.241352910868909643, -6.569501556381469598, 3.889181972941426313 ) ) ;
#7667=EDGE_LOOP ( 'NONE', ( #61627, #2129, #12260, #60180 ) ) ;
#7672=CARTESIAN_POINT ( 'NONE',  ( 2.242819959140645913, 7.208832857235912606, -2.514828506624997573 ) ) ;
#7675=B_SPLINE_CURVE_WITH_KNOTS ( 'NONE', 3,
 ( #58496, #12578, #49506, #32860, #34179, #3946, #38524, #8921, #58845, #27901, #48208, #2661, #22921, #63451, #17921, #34510, #34812, #4925, #14856, #65728, #30810, #40820 ),
 .UNSPECIFIED., .F., .F.,
 ( 4, 3, 3, 3, 3, 3, 3, 4 ),
 ( 3.150255712925088731E-18, 4.449119708436434972E-05, 6.626296329539814380E-05, 8.803456484962096553E-05, 0.0001098060367612739010, 0.0001315774408628451900, 0.0001760698110411101100, 0.0001829697163287813692 ),
 .UNSPECIFIED. ) ;
#7680=CARTESIAN_POINT ( 'NONE',  ( 2.259025283528087513, -2.741148848567716456, -7.131631878998416774 ) ) ;
#7689=CARTESIAN_POINT ( 'NONE',  ( 0.2638984909335716500, 0.1991813963115696973, -12.24571285024408951 ) ) ;
#7699=ORIENTED_EDGE ( 'NONE', *, *, #6051, .F. ) ;
#7702=CARTESIAN_POINT ( 'NONE',  ( 2.247206125382826603, -2.720255231377985083, 7.135412558555544571 ) ) ;
#7703=CARTESIAN_POINT ( 'NONE',  ( 2.280717697722503878, 6.699799459370877841, 3.687451363406097027 ) ) ;
#7704=ORIENTED_EDGE ( 'NONE', *, *, #16779, .T. ) ;
#7713=CARTESIAN_POINT ( 'NONE',  ( 2.941278708680199916, -0.1348063076486517853, -6.138172921908582325 ) ) ;
#7722=CARTESIAN_POINT ( 'NONE',  ( 0.2833330754217379677, -12.02930703389099598, -2.326361469893360567 ) ) ;
#7727=CARTESIAN_POINT ( 'NONE',  ( 0.2638984909335720941, -1.930290337334137130, 12.09426044257623722 ) ) ;
#7731=CARTESIAN_POINT ( 'NONE',  ( 2.899286259009695943, 5.316140236670850783, -5.780956296532465011 ) ) ;
#7739=CARTESIAN_POINT ( 'NONE',  ( 2.284126774967660811, -0.1584898568958421905, 7.647017279602163597 ) ) ;
#7744=VERTEX_POINT ( 'NONE', #8205 ) ;
#7745=CARTESIAN_POINT ( 'NONE',  ( 2.262775599887391742, 6.546038779271709629, 3.942403752833328223 ) ) ;
#7749=VERTEX_POINT ( 'NONE', #43777 ) ;
#7751=CARTESIAN_POINT ( 'NONE',  ( 0.2648978790185584908, -7.769924372105139199, -9.465406350830686932 ) ) ;
#7757=CARTESIAN_POINT ( 'NONE',  ( 2.350038591458511128, 10.60256821300654018, 0.6402934222728309255 ) ) ;
#7761=DIRECTION ( 'NONE',  ( 0.000000000000000000, 0.000000000000000000, 1.000000000000000000 ) ) ;
#7764=CARTESIAN_POINT ( 'NONE',  ( 2.241352910868908310, -1.407733736974815963, -7.503490710578247125 ) ) ;
#7766=VERTEX_POINT ( 'NONE', #14474 ) ;
#7774=CARTESIAN_POINT ( 'NONE',  ( 0.2647959493198558945, -4.049980114636448469, 11.55693259385004978 ) ) ;
#7776=CARTESIAN_POINT ( 'NONE',  ( 0.2647959493198558945, 9.474789498086993333, 7.758440170207198783 ) ) ;
#7780=ORIENTED_EDGE ( 'NONE', *, *, #33540, .F. ) ;
#7790=CARTESIAN_POINT ( 'NONE',  ( 0.2646305136544072623, -7.972778379581489716, -9.296005949277306613 ) ) ;
#7801=CARTESIAN_POINT ( 'NONE',  ( 2.251152103363650792, -4.812779263775054162, 5.930529991878074725 ) ) ;
#7804=B_SPLINE_CURVE_WITH_KNOTS ( 'NONE', 3,
 ( #12329, #28291, #24277, #33610, #18973, #13961, #28607, #44541, #23970, #17670, #37932, #27970, #38596, #4007, #59215, #32926, #58224, #3710, #54222 ),
 .UNSPECIFIED., .F., .F.,
 ( 4, 3, 3, 3, 3, 3, 4 ),
 ( 8.673617379884035472E-19, 2.831840207499595013E-05, 4.217266859840597111E-05, 5.602024318396033026E-05, 6.290810167969150990E-05, 9.120440630944968421E-05, 0.0001153103026479758458 ),
 .UNSPECIFIED. ) ;
#7809=CARTESIAN_POINT ( 'NONE',  ( 1.937114397841935398, 12.45230409340485878, -3.111612666689950846 ) ) ;
#7811=ORIENTED_EDGE ( 'NONE', *, *, #21976, .F. ) ;
#7813=CARTESIAN_POINT ( 'NONE',  ( 0.2648978790185593790, -11.55204314799266818, 4.063980959785006952 ) ) ;
#7817=ADVANCED_FACE ( 'NONE', ( #61344 ), #54401, .F. ) ;
#7830=VECTOR ( 'NONE', #33712, 1000.000000000000000 ) ;
#7839=CARTESIAN_POINT ( 'NONE',  ( 2.297017764050092392, -7.563558677601590396, -1.166330442180250726 ) ) ;
#7847=CARTESIAN_POINT ( 'NONE',  ( 1.109979610372329395, 4.732439402375099746, -11.59954799439127449 ) ) ;
#7849=CARTESIAN_POINT ( 'NONE',  ( 0.2652384529303136174, 10.57229402027116372, -6.180212112237552624 ) ) ;
#7862=CARTESIAN_POINT ( 'NONE',  ( 0.3675815128205894289, -0.2638082659429279997, 12.27743992903066150 ) ) ;
#7870=FACE_OUTER_BOUND ( 'NONE', #6679, .T. ) ;
#7876=CARTESIAN_POINT ( 'NONE',  ( 2.284126774967660811, 3.960764882115096697, -6.543266298866090125 ) ) ;
#7889=EDGE_LOOP ( 'NONE', ( #1777, #31982, #52803, #39873 ) ) ;
#7893=CARTESIAN_POINT ( 'NONE',  ( 2.262775599886256650, 1.465770593192990745, -7.499645832851591365 ) ) ;
#7897=CARTESIAN_POINT ( 'NONE',  ( 0.2653141617321031487, -6.084921229689344457, -10.62747662594936671 ) ) ;
#7900=DIRECTION ( 'NONE',  ( -0.3939253465568943180, -0.8603393047164982210, 0.3234796780324276089 ) ) ;
#7902=CARTESIAN_POINT ( 'NONE',  ( 2.247112776671468914, -0.1165461824817215913, -7.635437439951572536 ) ) ;
#7908=EDGE_CURVE ( 'NONE', #8359, #64295, #33459, .T. ) ;
#7909=CARTESIAN_POINT ( 'NONE',  ( 0.3040950598368144520, 6.347045025870913904, -10.49113473328024249 ) ) ;
#7920=VERTEX_POINT ( 'NONE', #17116 ) ;
#7921=CARTESIAN_POINT ( 'NONE',  ( 0.3106921474978504016, 1.896868624983064411, 12.11369598333777020 ) ) ;
#7925=CARTESIAN_POINT ( 'NONE',  ( 0.2834382757448022372, -9.514772331577374231, -7.719209397492075908 ) ) ;
#7926=DIRECTION ( 'NONE',  ( -1.000000000000000000, -0.000000000000000000, -0.000000000000000000 ) ) ;
#7930=CARTESIAN_POINT ( 'NONE',  ( 2.280717697723835258, -1.173604464351654331, 7.556934756535380160 ) ) ;
#7935=FILL_AREA_STYLE_COLOUR ( '', #41674 ) ;
#7939=CARTESIAN_POINT ( 'NONE',  ( 0.3675815128205894289, 12.04510820461659293, 2.391755495700645273 ) ) ;
#7944=CARTESIAN_POINT ( 'NONE',  ( 2.263328370261525446, 6.545781832005237000, -3.943189046766256478 ) ) ;
#7953=ORIENTED_EDGE ( 'NONE', *, *, #35915, .F. ) ;
#7963=ORIENTED_EDGE ( 'NONE', *, *, #34823, .T. ) ;
#7964=CARTESIAN_POINT ( 'NONE',  ( 2.241311220309555097, -1.417008678104535679, 7.501736494813740386 ) ) ;
#7966=CARTESIAN_POINT ( 'NONE',  ( 2.241317068080780128, 3.737686401539939141, -6.656851426547526707 ) ) ;
#7971=CARTESIAN_POINT ( 'NONE',  ( 0.3164563675027701195, -11.60369811966059217, -3.967501530099192930 ) ) ;
#7976=CARTESIAN_POINT ( 'NONE',  ( 2.373367633546869637, -7.151506276328608358, -2.795365972209146399 ) ) ;
#7980=CARTESIAN_POINT ( 'NONE',  ( 0.3218525148189836926, -0.2444206315274009833, 12.26259572563018452 ) ) ;
#7983=CARTESIAN_POINT ( 'NONE',  ( 2.373367633546870969, -4.795703124519850036, -5.996611082972014728 ) ) ;
#7985=EDGE_LOOP ( 'NONE', ( #34850, #64535, #17566, #57076 ) ) ;
#7987=CARTESIAN_POINT ( 'NONE',  ( 1.104777566491139229, 10.60111489796743278, -6.672212870706091259 ) ) ;
#7988=CARTESIAN_POINT ( 'NONE',  ( 2.305787727787083519, -3.682701754025559993, 6.711944854845811825 ) ) ;
#7990=CARTESIAN_POINT ( 'NONE',  ( 0.2653519890518167279, -2.126538543977996465, -12.06014856238022936 ) ) ;
#7995=CARTESIAN_POINT ( 'NONE',  ( 3.152665057735843490, -3.546019893114926713, 7.102135024646879735 ) ) ;
#7998=CARTESIAN_POINT ( 'NONE',  ( 2.305787727787084407, -3.971363876083918498, -6.545285700970570275 ) ) ;
#8001=VERTEX_POINT ( 'NONE', #28400 ) ;
#8006=CARTESIAN_POINT ( 'NONE',  ( 2.297017764050033772, 5.044319338147331244, 5.755222757172066217 ) ) ;
#8010=EDGE_CURVE ( 'NONE', #48073, #807, #21569, .T. ) ;
#8014=ORIENTED_EDGE ( 'NONE', *, *, #40213, .T. ) ;
#8015=CARTESIAN_POINT ( 'NONE',  ( 2.298277635560276977, 7.246601281227255775, -2.461898367585308556 ) ) ;
#8016=DIRECTION ( 'NONE',  ( 0.000000000000000000, 0.000000000000000000, 1.000000000000000000 ) ) ;
#8020=CARTESIAN_POINT ( 'NONE',  ( 2.268878695253354838, -7.551766617932575976, 1.181158368266927106 ) ) ;
#8030=CARTESIAN_POINT ( 'NONE',  ( 0.2648978790185584908, -4.312320170909314854, 11.46165506714226900 ) ) ;
#8035=CARTESIAN_POINT ( 'NONE',  ( 1.020182472822815711, -0.4462553704985123826, 12.48987306958583687 ) ) ;
#8038=CARTESIAN_POINT ( 'NONE',  ( 2.247206125382826158, -7.135412558555532136, -2.720255231378005956 ) ) ;
#8041=ORIENTED_EDGE ( 'NONE', *, *, #52887, .T. ) ;
#8042=CARTESIAN_POINT ( 'NONE',  ( 2.261269890822070749, -2.744033622443662779, 7.131324074141573988 ) ) ;
#8046=CARTESIAN_POINT ( 'NONE',  ( 0.2872850955227708725, 6.306790329742928414, 10.50585060073182753 ) ) ;
#8047=CARTESIAN_POINT ( 'NONE',  ( 0.2958664285830446272, -2.345117904768542871, -12.02992237133200426 ) ) ;
#8050=CARTESIAN_POINT ( 'NONE',  ( 2.556980015514201288, -6.815084337351986932, -3.668282146013173151 ) ) ;
#8064=CARTESIAN_POINT ( 'NONE',  ( 0.2653519890518174495, 7.871710682401907633, 9.381125756446593300 ) ) ;
#8066=CARTESIAN_POINT ( 'NONE',  ( 2.963017218115634677, 5.350609950027751971, -5.778072204777588539 ) ) ;
#8068=ORIENTED_EDGE ( 'NONE', *, *, #36143, .T. ) ;
#8069=CARTESIAN_POINT ( 'NONE',  ( 2.251139882113958990, -0.1241612276497191941, 7.636654603229074745 ) ) ;
#8077=CARTESIAN_POINT ( 'NONE',  ( 1.719304012338249921, 10.22720798541395837, 7.581471372740089976 ) ) ;
#8081=CARTESIAN_POINT ( 'NONE',  ( 0.2706063244538022827, -7.737788863017243557, -9.494160524941774426 ) ) ;
#8082=CONICAL_SURFACE ( 'NONE', #64359, 7.938172270156617749, 1.280189991382167047 ) ;
#8087=CARTESIAN_POINT ( 'NONE',  ( 2.034671305880900505, 11.65517003033663102, 0.7032348381690887162 ) ) ;
#8091=CARTESIAN_POINT ( 'NONE',  ( 0.3164563675027606271, -7.696930404785105040, 9.546944054903065080 ) ) ;
#8093=CARTESIAN_POINT ( 'NONE',  ( 2.288423627607477862, -1.486973602181100640, -7.504187945869075449 ) ) ;
#8094=LINE ( 'NONE', #8746, #4343 ) ;
#8096=FACE_OUTER_BOUND ( 'NONE', #60115, .T. ) ;
#8103=CARTESIAN_POINT ( 'NONE',  ( 0.2648978790185602672, -4.063980959785125080, 11.55204314799262555 ) ) ;
#8104=CARTESIAN_POINT ( 'NONE',  ( 0.2717059086739008755, 9.494961435243697068, 7.737372654246616577 ) ) ;
#8109=CARTESIAN_POINT ( 'NONE',  ( 1.452237505248552996, -12.55261342181976403, 1.611965288198690116 ) ) ;
#8110=VERTEX_POINT ( 'NONE', #20726 ) ;
#8113=FACE_OUTER_BOUND ( 'NONE', #13931, .T. ) ;
#8116=CARTESIAN_POINT ( 'NONE',  ( 0.2647959493198559500, -10.53111783886895125, 6.249846955854230224 ) ) ;
#8117=B_SPLINE_CURVE_WITH_KNOTS ( 'NONE', 3,
 ( #51594, #26300, #32259, #46580, #61873, #22279, #37591, #51914, #21656, #46917, #41583, #36606, #56910, #6355, #41913, #57558 ),
 .UNSPECIFIED., .F., .F.,
 ( 4, 3, 3, 3, 3, 4 ),
 ( 2.646037958931776106E-15, 0.0002126834539179706172, 0.0004253519300366259736, 0.0006380165497224161725, 0.0007442707582428239980, 0.0009453531351418035774 ),
 .UNSPECIFIED. ) ;
#8118=CARTESIAN_POINT ( 'NONE',  ( 5.536195898058073439, -0.006672323185952749695, 0.005266167600747576234 ) ) ;
#8122=CARTESIAN_POINT ( 'NONE',  ( 0.5547464869798250930, -10.83828453080460719, -5.905377260991333976 ) ) ;
#8129=B_SPLINE_CURVE_WITH_KNOTS ( 'NONE', 3,
 ( #20097, #40360, #10122, #50698, #21066, #11114, #5143, #41347, #61631, #16085, #2110, #62287, #23056 ),
 .UNSPECIFIED., .F., .F.,
 ( 4, 3, 3, 3, 4 ),
 ( 3.035766082959412415E-18, 6.607593386745364342E-05, 0.0001321518677373504551, 0.0001982171734706202092, 0.0002642860854759481208 ),
 .UNSPECIFIED. ) ;
#8141=CARTESIAN_POINT ( 'NONE',  ( 2.241352910868908754, -4.843133558968088614, -5.901537464758503937 ) ) ;
#8142=FACE_OUTER_BOUND ( 'NONE', #13794, .T. ) ;
#8149=EDGE_CURVE ( 'NONE', #11008, #34835, #3330, .T. ) ;
#8152=CARTESIAN_POINT ( 'NONE',  ( 1.287602823386723383, -12.28793447239711512, -2.727479899220638604 ) ) ;
#8155=CARTESIAN_POINT ( 'NONE',  ( 2.241352910868908310, 6.652881166698564108, -3.744764251556923274 ) ) ;
#8157=CARTESIAN_POINT ( 'NONE',  ( 2.368238019615318990, 3.681632831800480954, -6.736275681109146873 ) ) ;
#8158=CARTESIAN_POINT ( 'NONE',  ( 1.547277799337431592, 12.12286970032282873, 3.695326562729380981 ) ) ;
#8160=ORIENTED_EDGE ( 'NONE', *, *, #29869, .T. ) ;
#8161=CARTESIAN_POINT ( 'NONE',  ( 0.3040950598368144520, 9.229598020917689993, 8.072385578287505581 ) ) ;
#8170=CARTESIAN_POINT ( 'NONE',  ( 2.941278708680199916, -3.185832147968409966, -5.248410529370257649 ) ) ;
#8182=CARTESIAN_POINT ( 'NONE',  ( 2.241526690369556984, -1.308664175663819762, 7.521460607153596989 ) ) ;
#8183=CARTESIAN_POINT ( 'NONE',  ( 0.2648321136542702292, -10.53380804838493923, -6.245325033825842809 ) ) ;
#8184=CARTESIAN_POINT ( 'NONE',  ( 5.515539859299206427, -0.003740028639278315456, -0.004759416711441667551 ) ) ;
#8196=CARTESIAN_POINT ( 'NONE',  ( 1.198791140417948986, 3.806343609711437370, 11.96656299555031566 ) ) ;
#8205=CARTESIAN_POINT ( 'NONE',  ( 0.3675815128205912052, 11.44679196252415210, -4.447030445008065769 ) ) ;
#8208=CARTESIAN_POINT ( 'NONE',  ( 2.256373768223414178, 1.457292142211218611, 7.499124080223143807 ) ) ;
#8211=CARTESIAN_POINT ( 'NONE',  ( 2.717984159218836737, -6.148373979318608740, -4.788867404453649002 ) ) ;
#8213=CARTESIAN_POINT ( 'NONE',  ( 2.430348790457612207, -1.144258029164365142, 7.611893186157537627 ) ) ;
#8215=CARTESIAN_POINT ( 'NONE',  ( 2.260457164927189400, -0.1384509728648543325, -7.639515169785722648 ) ) ;
#8222=CARTESIAN_POINT ( 'NONE',  ( 0.2646305136544072623, 12.08286001766535556, 1.996350543473035755 ) ) ;
#8226=CARTESIAN_POINT ( 'NONE',  ( 0.2671309869109498303, -11.45180222993658070, 4.340541005679486197 ) ) ;
#8232=CARTESIAN_POINT ( 'NONE',  ( 2.255723233588949661, -7.222632368701285444, 2.488140745365843287 ) ) ;
#8234=CARTESIAN_POINT ( 'NONE',  ( 1.719304012338836563, -7.017415949612288095, 10.62216384465580710 ) ) ;
#8238=CARTESIAN_POINT ( 'NONE',  ( 2.247112776671466250, 7.539676020705989856, 1.211104213045398614 ) ) ;
#8239=CARTESIAN_POINT ( 'NONE',  ( 0.2648978790185584908, -1.996248716311547433, -12.08224454301450734 ) ) ;
#8252=CARTESIAN_POINT ( 'NONE',  ( 2.244591118396555895, 6.558116599718226247, -3.910457279126638319 ) ) ;
#8259=CARTESIAN_POINT ( 'NONE',  ( 5.536195898058073439, -0.002666509901870014500, 0.008071068258923596792 ) ) ;
#8267=CARTESIAN_POINT ( 'NONE',  ( 2.889800649504073782, -0.06738247734046161341, -6.121013568931507720 ) ) ;
#8275=CARTESIAN_POINT ( 'NONE',  ( 2.889800649504073782, 5.334644486274195074, 3.002151847318935030 ) ) ;
#8283=CARTESIAN_POINT ( 'NONE',  ( 0.2655924914740778187, 12.06787830249868243, -2.083162675473490655 ) ) ;
#8291=ADVANCED_FACE ( 'NONE', ( #41204 ), #34157, .T. ) ;
#8296=CARTESIAN_POINT ( 'NONE',  ( 0.7400311444011681283, 10.56075429936776366, -6.506979270898069601 ) ) ;
#8297=CARTESIAN_POINT ( 'NONE',  ( 2.276905613633648962, -3.688905863353259207, 6.697548486790754652 ) ) ;
#8298=LINE ( 'NONE', #22951, #36457 ) ;
#8300=CARTESIAN_POINT ( 'NONE',  ( 1.104777566491147445, 2.644034362100695645, 12.24382064406180071 ) ) ;
#8304=CARTESIAN_POINT ( 'NONE',  ( 1.104777566491144336, -8.411711248089032367, -9.281442536087567419 ) ) ;
#8312=CARTESIAN_POINT ( 'NONE',  ( 2.963017218115620910, -3.599595431209440477, -7.004145770368809920 ) ) ;
#8315=CARTESIAN_POINT ( 'NONE',  ( 0.2739690278137274504, 9.264642836915941260, -8.012873994335592442 ) ) ;
#8316=CARTESIAN_POINT ( 'NONE',  ( 2.889800649504073782, 0.9965440656173724099, 6.039722463373542460 ) ) ;
#8318=ADVANCED_FACE ( 'NONE', ( #61489 ), #33605, .F. ) ;
#8321=CARTESIAN_POINT ( 'NONE',  ( 2.261269890822072082, 7.226741992146827442, -2.481875047312865679 ) ) ;
#8323=VERTEX_POINT ( 'NONE', #50879 ) ;
#8328=CARTESIAN_POINT ( 'NONE',  ( 3.047904605210400408, 7.270585891216620134, 3.098478597269316737 ) ) ;
#8329=CARTESIAN_POINT ( 'NONE',  ( 2.256373768223415510, -2.737361830682274899, -7.132139410180991845 ) ) ;
#8332=ORIENTED_EDGE ( 'NONE', *, *, #36311, .F. ) ;
#8340=CARTESIAN_POINT ( 'NONE',  ( 0.3675815128205894289, -8.093875121226016489, -9.235491948680088825 ) ) ;
#8341=CARTESIAN_POINT ( 'NONE',  ( 0.2653141617321020385, 11.49253039221382444, 4.229807441322350314 ) ) ;
#8342=DIRECTION ( 'NONE',  ( 0.3865475372811021382, -0.7888450329201742717, -0.4778122177792066827 ) ) ;
#8345=CARTESIAN_POINT ( 'NONE',  ( 1.719304012338199517, 0.000000000000000000, 0.000000000000000000 ) ) ;
#8347=CARTESIAN_POINT ( 'NONE',  ( 2.245754705088392811, -7.136529175883343790, -2.715960966012167521 ) ) ;
#8348=( BOUNDED_SURFACE ( )  B_SPLINE_SURFACE ( 3, 1, ( 
 ( #34141, #64398 ),
 ( #8551, #39458 ),
 ( #29178, #59422 ),
 ( #43808, #12888 ) ),
 .UNSPECIFIED., .F., .F., .F. ) 
 B_SPLINE_SURFACE_WITH_KNOTS ( ( 4, 4 ),
 ( 2, 2 ),
 ( 0.000000000000000000, 1.000000000000000000 ),
 ( 0.000000000000000000, 1.000000000000000000 ),
 .UNSPECIFIED. ) 
 GEOMETRIC_REPRESENTATION_ITEM ( )  RATIONAL_B_SPLINE_SURFACE ( (
 ( 1.000000000000000000, 1.000000000000000000),
 ( 0.9942764183789327692, 0.8450855930916580938),
 ( 0.9942764183789327692, 0.8450855930916580938),
 ( 1.000000000000000000, 1.000000000000000000) ) ) 
 REPRESENTATION_ITEM ( '' )  SURFACE ( )  );
#8354=CARTESIAN_POINT ( 'NONE',  ( 3.152665057735335452, -7.719888720907720270, 1.848755561853250295 ) ) ;
#8355=EDGE_CURVE ( 'NONE', #13777, #43254, #25942, .T. ) ;
#8356=EDGE_CURVE ( 'NONE', #14146, #21447, #63576, .T. ) ;
#8359=VERTEX_POINT ( 'NONE', #43172 ) ;
#8364=CARTESIAN_POINT ( 'NONE',  ( 3.152665057736217413, -7.923639299008909731, 0.4801242025612903475 ) ) ;
#8370=CARTESIAN_POINT ( 'NONE',  ( 2.903928887688475680, -7.845932231841446836, -3.918141038919469299 ) ) ;
#8373=VECTOR ( 'NONE', #41650, 1000.000000000000114 ) ;
#8375=CARTESIAN_POINT ( 'NONE',  ( 2.770579946183332254, -7.633739187313462793, -1.653873933978953215 ) ) ;
#8388=CARTESIAN_POINT ( 'NONE',  ( 0.3675815128205894289, 1.872154644482245889, -12.13672785388548547 ) ) ;
#8401=CARTESIAN_POINT ( 'NONE',  ( 5.515539859299206427, 0.0001942659352250529969, 0.006049968793488821710 ) ) ;
#8402=CARTESIAN_POINT ( 'NONE',  ( 5.514624014163232779, 0.003498325728817810402, -0.002216125254993677428 ) ) ;
#8407=CARTESIAN_POINT ( 'NONE',  ( 2.276905613633650738, -1.479235344773113026, -7.501802783089495108 ) ) ;
#8410=CARTESIAN_POINT ( 'NONE',  ( 0.2638984909335716500, -12.09426044257625321, 1.930290337334017226 ) ) ;
#8416=CARTESIAN_POINT ( 'NONE',  ( 2.241352910868909643, 7.202080440908774861, -2.532612177304371048 ) ) ;
#8418=CARTESIAN_POINT ( 'NONE',  ( 0.2648978790185593790, 4.063980959785203240, -11.55204314799259890 ) ) ;
#8423=CARTESIAN_POINT ( 'NONE',  ( 0.2872850955227739256, 9.519656861923731839, 7.715220952083274852 ) ) ;
#8428=CARTESIAN_POINT ( 'NONE',  ( 5.536195898058073439, -0.004468797463753835728, -0.007230647766619673761 ) ) ;
#8430=VERTEX_POINT ( 'NONE', #37197 ) ;
#8431=CARTESIAN_POINT ( 'NONE',  ( 0.4613984246114872789, 1.858723191796632923, -12.17044190070615350 ) ) ;
#8436=CARTESIAN_POINT ( 'NONE',  ( 0.3665391374699465965, -10.76665847464308534, -5.911453292029717588 ) ) ;
#8442=CARTESIAN_POINT ( 'NONE',  ( 2.889800649504073782, 6.121013568931506832, -0.06738247734052572879 ) ) ;
#8443=CARTESIAN_POINT ( 'NONE',  ( 2.262775599886259315, -5.761998514039089692, -5.019217486251096538 ) ) ;
#8454=CARTESIAN_POINT ( 'NONE',  ( 2.305787727787084851, -1.493241775258474124, 7.508843116234150905 ) ) ;
#8462=CARTESIAN_POINT ( 'NONE',  ( 5.515539859299206427, 0.0008592514567752934825, -0.005991790098944302714 ) ) ;
#8463=CARTESIAN_POINT ( 'NONE',  ( 0.3160775863651099638, -12.11619190710940330, 1.892533050396128402 ) ) ;
#8466=CARTESIAN_POINT ( 'NONE',  ( 0.2834382757447992951, 2.326926314863310363, 12.02923522794682931 ) ) ;
#8467=CARTESIAN_POINT ( 'NONE',  ( 0.2651627923886316074, -4.105544202112473506, -11.53745192040746836 ) ) ;
#8469=ORIENTED_EDGE ( 'NONE', *, *, #23736, .T. ) ;
#8472=ORIENTED_EDGE ( 'NONE', *, *, #48669, .T. ) ;
#8473=CARTESIAN_POINT ( 'NONE',  ( 0.8375941296801562297, -12.17542732751302204, -2.537217542322243613 ) ) ;
#8476=CARTESIAN_POINT ( 'NONE',  ( 2.889800649504073782, 5.774917447013026006, -2.030191121417079358 ) ) ;
#8478=CARTESIAN_POINT ( 'NONE',  ( 1.375507693217270067, 7.647735792765331553, 10.03411718356051807 ) ) ;
#8498=ORIENTED_EDGE ( 'NONE', *, *, #37915, .T. ) ;
#8503=VECTOR ( 'NONE', #41097, 1000.000000000000114 ) ;
#8508=ORIENTED_EDGE ( 'NONE', *, *, #2763, .T. ) ;
#8512=CARTESIAN_POINT ( 'NONE',  ( 0.2653519991613803586, -11.50013121838206054, -4.209134909048866113 ) ) ;
#8515=CARTESIAN_POINT ( 'NONE',  ( 5.516018279890452902, -0.005331956019561682678, 0.004180585980735035401 ) ) ;
#8519=CARTESIAN_POINT ( 'NONE',  ( 3.152665057736003362, 6.378477742801834438, 4.725420687649379836 ) ) ;
#8530=CARTESIAN_POINT ( 'NONE',  ( 2.241352910868908310, -5.901537464758487062, 4.843133558968109043 ) ) ;
#8532=( BOUNDED_SURFACE ( )  B_SPLINE_SURFACE ( 3, 1, ( 
 ( #257, #15524 ),
 ( #46143, #35791 ),
 ( #40130, #36118 ),
 ( #15202, #14848 ) ),
 .UNSPECIFIED., .F., .F., .T. ) 
 B_SPLINE_SURFACE_WITH_KNOTS ( ( 4, 4 ),
 ( 2, 2 ),
 ( 0.000000000000000000, 1.000000000000000000 ),
 ( 0.000000000000000000, 1.000000000000000000 ),
 .UNSPECIFIED. ) 
 GEOMETRIC_REPRESENTATION_ITEM ( )  RATIONAL_B_SPLINE_SURFACE ( (
 ( 1.000000000000000000, 1.000000000000000000),
 ( 0.6933888150995267674, 0.9895912004443193632),
 ( 0.6933888150995267674, 0.9895912004443193632),
 ( 1.000000000000000000, 1.000000000000000000) ) ) 
 REPRESENTATION_ITEM ( '' )  SURFACE ( )  );
#8536=FACE_OUTER_BOUND ( 'NONE', #30578, .T. ) ;
#8539=EDGE_CURVE ( 'NONE', #47422, #60037, #59598, .T. ) ;
#8542=LINE ( 'NONE', #43452, #45574 ) ;
#8543=CARTESIAN_POINT ( 'NONE',  ( 0.2956976708475416160, -8.045468685196979663, 9.245952174682525282 ) ) ;
#8544=B_SPLINE_CURVE_WITH_KNOTS ( 'NONE', 3,
 ( #27442, #12802, #28119, #31768, #42078, #62358, #47429, #48082, #2864, #1864, #42727, #33090, #47102, #7486, #17488, #1557, #21831, #37760, #58053 ),
 .UNSPECIFIED., .F., .F.,
 ( 4, 3, 3, 3, 3, 3, 4 ),
 ( 7.566340834308382272E-18, 4.457896483014924563E-05, 6.639290541542123701E-05, 8.820687556479044501E-05, 0.0001100173248778947826, 0.0001545671401658086329, 0.0001830328308068585768 ),
 .UNSPECIFIED. ) ;
#8547=EDGE_CURVE ( 'NONE', #45693, #53897, #15121, .T. ) ;
#8551=CARTESIAN_POINT ( 'NONE',  ( 5.515188684475870851, -0.001485678338381548735, 0.005140903460551581733 ) ) ;
#8552=CARTESIAN_POINT ( 'NONE',  ( 1.719304012343089161, 12.64775761152706401, -1.452142814147889816 ) ) ;
#8553=CARTESIAN_POINT ( 'NONE',  ( 3.092491956585974311, -4.738927301401886893, 6.343509225035307786 ) ) ;
#8561=CARTESIAN_POINT ( 'NONE',  ( 0.3040950598368144520, 12.11647736519423901, -1.881452845810252628 ) ) ;
#8565=CARTESIAN_POINT ( 'NONE',  ( 2.665405856346787949, -9.171500569027768890, 2.723742051529419506 ) ) ;
#8571=CARTESIAN_POINT ( 'NONE',  ( 5.520433897694421610, -0.003119431460922320043, 0.01473594271720231851 ) ) ;
#8585=CARTESIAN_POINT ( 'NONE',  ( 5.514624014163232779, 0.001574979445069367000, 0.003830004412313181561 ) ) ;
#8608=CARTESIAN_POINT ( 'NONE',  ( 2.305787727787084851, -7.508843116234144688, -1.493241775258500770 ) ) ;
#8611=CARTESIAN_POINT ( 'NONE',  ( 0.2650492594609242802, 9.309909082761148369, 7.955687020697082446 ) ) ;
#8612=CARTESIAN_POINT ( 'NONE',  ( 5.516018279890452902, -0.004180585980734566158, 0.005331956019561453694 ) ) ;
#8618=CARTESIAN_POINT ( 'NONE',  ( 1.194176325881341594, 2.684784923266289258, 12.26540585042609521 ) ) ;
#8619=EDGE_CURVE ( 'NONE', #37098, #43663, #40971, .T. ) ;
#8622=ORIENTED_EDGE ( 'NONE', *, *, #55958, .T. ) ;
#8623=ADVANCED_FACE ( 'NONE', ( #62541 ), #36514, .F. ) ;
#8628=CARTESIAN_POINT ( 'NONE',  ( 3.031336079628799585, 5.773872239512944482, -5.388626255826449274 ) ) ;
#8636=EDGE_CURVE ( 'NONE', #44356, #20918, #62836, .T. ) ;
#8637=ORIENTED_EDGE ( 'NONE', *, *, #7352, .T. ) ;
#8641=CARTESIAN_POINT ( 'NONE',  ( 0.2648978790185584908, 12.24533305150758089, 0.1321385342562836074 ) ) ;
#8642=CARTESIAN_POINT ( 'NONE',  ( 0.3474126878361828430, 9.233692382639482332, -8.085727498271683800 ) ) ;
#8647=ORIENTED_EDGE ( 'NONE', *, *, #41138, .T. ) ;
#8650=EDGE_CURVE ( 'NONE', #28065, #51219, #61126, .T. ) ;
#8662=ORIENTED_EDGE ( 'NONE', *, *, #44969, .T. ) ;
#8675=CARTESIAN_POINT ( 'NONE',  ( 0.6473888112830248343, 11.51036712212685309, -4.540486098228861067 ) ) ;
#8677=VERTEX_POINT ( 'NONE', #44802 ) ;
#8686=FACE_OUTER_BOUND ( 'NONE', #50411, .T. ) ;
#8687=CARTESIAN_POINT ( 'NONE',  ( 0.3401186441510237746, 3.955862996551503752, 11.61600526280572332 ) ) ;
#8689=B_SPLINE_CURVE_WITH_KNOTS ( 'NONE', 3,
 ( #43639, #18404, #56153, #9360, #29645, #59942, #13701, #3775, #4411, #39641, #46207, #61156, #54930, #29021, #61463, #49632, #38983, #59603, #24034, #20908, #14362, #39302 ),
 .UNSPECIFIED., .F., .F.,
 ( 4, 3, 3, 3, 3, 3, 3, 4 ),
 ( 1.084202172485504434E-19, 4.449119708436757522E-05, 6.626296329540340218E-05, 8.803456484962588510E-05, 0.0001098060367612804469, 0.0001315774408628515326, 0.0001760698110411161002, 0.0001829697163287829413 ),
 .UNSPECIFIED. ) ;
#8690=ORIENTED_EDGE ( 'NONE', *, *, #19774, .F. ) ;
#8702=CARTESIAN_POINT ( 'NONE',  ( 1.104777566491146112, -9.281442536087537221, 8.411711248089069670 ) ) ;
#8704=EDGE_CURVE ( 'NONE', #42070, #19326, #9222, .T. ) ;
#8705=CARTESIAN_POINT ( 'NONE',  ( 2.241506898688419902, 3.783130304541519440, -6.631235260227124506 ) ) ;
#8706=DIRECTION ( 'NONE',  ( 0.000000000000000000, 0.000000000000000000, 1.000000000000000000 ) ) ;
#8710=CARTESIAN_POINT ( 'NONE',  ( 0.3632410797595259644, -12.13515851238022414, -1.872837903657321945 ) ) ;
#8712=CARTESIAN_POINT ( 'NONE',  ( 2.241352910868908310, 7.633946224498473931, 0.08337961031706864201 ) ) ;
#8720=ORIENTED_EDGE ( 'NONE', *, *, #48662, .T. ) ;
#8739=CARTESIAN_POINT ( 'NONE',  ( 0.2676618633000471537, 10.52491907319761033, 6.262131165853769055 ) ) ;
#8742=( BOUNDED_SURFACE ( )  B_SPLINE_SURFACE ( 3, 1, ( 
 ( #16466, #31728 ),
 ( #32390, #21791 ),
 ( #1171, #48035 ),
 ( #26427, #31421 ) ),
 .UNSPECIFIED., .F., .F., .F. ) 
 B_SPLINE_SURFACE_WITH_KNOTS ( ( 4, 4 ),
 ( 2, 2 ),
 ( 0.000000000000000000, 1.000000000000000000 ),
 ( 0.000000000000000000, 1.000000000000000000 ),
 .UNSPECIFIED. ) 
 GEOMETRIC_REPRESENTATION_ITEM ( )  RATIONAL_B_SPLINE_SURFACE ( (
 ( 1.000000000000000000, 1.000000000000000000),
 ( 0.9942764183789327692, 0.8450855930916585379),
 ( 0.9942764183789327692, 0.8450855930916585379),
 ( 1.000000000000000000, 1.000000000000000000) ) ) 
 REPRESENTATION_ITEM ( '' )  SURFACE ( )  );
#8746=CARTESIAN_POINT ( 'NONE',  ( 2.941278708680199916, -6.138172921908581436, 0.1348063076486732403 ) ) ;
#8749=FACE_OUTER_BOUND ( 'NONE', #40962, .T. ) ;
#8751=CARTESIAN_POINT ( 'NONE',  ( 0.2834382757448032364, -6.300836243950088900, -10.50792790568174517 ) ) ;
#8753=CARTESIAN_POINT ( 'NONE',  ( 2.241352910868908310, -7.145045428366559648, -2.689314586382423045 ) ) ;
#8755=CARTESIAN_POINT ( 'NONE',  ( 0.3006302518452061423, 3.979421585299272035, -11.59403866275562223 ) ) ;
#8757=CARTESIAN_POINT ( 'NONE',  ( 0.3006302518452061423, -3.979421585299194764, 11.59403866275565775 ) ) ;
#8761=ORIENTED_EDGE ( 'NONE', *, *, #65525, .F. ) ;
#8766=AXIS2_PLACEMENT_3D ( 'NONE', #42838, #63761, #37859 ) ;
#8770=FACE_OUTER_BOUND ( 'NONE', #6856, .T. ) ;
#8771=CARTESIAN_POINT ( 'NONE',  ( 5.514624014163232779, 0.001921576324372452002, 0.003668383633201380105 ) ) ;
#8772=B_SPLINE_CURVE_WITH_KNOTS ( 'NONE', 3,
 ( #55227, #30292, #14638, #9659, #20953, #15955, #50589, #50906, #14972, #45571, #41232, #54008, #29954, #56204, #5355, #30934 ),
 .UNSPECIFIED., .F., .F.,
 ( 4, 3, 3, 3, 3, 4 ),
 ( 0.000000000000000000, 0.0003017745587525231328, 0.0006035491769808714636, 0.0009053241094668142966, 0.001207275924541012383, 0.001510325902535035502 ),
 .UNSPECIFIED. ) ;
#8773=CARTESIAN_POINT ( 'NONE',  ( 0.2869720083484335049, 10.71444492121026038, -5.945302302873144207 ) ) ;
#8776=CONICAL_SURFACE ( 'NONE', #49130, 7.938172270156617749, 1.280189991382167047 ) ;
#8778=ORIENTED_EDGE ( 'NONE', *, *, #19384, .T. ) ;
#8784=ADVANCED_FACE ( 'NONE', ( #60425 ), #8532, .F. ) ;
#8786=CARTESIAN_POINT ( 'NONE',  ( 2.241352910868909643, -2.532612177304395029, -7.202080440908765979 ) ) ;
#8789=ORIENTED_EDGE ( 'NONE', *, *, #6098, .T. ) ;
#8796=CARTESIAN_POINT ( 'NONE',  ( 2.305787727787084407, 2.774453000917245671, -7.135468203929955067 ) ) ;
#8797=CARTESIAN_POINT ( 'NONE',  ( 2.827825597296803384, -0.5449445831287667019, 9.007857251166445423 ) ) ;
#8805=CARTESIAN_POINT ( 'NONE',  ( 0.2653519991613838558, -4.167757449530341773, -11.51519138201634718 ) ) ;
#8806=ORIENTED_EDGE ( 'NONE', *, *, #46922, .F. ) ;
#8821=CARTESIAN_POINT ( 'NONE',  ( 0.2652384770603679609, 10.63836422907232127, -6.065775245581053632 ) ) ;
#8823=VECTOR ( 'NONE', #36105, 999.9999999999998863 ) ;
#8838=VERTEX_POINT ( 'NONE', #61091 ) ;
#8841=CARTESIAN_POINT ( 'NONE',  ( 0.3401186441510237746, 0.2556125181571556881, -12.26845925752607336 ) ) ;
#8845=CARTESIAN_POINT ( 'NONE',  ( 0.3675815128205912052, -12.04510820461657516, -2.391755495700727874 ) ) ;
#8849=CARTESIAN_POINT ( 'NONE',  ( 0.2648978790185602672, 10.53870023327872474, -6.237101853238436355 ) ) ;
#8855=CARTESIAN_POINT ( 'NONE',  ( 1.937114397841932290, 11.72279974487463683, 5.226660192101627800 ) ) ;
#8860=EDGE_CURVE ( 'NONE', #27962, #19209, #43759, .T. ) ;
#8863=CARTESIAN_POINT ( 'NONE',  ( 2.430348790456744901, -6.019963855523536189, -4.796903114819428104 ) ) ;
#8872=CARTESIAN_POINT ( 'NONE',  ( 2.263328370261528555, -2.479726736363687234, 7.228205514767161333 ) ) ;
#8873=CARTESIAN_POINT ( 'NONE',  ( 5.514624014163232779, 0.0001700579043833964205, -0.004137701579365678402 ) ) ;
#8881=CARTESIAN_POINT ( 'NONE',  ( 1.948354844646284612, 10.97658859989913083, -4.761851831284683811 ) ) ;
#8885=VERTEX_POINT ( 'NONE', #897 ) ;
#8887=DIRECTION ( 'NONE',  ( -1.000000000000000000, -0.000000000000000000, -0.000000000000000000 ) ) ;
#8888=CARTESIAN_POINT ( 'NONE',  ( 0.3632410797595258534, -9.572936598843575950, -7.689504457927753833 ) ) ;
#8898=CARTESIAN_POINT ( 'NONE',  ( 0.2646305136544065406, 12.08286001766538398, -1.996350543472870109 ) ) ;
#8904=CARTESIAN_POINT ( 'NONE',  ( 0.2834382757447999057, 5.949714385480788792, -10.71064820518736305 ) ) ;
#8905=CARTESIAN_POINT ( 'NONE',  ( 2.770579946183331366, 1.653873933978976973, -7.633739187313457464 ) ) ;
#8909=CARTESIAN_POINT ( 'NONE',  ( 2.440552418640496324, 0.1974238147510335439, -7.698292014589403820 ) ) ;
#8913=ORIENTED_EDGE ( 'NONE', *, *, #1666, .T. ) ;
#8921=CARTESIAN_POINT ( 'NONE',  ( 0.2834382757447976298, 11.58108645293230943, 3.999440312567258626 ) ) ;
#8924=ORIENTED_EDGE ( 'NONE', *, *, #29128, .F. ) ;
#8925=CARTESIAN_POINT ( 'NONE',  ( 2.261269890822072082, -1.464004156081703201, 7.499479675451368621 ) ) ;
#8927=CARTESIAN_POINT ( 'NONE',  ( 0.2652384770603647413, 7.922175044417105738, -9.338499095996349197 ) ) ;
#8934=DIRECTION ( 'NONE',  ( 0.000000000000000000, 0.000000000000000000, 1.000000000000000000 ) ) ;
#8940=CARTESIAN_POINT ( 'NONE',  ( 0.2717059086739038176, 0.1760722388997856269, 12.24704971877459592 ) ) ;
#8941=( BOUNDED_SURFACE ( )  B_SPLINE_SURFACE ( 3, 1, ( 
 ( #6827, #16471 ),
 ( #11459, #27097 ),
 ( #52705, #47394 ),
 ( #63309, #59251 ) ),
 .UNSPECIFIED., .F., .F., .F. ) 
 B_SPLINE_SURFACE_WITH_KNOTS ( ( 4, 4 ),
 ( 2, 2 ),
 ( 0.000000000000000000, 1.000000000000000000 ),
 ( 0.000000000000000000, 1.000000000000000000 ),
 .UNSPECIFIED. ) 
 GEOMETRIC_REPRESENTATION_ITEM ( )  RATIONAL_B_SPLINE_SURFACE ( (
 ( 1.000000000000000000, 1.000000000000000000),
 ( 0.6933888150995267674, 0.9895912004443193632),
 ( 0.6933888150995267674, 0.9895912004443193632),
 ( 1.000000000000000000, 1.000000000000000000) ) ) 
 REPRESENTATION_ITEM ( '' )  SURFACE ( )  );
#8944=CARTESIAN_POINT ( 'NONE',  ( 2.241352910868909643, -7.503490710578223144, -1.407733736974942973 ) ) ;
#8960=CARTESIAN_POINT ( 'NONE',  ( 1.283627346226763333, -8.503905436511983496, -9.278077665801946594 ) ) ;
#8965=DIRECTION ( 'NONE',  ( 0.3939253465568944290, 0.5833358547425043783, 0.7103112711423510417 ) ) ;
#8969=CARTESIAN_POINT ( 'NONE',  ( 2.242418902651891255, 4.983487297755272216, 5.783980263416264478 ) ) ;
#8972=CARTESIAN_POINT ( 'NONE',  ( 0.2647959493198570047, 9.285851961022064671, -7.983607158780230861 ) ) ;
#8978=CARTESIAN_POINT ( 'NONE',  ( 1.014383007554946481, -2.605923236272049692, -12.22116704270660570 ) ) ;
#8981=CARTESIAN_POINT ( 'NONE',  ( 1.719304012338199295, 12.70777170743846796, -0.7661785589580241140 ) ) ;
#8986=CARTESIAN_POINT ( 'NONE',  ( 2.835339799623984636, 7.241165502254445663, 2.985412098050525209 ) ) ;
#9000=ADVANCED_FACE ( 'NONE', ( #27808 ), #38242, .F. ) ;
#9004=CARTESIAN_POINT ( 'NONE',  ( 1.014383007554947147, 11.03701226956417081, 5.859361736620373406 ) ) ;
#9005=ORIENTED_EDGE ( 'NONE', *, *, #20413, .F. ) ;
#9006=CARTESIAN_POINT ( 'NONE',  ( 2.241311220309554653, -2.698144003944842328, 7.141707286456117743 ) ) ;
#9007=EDGE_CURVE ( 'NONE', #5308, #38082, #63053, .T. ) ;
#9012=CARTESIAN_POINT ( 'NONE',  ( 5.515539859299206427, 0.002856745161749566376, 0.005336559634876450291 ) ) ;
#9016=ADVANCED_FACE ( 'NONE', ( #52101 ), #22536, .F. ) ;
#9017=CARTESIAN_POINT ( 'NONE',  ( 0.4613984246114865573, 6.399144685811715583, 10.51786362586216406 ) ) ;
#9021=CARTESIAN_POINT ( 'NONE',  ( 1.372161826075870117, 10.03232826862047133, 7.648244077827104803 ) ) ;
#9023=CARTESIAN_POINT ( 'NONE',  ( 2.241352910868908754, -6.652881166698538351, 3.744764251556969903 ) ) ;
#9027=CARTESIAN_POINT ( 'NONE',  ( 3.152665057736135701, -1.848755561854027452, -7.719888720907647439 ) ) ;
#9028=CARTESIAN_POINT ( 'NONE',  ( 3.152665057734040488, 0.000000000000000000, 0.000000000000000000 ) ) ;
#9031=CARTESIAN_POINT ( 'NONE',  ( 1.719304012338199517, 0.000000000000000000, 0.000000000000000000 ) ) ;
#9033=CARTESIAN_POINT ( 'NONE',  ( 2.705197763288545776, -5.217779042888482266, 5.783040721897918068 ) ) ;
#9038=B_SPLINE_CURVE_WITH_KNOTS ( 'NONE', 3,
 ( #64400, #18873, #64090, #9199, #12890, #53800, #3915 ),
 .UNSPECIFIED., .F., .F.,
 ( 4, 3, 4 ),
 ( 0.000000000000000000, 0.001700533616330545143, 0.005002426799371691157 ),
 .UNSPECIFIED. ) ;
#9044=CARTESIAN_POINT ( 'NONE',  ( 2.899286259009684841, -7.494390643303793453, 2.348384892629340470 ) ) ;
#9045=CARTESIAN_POINT ( 'NONE',  ( 2.241536586108913820, 3.822683724643463066, 6.608496983003799841 ) ) ;
#9049=ORIENTED_EDGE ( 'NONE', *, *, #39156, .F. ) ;
#9051=EDGE_CURVE ( 'NONE', #49400, #11115, #21441, .T. ) ;
#9065=ORIENTED_EDGE ( 'NONE', *, *, #23658, .T. ) ;
#9070=CARTESIAN_POINT ( 'NONE',  ( 0.3109076770649062960, 3.971171685427550724, -11.60048803586494692 ) ) ;
#9077=CARTESIAN_POINT ( 'NONE',  ( 2.827825597296803384, -3.592949031604475429, 8.278234963587699724 ) ) ;
#9087=CARTESIAN_POINT ( 'NONE',  ( 0.2638984909335716500, -11.43908195192326893, -4.375449752477248211 ) ) ;
#9097=EDGE_CURVE ( 'NONE', #16245, #35534, #13524, .T. ) ;
#9099=EDGE_CURVE ( 'NONE', #60300, #12134, #52430, .T. ) ;
#9111=CARTESIAN_POINT ( 'NONE',  ( 2.350038591458110560, -0.6402934222729476099, 10.60256821300787422 ) ) ;
#9114=DIRECTION ( 'NONE',  ( -0.3865475372811021382, -0.9114221272958260567, -0.1410344188397496257 ) ) ;
#9119=CARTESIAN_POINT ( 'NONE',  ( 2.080613030138687591, 0.000000000000000000, -1.000000000000000000 ) ) ;
#9120=ORIENTED_EDGE ( 'NONE', *, *, #44038, .T. ) ;
#9129=CARTESIAN_POINT ( 'NONE',  ( 0.2648978790185593790, 4.063980959785203240, -11.55204314799259890 ) ) ;
#9130=CARTESIAN_POINT ( 'NONE',  ( 2.241449424704145432, 0.06135604983228025444, 7.634218943782392408 ) ) ;
#9131=CARTESIAN_POINT ( 'NONE',  ( 2.241537034860905386, -7.634469414369387863, -0.004719967007756531788 ) ) ;
#9143=AXIS2_PLACEMENT_3D ( 'NONE', #39002, #29353, #38689 ) ;
#9144=CARTESIAN_POINT ( 'NONE',  ( 0.9232058338315048962, -12.21058493388772170, -2.536181247095490754 ) ) ;
#9146=ORIENTED_EDGE ( 'NONE', *, *, #12435, .T. ) ;
#9149=B_SPLINE_CURVE_WITH_KNOTS ( 'NONE', 3,
 ( #46022, #22631, #26066, #63182, #12301, #6115, #37590, #26374, #5464, #12623, #32901, #56302, #784, #42897, #46659, #37908, #30694, #21048, #7661 ),
 .UNSPECIFIED., .F., .F.,
 ( 4, 3, 3, 3, 3, 3, 4 ),
 ( 7.423420718681438206E-18, 2.825908398831030981E-05, 4.208813692483597913E-05, 5.591713746943513416E-05, 6.279584083231333285E-05, 9.105792820295870052E-05, 0.0001153131102488866381 ),
 .UNSPECIFIED. ) ;
#9151=EDGE_CURVE ( 'NONE', #5538, #59359, #65339, .T. ) ;
#9154=CARTESIAN_POINT ( 'NONE',  ( 0.3218525148189831375, 0.2444206315274874974, -12.26259572563018807 ) ) ;
#9156=EDGE_CURVE ( 'NONE', #56327, #62784, #15059, .T. ) ;
#9158=CARTESIAN_POINT ( 'NONE',  ( 1.719304012339893939, -12.38166659046436457, -2.961219984258754767 ) ) ;
#9161=ORIENTED_EDGE ( 'NONE', *, *, #15629, .T. ) ;
#9162=CARTESIAN_POINT ( 'NONE',  ( 1.020182472821641095, 3.852445298735904800, 11.88926988381970062 ) ) ;
#9171=EDGE_CURVE ( 'NONE', #38878, #32743, #44722, .T. ) ;
#9172=CARTESIAN_POINT ( 'NONE',  ( 3.031336079629019409, 6.309383307296303478, 4.750429016921764891 ) ) ;
#9175=CARTESIAN_POINT ( 'NONE',  ( 0.2651627682582915480, 12.07509313786332683, 2.039709641845623533 ) ) ;
#9176=CARTESIAN_POINT ( 'NONE',  ( 5.516018279890452902, -0.005976902763918694010, -0.003191189039764501679 ) ) ;
#9181=CARTESIAN_POINT ( 'NONE',  ( 3.100650473569728671, -6.622643684997354008, -4.345221797103567596 ) ) ;
#9187=VERTEX_POINT ( 'NONE', #17096 ) ;
#9191=CARTESIAN_POINT ( 'NONE',  ( 0.3675815128205894289, -10.50067073900656212, 6.367184624550128014 ) ) ;
#9192=CARTESIAN_POINT ( 'NONE',  ( 0.3675815128205912052, -11.44679196252412368, 4.447030445008141264 ) ) ;
#9193=CARTESIAN_POINT ( 'NONE',  ( 0.5547464869798230946, 12.09851097165512535, -2.442933571354846123 ) ) ;
#9199=CARTESIAN_POINT ( 'NONE',  ( 2.665405856346787061, -7.686816759402902655, 5.696318245876803132 ) ) ;
#9201=CARTESIAN_POINT ( 'NONE',  ( 0.3675815128205894289, -5.910255304480521055, 10.76447900494938459 ) ) ;
#9206=CARTESIAN_POINT ( 'NONE',  ( 0.2638984909335716500, 12.09426044257626742, -1.930290337333932627 ) ) ;
#9211=CARTESIAN_POINT ( 'NONE',  ( 0.2647959493198550618, 5.995292100780939215, -10.67808515296904837 ) ) ;
#9213=CARTESIAN_POINT ( 'NONE',  ( 2.273267844205340449, -5.029122824446064399, -5.758000272829230326 ) ) ;
#9216=CARTESIAN_POINT ( 'NONE',  ( 2.835339799623982859, 0.3287452556171773788, -7.825540862019408017 ) ) ;
#9220=ORIENTED_EDGE ( 'NONE', *, *, #3489, .T. ) ;
#9222=LINE ( 'NONE', #49807, #193 ) ;
#9232=CARTESIAN_POINT ( 'NONE',  ( 2.259830038565000532, -1.462175769136897285, 7.499347412930719159 ) ) ;
#9236=CARTESIAN_POINT ( 'NONE',  ( 2.241352910868908754, -7.532448145350516988, 1.243507963608069700 ) ) ;
#9243=CARTESIAN_POINT ( 'NONE',  ( 0.3341166715381279628, 0.2526177176100057875, 12.26652061402056049 ) ) ;
#9245=FACE_OUTER_BOUND ( 'NONE', #11503, .T. ) ;
#9246=CARTESIAN_POINT ( 'NONE',  ( 2.305787727787084851, -7.508843116234144688, -1.493241775258500770 ) ) ;
#9247=CARTESIAN_POINT ( 'NONE',  ( 2.241352910868908310, -4.970878533273800137, 5.794346703933830334 ) ) ;
#9251=CARTESIAN_POINT ( 'NONE',  ( 0.2638984909335720941, 7.718810690099187077, -9.508791614589117813 ) ) ;
#9266=VERTEX_POINT ( 'NONE', #22081 ) ;
#9271=CARTESIAN_POINT ( 'NONE',  ( 5.515539859299206427, 0.003193223631739254900, 0.005142293699651879005 ) ) ;
#9273=CARTESIAN_POINT ( 'NONE',  ( 2.261269890823173423, 6.546486799462753581, 3.940687015736990872 ) ) ;
#9275=CARTESIAN_POINT ( 'NONE',  ( 0.2717059086739047058, 9.268607328094642384, -8.007130974639942167 ) ) ;
#9278=EDGE_CURVE ( 'NONE', #49481, #44729, #51603, .T. ) ;
#9282=CARTESIAN_POINT ( 'NONE',  ( 1.194176325881334710, -2.684784923266205769, -12.26540585042612186 ) ) ;
#9289=CARTESIAN_POINT ( 'NONE',  ( 0.2646305136544072623, 1.996350543473155437, -12.08286001766533602 ) ) ;
#9292=ORIENTED_EDGE ( 'NONE', *, *, #54044, .T. ) ;
#9295=EDGE_CURVE ( 'NONE', #23378, #45003, #48419, .T. ) ;
#9297=ORIENTED_EDGE ( 'NONE', *, *, #19357, .F. ) ;
#9306=CARTESIAN_POINT ( 'NONE',  ( 2.298277635560276533, -7.133696409974374930, -2.772101951899035743 ) ) ;
#9307=ORIENTED_EDGE ( 'NONE', *, *, #53734, .T. ) ;
#9308=( BOUNDED_SURFACE ( )  B_SPLINE_SURFACE ( 3, 1, ( 
 ( #41469, #62108 ),
 ( #61122, #15556 ),
 ( #61766, #932 ),
 ( #36506, #56815 ) ),
 .UNSPECIFIED., .F., .F., .F. ) 
 B_SPLINE_SURFACE_WITH_KNOTS ( ( 4, 4 ),
 ( 2, 2 ),
 ( 0.000000000000000000, 1.000000000000000000 ),
 ( 0.000000000000000000, 1.000000000000000000 ),
 .UNSPECIFIED. ) 
 GEOMETRIC_REPRESENTATION_ITEM ( )  RATIONAL_B_SPLINE_SURFACE ( (
 ( 1.000000000000000000, 1.000000000000000000),
 ( 0.9942764183789327692, 0.8450855930916585379),
 ( 0.9942764183789327692, 0.8450855930916585379),
 ( 1.000000000000000000, 1.000000000000000000) ) ) 
 REPRESENTATION_ITEM ( '' )  SURFACE ( )  );
#9317=ORIENTED_EDGE ( 'NONE', *, *, #10327, .T. ) ;
#9319=CARTESIAN_POINT ( 'NONE',  ( 2.266490820343227242, -7.641399530653802508, 0.1453321357832486060 ) ) ;
#9322=CARTESIAN_POINT ( 'NONE',  ( 1.719304012338249921, 10.22720798541395837, 7.581471372740089976 ) ) ;
#9324=CARTESIAN_POINT ( 'NONE',  ( 0.2833330754217411873, -9.254504746325737941, -8.029341648258453645 ) ) ;
#9329=CARTESIAN_POINT ( 'NONE',  ( 1.198791140418550283, 1.670544840358248351, 12.44572864632773523 ) ) ;
#9331=CARTESIAN_POINT ( 'NONE',  ( 0.2872850955227769787, -12.10187515377841727, -1.921748909352280821 ) ) ;
#9332=CARTESIAN_POINT ( 'NONE',  ( 2.963017218115622686, -5.350609950027704009, 5.778072204777623178 ) ) ;
#9341=ADVANCED_FACE ( 'NONE', ( #58330 ), #29323, .F. ) ;
#9342=ORIENTED_EDGE ( 'NONE', *, *, #62596, .F. ) ;
#9360=CARTESIAN_POINT ( 'NONE',  ( 0.2717059086739019302, -9.268607328094583764, 8.007130974640009669 ) ) ;
#9371=CARTESIAN_POINT ( 'NONE',  ( 0.8375941296802502656, -9.769835228044227549, 7.696026447556238992 ) ) ;
#9372=ORIENTED_EDGE ( 'NONE', *, *, #37142, .F. ) ;
#9376=CARTESIAN_POINT ( 'NONE',  ( 0.9232167919969179737, -6.587352952801085237, -10.58277433962388159 ) ) ;
#9378=CARTESIAN_POINT ( 'NONE',  ( 0.3675815128205894289, -12.27743992903066328, 0.2638082659427993804 ) ) ;
#9389=CARTESIAN_POINT ( 'NONE',  ( 0.2801149460245128120, 8.024198546827475909, 9.257544930777182657 ) ) ;
#9392=CARTESIAN_POINT ( 'NONE',  ( 0.2648978790185584908, 0.1321385342564118659, -12.24533305150758089 ) ) ;
#9395=CARTESIAN_POINT ( 'NONE',  ( 2.269879328255106188, 7.232310762823190409, 2.474479066009427353 ) ) ;
#9402=CARTESIAN_POINT ( 'NONE',  ( 0.2651627682582908818, -7.938957913267695510, -9.324228491541607156 ) ) ;
#9410=CARTESIAN_POINT ( 'NONE',  ( 2.262775599886257538, 6.687241191563714438, -3.697834000591571524 ) ) ;
#9420=CARTESIAN_POINT ( 'NONE',  ( 2.269879328256732887, 0.1483462450597243520, 7.642470739868881147 ) ) ;
#9426=EDGE_CURVE ( 'NONE', #11008, #41431, #4709, .T. ) ;
#9434=CARTESIAN_POINT ( 'NONE',  ( 1.375507693218806837, -12.30831170622582071, -2.770709900326205233 ) ) ;
#9437=CARTESIAN_POINT ( 'NONE',  ( 0.3675815128205912052, -6.367184624550238148, 10.50067073900649461 ) ) ;
#9438=CARTESIAN_POINT ( 'NONE',  ( 0.2652384770603662401, 4.250454630553718971, -11.48486213386621380 ) ) ;
#9441=CARTESIAN_POINT ( 'NONE',  ( 0.3665391374699467075, -7.691255657244228772, -9.576575648339096247 ) ) ;
#9448=EDGE_LOOP ( 'NONE', ( #4080, #23351, #56160, #53985 ) ) ;
#9449=CIRCLE ( 'NONE', #20062, 12.73084802173761787 ) ;
#9459=VERTEX_POINT ( 'NONE', #34665 ) ;
#9465=CARTESIAN_POINT ( 'NONE',  ( 2.241352910868909643, -1.243507963608144751, 7.532448145350502777 ) ) ;
#9469=CARTESIAN_POINT ( 'NONE',  ( 2.903928887688550731, 6.032681461746162377, 6.365315087928729021 ) ) ;
#9470=VECTOR ( 'NONE', #39739, 999.9999999999998863 ) ;
#9473=VERTEX_POINT ( 'NONE', #34355 ) ;
#9477=B_SPLINE_CURVE_WITH_KNOTS ( 'NONE', 3,
 ( #6939, #12240, #33173, #58812, #32503, #58133, #52166, #16902, #63422, #53137, #57481, #11906, #12549, #32828, #22560, #53485, #27208, #7581, #26887 ),
 .UNSPECIFIED., .F., .F.,
 ( 4, 3, 3, 3, 3, 3, 4 ),
 ( 0.000000000000000000, 2.831840207625647068E-05, 4.217266860012731824E-05, 5.602024318566616653E-05, 6.290810168138950603E-05, 9.120440631110875748E-05, 0.0001153103026478308337 ),
 .UNSPECIFIED. ) ;
#9483=( BOUNDED_SURFACE ( )  B_SPLINE_SURFACE ( 3, 1, ( 
 ( #9856, #26459 ),
 ( #50446, #46745 ),
 ( #61701, #10183 ),
 ( #1206, #60734 ) ),
 .UNSPECIFIED., .F., .F., .F. ) 
 B_SPLINE_SURFACE_WITH_KNOTS ( ( 4, 4 ),
 ( 2, 2 ),
 ( 0.000000000000000000, 1.000000000000000000 ),
 ( 0.000000000000000000, 1.000000000000000000 ),
 .UNSPECIFIED. ) 
 GEOMETRIC_REPRESENTATION_ITEM ( )  RATIONAL_B_SPLINE_SURFACE ( (
 ( 1.000000000000000000, 1.000000000000000000),
 ( 0.9856612449720755231, 0.9999558406602322425),
 ( 0.9856612449720755231, 0.9999558406602322425),
 ( 1.000000000000000000, 1.000000000000000000) ) ) 
 REPRESENTATION_ITEM ( '' )  SURFACE ( )  );
#9489=CARTESIAN_POINT ( 'NONE',  ( 0.2652384529303136174, 12.07141085622972554, 2.061422456317067109 ) ) ;
#9496=CARTESIAN_POINT ( 'NONE',  ( 0.4613984246114885002, -4.475519447653911520, -11.46927345719241131 ) ) ;
#9504=CARTESIAN_POINT ( 'NONE',  ( 2.941278708680199916, 5.814102272488615775, -1.972702289975945433 ) ) ;
#9505=ADVANCED_FACE ( 'NONE', ( #64927 ), #49727, .F. ) ;
#9519=CARTESIAN_POINT ( 'NONE',  ( 2.263328370259786393, 1.186889399883084950, -7.548992860188940668 ) ) ;
#9520=ORIENTED_EDGE ( 'NONE', *, *, #19357, .T. ) ;
#9526=CARTESIAN_POINT ( 'NONE',  ( 0.2648978790185584908, 11.46165506714228322, 4.312320170909275774 ) ) ;
#9533=ORIENTED_EDGE ( 'NONE', *, *, #11053, .T. ) ;
#9538=VECTOR ( 'NONE', #64108, 1000.000000000000000 ) ;
#9543=CARTESIAN_POINT ( 'NONE',  ( 2.573738926104371938, -4.074516960797421206, 6.586859681822649470 ) ) ;
#9545=ORIENTED_EDGE ( 'NONE', *, *, #48662, .F. ) ;
#9546=CARTESIAN_POINT ( 'NONE',  ( 1.549075743845271358, -12.12370443967581224, 3.694639393664078231 ) ) ;
#9560=CARTESIAN_POINT ( 'NONE',  ( 0.3057689695767484839, 0.2309407641932738897, 12.25749431726081973 ) ) ;
#9566=CARTESIAN_POINT ( 'NONE',  ( 3.092491956585399659, -7.863103788722309417, -0.9322768171845581264 ) ) ;
#9568=ORIENTED_EDGE ( 'NONE', *, *, #30256, .F. ) ;
#9570=CARTESIAN_POINT ( 'NONE',  ( 2.242418902651939216, -3.730710532463405116, 6.661183998167589770 ) ) ;
#9571=EDGE_CURVE ( 'NONE', #37505, #62374, #2618, .T. ) ;
#9574=CIRCLE ( 'NONE', #14835, 7.938172270156617749 ) ;
#9579=ORIENTED_EDGE ( 'NONE', *, *, #56631, .F. ) ;
#9580=CARTESIAN_POINT ( 'NONE',  ( 0.2653519789438747445, 12.24619733037256353, -0.02203059356493299384 ) ) ;
#9593=CARTESIAN_POINT ( 'NONE',  ( 3.152665057735260845, 4.377619405893435456, 6.622010822086191517 ) ) ;
#9596=CARTESIAN_POINT ( 'NONE',  ( 0.3218525148189836371, 12.26259572563018629, 0.2444206315273586283 ) ) ;
#9600=ORIENTED_EDGE ( 'NONE', *, *, #17354, .F. ) ;
#9602=CARTESIAN_POINT ( 'NONE',  ( 0.3675815128205912052, -12.04510820461657516, -2.391755495700727874 ) ) ;
#9604=ORIENTED_EDGE ( 'NONE', *, *, #25662, .T. ) ;
#9607=CIRCLE ( 'NONE', #57382, 7.938172270156617749 ) ;
#9615=CARTESIAN_POINT ( 'NONE',  ( 2.655192694324876257, 9.539062147539249636, 1.093661162899515205 ) ) ;
#9620=ORIENTED_EDGE ( 'NONE', *, *, #50827, .F. ) ;
#9625=ORIENTED_EDGE ( 'NONE', *, *, #3052, .T. ) ;
#9639=CARTESIAN_POINT ( 'NONE',  ( 3.152665057736003362, 6.378477742801834438, 4.725420687649379836 ) ) ;
#9642=CARTESIAN_POINT ( 'NONE',  ( 0.3002738374340808702, -10.72659044316167432, 5.932527270856367885 ) ) ;
#9643=CARTESIAN_POINT ( 'NONE',  ( 0.2833330754217391889, 3.999965385632591186, 11.58086621621908385 ) ) ;
#9645=CARTESIAN_POINT ( 'NONE',  ( 0.2648978790185602672, 11.55204314799263798, 4.063980959785085112 ) ) ;
#9653=CARTESIAN_POINT ( 'NONE',  ( 2.889800649504073782, -5.267262008933648154, -3.118861721612621096 ) ) ;
#9657=EDGE_LOOP ( 'NONE', ( #17365, #12491, #45427, #13759 ) ) ;
#9659=CARTESIAN_POINT ( 'NONE',  ( 0.6473888112830221697, 5.898884566269161134, -10.87693551365365074 ) ) ;
#9660=CARTESIAN_POINT ( 'NONE',  ( 1.719304012341273280, -2.961219984259375160, -12.38166659046469675 ) ) ;
#9670=ADVANCED_FACE ( 'NONE', ( #31338 ), #46128, .T. ) ;
#9671=CARTESIAN_POINT ( 'NONE',  ( 5.530133899448235191, -0.009387834778845241188, -0.01293763278443419047 ) ) ;
#9686=ORIENTED_EDGE ( 'NONE', *, *, #46922, .T. ) ;
#9691=EDGE_CURVE ( 'NONE', #38228, #53897, #37192, .T. ) ;
#9692=CARTESIAN_POINT ( 'NONE',  ( 3.092491956585758039, 3.565393530441273828, -7.070043156103592352 ) ) ;
#9700=( BOUNDED_SURFACE ( )  B_SPLINE_SURFACE ( 3, 1, ( 
 ( #12719, #3449 ),
 ( #3776, #53962 ),
 ( #8402, #48992 ),
 ( #43984, #64258 ) ),
 .UNSPECIFIED., .F., .F., .F. ) 
 B_SPLINE_SURFACE_WITH_KNOTS ( ( 4, 4 ),
 ( 2, 2 ),
 ( 0.000000000000000000, 1.000000000000000000 ),
 ( 0.000000000000000000, 1.000000000000000000 ),
 .UNSPECIFIED. ) 
 GEOMETRIC_REPRESENTATION_ITEM ( )  RATIONAL_B_SPLINE_SURFACE ( (
 ( 1.000000000000000000, 1.000000000000000000),
 ( 0.9856612449720755231, 0.9999558406602322425),
 ( 0.9856612449720755231, 0.9999558406602322425),
 ( 1.000000000000000000, 1.000000000000000000) ) ) 
 REPRESENTATION_ITEM ( '' )  SURFACE ( )  );
#9708=CARTESIAN_POINT ( 'NONE',  ( 0.3341166715381334584, -6.352033667906535896, -10.49680960898233195 ) ) ;
#9711=LINE ( 'NONE', #14376, #46813 ) ;
#9713=CARTESIAN_POINT ( 'NONE',  ( 0.8320506296491635423, -6.546053790694106311, -10.57268643647781126 ) ) ;
#9717=CARTESIAN_POINT ( 'NONE',  ( 0.2717059086739037066, -12.24704971877459592, 0.1760722388997425225 ) ) ;
#9730=CARTESIAN_POINT ( 'NONE',  ( 5.514970785353741078, 0.004588761610585026345, -0.001117786416802573094 ) ) ;
#9739=CARTESIAN_POINT ( 'NONE',  ( 2.781367136451533995, 0.3081277311322765944, 7.808329083463359410 ) ) ;
#9742=EDGE_CURVE ( 'NONE', #4955, #47398, #3893, .T. ) ;
#9743=CARTESIAN_POINT ( 'NONE',  ( 1.198791140417704515, 12.26651935498904678, 2.686891236232352487 ) ) ;
#9744=ORIENTED_EDGE ( 'NONE', *, *, #20406, .T. ) ;
#9746=B_SPLINE_CURVE_WITH_KNOTS ( 'NONE', 3,
 ( #7998, #63175, #17957, #48246, #44201, #63816, #48556, #33245, #12298, #37902, #28915, #22958, #23270, #27936, #43534, #43879, #64469, #58534, #18297 ),
 .UNSPECIFIED., .F., .F.,
 ( 4, 3, 3, 3, 3, 3, 4 ),
 ( 7.046480070129584215E-18, 2.825908398830993712E-05, 4.208813692483719885E-05, 5.591713746943548653E-05, 6.279584083231588073E-05, 9.105792820296273917E-05, 0.0001153131102488845510 ),
 .UNSPECIFIED. ) ;
#9753=CARTESIAN_POINT ( 'NONE',  ( 2.249013661412230913, 6.673008335691913651, -3.714035584818151214 ) ) ;
#9759=EDGE_CURVE ( 'NONE', #44286, #19660, #42717, .T. ) ;
#9761=CARTESIAN_POINT ( 'NONE',  ( 2.889800649504073782, -6.121013568931507720, 0.06738247734048298521 ) ) ;
#9763=CARTESIAN_POINT ( 'NONE',  ( 2.241352910868908754, 2.689314586382447914, -7.145045428366549878 ) ) ;
#9764=CARTESIAN_POINT ( 'NONE',  ( 0.2648978790185584908, -12.08224454301450201, 1.996248716311589400 ) ) ;
#9765=B_SPLINE_CURVE_WITH_KNOTS ( 'NONE', 3,
 ( #39181, #34191, #3655, #59471, #42865, #53181, #13897, #23919, #44178, #7630, #27913, #28240, #2983, #58858, #63788, #13274 ),
 .UNSPECIFIED., .F., .F.,
 ( 4, 3, 3, 3, 3, 4 ),
 ( 0.000000000000000000, 0.0002999043160757247639, 0.0005998071753050776903, 0.0008997092107374208420, 0.001204458948194734799, 0.001510329163474717629 ),
 .UNSPECIFIED. ) ;
#9771=B_SPLINE_CURVE_WITH_KNOTS ( 'NONE', 3,
 ( #22303, #32598, #21991, #17342, #37620, #3046, #42245 ),
 .UNSPECIFIED., .F., .F.,
 ( 4, 3, 4 ),
 ( 0.000000000000000000, 0.001700533616330532566, 0.005002426799371325131 ),
 .UNSPECIFIED. ) ;
#9776=VERTEX_POINT ( 'NONE', #9645 ) ;
#9788=CARTESIAN_POINT ( 'NONE',  ( 5.515188684475870851, 0.002355816063606930213, 0.004804816249378836106 ) ) ;
#9791=CARTESIAN_POINT ( 'NONE',  ( 0.3401186441510281044, 9.562489599411641450, -7.690203051555926095 ) ) ;
#9796=CARTESIAN_POINT ( 'NONE',  ( 2.373367633546872302, 7.591069096729010646, -1.154895193356554550 ) ) ;
#9797=DIRECTION ( 'NONE',  ( -1.000000000000000000, -0.000000000000000000, -0.000000000000000000 ) ) ;
#9805=CARTESIAN_POINT ( 'NONE',  ( 0.3665391374699465965, -3.952034409876375332, 11.62960183138725689 ) ) ;
#9808=CARTESIAN_POINT ( 'NONE',  ( 2.258463476536646031, 7.638896687393374130, 0.1358786215988430079 ) ) ;
#9811=EDGE_CURVE ( 'NONE', #34853, #47440, #467, .T. ) ;
#9813=ORIENTED_EDGE ( 'NONE', *, *, #27217, .T. ) ;
#9814=EDGE_CURVE ( 'NONE', #23038, #19720, #29315, .T. ) ;
#9817=CARTESIAN_POINT ( 'NONE',  ( 0.3675815128205894289, 12.27743992903066150, 0.2638082659428850896 ) ) ;
#9818=CARTESIAN_POINT ( 'NONE',  ( 2.273267844204863941, 7.501135923490796387, -1.476347988307392001 ) ) ;
#9825=CARTESIAN_POINT ( 'NONE',  ( 5.515539859299206427, 0.005924322247675109683, -0.001241880655086952893 ) ) ;
#9833=CARTESIAN_POINT ( 'NONE',  ( 1.937114397841935398, 12.80345148322679272, -0.9020203649532142487 ) ) ;
#9838=CARTESIAN_POINT ( 'NONE',  ( 1.452237505248552996, 12.34692280296791900, 2.778494755359096846 ) ) ;
#9840=B_SPLINE_CURVE_WITH_KNOTS ( 'NONE', 3,
 ( #60654, #1787, #36014, #6778, #37007, #21406, #51998, #12070, #57310, #22052, #32018, #62280, #16426, #51361, #21058, #56673 ),
 .UNSPECIFIED., .F., .F.,
 ( 4, 3, 3, 3, 3, 4 ),
 ( 0.000000000000000000, 0.0002999043160757397259, 0.0005998071753051095658, 0.0008997092107374688721, 0.001204458948196129951, 0.001510329163477477140 ),
 .UNSPECIFIED. ) ;
#9841=CARTESIAN_POINT ( 'NONE',  ( 5.514970785353741078, 0.0005190732562555076942, -0.004694330894494710103 ) ) ;
#9842=CARTESIAN_POINT ( 'NONE',  ( 2.305787727787084407, 6.545285700970527643, 3.971363876083986888 ) ) ;
#9853=CARTESIAN_POINT ( 'NONE',  ( 2.655192694323172731, 8.807900729502561532, -3.822392723568370343 ) ) ;
#9856=CARTESIAN_POINT ( 'NONE',  ( 5.514970785353741078, -0.004694330894494374434, 0.0005190732562558384843 ) ) ;
#9861=CARTESIAN_POINT ( 'NONE',  ( 0.8375941296813791404, -1.780036797758159262, -12.30893872205299111 ) ) ;
#9869=ORIENTED_EDGE ( 'NONE', *, *, #3568, .F. ) ;
#9887=CARTESIAN_POINT ( 'NONE',  ( 2.256373768223415954, 7.132139410181004280, -2.737361830682253139 ) ) ;
#9889=CARTESIAN_POINT ( 'NONE',  ( 0.2650492433740071485, -10.54996000109279386, 6.218175523534253735 ) ) ;
#9892=B_SPLINE_CURVE_WITH_KNOTS ( 'NONE', 3,
 ( #52016, #62961, #41699, #37360, #2121, #57671, #11435, #7421, #22747, #6462, #42326, #43010, #31706, #62299, #61992, #37026 ),
 .UNSPECIFIED., .F., .F.,
 ( 4, 3, 3, 3, 3, 4 ),
 ( 5.963111948670274387E-19, 0.0003017745587525250302, 0.0006035491769808758004, 0.0009053241094668193923, 0.001207275924539141483, 0.001510325902531265080 ),
 .UNSPECIFIED. ) ;
#9896=CARTESIAN_POINT ( 'NONE',  ( 1.020182472822803499, -11.88926988382020333, 3.852445298735596158 ) ) ;
#9897=B_SPLINE_CURVE_WITH_KNOTS ( 'NONE', 3,
 ( #37489, #32483, #43443, #64381, #23514, #18849, #23178, #39113, #49129, #8215, #59405, #18202, #58439, #38469, #7902, #48147, #3588, #12867, #63396 ),
 .UNSPECIFIED., .F., .F.,
 ( 4, 3, 3, 3, 3, 3, 4 ),
 ( 6.759600587344756714E-18, 2.825908398830881564E-05, 4.208813692483547768E-05, 5.591713746943374503E-05, 6.279584083231433574E-05, 9.105792820296101800E-05, 0.0001153131102488855539 ),
 .UNSPECIFIED. ) ;
#9911=CARTESIAN_POINT ( 'NONE',  ( 0.2872850955227752023, 0.2089153415334872865, 12.25172867346922700 ) ) ;
#9913=CARTESIAN_POINT ( 'NONE',  ( 0.2655924914740778742, -12.05257978623655291, 2.169924872618023581 ) ) ;
#9915=EDGE_CURVE ( 'NONE', #45003, #16245, #20619, .T. ) ;
#9919=CARTESIAN_POINT ( 'NONE',  ( 2.256373768223204124, 2.487510024221536220, -7.223078030710271769 ) ) ;
#9927=EDGE_CURVE ( 'NONE', #64920, #7749, #14236, .T. ) ;
#9938=CARTESIAN_POINT ( 'NONE',  ( 0.3474126878361792348, -0.2587235634077174606, -12.27082419038178784 ) ) ;
#9948=CARTESIAN_POINT ( 'NONE',  ( 5.515539859299206427, -0.004759416711441706582, 0.003740028639278266016 ) ) ;
#9953=CARTESIAN_POINT ( 'NONE',  ( 1.287602823386727158, -12.57487505104549541, -0.5522659225150269302 ) ) ;
#9963=B_SPLINE_CURVE_WITH_KNOTS ( 'NONE', 3,
 ( #31627, #31952, #26322, #41937, #57247, #16995, #61899, #32285, #51938, #16673 ),
 .UNSPECIFIED., .F., .F.,
 ( 4, 3, 3, 4 ),
 ( 1.939479807224432123E-18, 6.607638129004445515E-05, 9.911389841680619836E-05, 0.0001667630577588621486 ),
 .UNSPECIFIED. ) ;
#9966=EDGE_LOOP ( 'NONE', ( #41868, #1139, #20932, #33028 ) ) ;
#9970=CARTESIAN_POINT ( 'NONE',  ( 2.717984159219516194, 7.221467817271548739, -2.930214355830588868 ) ) ;
#9971=EDGE_LOOP ( 'NONE', ( #19100, #13327, #49482, #62718 ) ) ;
#9976=CARTESIAN_POINT ( 'NONE',  ( 0.2956976708475478333, 11.59055635407407081, -3.984495122852460103 ) ) ;
#9987=DIRECTION ( 'NONE',  ( -1.000000000000000000, -0.000000000000000000, -0.000000000000000000 ) ) ;
#9996=CARTESIAN_POINT ( 'NONE',  ( 5.536195898058073439, 0.008411485181669240210, 0.001224473329858010925 ) ) ;
#9997=CARTESIAN_POINT ( 'NONE',  ( 0.2646305136544065406, -12.08286001766534312, -1.996350543473116801 ) ) ;
#10006=CARTESIAN_POINT ( 'NONE',  ( 2.268878695252930733, -3.692782103667504146, -6.692359410363332373 ) ) ;
#10007=LINE ( 'NONE', #20647, #28572 ) ;
#10012=CARTESIAN_POINT ( 'NONE',  ( 2.889800649504073782, 5.334644486274237707, -3.002151847318860867 ) ) ;
#10013=CARTESIAN_POINT ( 'NONE',  ( 2.639814597422734277, 3.659458430304349807, 6.851176153958492776 ) ) ;
#10015=EDGE_CURVE ( 'NONE', #18779, #38082, #57844, .T. ) ;
#10016=CARTESIAN_POINT ( 'NONE',  ( 0.3474126878361842308, -12.12932967384299232, -1.876013288000176971 ) ) ;
#10020=CARTESIAN_POINT ( 'NONE',  ( 2.655192694323997848, -1.093661162899882022, 9.539062147542148651 ) ) ;
#10021=DIRECTION ( 'NONE',  ( 0.3865475372811021382, -0.01937500237529702143, 0.9220659470476458841 ) ) ;
#10023=VECTOR ( 'NONE', #58821, 1000.000000000000227 ) ;
#10025=ORIENTED_EDGE ( 'NONE', *, *, #9426, .F. ) ;
#10036=CARTESIAN_POINT ( 'NONE',  ( 2.639814597422740494, 2.896050884406630388, -7.207158938903913459 ) ) ;
#10040=CARTESIAN_POINT ( 'NONE',  ( 0.000000000000000000, 0.000000000000000000, 0.000000000000000000 ) ) ;
#10045=CARTESIAN_POINT ( 'NONE',  ( 2.263328370262056133, 4.802372801874240871, -5.944174889971576725 ) ) ;
#10059=CARTESIAN_POINT ( 'NONE',  ( 0.2915757698887292970, -12.25305747416128099, 0.2147157799034387915 ) ) ;
#10076=FACE_OUTER_BOUND ( 'NONE', #51856, .T. ) ;
#10084=CARTESIAN_POINT ( 'NONE',  ( 1.462291587748590027, 12.32753368892810286, 2.816455204775825560 ) ) ;
#10085=ORIENTED_EDGE ( 'NONE', *, *, #3840, .T. ) ;
#10102=LINE ( 'NONE', #55322, #56738 ) ;
#10106=DIRECTION ( 'NONE',  ( -1.000000000000000000, -0.000000000000000000, -0.000000000000000000 ) ) ;
#10112=B_SPLINE_CURVE_WITH_KNOTS ( 'NONE', 3,
 ( #5531, #25797, #30756, #51072, #31433, #46088, #538, #36068, #14798, #61349, #20803, #41070, #15789 ),
 .UNSPECIFIED., .F., .F.,
 ( 4, 3, 3, 3, 4 ),
 ( 3.127317220692750759E-18, 6.607593386745688247E-05, 0.0001321518677373565267, 0.0001982171734706204261, 0.0002642860854759485545 ),
 .UNSPECIFIED. ) ;
#10119=CARTESIAN_POINT ( 'NONE',  ( 2.406456491625455829, 8.704497555694503674, -5.751891873092491281 ) ) ;
#10122=CARTESIAN_POINT ( 'NONE',  ( 0.2651627923886318849, -12.04449855907066791, -2.213220384814395647 ) ) ;
#10129=ORIENTED_EDGE ( 'NONE', *, *, #51586, .T. ) ;
#10130=CARTESIAN_POINT ( 'NONE',  ( 0.2869720083484446627, 9.519277517057210147, -7.715523637151659564 ) ) ;
#10137=CARTESIAN_POINT ( 'NONE',  ( 0.3665391374699464300, -11.62960183138730130, 3.952034409876256316 ) ) ;
#10139=EDGE_LOOP ( 'NONE', ( #49889, #45438, #616, #63226 ) ) ;
#10143=ORIENTED_EDGE ( 'NONE', *, *, #42753, .T. ) ;
#10144=CARTESIAN_POINT ( 'NONE',  ( 1.452237505248555660, -3.767214359061207052, 12.08199618361511796 ) ) ;
#10145=CARTESIAN_POINT ( 'NONE',  ( 0.2648978790185602672, 10.53870023327872474, -6.237101853238436355 ) ) ;
#10148=CARTESIAN_POINT ( 'NONE',  ( 2.247206125382827935, 7.635476611656033974, 0.1157489416151797346 ) ) ;
#10150=CARTESIAN_POINT ( 'NONE',  ( 3.152665057735448251, 0.9030954876725900693, -7.886634106564547331 ) ) ;
#10154=CARTESIAN_POINT ( 'NONE',  ( 2.276905613633648962, 7.501802783089493332, -1.479235344773081939 ) ) ;
#10161=CARTESIAN_POINT ( 'NONE',  ( 2.368238019615093393, 5.994627685102951631, 4.795442552787996249 ) ) ;
#10163=CARTESIAN_POINT ( 'NONE',  ( 2.305787727787084407, -0.1666591538753222634, 7.654065630109506024 ) ) ;
#10168=FACE_OUTER_BOUND ( 'NONE', #21414, .T. ) ;
#10172=CARTESIAN_POINT ( 'NONE',  ( 0.3040950598368152291, -12.02925914197706447, 2.376091969481177291 ) ) ;
#10174=ORIENTED_EDGE ( 'NONE', *, *, #9007, .F. ) ;
#10175=CARTESIAN_POINT ( 'NONE',  ( 1.634816307075121378, -6.964001572435194021, 10.62369813896840043 ) ) ;
#10180=DIRECTION ( 'NONE',  ( 0.000000000000000000, 0.000000000000000000, -1.000000000000000000 ) ) ;
#10183=CARTESIAN_POINT ( 'NONE',  ( 0.2655924914740778187, 9.409507842006130218, -7.838010948424953384 ) ) ;
#10185=CARTESIAN_POINT ( 'NONE',  ( 0.2706063244538031154, 7.737788863017306618, 9.494160524941712254 ) ) ;
#10192=CARTESIAN_POINT ( 'NONE',  ( 0.3223008802179261889, 11.43958962819738900, -4.423848692584580355 ) ) ;
#10199=CARTESIAN_POINT ( 'NONE',  ( 0.2657645697724688727, 11.45515365350261838, 4.330388001246444851 ) ) ;
#10208=VERTEX_POINT ( 'NONE', #24216 ) ;
#10211=CARTESIAN_POINT ( 'NONE',  ( 0.3040950598368152291, 2.376091969481216370, 12.02925914197705559 ) ) ;
#10213=CARTESIAN_POINT ( 'NONE',  ( 5.514970785353741078, 0.0005190732562555056342, -0.004694330894494712705 ) ) ;
#10220=CARTESIAN_POINT ( 'NONE',  ( 2.251152103363646351, 7.636644423939539905, -0.1252683866805369139 ) ) ;
#10223=CARTESIAN_POINT ( 'NONE',  ( 0.3665391374699467075, -10.50279796150432610, -6.368473106897240221 ) ) ;
#10227=CARTESIAN_POINT ( 'NONE',  ( 2.665405856346780844, 8.776564688671614434, 3.808819464940459643 ) ) ;
#10237=CARTESIAN_POINT ( 'NONE',  ( 2.556980015513528048, -7.658710847181453119, -1.116161541731783835 ) ) ;
#10242=LINE ( 'NONE', #20568, #33281 ) ;
#10243=CARTESIAN_POINT ( 'NONE',  ( 2.241451721903217731, -6.581017239736936197, -3.869794645251186882 ) ) ;
#10248=CARTESIAN_POINT ( 'NONE',  ( 0.9232058338315048962, 12.34162163148536351, -1.793035206307219243 ) ) ;
#10254=CARTESIAN_POINT ( 'NONE',  ( 0.3537226245948391634, -11.62199823003436805, 3.952322262392347518 ) ) ;
#10257=ORIENTED_EDGE ( 'NONE', *, *, #51663, .F. ) ;
#10258=FACE_OUTER_BOUND ( 'NONE', #22737, .T. ) ;
#10259=B_SPLINE_CURVE_WITH_KNOTS ( 'NONE', 3,
 ( #55515, #15270, #19286, #45206, #29260, #29565, #65468 ),
 .UNSPECIFIED., .F., .F.,
 ( 4, 3, 4 ),
 ( 6.408539315702728266E-15, 0.002398160485434724411, 0.005002426799383169823 ),
 .UNSPECIFIED. ) ;
#10263=CARTESIAN_POINT ( 'NONE',  ( 5.530133899448235191, -0.006998616117863969491, 0.01437126147332079724 ) ) ;
#10264=CARTESIAN_POINT ( 'NONE',  ( 0.4626703367442814852, 9.247028139127523971, 8.128802338754262280 ) ) ;
#10265=CARTESIAN_POINT ( 'NONE',  ( 1.459561108994217760, 9.267924853468691992, -8.601340491611662031 ) ) ;
#10266=CARTESIAN_POINT ( 'NONE',  ( 0.4626703367448971038, 10.80124546303580324, -5.909149965570888341 ) ) ;
#10270=CARTESIAN_POINT ( 'NONE',  ( 2.705197763288551993, -2.399370654839219963, -7.410249563424446961 ) ) ;
#10279=( BOUNDED_SURFACE ( )  B_SPLINE_SURFACE ( 3, 1, ( 
 ( #13456, #9441 ),
 ( #29728, #53723 ),
 ( #48730, #23120 ),
 ( #64007, #14112 ) ),
 .UNSPECIFIED., .F., .F., .F. ) 
 B_SPLINE_SURFACE_WITH_KNOTS ( ( 4, 4 ),
 ( 2, 2 ),
 ( 0.000000000000000000, 1.000000000000000000 ),
 ( 0.000000000000000000, 1.000000000000000000 ),
 .UNSPECIFIED. ) 
 GEOMETRIC_REPRESENTATION_ITEM ( )  RATIONAL_B_SPLINE_SURFACE ( (
 ( 1.000000000000000000, 1.000000000000000000),
 ( 0.6933888150995267674, 0.9895912004443193632),
 ( 0.6933888150995267674, 0.9895912004443193632),
 ( 1.000000000000000000, 1.000000000000000000) ) ) 
 REPRESENTATION_ITEM ( '' )  SURFACE ( )  );
#10286=CARTESIAN_POINT ( 'NONE',  ( 2.963017218115620022, -7.004145770368796597, 3.599595431209464902 ) ) ;
#10294=LINE ( 'NONE', #55863, #26701 ) ;
#10296=CARTESIAN_POINT ( 'NONE',  ( 1.719304012338199517, 0.000000000000000000, 0.000000000000000000 ) ) ;
#10308=CARTESIAN_POINT ( 'NONE',  ( 0.2706063244537997847, -10.69357582853951172, 5.971590789837488700 ) ) ;
#10309=CARTESIAN_POINT ( 'NONE',  ( 1.937114397841932290, -9.228205347192393049, -8.920887662793566264 ) ) ;
#10317=CARTESIAN_POINT ( 'NONE',  ( 2.705197763288547552, 6.881024880055393922, -3.649695155981438344 ) ) ;
#10318=CARTESIAN_POINT ( 'NONE',  ( 2.781367136451930566, 4.171010984502898644, 6.608147481822022939 ) ) ;
#10319=CARTESIAN_POINT ( 'NONE',  ( 3.092491956584929369, 7.863103788722181520, 0.9322768171848894170 ) ) ;
#10326=B_SPLINE_CURVE_WITH_KNOTS ( 'NONE', 3,
 ( #9437, #23793, #39381, #44059, #60013, #14110, #64977, #14433, #35026, #3847, #60655, #15093, #13772, #34064, #24103, #34708, #29411, #44363, #34404 ),
 .UNSPECIFIED., .F., .F.,
 ( 4, 3, 3, 3, 3, 3, 4 ),
 ( 9.600547486887170186E-18, 4.457896483015377217E-05, 6.639290541542671223E-05, 8.820687556479552720E-05, 0.0001100173248778994853, 0.0001545671401658188244, 0.0001830328308068574113 ),
 .UNSPECIFIED. ) ;
#10327=EDGE_CURVE ( 'NONE', #14666, #43301, #37063, .T. ) ;
#10331=CARTESIAN_POINT ( 'NONE',  ( 0.3665391374699465965, 11.44911061034392574, -4.447929964102732114 ) ) ;
#10332=CARTESIAN_POINT ( 'NONE',  ( 1.452237505248555660, 9.303501428256145900, -8.579708443906651993 ) ) ;
#10333=CARTESIAN_POINT ( 'NONE',  ( 2.290907136833252533, 0.1622757685886151990, -7.649199419879185058 ) ) ;
#10336=ORIENTED_EDGE ( 'NONE', *, *, #36913, .T. ) ;
#10343=ORIENTED_EDGE ( 'NONE', *, *, #40054, .T. ) ;
#10348=ORIENTED_EDGE ( 'NONE', *, *, #37229, .T. ) ;
#10349=CARTESIAN_POINT ( 'NONE',  ( 2.177405672431371730, -0.6747479782259577785, -11.17876532285605151 ) ) ;
#10360=CARTESIAN_POINT ( 'NONE',  ( 0.3654063281920756356, -6.366443614636611237, -10.50027211615253542 ) ) ;
#10371=CARTESIAN_POINT ( 'NONE',  ( 0.3160775863651080209, -3.967735865794275618, -11.60348481172939472 ) ) ;
#10374=EDGE_CURVE ( 'NONE', #29318, #24195, #53010, .T. ) ;
#10375=CARTESIAN_POINT ( 'NONE',  ( 1.719304012338199517, 12.20344780065974888, 3.626341562670754914 ) ) ;
#10376=VERTEX_POINT ( 'NONE', #17447 ) ;
#10377=CARTESIAN_POINT ( 'NONE',  ( 0.3401186441510225533, -4.436257390736900952, 11.44115600261389254 ) ) ;
#10378=ORIENTED_EDGE ( 'NONE', *, *, #64756, .F. ) ;
#10383=CARTESIAN_POINT ( 'NONE',  ( 1.287602823388412254, 12.00540336274551656, -3.781900355161493366 ) ) ;
#10389=ORIENTED_EDGE ( 'NONE', *, *, #60502, .T. ) ;
#10396=EDGE_CURVE ( 'NONE', #49910, #9776, #64297, .T. ) ;
#10406=CARTESIAN_POINT ( 'NONE',  ( 1.198791140419924739, -3.806343609710814757, -11.96656299555120029 ) ) ;
#10420=EDGE_CURVE ( 'NONE', #45313, #43566, #57004, .T. ) ;
#10427=CARTESIAN_POINT ( 'NONE',  ( 0.2653141334712546540, 6.084912053827487455, -10.62748186152491492 ) ) ;
#10433=DIRECTION ( 'NONE',  ( -1.000000000000000000, 0.000000000000000000, 0.000000000000000000 ) ) ;
#10437=ORIENTED_EDGE ( 'NONE', *, *, #28967, .T. ) ;
#10447=CARTESIAN_POINT ( 'NONE',  ( 0.8375941296792197566, -2.537217542321857255, 12.17542732751276979 ) ) ;
#10449=ORIENTED_EDGE ( 'NONE', *, *, #50429, .T. ) ;
#10454=CARTESIAN_POINT ( 'NONE',  ( 0.3537226245948369430, 12.04110684114372809, 2.388187631842557668 ) ) ;
#10457=ORIENTED_EDGE ( 'NONE', *, *, #36148, .T. ) ;
#10461=CARTESIAN_POINT ( 'NONE',  ( 0.2676618633000450442, 0.1607051348609344621, -12.24591287309138998 ) ) ;
#10469=CARTESIAN_POINT ( 'NONE',  ( 2.297017764050093280, 7.506328781223023938, -1.490897313050607353 ) ) ;
#10470=CARTESIAN_POINT ( 'NONE',  ( 2.827825597296806492, 8.965636292765729820, -1.027532345921593260 ) ) ;
#10477=CARTESIAN_POINT ( 'NONE',  ( 1.462291587751446409, 2.816455204777454480, -12.32753368892871393 ) ) ;
#10481=CARTESIAN_POINT ( 'NONE',  ( 2.430348790457661057, 1.144258029164405777, -7.611893186157544733 ) ) ;
#10485=CARTESIAN_POINT ( 'NONE',  ( 2.931247277082683844, -6.618030015945706168, -4.248542803114408350 ) ) ;
#10486=CARTESIAN_POINT ( 'NONE',  ( 2.589278595513622605, -7.197074516942377542, 2.875840518181560501 ) ) ;
#10492=CONICAL_SURFACE ( 'NONE', #13681, 7.938172270156617749, 1.280189991382167047 ) ;
#10495=CARTESIAN_POINT ( 'NONE',  ( 5.514970785353741078, 0.003929719953530106356, -0.002619824551223715308 ) ) ;
#10500=DIRECTION ( 'NONE',  ( -0.3939253465568944290, 0.3234796780324307175, 0.8603393047164971108 ) ) ;
#10502=CARTESIAN_POINT ( 'NONE',  ( 0.3002738374340832572, 7.705051734330280233, 9.533456882268664501 ) ) ;
#10510=CARTESIAN_POINT ( 'NONE',  ( 2.247206125382828379, -4.996658593545098448, 5.774712443419435459 ) ) ;
#10512=( NAMED_UNIT ( * ) PLANE_ANGLE_UNIT ( ) SI_UNIT ( $, .RADIAN. ) );
#10525=CARTESIAN_POINT ( 'NONE',  ( 2.653899356899941164, 7.604196386057505919, -1.606012885791470168 ) ) ;
#10543=CARTESIAN_POINT ( 'NONE',  ( 0.2671309869109518842, -10.68612389951472608, -5.982543484153332258 ) ) ;
#10549=CARTESIAN_POINT ( 'NONE',  ( 0.3665391374699465965, -10.50279796150441314, 6.368473106897091895 ) ) ;
#10554=CARTESIAN_POINT ( 'NONE',  ( 0.2655924914740778187, 0.04405032194320256805, -12.24627751708824341 ) ) ;
#10555=CARTESIAN_POINT ( 'NONE',  ( 0.2653141334712572075, -12.05242949860145707, 2.169900597054481572 ) ) ;
#10557=CARTESIAN_POINT ( 'NONE',  ( 2.941278708680199916, -5.721889327162167582, 2.226055275041770809 ) ) ;
#10563=B_SPLINE_CURVE_WITH_KNOTS ( 'NONE', 3,
 ( #22877, #28188, #33802, #22196, #28494, #42454, #3251 ),
 .UNSPECIFIED., .F., .F.,
 ( 4, 3, 4 ),
 ( 0.000000000000000000, 0.001700533616330527579, 0.005002426799372427547 ),
 .UNSPECIFIED. ) ;
#10567=CARTESIAN_POINT ( 'NONE',  ( 2.080613030138687591, 0.000000000000000000, 1.000000000000000000 ) ) ;
#10571=CARTESIAN_POINT ( 'NONE',  ( 5.520433897694421610, 0.0005131706886598308426, 0.01505375422439123381 ) ) ;
#10572=ORIENTED_EDGE ( 'NONE', *, *, #8636, .T. ) ;
#10573=CARTESIAN_POINT ( 'NONE',  ( 0.2653519991613815243, 12.24619736885324350, 0.02201648635046494357 ) ) ;
#10582=VERTEX_POINT ( 'NONE', #19746 ) ;
#10588=CARTESIAN_POINT ( 'NONE',  ( 0.6473888112830228359, 9.263269341114897415, -8.203438694127560993 ) ) ;
#10592=CARTESIAN_POINT ( 'NONE',  ( 2.899286259009693278, -2.348384892629313825, -7.494390643303798782 ) ) ;
#10594=ORIENTED_EDGE ( 'NONE', *, *, #17917, .T. ) ;
#10598=EDGE_LOOP ( 'NONE', ( #38697, #19696, #24129, #16519 ) ) ;
#10601=CARTESIAN_POINT ( 'NONE',  ( 2.177405672433375017, 11.12610351584940815, 1.276675186593112743 ) ) ;
#10603=CARTESIAN_POINT ( 'NONE',  ( 2.653899356899894091, 7.209790345489538232, -2.902068786425278546 ) ) ;
#10621=CARTESIAN_POINT ( 'NONE',  ( 1.459561108992494027, 11.25243317554858713, 5.767168887069277439 ) ) ;
#10625=CARTESIAN_POINT ( 'NONE',  ( 2.305787727787084407, -5.970480882365190034, -4.792270232040956479 ) ) ;
#10627=CARTESIAN_POINT ( 'NONE',  ( 2.990245332647858856, -3.789007530133526203, -7.587819667496388476 ) ) ;
#10628=CARTESIAN_POINT ( 'NONE',  ( 1.287602823388592554, -10.61402828236312423, -6.765713844066213234 ) ) ;
#10640=ORIENTED_EDGE ( 'NONE', *, *, #60930, .T. ) ;
#10644=CARTESIAN_POINT ( 'NONE',  ( 2.406456491626456806, 2.427896847126206126, 10.14681500356066124 ) ) ;
#10646=B_SPLINE_CURVE_WITH_KNOTS ( 'NONE', 3,
 ( #10655, #5708, #36602, #17553, #35608, #30301, #36257, #61216, #30608, #50597, #1030, #40600, #16325, #5040, #55899, #25981, #10333, #21297, #56904 ),
 .UNSPECIFIED., .F., .F.,
 ( 4, 3, 3, 3, 3, 3, 4 ),
 ( 1.355252715606880543E-20, 2.831840207499286354E-05, 4.217266859840029938E-05, 5.602024318395480761E-05, 6.290810167968589916E-05, 9.120440630944714989E-05, 0.0001153103026479765912 ),
 .UNSPECIFIED. ) ;
#10649=CARTESIAN_POINT ( 'NONE',  ( 0.3223008802179241905, 12.26274332232494224, -0.2444878876723663164 ) ) ;
#10655=CARTESIAN_POINT ( 'NONE',  ( 2.241352910868908310, 0.08337961031714861970, -7.633946224498473043 ) ) ;
#10669=ORIENTED_EDGE ( 'NONE', *, *, #25384, .T. ) ;
#10672=CARTESIAN_POINT ( 'NONE',  ( 2.440552418640498544, 2.818488640081671548, -7.166505277347694047 ) ) ;
#10681=CARTESIAN_POINT ( 'NONE',  ( 2.269879328257222717, 4.798845682293883641, -5.949827370244219260 ) ) ;
#10684=ORIENTED_EDGE ( 'NONE', *, *, #40794, .T. ) ;
#10693=CARTESIAN_POINT ( 'NONE',  ( 2.259025283528086181, 3.937899517809479999, 6.547290863799049454 ) ) ;
#10706=CARTESIAN_POINT ( 'NONE',  ( 2.994568964204217920, -5.775954174106896488, -5.368337437440318105 ) ) ;
#10708=ORIENTED_EDGE ( 'NONE', *, *, #24455, .F. ) ;
#10711=CARTESIAN_POINT ( 'NONE',  ( 5.520433897694421610, 0.007971295965052416221, -0.01278034823631966389 ) ) ;
#10714=CARTESIAN_POINT ( 'NONE',  ( 5.514970785353741078, -0.002093325033903842454, 0.004233694591582945477 ) ) ;
#10723=CARTESIAN_POINT ( 'NONE',  ( 2.969415267403874292, 0.3878973768015938628, 7.867532449842894238 ) ) ;
#10735=DIRECTION ( 'NONE',  ( 0.000000000000000000, 0.000000000000000000, 1.000000000000000000 ) ) ;
#10739=CARTESIAN_POINT ( 'NONE',  ( 0.6511581176968128659, -3.919972364658588670, -11.73752429815142229 ) ) ;
#10747=DIRECTION ( 'NONE',  ( -0.3939253465568943735, -0.3234796780324251109, -0.8603393047164992202 ) ) ;
#10753=ORIENTED_EDGE ( 'NONE', *, *, #64156, .T. ) ;
#10760=ORIENTED_EDGE ( 'NONE', *, *, #44969, .F. ) ;
#10763=DIRECTION ( 'NONE',  ( -0.3939253465568944290, -0.4679616473074788563, -0.7910971609033250473 ) ) ;
#10771=CARTESIAN_POINT ( 'NONE',  ( 5.516018279890452902, 0.001397286410094317416, -0.006629829924290979969 ) ) ;
#10780=DIRECTION ( 'NONE',  ( -1.000000000000000000, -0.000000000000000000, -0.000000000000000000 ) ) ;
#10785=FACE_OUTER_BOUND ( 'NONE', #36261, .T. ) ;
#10786=CARTESIAN_POINT ( 'NONE',  ( 0.2739690278137256185, -12.02985305092652268, 2.307031017960411656 ) ) ;
#10804=EDGE_CURVE ( 'NONE', #32432, #15657, #36380, .T. ) ;
#10808=AXIS2_PLACEMENT_3D ( 'NONE', #52493, #6927, #32815 ) ;
#10818=CARTESIAN_POINT ( 'NONE',  ( 2.305787727787084407, 1.164987321564833422, -7.566723232958059597 ) ) ;
#10827=ORIENTED_EDGE ( 'NONE', *, *, #8636, .F. ) ;
#10835=CARTESIAN_POINT ( 'NONE',  ( 5.514970785353741078, 0.003929719953530106356, -0.002619824551223718344 ) ) ;
#10838=CARTESIAN_POINT ( 'NONE',  ( 2.835339799623980639, 1.035140033450052011, 7.763739326985116485 ) ) ;
#10844=AXIS2_PLACEMENT_3D ( 'NONE', #38438, #53749, #18822 ) ;
#10846=CARTESIAN_POINT ( 'NONE',  ( 0.2651627682582891055, -7.803986935114077816, 9.437482589529949450 ) ) ;
#10847=CARTESIAN_POINT ( 'NONE',  ( 0.5572780756289471560, -1.841882550626719794, -12.20533540249727800 ) ) ;
#10852=ORIENTED_EDGE ( 'NONE', *, *, #1281, .T. ) ;
#10853=CARTESIAN_POINT ( 'NONE',  ( 3.152665057734121756, -0.4801242025592447060, 7.923639299008720549 ) ) ;
#10859=CARTESIAN_POINT ( 'NONE',  ( 0.2833330754217355252, 11.44258640049861242, 4.379886056890929247 ) ) ;
#10864=ADVANCED_FACE ( 'NONE', ( #53928 ), #63301, .F. ) ;
#10866=CARTESIAN_POINT ( 'NONE',  ( 5.514970785353741078, -0.004588761610584819045, -0.001117786416802158496 ) ) ;
#10882=ORIENTED_EDGE ( 'NONE', *, *, #14239, .F. ) ;
#10883=CARTESIAN_POINT ( 'NONE',  ( 1.283627346226323240, 12.57362488724964145, -0.5505361391623029288 ) ) ;
#10884=CIRCLE ( 'NONE', #21530, 6.000000000000000888 ) ;
#10887=CARTESIAN_POINT ( 'NONE',  ( 0.9232058338315048962, -10.60677148422239924, -6.559496812049772529 ) ) ;
#10903=ORIENTED_EDGE ( 'NONE', *, *, #21371, .T. ) ;
#10910=EDGE_CURVE ( 'NONE', #35534, #64984, #54899, .T. ) ;
#10913=CARTESIAN_POINT ( 'NONE',  ( 0.9232058338315048962, 12.46548196349786153, 0.3773051331668418329 ) ) ;
#10920=VECTOR ( 'NONE', #5183, 1000.000000000000000 ) ;
#10922=CARTESIAN_POINT ( 'NONE',  ( 0.3401186441510284375, -11.61600526280573220, 3.955862996551460231 ) ) ;
#10929=CARTESIAN_POINT ( 'NONE',  ( 2.290907136833248980, -6.543263131934267562, -3.965134647955961711 ) ) ;
#10931=DIRECTION ( 'NONE',  ( -1.000000000000000000, -0.000000000000000000, -0.000000000000000000 ) ) ;
#10932=DIRECTION ( 'NONE',  ( 0.000000000000000000, 0.000000000000000000, 1.000000000000000000 ) ) ;
#10937=CARTESIAN_POINT ( 'NONE',  ( 1.634816307079405506, 12.61459884933078435, -1.494046826340906575 ) ) ;
#10939=CARTESIAN_POINT ( 'NONE',  ( 1.549075743845170772, -11.29795072957498547, 5.743768701986912362 ) ) ;
#10944=B_SPLINE_CURVE_WITH_KNOTS ( 'NONE', 3,
 ( #25456, #30123, #36421, #35430, #35081, #26439, #46723 ),
 .UNSPECIFIED., .F., .F.,
 ( 4, 3, 4 ),
 ( 1.191827804620218263E-14, 0.002398160485435229215, 0.005002426799390250096 ),
 .UNSPECIFIED. ) ;
#10949=EDGE_CURVE ( 'NONE', #6328, #14103, #65554, .T. ) ;
#10950=DIRECTION ( 'NONE',  ( 0.000000000000000000, 0.000000000000000000, 1.000000000000000000 ) ) ;
#10951=CARTESIAN_POINT ( 'NONE',  ( 3.092491956585685653, 3.124176487320323936, 7.275786042219381855 ) ) ;
#10964=CARTESIAN_POINT ( 'NONE',  ( 1.109979610368935665, 11.59954799439076112, 4.732439402373389115 ) ) ;
#10967=CARTESIAN_POINT ( 'NONE',  ( 2.507146904658099640, -1.127530020444445613, -7.640248566386912188 ) ) ;
#10968=CARTESIAN_POINT ( 'NONE',  ( 1.937114397841932290, 5.620553190832977108, 11.53912442307257358 ) ) ;
#10979=CARTESIAN_POINT ( 'NONE',  ( 0.2739690278137251744, -8.012873994335626193, -9.264642836915912838 ) ) ;
#10981=CARTESIAN_POINT ( 'NONE',  ( 5.516018279890452902, 0.006440244342253413461, -0.002104829434641034870 ) ) ;
#10982=CARTESIAN_POINT ( 'NONE',  ( 2.994568964204210815, -7.875338388187470784, -0.3996732855055539768 ) ) ;
#10988=DIRECTION ( 'NONE',  ( 0.000000000000000000, 0.000000000000000000, 1.000000000000000000 ) ) ;
#10993=CARTESIAN_POINT ( 'NONE',  ( 2.241352910868908754, 7.532448145350508995, 1.243507963608119438 ) ) ;
#10996=CARTESIAN_POINT ( 'NONE',  ( 0.2676618633000454328, 2.284744117040236500, -12.03196378632208763 ) ) ;
#10999=CARTESIAN_POINT ( 'NONE',  ( 0.2872850955227737590, 12.25172867346923233, -0.2089153415335295583 ) ) ;
#11000=CARTESIAN_POINT ( 'NONE',  ( 2.241526690369557429, 2.627393882429315930, 7.168108047190845156 ) ) ;
#11001=CARTESIAN_POINT ( 'NONE',  ( 0.4626703367447430049, -5.909149965570928309, -10.80124546303572330 ) ) ;
#11007=EDGE_CURVE ( 'NONE', #31314, #41256, #38619, .T. ) ;
#11008=VERTEX_POINT ( 'NONE', #52222 ) ;
#11015=CARTESIAN_POINT ( 'NONE',  ( 0.2767916011545371036, -1.940025653808925554, 12.09541651105896776 ) ) ;
#11016=ORIENTED_EDGE ( 'NONE', *, *, #20103, .F. ) ;
#11018=VERTEX_POINT ( 'NONE', #16633 ) ;
#11020=CARTESIAN_POINT ( 'NONE',  ( 2.994568964204215256, 7.875338388187474337, 0.3996732855055006306 ) ) ;
#11024=ORIENTED_EDGE ( 'NONE', *, *, #34159, .T. ) ;
#11035=EDGE_CURVE ( 'NONE', #58225, #32302, #11630, .T. ) ;
#11040=CARTESIAN_POINT ( 'NONE',  ( 5.514970785353741078, 0.004588761610585025477, -0.001117786416802570059 ) ) ;
#11047=CARTESIAN_POINT ( 'NONE',  ( 0.2653141617321028156, 4.147035654172719354, 11.52265685897330449 ) ) ;
#11052=CARTESIAN_POINT ( 'NONE',  ( 1.937114397841935398, -1.334979369128509674, 12.76557247858998068 ) ) ;
#11053=EDGE_CURVE ( 'NONE', #58632, #17370, #41784, .T. ) ;
#11060=CARTESIAN_POINT ( 'NONE',  ( 3.152665057734040488, 0.000000000000000000, 0.000000000000000000 ) ) ;
#11067=VECTOR ( 'NONE', #29790, 1000.000000000000000 ) ;
#11073=VERTEX_POINT ( 'NONE', #53539 ) ;
#11078=( BOUNDED_SURFACE ( )  B_SPLINE_SURFACE ( 3, 1, ( 
 ( #41344, #15739 ),
 ( #40704, #52002 ),
 ( #61628, #30709 ),
 ( #5139, #36019 ) ),
 .UNSPECIFIED., .F., .F., .T. ) 
 B_SPLINE_SURFACE_WITH_KNOTS ( ( 4, 4 ),
 ( 2, 2 ),
 ( 0.000000000000000000, 1.000000000000000000 ),
 ( 0.000000000000000000, 1.000000000000000000 ),
 .UNSPECIFIED. ) 
 GEOMETRIC_REPRESENTATION_ITEM ( )  RATIONAL_B_SPLINE_SURFACE ( (
 ( 1.000000000000000000, 1.000000000000000000),
 ( 0.9942764183789327692, 0.8450855930916580938),
 ( 0.9942764183789327692, 0.8450855930916580938),
 ( 1.000000000000000000, 1.000000000000000000) ) ) 
 REPRESENTATION_ITEM ( '' )  SURFACE ( )  );
#11089=VERTEX_POINT ( 'NONE', #23926 ) ;
#11095=CARTESIAN_POINT ( 'NONE',  ( 5.516018279890452902, -0.005976902763919015801, 0.003191189039764900665 ) ) ;
#11100=CARTESIAN_POINT ( 'NONE',  ( 0.2648978790185610999, -6.008231198269058382, 10.67083876753489946 ) ) ;
#11101=VERTEX_POINT ( 'NONE', #54170 ) ;
#11102=VERTEX_POINT ( 'NONE', #44186 ) ;
#11114=CARTESIAN_POINT ( 'NONE',  ( 0.2653519991613820239, -12.05632699103097494, -2.148211862903036451 ) ) ;
#11115=VERTEX_POINT ( 'NONE', #48541 ) ;
#11129=CARTESIAN_POINT ( 'NONE',  ( 5.515188684475870851, 0.002355816063606810083, -0.004804816249379317492 ) ) ;
#11133=ORIENTED_EDGE ( 'NONE', *, *, #63620, .T. ) ;
#11137=CARTESIAN_POINT ( 'NONE',  ( 1.937114397841935398, -3.531416430611377777, 12.33981801388256550 ) ) ;
#11140=B_SPLINE_CURVE_WITH_KNOTS ( 'NONE', 3,
 ( #10993, #45568, #30931, #26281, #15631, #46559, #5352, #20, #50586, #35902 ),
 .UNSPECIFIED., .F., .F.,
 ( 4, 3, 3, 4 ),
 ( 8.673617379884035472E-19, 6.607638129004486172E-05, 9.911389841680512771E-05, 0.0001667630577588619318 ),
 .UNSPECIFIED. ) ;
#11145=EDGE_CURVE ( 'NONE', #14988, #31123, #29261, .T. ) ;
#11148=ADVANCED_FACE ( 'NONE', ( #47873 ), #45433, .F. ) ;
#11151=CARTESIAN_POINT ( 'NONE',  ( 2.241352910868909643, -7.202080440908757986, 2.532612177304417678 ) ) ;
#11157=CARTESIAN_POINT ( 'NONE',  ( 0.3665391374699472626, 0.2638605131387167790, 12.27992639892678461 ) ) ;
#11162=ADVANCED_FACE ( 'NONE', ( #59814 ), #59065, .F. ) ;
#11163=CARTESIAN_POINT ( 'NONE',  ( 0.2646305136544072623, -12.03696649559613441, -2.256625640822436996 ) ) ;
#11164=CARTESIAN_POINT ( 'NONE',  ( 2.653899356900250694, -7.209790345489586194, 2.902068786425478386 ) ) ;
#11165=ORIENTED_EDGE ( 'NONE', *, *, #50001, .F. ) ;
#11168=CARTESIAN_POINT ( 'NONE',  ( 2.268878695253355726, 1.181158368266951308, 7.551766617932576864 ) ) ;
#11174=CARTESIAN_POINT ( 'NONE',  ( 3.152665057733966769, 0.9030954876739563097, 7.886634106564108571 ) ) ;
#11179=VERTEX_POINT ( 'NONE', #14554 ) ;
#11180=CARTESIAN_POINT ( 'NONE',  ( 0.2833330754217382452, 7.719627479384659985, 9.514385791198117559 ) ) ;
#11181=CARTESIAN_POINT ( 'NONE',  ( 0.2646305136544065406, -6.008537389229490877, 10.67138229758227652 ) ) ;
#11184=CARTESIAN_POINT ( 'NONE',  ( 0.2648321136542705623, -11.45826514585340306, -4.321267941897623643 ) ) ;
#11185=CARTESIAN_POINT ( 'NONE',  ( 2.241526690369556096, 2.594870554108938521, -7.179945570618733619 ) ) ;
#11186=CARTESIAN_POINT ( 'NONE',  ( 0.2655924914740778742, 10.62761259256416935, 6.084990060696545910 ) ) ;
#11193=EDGE_CURVE ( 'NONE', #54941, #37857, #44144, .T. ) ;
#11198=CARTESIAN_POINT ( 'NONE',  ( 1.452237505248552996, 8.579708443906870485, -9.303501428255941619 ) ) ;
#11200=CARTESIAN_POINT ( 'NONE',  ( 0.2638984909335720941, 1.930290337334216622, -12.09426044257622479 ) ) ;
#11202=ORIENTED_EDGE ( 'NONE', *, *, #8619, .T. ) ;
#11204=CARTESIAN_POINT ( 'NONE',  ( 2.844750968615874509, 7.651810733888815719, -1.686994672842110798 ) ) ;
#11207=CARTESIAN_POINT ( 'NONE',  ( 0.2638984909335720941, -4.001111175853819368, 11.57533005135177717 ) ) ;
#11215=CARTESIAN_POINT ( 'NONE',  ( 2.242819959140647246, 7.500446639314770181, 1.426511055719334564 ) ) ;
#11217=CARTESIAN_POINT ( 'NONE',  ( 1.719304012338199295, 12.70777170743846796, -0.7661785589580241140 ) ) ;
#11221=CARTESIAN_POINT ( 'NONE',  ( 5.515188684475870851, 0.002983184900675330160, 0.004442604682416625983 ) ) ;
#11223=CARTESIAN_POINT ( 'NONE',  ( 5.520433897694421610, -0.01278034823632010972, 0.007971295965052730206 ) ) ;
#11230=B_SPLINE_CURVE_WITH_KNOTS ( 'NONE', 3,
 ( #44089, #65655, #64361, #60694, #64668, #54736, #9158 ),
 .UNSPECIFIED., .F., .F.,
 ( 4, 3, 4 ),
 ( 0.000000000000000000, 0.001700533616330602389, 0.005002426799371321661 ),
 .UNSPECIFIED. ) ;
#11234=CARTESIAN_POINT ( 'NONE',  ( 1.547277799339146664, -10.12789507952348167, -7.618736734813534639 ) ) ;
#11237=CARTESIAN_POINT ( 'NONE',  ( 2.241531873784870399, -0.01153688368838857656, -7.634454672504356054 ) ) ;
#11247=VERTEX_POINT ( 'NONE', #46800 ) ;
#11250=CARTESIAN_POINT ( 'NONE',  ( 1.719304012339867516, -12.38166659046446938, 2.961219984258617544 ) ) ;
#11251=ADVANCED_FACE ( 'NONE', ( #32147 ), #6820, .F. ) ;
#11253=FACE_OUTER_BOUND ( 'NONE', #49004, .T. ) ;
#11255=CIRCLE ( 'NONE', #20794, 7.938172270156617749 ) ;
#11265=CARTESIAN_POINT ( 'NONE',  ( 1.375507693219674143, -7.647735792764906115, -10.03411718356184856 ) ) ;
#11271=CARTESIAN_POINT ( 'NONE',  ( 0.8375941296801195923, -10.95781044612433064, 5.882592429484332364 ) ) ;
#11275=CARTESIAN_POINT ( 'NONE',  ( 1.198791140421116008, 8.460175745279389758, -9.279671759317686508 ) ) ;
#11284=CARTESIAN_POINT ( 'NONE',  ( 5.514970785353741078, -0.001897634820904511074, 0.004324946436530178843 ) ) ;
#11290=CARTESIAN_POINT ( 'NONE',  ( 2.556980015513156790, -5.777953785406852560, 5.149458076504425996 ) ) ;
#11291=ADVANCED_FACE ( 'NONE', ( #51154 ), #13357, .T. ) ;
#11293=CARTESIAN_POINT ( 'NONE',  ( 2.963017218115627127, -0.9869543242667578875, -7.812878240621082604 ) ) ;
#11294=CARTESIAN_POINT ( 'NONE',  ( 2.245754705088393255, 2.715960966012193278, -7.136529175883334020 ) ) ;
#11296=VERTEX_POINT ( 'NONE', #41465 ) ;
#11297=CIRCLE ( 'NONE', #65423, 7.938172270156617749 ) ;
#11305=CARTESIAN_POINT ( 'NONE',  ( 2.665405856346790170, -4.274976649834401954, -8.559192023451558384 ) ) ;
#11310=FACE_OUTER_BOUND ( 'NONE', #21277, .T. ) ;
#11312=CARTESIAN_POINT ( 'NONE',  ( 1.937114397841935398, 8.920887662793472117, 9.228205347192481867 ) ) ;
#11320=CARTESIAN_POINT ( 'NONE',  ( 2.899286259009681288, 3.614094927251937595, 6.972741252562068226 ) ) ;
#11323=CARTESIAN_POINT ( 'NONE',  ( 2.241506898688419902, 2.648071636522731698, 7.160521809579504016 ) ) ;
#11324=CARTESIAN_POINT ( 'NONE',  ( 0.8375941296809087389, -5.882592429484210683, -10.95781044612470012 ) ) ;
#11326=CARTESIAN_POINT ( 'NONE',  ( 0.9232058338315058954, 7.723624854284846464, -9.791640253608070665 ) ) ;
#11333=CARTESIAN_POINT ( 'NONE',  ( 0.2646305136544065406, -9.465888453932908675, -7.770320294339271960 ) ) ;
#11342=CARTESIAN_POINT ( 'NONE',  ( 0.3675815128205894289, 1.872154644482245889, -12.13672785388548547 ) ) ;
#11343=ORIENTED_EDGE ( 'NONE', *, *, #30281, .F. ) ;
#11346=ORIENTED_EDGE ( 'NONE', *, *, #1936, .T. ) ;
#11353=CARTESIAN_POINT ( 'NONE',  ( 0.4613984246114869459, 7.694922453052268629, -9.610550265395774616 ) ) ;
#11357=CARTESIAN_POINT ( 'NONE',  ( 5.515539859299206427, -0.005924322247674730646, -0.001241880655086653002 ) ) ;
#11359=CARTESIAN_POINT ( 'NONE',  ( 1.020182472824531672, 6.631405022220766554, -10.59341968305531623 ) ) ;
#11365=CARTESIAN_POINT ( 'NONE',  ( 0.9232058338315058954, -1.793035206307428853, 12.34162163148533153 ) ) ;
#11393=CARTESIAN_POINT ( 'NONE',  ( 0.9232167919969077596, 4.649596781010405522, 11.56588005394299934 ) ) ;
#11399=CARTESIAN_POINT ( 'NONE',  ( 0.3160775863651104634, -12.26075464248083868, -0.2401734240704150591 ) ) ;
#11401=CARTESIAN_POINT ( 'NONE',  ( 1.287602823384993878, 10.61402828236296436, 6.765713844064224602 ) ) ;
#11407=VERTEX_POINT ( 'NONE', #28167 ) ;
#11412=CARTESIAN_POINT ( 'NONE',  ( 2.941278708680199916, 1.972702289976081991, -5.814102272488566925 ) ) ;
#11414=ORIENTED_EDGE ( 'NONE', *, *, #32713, .T. ) ;
#11420=ORIENTED_EDGE ( 'NONE', *, *, #9927, .T. ) ;
#11423=CARTESIAN_POINT ( 'NONE',  ( 5.536195898058073439, -0.008411485181669250619, -0.001224473329857952162 ) ) ;
#11427=B_SPLINE_CURVE_WITH_KNOTS ( 'NONE', 3,
 ( #65474, #46213, #10601, #30885, #9615, #29912, #655 ),
 .UNSPECIFIED., .F., .F.,
 ( 4, 3, 4 ),
 ( 3.660687858773823404E-18, 0.002398160485434294199, 0.005002426799376703641 ),
 .UNSPECIFIED. ) ;
#11433=CARTESIAN_POINT ( 'NONE',  ( 2.276198483117257698, -7.644465698238554374, -0.1540629821339100092 ) ) ;
#11434=ORIENTED_EDGE ( 'NONE', *, *, #16204, .T. ) ;
#11435=CARTESIAN_POINT ( 'NONE',  ( 0.9232167919969117564, 8.324955738482477940, 9.278116382137406859 ) ) ;
#11437=CARTESIAN_POINT ( 'NONE',  ( 0.3040950598368144520, -11.60568999039897875, 3.956873563689492279 ) ) ;
#11448=CARTESIAN_POINT ( 'NONE',  ( 0.2646305136544065406, -6.237419468587005689, -10.53923716745253003 ) ) ;
#11454=( BOUNDED_SURFACE ( )  B_SPLINE_SURFACE ( 3, 1, ( 
 ( #57495, #52823 ),
 ( #6950, #22571 ),
 ( #22904, #1955 ),
 ( #63124, #42487 ) ),
 .UNSPECIFIED., .F., .F., .F. ) 
 B_SPLINE_SURFACE_WITH_KNOTS ( ( 4, 4 ),
 ( 2, 2 ),
 ( 0.000000000000000000, 1.000000000000000000 ),
 ( 0.000000000000000000, 1.000000000000000000 ),
 .UNSPECIFIED. ) 
 GEOMETRIC_REPRESENTATION_ITEM ( )  RATIONAL_B_SPLINE_SURFACE ( (
 ( 1.000000000000000000, 1.000000000000000000),
 ( 0.6933888150995267674, 0.9895912004443193632),
 ( 0.6933888150995267674, 0.9895912004443193632),
 ( 1.000000000000000000, 1.000000000000000000) ) ) 
 REPRESENTATION_ITEM ( '' )  SURFACE ( )  );
#11455=ORIENTED_EDGE ( 'NONE', *, *, #59667, .T. ) ;
#11459=CARTESIAN_POINT ( 'NONE',  ( 5.530133899448235191, 0.009387834778845326189, 0.01293763278443411935 ) ) ;
#11460=CARTESIAN_POINT ( 'NONE',  ( 0.2651627923886318294, 12.07509237025073645, -2.039714259676051800 ) ) ;
#11461=ADVANCED_FACE ( 'NONE', ( #63387 ), #45063, .F. ) ;
#11462=CARTESIAN_POINT ( 'NONE',  ( 0.3675815128205894289, 2.391755495700764289, -12.04510820461657161 ) ) ;
#11471=CARTESIAN_POINT ( 'NONE',  ( 5.530133899448235191, -0.01437126147332039479, 0.006998616117863549688 ) ) ;
#11479=CARTESIAN_POINT ( 'NONE',  ( 0.2648978790185593790, 4.063980959785203240, -11.55204314799259890 ) ) ;
#11481=CARTESIAN_POINT ( 'NONE',  ( 0.2646305136544072623, -10.53923716745242700, -6.237419468587187765 ) ) ;
#11482=EDGE_CURVE ( 'NONE', #21985, #36221, #59236, .T. ) ;
#11484=EDGE_LOOP ( 'NONE', ( #55180, #30582, #22314, #37029 ) ) ;
#11489=ORIENTED_EDGE ( 'NONE', *, *, #14063, .T. ) ;
#11492=CARTESIAN_POINT ( 'NONE',  ( 0.3665391374699472626, -5.911453292029678508, 10.76665847464310843 ) ) ;
#11500=CARTESIAN_POINT ( 'NONE',  ( 5.514624014163232779, -0.003060352188290796274, -0.002789935220458035839 ) ) ;
#11503=EDGE_LOOP ( 'NONE', ( #49978, #4082, #63642, #29431 ) ) ;
#11506=VECTOR ( 'NONE', #46788, 1000.000000000000114 ) ;
#11509=CARTESIAN_POINT ( 'NONE',  ( 1.452237505248552996, -10.06489946308207095, 7.672309600508662619 ) ) ;
#11517=CARTESIAN_POINT ( 'NONE',  ( 3.092491956585539103, 7.707758057368735649, -1.813286239165393665 ) ) ;
#11519=CARTESIAN_POINT ( 'NONE',  ( 2.241536586108911600, 1.319514354261297484, -7.519576125149795232 ) ) ;
#11523=EDGE_CURVE ( 'NONE', #46786, #60151, #50265, .T. ) ;
#11524=CARTESIAN_POINT ( 'NONE',  ( 2.931247277082686065, -7.800615791174664082, 0.9994150891046047480 ) ) ;
#11527=ORIENTED_EDGE ( 'NONE', *, *, #35566, .F. ) ;
#11549=CARTESIAN_POINT ( 'NONE',  ( 2.261269890822091622, 4.803890999604312206, 5.942064862945645842 ) ) ;
#11550=CARTESIAN_POINT ( 'NONE',  ( 0.2652384529303136174, -0.06607367983845134629, -12.24598125395191772 ) ) ;
#11552=ORIENTED_EDGE ( 'NONE', *, *, #54959, .T. ) ;
#11554=DIRECTION ( 'NONE',  ( 0.3939253465568943735, 0.5982248387291241309, -0.6978179301705739190 ) ) ;
#11559=CARTESIAN_POINT ( 'NONE',  ( 2.266490820343225465, 2.750080098241514115, 7.130860233521858049 ) ) ;
#11576=CARTESIAN_POINT ( 'NONE',  ( 0.2648978790185619880, -10.53870023327867855, 6.237101853238509186 ) ) ;
#11578=DIRECTION ( 'NONE',  ( -1.000000000000000000, -0.000000000000000000, -0.000000000000000000 ) ) ;
#11580=CARTESIAN_POINT ( 'NONE',  ( 2.556980015511752136, 7.736177238086046515, -0.2307166419790108725 ) ) ;
#11590=FACE_OUTER_BOUND ( 'NONE', #9657, .T. ) ;
#11602=B_SPLINE_CURVE_WITH_KNOTS ( 'NONE', 3,
 ( #34474, #54455, #9193, #49470, #24168, #3257, #44433, #24836, #19182, #65052, #39454, #19528, #59757, #55081, #4224, #14185 ),
 .UNSPECIFIED., .F., .F.,
 ( 4, 3, 3, 3, 3, 4 ),
 ( 1.946286347258496500E-18, 0.0003017745587525237291, 0.0006035491769808725478, 0.0009053241094668148387, 0.001207275924542836228, 0.001510325902538653484 ),
 .UNSPECIFIED. ) ;
#11606=CARTESIAN_POINT ( 'NONE',  ( 0.3109076770649015220, 4.414555973477820139, 11.43910935267333784 ) ) ;
#11617=CARTESIAN_POINT ( 'NONE',  ( 2.705197763288458734, 4.789125516644123337, 6.142723737672358908 ) ) ;
#11618=CARTESIAN_POINT ( 'NONE',  ( 2.257661810676945713, 3.702552158175147046, -6.682681612748679889 ) ) ;
#11619=CARTESIAN_POINT ( 'NONE',  ( 0.2834382757448010715, -8.029794915379490305, -9.254160138069030594 ) ) ;
#11620=CARTESIAN_POINT ( 'NONE',  ( 0.2638984909335720941, 11.57533005135178783, 4.001111175853780288 ) ) ;
#11624=ORIENTED_EDGE ( 'NONE', *, *, #63552, .T. ) ;
#11630=LINE ( 'NONE', #52555, #54759 ) ;
#11642=CARTESIAN_POINT ( 'NONE',  ( 0.3665391374699467075, -10.76665847464316883, 5.911453292029565709 ) ) ;
#11645=CARTESIAN_POINT ( 'NONE',  ( 2.241451721903216843, 2.553895636571935857, 7.194631024842649047 ) ) ;
#11650=EDGE_CURVE ( 'NONE', #19209, #63267, #19543, .T. ) ;
#11652=CARTESIAN_POINT ( 'NONE',  ( 0.2650492594609224484, 2.017987075343959269, 12.07870403910582269 ) ) ;
#11669=CARTESIAN_POINT ( 'NONE',  ( 2.305787727787083519, 7.135468203929983488, 2.774453000917173284 ) ) ;
#11673=CARTESIAN_POINT ( 'NONE',  ( 1.014383007554944705, 7.686901933424285183, -9.851867765302106505 ) ) ;
#11681=AXIS2_PLACEMENT_3D ( 'NONE', #52070, #43056, #57385 ) ;
#11685=CARTESIAN_POINT ( 'NONE',  ( 0.2657645697724701495, -4.330388001246489260, 11.45515365350260240 ) ) ;
#11689=CARTESIAN_POINT ( 'NONE',  ( 0.9232058338315058954, 9.791640253608150601, 7.723624854284749652 ) ) ;
#11699=CARTESIAN_POINT ( 'NONE',  ( 5.536195898058073439, 0.007896796515810338216, 0.003145317580921177386 ) ) ;
#11700=EDGE_CURVE ( 'NONE', #26284, #47440, #46494, .T. ) ;
#11707=CARTESIAN_POINT ( 'NONE',  ( 2.406456491626455474, 0.6290357040720031545, 10.41426194695389995 ) ) ;
#11716=CARTESIAN_POINT ( 'NONE',  ( 0.2655924914740778742, 9.409507842006028966, 7.838010948425079505 ) ) ;
#11717=CARTESIAN_POINT ( 'NONE',  ( 0.2676618633000463210, -12.24591287309138821, -0.1607051348608917463 ) ) ;
#11720=CARTESIAN_POINT ( 'NONE',  ( 1.549075743846920483, -9.261503792573559934, -8.652116335902379163 ) ) ;
#11727=VERTEX_POINT ( 'NONE', #29665 ) ;
#11731=CARTESIAN_POINT ( 'NONE',  ( 3.152665057734040488, 0.000000000000000000, 0.000000000000000000 ) ) ;
#11735=CARTESIAN_POINT ( 'NONE',  ( 1.372161826076905067, -0.5897614319405121153, -12.60140585080819875 ) ) ;
#11739=CARTESIAN_POINT ( 'NONE',  ( 2.941278708680199916, 0.9331242451665799909, -6.068329152486366063 ) ) ;
#11745=CARTESIAN_POINT ( 'NONE',  ( 0.2652384770603688491, 9.423432754625833851, -7.820955051613227127 ) ) ;
#11749=CARTESIAN_POINT ( 'NONE',  ( 1.198791140417940326, -4.776130053252316543, 11.61358959650655187 ) ) ;
#11757=EDGE_CURVE ( 'NONE', #21481, #4753, #29672, .T. ) ;
#11766=CARTESIAN_POINT ( 'NONE',  ( 2.241536586108915152, -7.176205604390190729, -2.605228657247420365 ) ) ;
#11767=FACE_OUTER_BOUND ( 'NONE', #42712, .T. ) ;
#11768=CARTESIAN_POINT ( 'NONE',  ( 1.719304012341412724, 1.452142814149018690, -12.64775761152637301 ) ) ;
#11774=EDGE_LOOP ( 'NONE', ( #17526, #21089, #25097, #19387 ) ) ;
#11776=LINE ( 'NONE', #46710, #19019 ) ;
#11789=CARTESIAN_POINT ( 'NONE',  ( 2.717984159220126816, 1.073093837952427965, -7.719081760284447036 ) ) ;
#11799=CARTESIAN_POINT ( 'NONE',  ( 2.261269890821705264, -4.803890999604552015, -5.942064862945291459 ) ) ;
#11800=CARTESIAN_POINT ( 'NONE',  ( 2.276198483117263915, 1.175725118478853526, 7.555081843354693127 ) ) ;
#11802=CARTESIAN_POINT ( 'NONE',  ( 3.152665057735396736, -5.761241965768377327, 5.461013642406604696 ) ) ;
#11815=( BOUNDED_SURFACE ( )  B_SPLINE_SURFACE ( 3, 1, ( 
 ( #44695, #64986 ),
 ( #43730, #64010 ),
 ( #59051, #8161 ),
 ( #19458, #24109 ) ),
 .UNSPECIFIED., .F., .F., .F. ) 
 B_SPLINE_SURFACE_WITH_KNOTS ( ( 4, 4 ),
 ( 2, 2 ),
 ( 0.000000000000000000, 1.000000000000000000 ),
 ( 0.000000000000000000, 1.000000000000000000 ),
 .UNSPECIFIED. ) 
 GEOMETRIC_REPRESENTATION_ITEM ( )  RATIONAL_B_SPLINE_SURFACE ( (
 ( 1.000000000000000000, 1.000000000000000000),
 ( 0.9942764183789327692, 0.8450855930916580938),
 ( 0.9942764183789327692, 0.8450855930916580938),
 ( 1.000000000000000000, 1.000000000000000000) ) ) 
 REPRESENTATION_ITEM ( '' )  SURFACE ( )  );
#11818=B_SPLINE_CURVE_WITH_KNOTS ( 'NONE', 3,
 ( #38199, #7976, #53847, #12595, #47867, #58861, #32875, #28242, #2986, #11952, #43511, #2326, #32233, #63793, #18277, #13277 ),
 .UNSPECIFIED., .F., .F.,
 ( 4, 3, 3, 3, 3, 4 ),
 ( 0.000000000000000000, 0.0002176109881720225063, 0.0004352086762394585524, 0.0006528017811446870742, 0.0007615147961451692411, 0.0009453342004947387980 ),
 .UNSPECIFIED. ) ;
#11819=CARTESIAN_POINT ( 'NONE',  ( 0.2833330754217405767, -11.44258640049858577, -4.379886056891013624 ) ) ;
#11842=EDGE_CURVE ( 'NONE', #28065, #12917, #45288, .T. ) ;
#11849=AXIS2_PLACEMENT_3D ( 'NONE', #10296, #15610, #30901 ) ;
#11852=EDGE_CURVE ( 'NONE', #9459, #48048, #47957, .T. ) ;
#11855=DIRECTION ( 'NONE',  ( -1.000000000000000000, -0.000000000000000000, -0.000000000000000000 ) ) ;
#11871=CARTESIAN_POINT ( 'NONE',  ( 0.3341166715381309604, 7.691251065848466517, -9.559079491641789161 ) ) ;
#11873=VECTOR ( 'NONE', #34252, 1000.000000000000114 ) ;
#11875=CARTESIAN_POINT ( 'NONE',  ( 2.268878695253375710, 4.798796461778038314, 5.949442550447435529 ) ) ;
#11880=CARTESIAN_POINT ( 'NONE',  ( 2.368238019615397150, -1.155661230551800145, 7.589221137922757876 ) ) ;
#11890=VECTOR ( 'NONE', #55758, 1000.000000000000000 ) ;
#11904=CARTESIAN_POINT ( 'NONE',  ( 1.014383007554950700, 3.853787798429566092, -11.88680274101309564 ) ) ;
#11906=CARTESIAN_POINT ( 'NONE',  ( 2.261269890823179640, 5.762737836064523833, 5.017604628139654466 ) ) ;
#11908=ORIENTED_EDGE ( 'NONE', *, *, #21422, .T. ) ;
#11914=CARTESIAN_POINT ( 'NONE',  ( 0.3675815128205912052, 8.093875121226199454, -9.235491948679927177 ) ) ;
#11923=AXIS2_PLACEMENT_3D ( 'NONE', #3283, #47841, #58151 ) ;
#11926=EDGE_CURVE ( 'NONE', #61427, #28685, #41575, .T. ) ;
#11928=VERTEX_POINT ( 'NONE', #12639 ) ;
#11931=CARTESIAN_POINT ( 'NONE',  ( 2.241352910868909643, -7.145045428366594287, 2.689314586382326677 ) ) ;
#11943=CARTESIAN_POINT ( 'NONE',  ( 2.297017764050233612, 3.682881532880140529, -6.708511771223914621 ) ) ;
#11948=VECTOR ( 'NONE', #15003, 1000.000000000000114 ) ;
#11952=CARTESIAN_POINT ( 'NONE',  ( 2.899286259009683953, -7.250549018622921338, -3.018334250363155835 ) ) ;
#11962=CARTESIAN_POINT ( 'NONE',  ( 1.719304012339819332, -8.755325027794356174, 9.242227816401850760 ) ) ;
#11969=ORIENTED_EDGE ( 'NONE', *, *, #16528, .F. ) ;
#11970=UNCERTAINTY_MEASURE_WITH_UNIT (LENGTH_MEASURE( 1.000000000000000082E-05 ), #60747, 'distance_accuracy_value', 'NONE');
#11971=CARTESIAN_POINT ( 'NONE',  ( 0.2655924914740778187, 7.838010948425048419, 9.409507842006050282 ) ) ;
#11972=CARTESIAN_POINT ( 'NONE',  ( 0.5572780756287527559, -5.905274004878251937, -10.83930267798922564 ) ) ;
#11986=EDGE_LOOP ( 'NONE', ( #1417, #7354, #23623, #35565 ) ) ;
#11988=CARTESIAN_POINT ( 'NONE',  ( 2.507146904658100972, 7.719969556433170510, 0.2163149345876847485 ) ) ;
#11996=CARTESIAN_POINT ( 'NONE',  ( 0.2653519789438771315, 11.50012635727061117, -4.209148152332801374 ) ) ;
#12002=EDGE_CURVE ( 'NONE', #22893, #3903, #24991, .T. ) ;
#12003=EDGE_LOOP ( 'NONE', ( #37948, #42584, #31771, #14442 ) ) ;
#12016=DIRECTION ( 'NONE',  ( 0.000000000000000000, 0.000000000000000000, 1.000000000000000000 ) ) ;
#12022=CARTESIAN_POINT ( 'NONE',  ( 3.031336079629604718, 7.553623348802402049, 2.306006909710363040 ) ) ;
#12027=EDGE_LOOP ( 'NONE', ( #9600, #15000, #40646, #4014 ) ) ;
#12028=CARTESIAN_POINT ( 'NONE',  ( 2.368238019615387824, -6.736275681109187730, -3.681632831800456973 ) ) ;
#12030=( BOUNDED_SURFACE ( )  B_SPLINE_SURFACE ( 3, 1, ( 
 ( #32141, #37132 ),
 ( #51489, #606 ),
 ( #51798, #16855 ),
 ( #20866, #41134 ) ),
 .UNSPECIFIED., .F., .F., .F. ) 
 B_SPLINE_SURFACE_WITH_KNOTS ( ( 4, 4 ),
 ( 2, 2 ),
 ( 0.000000000000000000, 1.000000000000000000 ),
 ( 0.000000000000000000, 1.000000000000000000 ),
 .UNSPECIFIED. ) 
 GEOMETRIC_REPRESENTATION_ITEM ( )  RATIONAL_B_SPLINE_SURFACE ( (
 ( 1.000000000000000000, 1.000000000000000000),
 ( 0.9942764183789327692, 0.8450855930916585379),
 ( 0.9942764183789327692, 0.8450855930916585379),
 ( 1.000000000000000000, 1.000000000000000000) ) ) 
 REPRESENTATION_ITEM ( '' )  SURFACE ( )  );
#12034=EDGE_CURVE ( 'NONE', #59522, #44220, #54556, .T. ) ;
#12036=CARTESIAN_POINT ( 'NONE',  ( 0.9232058338315058954, 0.3773051331667984232, 12.46548196349786330 ) ) ;
#12040=FACE_OUTER_BOUND ( 'NONE', #53072, .T. ) ;
#12046=CARTESIAN_POINT ( 'NONE',  ( 1.948354844646953188, -3.407825014329060043, 11.46941405766422051 ) ) ;
#12049=CARTESIAN_POINT ( 'NONE',  ( 2.305787727787084407, -5.756228004061490822, 5.047606869483037606 ) ) ;
#12053=EDGE_LOOP ( 'NONE', ( #38949, #11624, #4817, #27281 ) ) ;
#12070=CARTESIAN_POINT ( 'NONE',  ( 1.109979610371582215, -11.59954799439117679, -4.732439402374714277 ) ) ;
#12074=CARTESIAN_POINT ( 'NONE',  ( 0.2648978790185602672, -7.769924372105269761, 9.465406350830582127 ) ) ;
#12076=CARTESIAN_POINT ( 'NONE',  ( 2.653899356900501161, -7.767552767344323428, 0.2611590963048452396 ) ) ;
#12083=CARTESIAN_POINT ( 'NONE',  ( 2.665405856346779512, 4.274976649834481002, 8.559192023451563713 ) ) ;
#12086=CARTESIAN_POINT ( 'NONE',  ( 0.2676618633000485414, 9.484212776852446680, -7.748413788583108364 ) ) ;
#12087=CARTESIAN_POINT ( 'NONE',  ( 2.241509619876137283, -4.877966158328267632, -5.872890204493071309 ) ) ;
#12088=EDGE_CURVE ( 'NONE', #22962, #14666, #3577, .T. ) ;
#12090=CARTESIAN_POINT ( 'NONE',  ( 0.4626703367443957271, -4.475905684073789637, 11.46957824750455934 ) ) ;
#12093=CARTESIAN_POINT ( 'NONE',  ( 3.152665057735899001, -7.886634106564667235, -0.9030954876721221103 ) ) ;
#12097=CARTESIAN_POINT ( 'NONE',  ( 2.931247277082681180, 7.672001188570258812, 1.728824746592295902 ) ) ;
#12100=ORIENTED_EDGE ( 'NONE', *, *, #63412, .F. ) ;
#12102=CARTESIAN_POINT ( 'NONE',  ( 5.515539859299206427, -0.002856745161749602371, -0.005336559634876431209 ) ) ;
#12103=CARTESIAN_POINT ( 'NONE',  ( 2.350038591457964454, -8.861946706686103070, -5.855794476068694188 ) ) ;
#12105=B_SPLINE_CURVE_WITH_KNOTS ( 'NONE', 3,
 ( #4387, #4049, #60889, #34927, #15641, #60225, #25634, #55578, #14644, #4729, #20658, #50270, #40257, #44931, #29964, #45582, #61214, #39614, #44582 ),
 .UNSPECIFIED., .F., .F.,
 ( 4, 3, 3, 3, 3, 3, 4 ),
 ( 5.502793334042459344E-18, 2.825908398831507014E-05, 4.208813692484323650E-05, 5.591713746944412626E-05, 6.279584083232467632E-05, 9.105792820297537013E-05, 0.0001153131102488882644 ),
 .UNSPECIFIED. ) ;
#12106=CARTESIAN_POINT ( 'NONE',  ( 0.2638984909335720941, -6.295352574288911818, -10.50550771760526381 ) ) ;
#12118=AXIS2_PLACEMENT_3D ( 'NONE', #21352, #6733, #27008 ) ;
#12122=B_SPLINE_CURVE_WITH_KNOTS ( 'NONE', 3,
 ( #18980, #24954, #23646, #59879, #8341, #64829, #18338, #38603, #19309, #39242, #14610, #59539, #14300 ),
 .UNSPECIFIED., .F., .F.,
 ( 4, 3, 3, 3, 4 ),
 ( 3.127317220692750759E-18, 6.607593386745478183E-05, 0.0001321518677373528946, 0.0001982171734706228655, 0.0002642860854759485002 ),
 .UNSPECIFIED. ) ;
#12134=VERTEX_POINT ( 'NONE', #328 ) ;
#12137=CARTESIAN_POINT ( 'NONE',  ( 0.2759803524722238000, 9.260954523383741588, 8.018167820447541061 ) ) ;
#12141=CARTESIAN_POINT ( 'NONE',  ( 1.948354844646903672, -8.685970062895167487, 8.228891433297592428 ) ) ;
#12144=CARTESIAN_POINT ( 'NONE',  ( 0.2650492433740058718, -12.24562113162319399, 0.1101179680248548648 ) ) ;
#12146=DIRECTION ( 'NONE',  ( -0.3939253465568944290, 0.4511294145502875996, -0.8008152550167518813 ) ) ;
#12151=CARTESIAN_POINT ( 'NONE',  ( 0.3401186441510218872, -9.562489599411579277, 7.690203051555989155 ) ) ;
#12157=CARTESIAN_POINT ( 'NONE',  ( 1.104777566491147667, 11.92547689818822576, 3.832109395972688848 ) ) ;
#12160=CARTESIAN_POINT ( 'NONE',  ( 1.634816307077735287, 5.013416918609651773, -11.67158647524072990 ) ) ;
#12162=ORIENTED_EDGE ( 'NONE', *, *, #52488, .F. ) ;
#12168=B_SPLINE_CURVE_WITH_KNOTS ( 'NONE', 3,
 ( #53858, #60141, #14561, #39193, #64462, #59823, #14256, #54835, #8300, #8618, #24563, #34839, #55145, #29868, #43525, #54177 ),
 .UNSPECIFIED., .F., .F.,
 ( 4, 3, 3, 3, 3, 4 ),
 ( 0.000000000000000000, 0.0003017745587525263854, 0.0006035491769808769931, 0.0009053241094668204765, 0.001207275924539398439, 0.001510325902531783112 ),
 .UNSPECIFIED. ) ;
#12172=CARTESIAN_POINT ( 'NONE',  ( 5.515539859299206427, -0.005336559634876458097, 0.002856745161749549462 ) ) ;
#12174=ORIENTED_EDGE ( 'NONE', *, *, #31265, .F. ) ;
#12176=CARTESIAN_POINT ( 'NONE',  ( 2.941278708680199916, 6.138172921908581436, 0.1348063076487163725 ) ) ;
#12183=B_SPLINE_CURVE_WITH_KNOTS ( 'NONE', 3,
 ( #51345, #6111, #1455, #41987, #27037, #11401, #36350, #61291, #22037, #56657, #31365, #26370, #5795, #15722, #472, #41324 ),
 .UNSPECIFIED., .F., .F.,
 ( 4, 3, 3, 3, 3, 4 ),
 ( 0.000000000000000000, 0.0002999043160757237339, 0.0005998071753050776903, 0.0008997092107374217093, 0.001204458948194628547, 0.001510329163474499270 ),
 .UNSPECIFIED. ) ;
#12185=CARTESIAN_POINT ( 'NONE',  ( 2.440552418640496768, -7.615619946579181843, 1.142369876085300273 ) ) ;
#12186=CARTESIAN_POINT ( 'NONE',  ( 2.241352910868908754, 7.503490710578232914, 1.407733736974891681 ) ) ;
#12194=CARTESIAN_POINT ( 'NONE',  ( 2.261269890822073858, -3.940687015735691467, 6.546486799463097306 ) ) ;
#12202=CARTESIAN_POINT ( 'NONE',  ( 0.2801149460245155876, 7.723514566794102087, -9.509848747524097590 ) ) ;
#12204=CARTESIAN_POINT ( 'NONE',  ( 0.4613984246114878340, -9.610550265395797709, -7.694922453052239320 ) ) ;
#12205=CARTESIAN_POINT ( 'NONE',  ( 3.152665057735933640, -5.461013642407022139, -5.761241965768077122 ) ) ;
#12213=CARTESIAN_POINT ( 'NONE',  ( 0.2869720083484346707, 6.306330337780659434, -10.50600528807140321 ) ) ;
#12224=CARTESIAN_POINT ( 'NONE',  ( 0.2646305136544072623, 12.24595685781654630, 0.1321451301298244563 ) ) ;
#12227=CARTESIAN_POINT ( 'NONE',  ( 0.2648978790185619880, -11.46165506714231341, 4.312320170909196726 ) ) ;
#12237=CARTESIAN_POINT ( 'NONE',  ( 2.241451721903216843, 0.06083185034806753988, -7.634225434981126490 ) ) ;
#12239=EDGE_CURVE ( 'NONE', #42211, #11101, #11427, .T. ) ;
#12240=CARTESIAN_POINT ( 'NONE',  ( 2.241311220309654129, 5.788190037953024003, 4.978033760028732324 ) ) ;
#12241=PLANE ( 'NONE',  #5341 ) ;
#12242=ORIENTED_EDGE ( 'NONE', *, *, #38292, .F. ) ;
#12259=CARTESIAN_POINT ( 'NONE',  ( 2.242418902651940993, 3.903399295463838126, 6.561482094363259243 ) ) ;
#12260=ORIENTED_EDGE ( 'NONE', *, *, #37692, .F. ) ;
#12269=ORIENTED_EDGE ( 'NONE', *, *, #49502, .T. ) ;
#12271=CARTESIAN_POINT ( 'NONE',  ( 3.152665057734086229, 4.725420687650732532, 6.378477742800449768 ) ) ;
#12272=CARTESIAN_POINT ( 'NONE',  ( 0.2655924914740778742, 0.04405032194303384191, 12.24627751708824341 ) ) ;
#12273=CARTESIAN_POINT ( 'NONE',  ( 0.3675815128205912052, -2.391755495700685241, 12.04510820461658582 ) ) ;
#12275=CARTESIAN_POINT ( 'NONE',  ( 0.2834382757448011270, -11.58108645293228633, -3.999440312567330569 ) ) ;
#12281=CARTESIAN_POINT ( 'NONE',  ( 2.298277635560276089, 5.967558917212202552, -4.791911337974113394 ) ) ;
#12288=DIRECTION ( 'NONE',  ( 0.000000000000000000, 8.881784197001252323E-16, 1.000000000000000000 ) ) ;
#12292=ADVANCED_FACE ( 'NONE', ( #52519 ), #11454, .F. ) ;
#12296=CARTESIAN_POINT ( 'NONE',  ( 1.719304012338701115, -5.690355757827699534, 11.38834240361771677 ) ) ;
#12298=CARTESIAN_POINT ( 'NONE',  ( 2.263328370261528111, -3.943189046766291117, -6.545781832005235223 ) ) ;
#12301=CARTESIAN_POINT ( 'NONE',  ( 2.276905613633651626, -6.543460433228672990, 3.955794200962185592 ) ) ;
#12302=CARTESIAN_POINT ( 'NONE',  ( 2.305787727787084407, -3.682701754025465846, -6.711944854845862451 ) ) ;
#12304=CARTESIAN_POINT ( 'NONE',  ( 1.372161826076364388, -7.648244077827067500, 10.03232826862070759 ) ) ;
#12306=CARTESIAN_POINT ( 'NONE',  ( 2.305787727787083519, -6.711944854845849129, 3.682701754025489826 ) ) ;
#12309=B_SPLINE_CURVE_WITH_KNOTS ( 'NONE', 3,
 ( #47011, #1466, #62276, #32013, #52334, #58293, #43304, #43635, #57975, #63579, #3103, #28037, #63920, #53307, #2787, #43977, #12384, #27684, #19621 ),
 .UNSPECIFIED., .F., .F.,
 ( 4, 3, 3, 3, 3, 3, 4 ),
 ( 5.311484201212962216E-18, 2.825908398831288479E-05, 4.208813692483985515E-05, 5.591713746943959972E-05, 6.279584083232024464E-05, 9.105792820296832281E-05, 0.0001153131102488849034 ),
 .UNSPECIFIED. ) ;
#12314=CARTESIAN_POINT ( 'NONE',  ( 1.719304012338199517, 0.000000000000000000, 0.000000000000000000 ) ) ;
#12315=ORIENTED_EDGE ( 'NONE', *, *, #27047, .T. ) ;
#12319=CARTESIAN_POINT ( 'NONE',  ( 2.298277635560283194, -7.564013289873168233, 1.166137492762201022 ) ) ;
#12323=B_SPLINE_CURVE_WITH_KNOTS ( 'NONE', 3,
 ( #56746, #41747, #31445, #6190, #26451, #46735, #21476, #42062, #62041, #57377, #16491, #16799, #36760, #32085, #57056, #52402 ),
 .UNSPECIFIED., .F., .F.,
 ( 4, 3, 3, 3, 3, 4 ),
 ( 3.270724739007979762E-15, 0.0002126834539179725146, 0.0004253519300366287925, 0.0006380165497224213767, 0.0007442707582428297443, 0.0009453531351416891940 ),
 .UNSPECIFIED. ) ;
#12324=CARTESIAN_POINT ( 'NONE',  ( 2.241352910868908310, -2.689314586382304917, -7.145045428366603169 ) ) ;
#12325=CARTESIAN_POINT ( 'NONE',  ( 2.245754705088788938, 7.136529175883056908, 2.715960966013291067 ) ) ;
#12326=EDGE_LOOP ( 'NONE', ( #19273, #19333, #51960, #17542 ) ) ;
#12329=CARTESIAN_POINT ( 'NONE',  ( 2.241352910868908754, 2.532612177304442991, 7.202080440908749992 ) ) ;
#12333=CARTESIAN_POINT ( 'NONE',  ( 1.719304012341584365, 10.22720798541559439, -7.581471372738991299 ) ) ;
#12338=CARTESIAN_POINT ( 'NONE',  ( 1.198791140420808699, 6.720248575444026429, -10.60778679489420284 ) ) ;
#12344=CARTESIAN_POINT ( 'NONE',  ( 2.241317068080787678, 6.656851426546641193, 3.737686401541526315 ) ) ;
#12348=CARTESIAN_POINT ( 'NONE',  ( 2.969415267404084791, -7.680649281077092105, 1.748187016698054652 ) ) ;
#12352=CARTESIAN_POINT ( 'NONE',  ( 3.152665057736261822, -7.102135024647099115, -3.546019893114602972 ) ) ;
#12358=ORIENTED_EDGE ( 'NONE', *, *, #13420, .F. ) ;
#12362=CARTESIAN_POINT ( 'NONE',  ( 2.963017218115624019, -7.679262289252030804, -1.744728040076983788 ) ) ;
#12368=CARTESIAN_POINT ( 'NONE',  ( 2.273267844204863053, -5.758000272829339572, 5.029122824445697582 ) ) ;
#12369=CARTESIAN_POINT ( 'NONE',  ( 2.931247277082693614, 5.333206743525327198, -5.779735553870047227 ) ) ;
#12371=CARTESIAN_POINT ( 'NONE',  ( 2.241352910868908310, -4.970878533273800137, 5.794346703933830334 ) ) ;
#12378=CARTESIAN_POINT ( 'NONE',  ( 2.241451721903215066, 4.953785420083490543, -5.809054012306810399 ) ) ;
#12384=CARTESIAN_POINT ( 'NONE',  ( 2.242418902651940549, -7.139616612143407259, 2.704708480794779657 ) ) ;
#12392=CARTESIAN_POINT ( 'NONE',  ( 2.889800649504073782, 1.129261637821690423, -6.016320774579795305 ) ) ;
#12395=ORIENTED_EDGE ( 'NONE', *, *, #62981, .F. ) ;
#12405=EDGE_LOOP ( 'NONE', ( #31234, #7099, #38833, #12162 ) ) ;
#12413=CARTESIAN_POINT ( 'NONE',  ( 0.2648321136542672871, 12.03456865502706208, 2.265911310221853991 ) ) ;
#12414=VERTEX_POINT ( 'NONE', #19205 ) ;
#12418=CARTESIAN_POINT ( 'NONE',  ( 2.241526690369558761, -7.179945570618739836, -2.594870554108910543 ) ) ;
#12419=CARTESIAN_POINT ( 'NONE',  ( 0.3675815128205912052, -12.13672785388549080, -1.872154644482208585 ) ) ;
#12429=B_SPLINE_CURVE_WITH_KNOTS ( 'NONE', 3,
 ( #48933, #9006, #47938, #42939, #7702, #2741, #22999, #58587, #13013, #33295, #53598, #8042, #28306, #48601, #38612, #3388, #58926, #13338, #23657 ),
 .UNSPECIFIED., .F., .F.,
 ( 4, 3, 3, 3, 3, 3, 4 ),
 ( 4.336808689942017736E-19, 2.831840207499681410E-05, 4.217266859840561197E-05, 5.602024318395812120E-05, 6.290810167968882650E-05, 9.120440630945197459E-05, 0.0001153103026479751004 ),
 .UNSPECIFIED. ) ;
#12430=CARTESIAN_POINT ( 'NONE',  ( 2.280717697723841919, -4.794838658391056718, 5.957695241725387447 ) ) ;
#12432=CARTESIAN_POINT ( 'NONE',  ( 2.241352910868908310, 6.569501556381442953, 3.889181972941473386 ) ) ;
#12435=EDGE_CURVE ( 'NONE', #9473, #61317, #36026, .T. ) ;
#12438=FACE_OUTER_BOUND ( 'NONE', #19316, .T. ) ;
#12441=CARTESIAN_POINT ( 'NONE',  ( 3.092491956585992074, -1.813286239165846636, -7.707758057368695681 ) ) ;
#12449=CARTESIAN_POINT ( 'NONE',  ( 2.177405672431146133, 8.129711416440880356, -7.702458780351681078 ) ) ;
#12450=CARTESIAN_POINT ( 'NONE',  ( 0.9232058338315048962, -1.793035206307261875, -12.34162163148535463 ) ) ;
#12451=CARTESIAN_POINT ( 'NONE',  ( 0.3218525148189844698, 9.236582760335979359, 8.069481661595380828 ) ) ;
#12456=ORIENTED_EDGE ( 'NONE', *, *, #19154, .F. ) ;
#12463=CARTESIAN_POINT ( 'NONE',  ( 0.2648978790185584908, -9.465406350830660287, 7.769924372105172949 ) ) ;
#12464=CARTESIAN_POINT ( 'NONE',  ( 1.719304012338199295, 11.67935079956398958, 5.066286238785226992 ) ) ;
#12465=CARTESIAN_POINT ( 'NONE',  ( 2.241352910868909643, 7.532448145350525870, -1.243507963608017075 ) ) ;
#12467=CARTESIAN_POINT ( 'NONE',  ( 2.844750968616139630, 3.626176236708114953, -6.946006365803918392 ) ) ;
#12477=CARTESIAN_POINT ( 'NONE',  ( 1.104777566491146112, -11.59867774809547569, 4.729982681549492085 ) ) ;
#12484=AXIS2_PLACEMENT_3D ( 'NONE', #42422, #2575, #62717 ) ;
#12487=CARTESIAN_POINT ( 'NONE',  ( 1.547277799339151771, -12.12286970032358724, -3.695326562728837416 ) ) ;
#12491=ORIENTED_EDGE ( 'NONE', *, *, #6524, .F. ) ;
#12494=CARTESIAN_POINT ( 'NONE',  ( 5.514970785353741078, -0.004233694591582968896, -0.002093325033903797351 ) ) ;
#12496=CARTESIAN_POINT ( 'NONE',  ( 1.937114397841935398, 3.531416430611461266, -12.33981801388254240 ) ) ;
#12501=ORIENTED_EDGE ( 'NONE', *, *, #59275, .T. ) ;
#12504=CARTESIAN_POINT ( 'NONE',  ( 0.2652384529303130623, -6.065769141714278945, 10.63836770010964194 ) ) ;
#12506=CARTESIAN_POINT ( 'NONE',  ( 2.305787727787085295, -3.971363876084009537, 6.545285700970515208 ) ) ;
#12508=ORIENTED_EDGE ( 'NONE', *, *, #18758, .F. ) ;
#12518=CARTESIAN_POINT ( 'NONE',  ( 0.2650492594609250019, -6.027447650185294492, -10.66007682546623592 ) ) ;
#12523=CARTESIAN_POINT ( 'NONE',  ( 0.3053067050349157485, 6.328522421120416297, -10.49978800868453988 ) ) ;
#12524=DIRECTION ( 'NONE',  ( 0.000000000000000000, 0.000000000000000000, 1.000000000000000000 ) ) ;
#12526=ORIENTED_EDGE ( 'NONE', *, *, #42048, .F. ) ;
#12534=CARTESIAN_POINT ( 'NONE',  ( 2.177405672431842465, -10.89176600224772606, 2.605669267166142333 ) ) ;
#12537=CARTESIAN_POINT ( 'NONE',  ( 0.2648978790185619880, -1.996248716311710414, 12.08224454301447892 ) ) ;
#12547=CARTESIAN_POINT ( 'NONE',  ( 1.194176325881345813, 3.807610977967081922, -11.96454551582839798 ) ) ;
#12548=CARTESIAN_POINT ( 'NONE',  ( 3.152665057736163678, 7.923639299009212600, -0.4801242025614006481 ) ) ;
#12549=CARTESIAN_POINT ( 'NONE',  ( 2.262775599887398403, 5.761998514038564778, 5.019217486252278704 ) ) ;
#12563=CARTESIAN_POINT ( 'NONE',  ( 2.963017218115626239, -1.744728040076958919, 7.679262289252037910 ) ) ;
#12564=ORIENTED_EDGE ( 'NONE', *, *, #35444, .F. ) ;
#12576=DIRECTION ( 'NONE',  ( 0.000000000000000000, 0.000000000000000000, 1.000000000000000000 ) ) ;
#12577=CARTESIAN_POINT ( 'NONE',  ( 5.514970785353741078, 0.003262412238248711249, 0.003415090918276149964 ) ) ;
#12578=CARTESIAN_POINT ( 'NONE',  ( 0.2647959493198558945, 11.55693259385006222, 4.049980114636408501 ) ) ;
#12582=CARTESIAN_POINT ( 'NONE',  ( 3.152665057734040488, 0.000000000000000000, 0.000000000000000000 ) ) ;
#12589=CARTESIAN_POINT ( 'NONE',  ( 5.514970785353741078, -0.002796696073589895887, -0.003805873180274304147 ) ) ;
#12591=CARTESIAN_POINT ( 'NONE',  ( 0.3675815128205894289, -11.62724744438063063, -3.951233083390586209 ) ) ;
#12592=CARTESIAN_POINT ( 'NONE',  ( 2.177405672431937500, -11.17876532285415792, 0.6747479782258832826 ) ) ;
#12595=CARTESIAN_POINT ( 'NONE',  ( 2.507146904658097419, -7.180414359940930247, -2.843654641958959672 ) ) ;
#12596=( BOUNDED_SURFACE ( )  B_SPLINE_SURFACE ( 3, 1, ( 
 ( #28384, #29051 ),
 ( #48680, #49360 ),
 ( #3138, #3806 ),
 ( #59636, #24369 ) ),
 .UNSPECIFIED., .F., .F., .F. ) 
 B_SPLINE_SURFACE_WITH_KNOTS ( ( 4, 4 ),
 ( 2, 2 ),
 ( 0.000000000000000000, 1.000000000000000000 ),
 ( 0.000000000000000000, 1.000000000000000000 ),
 .UNSPECIFIED. ) 
 GEOMETRIC_REPRESENTATION_ITEM ( )  RATIONAL_B_SPLINE_SURFACE ( (
 ( 1.000000000000000000, 1.000000000000000000),
 ( 0.9856612449720755231, 0.9999558406602322425),
 ( 0.9856612449720755231, 0.9999558406602322425),
 ( 1.000000000000000000, 1.000000000000000000) ) ) 
 REPRESENTATION_ITEM ( '' )  SURFACE ( )  );
#12602=CARTESIAN_POINT ( 'NONE',  ( 2.589278595512544356, 7.670769623692099692, 1.107986312493582925 ) ) ;
#12606=CARTESIAN_POINT ( 'NONE',  ( 2.297017764050091504, -3.682881532880131648, 6.708511771223863995 ) ) ;
#12611=B_SPLINE_CURVE_WITH_KNOTS ( 'NONE', 3,
 ( #38927, #3038, #63848, #60842, #45221, #50551, #61170 ),
 .UNSPECIFIED., .F., .F.,
 ( 4, 3, 4 ),
 ( 6.914360523903184076E-15, 0.002398160485434806810, 0.005002426799384151676 ),
 .UNSPECIFIED. ) ;
#12615=CARTESIAN_POINT ( 'NONE',  ( 2.655192694322927593, -4.290256727313598972, 8.589732161582016801 ) ) ;
#12623=CARTESIAN_POINT ( 'NONE',  ( 2.260457164927188511, -6.546788723198579518, 3.939659644572524488 ) ) ;
#12624=LINE ( 'NONE', #58889, #41724 ) ;
#12636=CARTESIAN_POINT ( 'NONE',  ( 3.152665057734040488, 0.000000000000000000, 0.000000000000000000 ) ) ;
#12639=CARTESIAN_POINT ( 'NONE',  ( 2.305787727787084407, 0.1666591538753756929, -7.654065630109506024 ) ) ;
#12648=CARTESIAN_POINT ( 'NONE',  ( 2.290907136833256530, 3.684064771923258874, 6.705538900522838297 ) ) ;
#12651=AXIS2_PLACEMENT_3D ( 'NONE', #53411, #2878, #54396 ) ;
#12665=ORIENTED_EDGE ( 'NONE', *, *, #43745, .F. ) ;
#12667=CARTESIAN_POINT ( 'NONE',  ( 0.2767916011545393240, 6.288637995698108440, 10.51265105824864676 ) ) ;
#12669=CARTESIAN_POINT ( 'NONE',  ( 0.2653141334712555421, -9.409392642815692653, -7.837911425448877090 ) ) ;
#12676=ADVANCED_FACE ( 'NONE', ( #56081 ), #28941, .F. ) ;
#12677=CARTESIAN_POINT ( 'NONE',  ( 2.305787727787083519, -2.774453000917197265, 7.135468203929974607 ) ) ;
#12678=CARTESIAN_POINT ( 'NONE',  ( 0.2646305136544072623, -9.465888453932908675, -7.770320294339273737 ) ) ;
#12683=CARTESIAN_POINT ( 'NONE',  ( 0.3675815128205894289, -4.447030445008105737, -11.44679196252413789 ) ) ;
#12687=B_SPLINE_CURVE_WITH_KNOTS ( 'NONE', 3,
 ( #315, #15261, #65460, #10588, #14906, #35541, #20900, #39878, #55507, #30867, #60158, #61149, #10265, #20594, #5295, #25565 ),
 .UNSPECIFIED., .F., .F.,
 ( 4, 3, 3, 3, 3, 4 ),
 ( 7.589415207398531038E-19, 0.0003017745587525230244, 0.0006035491769808683194, 0.0009053241094668093092, 0.001207275924541010865, 0.001510325902535037453 ),
 .UNSPECIFIED. ) ;
#12693=CARTESIAN_POINT ( 'NONE',  ( 2.835339799623992629, 5.281994181469073624, -5.783398714696503795 ) ) ;
#12702=CARTESIAN_POINT ( 'NONE',  ( 2.241352910868909643, -7.532448145350499225, -1.243507963608171174 ) ) ;
#12704=CARTESIAN_POINT ( 'NONE',  ( 2.241352910868908310, 4.970878533273838329, -5.794346703933798359 ) ) ;
#12711=CARTESIAN_POINT ( 'NONE',  ( 0.3278977287071234148, -12.03512402322222208, -2.374069413450269561 ) ) ;
#12716=CARTESIAN_POINT ( 'NONE',  ( 2.990245332647783805, 8.465748356454174228, 0.5125330575219991802 ) ) ;
#12719=CARTESIAN_POINT ( 'NONE',  ( 5.514970785353741078, 0.004588761610584827719, 0.001117786416802128355 ) ) ;
#12723=CARTESIAN_POINT ( 'NONE',  ( 0.9232058338315048962, -6.559496812049736114, 10.60677148422242411 ) ) ;
#12728=CARTESIAN_POINT ( 'NONE',  ( 0.2767916011545407673, -6.288637995698039163, -10.51265105824868762 ) ) ;
#12733=CARTESIAN_POINT ( 'NONE',  ( 0.2717059086739025964, 4.023283916512583325, -11.56868249951477701 ) ) ;
#12734=CARTESIAN_POINT ( 'NONE',  ( 0.3665391374699467075, 8.095513416941352958, -9.237363111276685856 ) ) ;
#12737=ADVANCED_FACE ( 'NONE', ( #3125 ), #35716, .F. ) ;
#12738=CARTESIAN_POINT ( 'NONE',  ( 2.941278708680199916, 6.138172921908580548, -0.1348063076487160949 ) ) ;
#12749=CARTESIAN_POINT ( 'NONE',  ( 0.2915757698887260219, -10.50410115670273647, 6.312478057070419091 ) ) ;
#12751=CARTESIAN_POINT ( 'NONE',  ( 2.241526690369556984, -7.521460607153588995, -1.308664175663846185 ) ) ;
#12757=DIRECTION ( 'NONE',  ( 0.000000000000000000, 0.000000000000000000, 1.000000000000000000 ) ) ;
#12758=EDGE_CURVE ( 'NONE', #63698, #7920, #22374, .T. ) ;
#12763=ADVANCED_FACE ( 'NONE', ( #58660 ), #19155, .T. ) ;
#12767=CARTESIAN_POINT ( 'NONE',  ( 0.3665391374699465965, 12.04754782681760794, -2.392238720110335226 ) ) ;
#12770=CARTESIAN_POINT ( 'NONE',  ( 0.2833330754217402991, -1.928200609300391610, -12.09951353627562298 ) ) ;
#12771=CARTESIAN_POINT ( 'NONE',  ( 0.9232058338315058954, -8.301689855530105078, -9.306586124266681637 ) ) ;
#12775=CARTESIAN_POINT ( 'NONE',  ( 0.9232058338315058954, -6.559496812049588677, -10.60677148422251115 ) ) ;
#12780=CARTESIAN_POINT ( 'NONE',  ( 1.194176325881340928, -12.44396189284383780, -1.672143286119688321 ) ) ;
#12782=CARTESIAN_POINT ( 'NONE',  ( 0.3341166715381307939, 2.378838837789095439, 12.03629799686216195 ) ) ;
#12791=ADVANCED_FACE ( 'NONE', ( #19392 ), #13581, .F. ) ;
#12797=CARTESIAN_POINT ( 'NONE',  ( 5.516018279890452902, -0.0009545156522407517155, -0.006707902355169297580 ) ) ;
#12799=CARTESIAN_POINT ( 'NONE',  ( 2.288423627607478306, -7.560204962263194162, -1.169285315515855350 ) ) ;
#12802=CARTESIAN_POINT ( 'NONE',  ( 0.3537226245948378867, 5.910416419900530904, 10.75912040401511049 ) ) ;
#12804=EDGE_LOOP ( 'NONE', ( #53739, #1649, #22283, #17798 ) ) ;
#12806=ORIENTED_EDGE ( 'NONE', *, *, #41718, .T. ) ;
#12819=ORIENTED_EDGE ( 'NONE', *, *, #31019, .F. ) ;
#12823=CARTESIAN_POINT ( 'NONE',  ( 0.8320506296491579912, -11.81055997318801332, -3.891425424503422992 ) ) ;
#12827=FACE_OUTER_BOUND ( 'NONE', #14588, .T. ) ;
#12844=DIRECTION ( 'NONE',  ( -1.000000000000000000, -0.000000000000000000, -0.000000000000000000 ) ) ;
#12846=CARTESIAN_POINT ( 'NONE',  ( 0.2648978790185602672, -7.769924372105269761, 9.465406350830582127 ) ) ;
#12848=AXIS2_PLACEMENT_3D ( 'NONE', #59331, #29083, #39700 ) ;
#12851=CARTESIAN_POINT ( 'NONE',  ( 0.2646305136544072623, 11.46223899740600238, 4.312539723326168861 ) ) ;
#12854=VECTOR ( 'NONE', #22155, 999.9999999999998863 ) ;
#12855=CARTESIAN_POINT ( 'NONE',  ( 0.3632410797595260199, 7.689504457927780479, -9.572936598843549305 ) ) ;
#12858=CARTESIAN_POINT ( 'NONE',  ( 2.269879328256730666, 1.473193649116136372, 7.500604381673465326 ) ) ;
#12860=ORIENTED_EDGE ( 'NONE', *, *, #264, .F. ) ;
#12867=CARTESIAN_POINT ( 'NONE',  ( 2.241317068080782793, -0.09149433816010646425, -7.633845645378813494 ) ) ;
#12870=CARTESIAN_POINT ( 'NONE',  ( 3.152665057734040488, 0.000000000000000000, 0.000000000000000000 ) ) ;
#12878=CARTESIAN_POINT ( 'NONE',  ( 0.9296196016833688791, -8.327938962579976234, 9.278306863859505427 ) ) ;
#12882=CARTESIAN_POINT ( 'NONE',  ( 0.2958664285830422402, -11.43993536884559425, 4.398464391600280798 ) ) ;
#12885=VERTEX_POINT ( 'NONE', #24697 ) ;
#12888=CARTESIAN_POINT ( 'NONE',  ( 0.3665391374699464300, 10.76665847464320969, -5.911453292029489326 ) ) ;
#12889=CARTESIAN_POINT ( 'NONE',  ( 2.440552418640498100, 7.301551120181799526, -2.447453236303752888 ) ) ;
#12890=CARTESIAN_POINT ( 'NONE',  ( 2.350038591458110560, -8.533611140765442471, 6.324706260079973497 ) ) ;
#12891=CARTESIAN_POINT ( 'NONE',  ( 2.241532322987418002, 0.01048837931145292675, -7.634455956583347636 ) ) ;
#12893=CARTESIAN_POINT ( 'NONE',  ( 5.515539859299206427, 0.004759416711441679694, -0.003740028639278299410 ) ) ;
#12898=VERTEX_POINT ( 'NONE', #24049 ) ;
#12901=B_SPLINE_CURVE_WITH_KNOTS ( 'NONE', 3,
 ( #58686, #53686, #18764, #54675, #14399, #45004, #33706 ),
 .UNSPECIFIED., .F., .F.,
 ( 4, 3, 4 ),
 ( 0.000000000000000000, 0.001700533616330578320, 0.005002426799374390387 ),
 .UNSPECIFIED. ) ;
#12909=CARTESIAN_POINT ( 'NONE',  ( 2.899286259009683953, 1.713434346771327776, -7.664525129300146844 ) ) ;
#12912=VERTEX_POINT ( 'NONE', #44001 ) ;
#12916=CARTESIAN_POINT ( 'NONE',  ( 2.260457164927186291, 3.939659644572543584, 6.546788723198565307 ) ) ;
#12917=VERTEX_POINT ( 'NONE', #49347 ) ;
#12925=DIRECTION ( 'NONE',  ( -1.000000000000000000, -0.000000000000000000, -0.000000000000000000 ) ) ;
#12928=LINE ( 'NONE', #8267, #44962 ) ;
#12931=CARTESIAN_POINT ( 'NONE',  ( 2.639814597422663667, 4.793557287999632877, 6.111633106000409654 ) ) ;
#12937=CARTESIAN_POINT ( 'NONE',  ( 2.844750968616010400, -4.202329849280510565, -6.613363922490621327 ) ) ;
#12942=DIRECTION ( 'NONE',  ( 0.000000000000000000, 0.000000000000000000, 1.000000000000000000 ) ) ;
#12946=CARTESIAN_POINT ( 'NONE',  ( 2.305787727787085295, 5.970480882365287734, -4.792270232040832134 ) ) ;
#12949=CARTESIAN_POINT ( 'NONE',  ( 2.305787727787084407, 7.566723232958072032, 1.164987321564758371 ) ) ;
#12959=B_SPLINE_CURVE_WITH_KNOTS ( 'NONE', 3,
 ( #43617, #52952, #57960, #42970, #37662, #58624, #8069, #48323, #7384, #18384, #27666, #43287, #63247, #17717, #37975, #7739, #28660, #23350, #28024 ),
 .UNSPECIFIED., .F., .F.,
 ( 4, 3, 3, 3, 3, 3, 4 ),
 ( 5.421010862427522170E-20, 2.831840207499432383E-05, 4.217266859840160720E-05, 5.602024318395529550E-05, 6.290810167968680718E-05, 9.120440630944731252E-05, 0.0001153103026479744499 ),
 .UNSPECIFIED. ) ;
#12960=CARTESIAN_POINT ( 'NONE',  ( 2.781367136451806665, -0.3081277311323283308, -7.808329083463450893 ) ) ;
#12966=AXIS2_PLACEMENT_3D ( 'NONE', #55967, #50987, #10735 ) ;
#12969=ORIENTED_EDGE ( 'NONE', *, *, #26792, .T. ) ;
#12980=DIRECTION ( 'NONE',  ( -1.000000000000000000, -0.000000000000000000, -0.000000000000000000 ) ) ;
#12981=CARTESIAN_POINT ( 'NONE',  ( 3.152665057736111720, -7.281573230473792790, 3.161213418915395312 ) ) ;
#12987=CARTESIAN_POINT ( 'NONE',  ( 2.258463476536646919, -7.546439757228810663, 1.192666169132608145 ) ) ;
#12988=VERTEX_POINT ( 'NONE', #36292 ) ;
#12990=CARTESIAN_POINT ( 'NONE',  ( 2.266490820343225465, -2.750080098241469706, -7.130860233521876701 ) ) ;
#12995=EDGE_LOOP ( 'NONE', ( #28920, #51570, #10378, #10457 ) ) ;
#12998=AXIS2_PLACEMENT_3D ( 'NONE', #22645, #27285, #38234 ) ;
#12999=FACE_OUTER_BOUND ( 'NONE', #44801, .T. ) ;
#13006=CARTESIAN_POINT ( 'NONE',  ( 0.4626703367445938464, -0.2831487465613948817, 12.30872794628576550 ) ) ;
#13010=CARTESIAN_POINT ( 'NONE',  ( 0.8320506296491574361, 10.95539209551947479, 5.883188144889816229 ) ) ;
#13011=( BOUNDED_SURFACE ( )  B_SPLINE_SURFACE ( 3, 1, ( 
 ( #61610, #17312 ),
 ( #51006, #58202 ),
 ( #15726, #5799 ),
 ( #11095, #47898 ) ),
 .UNSPECIFIED., .F., .F., .F. ) 
 B_SPLINE_SURFACE_WITH_KNOTS ( ( 4, 4 ),
 ( 2, 2 ),
 ( 0.000000000000000000, 1.000000000000000000 ),
 ( 0.000000000000000000, 1.000000000000000000 ),
 .UNSPECIFIED. ) 
 GEOMETRIC_REPRESENTATION_ITEM ( )  RATIONAL_B_SPLINE_SURFACE ( (
 ( 1.000000000000000000, 1.000000000000000000),
 ( 0.9942764183789327692, 0.8450855930916580938),
 ( 0.9942764183789327692, 0.8450855930916580938),
 ( 1.000000000000000000, 1.000000000000000000) ) ) 
 REPRESENTATION_ITEM ( '' )  SURFACE ( )  );
#13013=CARTESIAN_POINT ( 'NONE',  ( 2.255723233588951437, -2.736592204236698134, 7.132203433012278104 ) ) ;
#13014=CARTESIAN_POINT ( 'NONE',  ( 5.516018279890452902, 0.004525000489649771626, 0.005042957932158598396 ) ) ;
#13019=( GEOMETRIC_REPRESENTATION_CONTEXT ( 3 ) GLOBAL_UNCERTAINTY_ASSIGNED_CONTEXT ( ( #37671 ) ) GLOBAL_UNIT_ASSIGNED_CONTEXT ( ( #18881, #43817, #13858 ) ) REPRESENTATION_CONTEXT ( 'NONE', 'WORKASPACE' ) );
#13029=CARTESIAN_POINT ( 'NONE',  ( 0.2646305136544072623, -9.296005949277173386, -7.972778379581646924 ) ) ;
#13044=EDGE_CURVE ( 'NONE', #56327, #53890, #51939, .T. ) ;
#13049=ADVANCED_FACE ( 'NONE', ( #56598 ), #4278, .F. ) ;
#13051=CARTESIAN_POINT ( 'NONE',  ( 0.3675815128205894289, 9.235491948680119023, -8.093875121225982738 ) ) ;
#13052=ORIENTED_EDGE ( 'NONE', *, *, #3351, .F. ) ;
#13053=CARTESIAN_POINT ( 'NONE',  ( 2.241536586108913820, 4.902521014023406565, -5.852386772940019632 ) ) ;
#13061=VECTOR ( 'NONE', #59507, 1000.000000000000114 ) ;
#13074=CARTESIAN_POINT ( 'NONE',  ( 2.269879328256734219, -1.473193649116087078, -7.500604381673475984 ) ) ;
#13082=CARTESIAN_POINT ( 'NONE',  ( 3.152665057734040488, 0.000000000000000000, 0.000000000000000000 ) ) ;
#13083=DIRECTION ( 'NONE',  ( 0.000000000000000000, 0.000000000000000000, 1.000000000000000000 ) ) ;
#13103=CARTESIAN_POINT ( 'NONE',  ( 1.104777566491143448, -11.07886329447272900, -5.844728374724383002 ) ) ;
#13121=EDGE_CURVE ( 'NONE', #43985, #56943, #9771, .T. ) ;
#13126=CARTESIAN_POINT ( 'NONE',  ( 2.268878695252929845, -4.798796461778220390, -5.949442550447101574 ) ) ;
#13156=ORIENTED_EDGE ( 'NONE', *, *, #64756, .T. ) ;
#13168=CARTESIAN_POINT ( 'NONE',  ( 0.7400311444011711259, -3.907401494355001059, 11.77295732453933041 ) ) ;
#13173=CARTESIAN_POINT ( 'NONE',  ( 2.941278708680199916, 5.248410529370268307, -3.185832147968391759 ) ) ;
#13175=CARTESIAN_POINT ( 'NONE',  ( 2.257661810676419911, -7.499185766072598902, 1.459225434025957835 ) ) ;
#13176=CARTESIAN_POINT ( 'NONE',  ( 0.3401186441510234970, -10.49699112323338213, -6.355596563012414713 ) ) ;
#13177=CARTESIAN_POINT ( 'NONE',  ( 5.516018279890452902, -0.003580555109620837603, -0.005752102158673828673 ) ) ;
#13188=CARTESIAN_POINT ( 'NONE',  ( 2.589278595513707870, 4.794929105510967737, -6.089088204449037534 ) ) ;
#13199=AXIS2_PLACEMENT_3D ( 'NONE', #45322, #15050, #35662 ) ;
#13206=CARTESIAN_POINT ( 'NONE',  ( 0.7400311444011745676, -4.574267895796777061, -11.53023780418230970 ) ) ;
#13210=CARTESIAN_POINT ( 'NONE',  ( 5.530133899448235191, -0.01594518557925637958, 0.001124651387254935967 ) ) ;
#13214=CARTESIAN_POINT ( 'NONE',  ( 0.6511581176963219253, -8.205008037406710031, 9.263557799003001136 ) ) ;
#13219=CARTESIAN_POINT ( 'NONE',  ( 0.3474126878361781801, -11.44231427242452881, 4.439989671676180194 ) ) ;
#13223=CARTESIAN_POINT ( 'NONE',  ( 2.245754705088394587, -7.212684575686793664, 2.506725724682641765 ) ) ;
#13225=CARTESIAN_POINT ( 'NONE',  ( 2.770579946183332254, 7.437949029067727480, -2.384572752174010990 ) ) ;
#13226=CARTESIAN_POINT ( 'NONE',  ( 2.556980015514275006, -4.795979673457624770, 6.074557383033025282 ) ) ;
#13230=CARTESIAN_POINT ( 'NONE',  ( 0.2646305136544065406, 7.770320294339174261, 9.465888453932986835 ) ) ;
#13244=CARTESIAN_POINT ( 'NONE',  ( 0.3610902822527229383, 5.910495176556332275, -10.76187877352507094 ) ) ;
#13246=CARTESIAN_POINT ( 'NONE',  ( 2.305787727787083519, 1.493241775258524084, -7.508843116234142911 ) ) ;
#13250=EDGE_CURVE ( 'NONE', #30538, #9776, #12122, .T. ) ;
#13254=CARTESIAN_POINT ( 'NONE',  ( 0.9232058338315048962, 9.306586124266598148, 8.301689855530199225 ) ) ;
#13267=CARTESIAN_POINT ( 'NONE',  ( 2.990245332647872623, 1.974808303407790344, -8.248134185053331180 ) ) ;
#13274=CARTESIAN_POINT ( 'NONE',  ( 0.3675815128205894289, 5.910255304480445560, 10.76447900494942367 ) ) ;
#13277=CARTESIAN_POINT ( 'NONE',  ( 3.152665057734127529, -7.281573230474269742, -3.161213418913537687 ) ) ;
#13278=EDGE_CURVE ( 'NONE', #19899, #26297, #49892, .T. ) ;
#13280=CARTESIAN_POINT ( 'NONE',  ( 0.3665391374699465965, 8.095513416941230389, 9.237363111276794214 ) ) ;
#13284=CARTESIAN_POINT ( 'NONE',  ( 0.2646305136544065406, -4.312539723326059615, -11.46223899740604324 ) ) ;
#13292=CARTESIAN_POINT ( 'NONE',  ( 2.491965175173673774, -0.2120508241296135687, -7.715025372670731407 ) ) ;
#13293=CARTESIAN_POINT ( 'NONE',  ( 2.589278595512710002, 5.779442428606824222, -5.163950571302039272 ) ) ;
#13313=CARTESIAN_POINT ( 'NONE',  ( 2.941278708680199916, 4.048809123187997905, -4.615461433467216601 ) ) ;
#13315=DIRECTION ( 'NONE',  ( 0.000000000000000000, 0.000000000000000000, 1.000000000000000000 ) ) ;
#13319=CARTESIAN_POINT ( 'NONE',  ( 2.241536586108912044, 6.608496983003842473, -3.822683724643396008 ) ) ;
#13323=ORIENTED_EDGE ( 'NONE', *, *, #65504, .T. ) ;
#13324=LINE ( 'NONE', #59531, #11873 ) ;
#13327=ORIENTED_EDGE ( 'NONE', *, *, #49502, .F. ) ;
#13328=CARTESIAN_POINT ( 'NONE',  ( 0.2653141334712599830, -4.147025708564500590, 11.52266042163704718 ) ) ;
#13337=ORIENTED_EDGE ( 'NONE', *, *, #20413, .T. ) ;
#13338=CARTESIAN_POINT ( 'NONE',  ( 2.298277635560275645, -2.772101951899011762, 7.133696409974386476 ) ) ;
#13340=ORIENTED_EDGE ( 'NONE', *, *, #22497, .T. ) ;
#13342=CARTESIAN_POINT ( 'NONE',  ( 0.2739690278137235091, 6.282352088166262227, 10.51531306167489177 ) ) ;
#13343=CARTESIAN_POINT ( 'NONE',  ( 0.2652384529303120075, -9.423437232855615520, -7.820949643217239178 ) ) ;
#13356=CARTESIAN_POINT ( 'NONE',  ( 2.241352910868908310, -1.407733736974815963, -7.503490710578247125 ) ) ;
#13357=CONICAL_SURFACE ( 'NONE', #30360, 7.938172270156617749, 1.280189991382167047 ) ;
#13370=CARTESIAN_POINT ( 'NONE',  ( 0.3474126878361825654, 1.876013288000214274, -12.12932967384298522 ) ) ;
#13378=B_SPLINE_CURVE_WITH_KNOTS ( 'NONE', 3,
 ( #1943, #62772, #28200, #2628, #22211, #27525, #47820, #42472, #42822, #17891, #63110, #48489, #17239, #22891, #8238, #55088, #18877, #29183, #18574 ),
 .UNSPECIFIED., .F., .F.,
 ( 4, 3, 3, 3, 3, 3, 4 ),
 ( 6.952433221959954168E-18, 2.825908398831159730E-05, 4.208813692483961120E-05, 5.591713746943971492E-05, 6.279584083232174897E-05, 9.105792820297123661E-05, 0.0001153131102488859469 ),
 .UNSPECIFIED. ) ;
#13383=CARTESIAN_POINT ( 'NONE',  ( 2.639814597422734721, 5.782006333156068045, 5.186391178752146836 ) ) ;
#13388=( BOUNDED_SURFACE ( )  B_SPLINE_SURFACE ( 3, 1, ( 
 ( #35802, #10223 ),
 ( #51139, #10887 ),
 ( #40824, #45155 ),
 ( #61103, #5251 ) ),
 .UNSPECIFIED., .F., .F., .F. ) 
 B_SPLINE_SURFACE_WITH_KNOTS ( ( 4, 4 ),
 ( 2, 2 ),
 ( 0.000000000000000000, 1.000000000000000000 ),
 ( 0.000000000000000000, 1.000000000000000000 ),
 .UNSPECIFIED. ) 
 GEOMETRIC_REPRESENTATION_ITEM ( )  RATIONAL_B_SPLINE_SURFACE ( (
 ( 1.000000000000000000, 1.000000000000000000),
 ( 0.6933888150995267674, 0.9895912004443193632),
 ( 0.6933888150995267674, 0.9895912004443193632),
 ( 1.000000000000000000, 1.000000000000000000) ) ) 
 REPRESENTATION_ITEM ( '' )  SURFACE ( )  );
#13393=EDGE_LOOP ( 'NONE', ( #55361, #31866, #6143, #19865 ) ) ;
#13394=DIRECTION ( 'NONE',  ( -1.000000000000000000, -0.000000000000000000, -0.000000000000000000 ) ) ;
#13401=CARTESIAN_POINT ( 'NONE',  ( 5.530133899448235191, 0.01293763278443438476, 0.009387834778845891709 ) ) ;
#13415=CARTESIAN_POINT ( 'NONE',  ( 0.9232058338315058954, -10.98407661738924546, -5.905985151448264858 ) ) ;
#13417=EDGE_CURVE ( 'NONE', #35243, #29318, #46309, .T. ) ;
#13420=EDGE_CURVE ( 'NONE', #54941, #35302, #10294, .T. ) ;
#13423=CARTESIAN_POINT ( 'NONE',  ( 2.255723233588952326, -5.766109278028596741, -5.010912740808180388 ) ) ;
#13426=CARTESIAN_POINT ( 'NONE',  ( 2.242418902651940549, -4.830735119000173938, 5.912154560271213555 ) ) ;
#13428=EDGE_CURVE ( 'NONE', #41836, #17260, #5669, .T. ) ;
#13429=CARTESIAN_POINT ( 'NONE',  ( 2.241537034860906719, -2.606707005150495249, -7.175668896091119464 ) ) ;
#13440=CARTESIAN_POINT ( 'NONE',  ( 5.516018279890452902, 0.006286471671802441874, 0.002527316374434314221 ) ) ;
#13449=CARTESIAN_POINT ( 'NONE',  ( 2.080613030138687147, 9.502643082083353612E-16, 7.580821595991582562 ) ) ;
#13450=B_SPLINE_CURVE_WITH_KNOTS ( 'NONE', 3,
 ( #4750, #55918, #10349, #60568, #65542, #404, #59940 ),
 .UNSPECIFIED., .F., .F.,
 ( 4, 3, 4 ),
 ( 6.950728994019374331E-15, 0.002398160485434793366, 0.005002426799384073614 ),
 .UNSPECIFIED. ) ;
#13451=VECTOR ( 'NONE', #14361, 1000.000000000000114 ) ;
#13453=CARTESIAN_POINT ( 'NONE',  ( 1.020182472822747766, -12.22263240120535954, -2.608319446515142470 ) ) ;
#13456=CARTESIAN_POINT ( 'NONE',  ( 5.516018279890452902, 0.006707902355169300182, -0.0009545156522407284051 ) ) ;
#13463=B_SPLINE_CURVE_WITH_KNOTS ( 'NONE', 3,
 ( #43197, #43520, #63801, #18284, #31902, #52227, #1686, #21952, #16955, #62490, #37221, #27259, #57537, #22262, #42526, #62827, #37574, #54830, #59173 ),
 .UNSPECIFIED., .F., .F.,
 ( 4, 3, 3, 3, 3, 3, 4 ),
 ( 4.336808689942017736E-19, 2.831840207499592302E-05, 4.217266859840494790E-05, 5.602024318395987625E-05, 6.290810167969022241E-05, 9.120440630944991460E-05, 0.0001153103026479746938 ),
 .UNSPECIFIED. ) ;
#13468=EDGE_CURVE ( 'NONE', #51219, #21179, #28730, .T. ) ;
#13472=ORIENTED_EDGE ( 'NONE', *, *, #60376, .T. ) ;
#13473=CARTESIAN_POINT ( 'NONE',  ( 2.241352910868909643, -5.794346703933810794, -4.970878533273820565 ) ) ;
#13479=CARTESIAN_POINT ( 'NONE',  ( 2.276905613633651182, -7.501802783089482674, 1.479235344773136784 ) ) ;
#13480=CARTESIAN_POINT ( 'NONE',  ( 0.2833330754217370795, -10.50818856955514313, -6.300330022379329264 ) ) ;
#13481=CARTESIAN_POINT ( 'NONE',  ( 0.3665391374699472626, 12.27992639892678284, -0.2638605131387596336 ) ) ;
#13486=CARTESIAN_POINT ( 'NONE',  ( 2.241352910868908754, 3.889181972941541776, -6.569501556381402096 ) ) ;
#13488=EDGE_CURVE ( 'NONE', #20597, #239, #27091, .T. ) ;
#13492=CARTESIAN_POINT ( 'NONE',  ( 3.152665057735760445, 4.725420687649616092, -6.378477742801607953 ) ) ;
#13513=CARTESIAN_POINT ( 'NONE',  ( 2.255723233588950549, -5.936060085173580525, 4.808373255828864323 ) ) ;
#13516=CARTESIAN_POINT ( 'NONE',  ( 5.536195898058073439, -0.007896796515810905470, 0.003145317580921124911 ) ) ;
#13518=ADVANCED_FACE ( 'NONE', ( #48514 ), #6416, .F. ) ;
#13520=CARTESIAN_POINT ( 'NONE',  ( 0.4626703367445764159, -8.128802338754399059, 9.247028139127525748 ) ) ;
#13521=B_SPLINE_CURVE_WITH_KNOTS ( 'NONE', 3,
 ( #44478, #59796, #18909, #65412, #39173, #54492, #19230, #29214, #59464, #38529, #59158, #45154, #23913 ),
 .UNSPECIFIED., .F., .F.,
 ( 4, 3, 3, 3, 4 ),
 ( 3.127317220692750759E-18, 6.607593386745536459E-05, 0.0001321518677373519188, 0.0001982171734706205887, 0.0002642860854759490966 ),
 .UNSPECIFIED. ) ;
#13524=B_SPLINE_CURVE_WITH_KNOTS ( 'NONE', 3,
 ( #13799, #48757, #13176, #53748, #54733, #49735, #3554, #63366, #18519, #17833, #28455, #39411, #13480, #59377, #59072, #48440, #64665, #8183, #2889 ),
 .UNSPECIFIED., .F., .F.,
 ( 4, 3, 3, 3, 3, 3, 4 ),
 ( 9.407601696150301793E-18, 4.457896483015181383E-05, 6.639290541542492330E-05, 8.820687556479444300E-05, 0.0001100173248778943082, 0.0001545671401658154634, 0.0001830328308068594170 ),
 .UNSPECIFIED. ) ;
#13532=CARTESIAN_POINT ( 'NONE',  ( 0.3057689695767493721, -9.538231270095055336, -7.702054583838566337 ) ) ;
#13535=CARTESIAN_POINT ( 'NONE',  ( 2.241451721903216399, -3.869794645251166010, 6.581017239736953073 ) ) ;
#13537=CARTESIAN_POINT ( 'NONE',  ( 5.516018279890452902, -0.006707902355169293243, 0.0009545156522407741585 ) ) ;
#13540=CARTESIAN_POINT ( 'NONE',  ( 2.034671305879985237, -8.030508024279507495, 8.476347594673388386 ) ) ;
#13545=LINE ( 'NONE', #33524, #50231 ) ;
#13551=CARTESIAN_POINT ( 'NONE',  ( 2.241352910868908754, 6.569501556381497132, -3.889181972941381460 ) ) ;
#13561=CARTESIAN_POINT ( 'NONE',  ( 0.3654063281920738593, 10.50027211615256562, -6.366443614636578374 ) ) ;
#13565=CARTESIAN_POINT ( 'NONE',  ( 0.3675815128205894289, -10.76447900494936327, -5.910255304480558358 ) ) ;
#13567=CARTESIAN_POINT ( 'NONE',  ( 2.253265082352432724, -1.452519439326509287, 7.498995607278134301 ) ) ;
#13572=CARTESIAN_POINT ( 'NONE',  ( 2.305787727787084407, 1.164987321564833422, -7.566723232958059597 ) ) ;
#13575=CARTESIAN_POINT ( 'NONE',  ( 0.2739690278137263402, -11.57167385487630362, -4.016979056590882280 ) ) ;
#13581=( BOUNDED_SURFACE ( )  B_SPLINE_SURFACE ( 3, 1, ( 
 ( #64274, #4769 ),
 ( #59958, #34004 ),
 ( #34339, #28694 ),
 ( #64578, #54946 ) ),
 .UNSPECIFIED., .F., .F., .F. ) 
 B_SPLINE_SURFACE_WITH_KNOTS ( ( 4, 4 ),
 ( 2, 2 ),
 ( 0.000000000000000000, 1.000000000000000000 ),
 ( 0.000000000000000000, 1.000000000000000000 ),
 .UNSPECIFIED. ) 
 GEOMETRIC_REPRESENTATION_ITEM ( )  RATIONAL_B_SPLINE_SURFACE ( (
 ( 1.000000000000000000, 1.000000000000000000),
 ( 0.6933888150995267674, 0.9895912004443193632),
 ( 0.6933888150995267674, 0.9895912004443193632),
 ( 1.000000000000000000, 1.000000000000000000) ) ) 
 REPRESENTATION_ITEM ( '' )  SURFACE ( )  );
#13585=CARTESIAN_POINT ( 'NONE',  ( 1.719304012338199517, 0.000000000000000000, 0.000000000000000000 ) ) ;
#13600=CARTESIAN_POINT ( 'NONE',  ( 5.514624014163232779, 0.002789935220458047982, -0.003060352188290787166 ) ) ;
#13613=CARTESIAN_POINT ( 'NONE',  ( 0.3610902822527237710, 9.234828023175207790, -8.091349661862537346 ) ) ;
#13619=FACE_OUTER_BOUND ( 'NONE', #31738, .T. ) ;
#13635=CARTESIAN_POINT ( 'NONE',  ( 2.941278708680199916, -0.9331242451665402449, 6.068329152486373168 ) ) ;
#13638=ORIENTED_EDGE ( 'NONE', *, *, #17962, .F. ) ;
#13639=ADVANCED_FACE ( 'NONE', ( #25506 ), #27189, .F. ) ;
#13640=VERTEX_POINT ( 'NONE', #56427 ) ;
#13642=CARTESIAN_POINT ( 'NONE',  ( 0.2651627923886317739, -4.271101819784433040, 11.47719387551885362 ) ) ;
#13644=CARTESIAN_POINT ( 'NONE',  ( 2.941278708680199916, 5.248410529370224786, 3.185832147968465478 ) ) ;
#13646=CARTESIAN_POINT ( 'NONE',  ( 0.2648978790185593790, -6.237101853238620208, 10.53870023327861283 ) ) ;
#13654=ORIENTED_EDGE ( 'NONE', *, *, #34916, .F. ) ;
#13659=VERTEX_POINT ( 'NONE', #55448 ) ;
#13664=EDGE_LOOP ( 'NONE', ( #44791, #39688, #31526, #50056 ) ) ;
#13669=CARTESIAN_POINT ( 'NONE',  ( 1.633930747251798099, -9.253127167384873175, 8.702439996574970138 ) ) ;
#13673=CARTESIAN_POINT ( 'NONE',  ( 1.549075743844778419, 1.533250336942787007, 12.58108552526728019 ) ) ;
#13678=CARTESIAN_POINT ( 'NONE',  ( 0.3109076770649069621, -12.11383728282217476, -1.896437056876588256 ) ) ;
#13681=AXIS2_PLACEMENT_3D ( 'NONE', #56096, #11855, #56437 ) ;
#13682=CARTESIAN_POINT ( 'NONE',  ( 1.452237505248552996, 10.06489946308212957, -7.672309600508594229 ) ) ;
#13696=CARTESIAN_POINT ( 'NONE',  ( 0.3675815128205894289, -7.689697408877210094, -9.574637318042043432 ) ) ;
#13699=CARTESIAN_POINT ( 'NONE',  ( 2.963017218115616913, 5.778072204777641829, 5.350609950027682693 ) ) ;
#13701=CARTESIAN_POINT ( 'NONE',  ( 0.2801149460245113687, -9.257544930777214631, 8.024198546827449263 ) ) ;
#13708=CARTESIAN_POINT ( 'NONE',  ( 2.260457164927188511, -1.462935478981556514, -7.499412009325157946 ) ) ;
#13712=CARTESIAN_POINT ( 'NONE',  ( 0.2671309869109494417, -6.263183022891106511, -10.52409658627922440 ) ) ;
#13714=CARTESIAN_POINT ( 'NONE',  ( 1.719304012338833676, 3.626341562670448493, 12.20344780066006152 ) ) ;
#13721=CARTESIAN_POINT ( 'NONE',  ( 0.2653519890518174495, -11.50765826381080359, 4.188454465438642416 ) ) ;
#13729=VERTEX_POINT ( 'NONE', #40132 ) ;
#13737=CARTESIAN_POINT ( 'NONE',  ( 0.3002738374340830907, 10.72659044316170984, -5.932527270856288837 ) ) ;
#13738=CARTESIAN_POINT ( 'NONE',  ( 0.8320506296491593234, -10.95539209551942683, -5.883188144889889948 ) ) ;
#13741=CARTESIAN_POINT ( 'NONE',  ( 2.241311220309555097, -5.788190037953238942, -4.978033760028431232 ) ) ;
#13747=CARTESIAN_POINT ( 'NONE',  ( 2.241352910868908310, -2.689314586382304917, -7.145045428366603169 ) ) ;
#13750=CARTESIAN_POINT ( 'NONE',  ( 0.3665391374699467075, -3.952034409876221677, -11.62960183138731196 ) ) ;
#13758=( BOUNDED_SURFACE ( )  B_SPLINE_SURFACE ( 3, 1, ( 
 ( #18951, #48892 ),
 ( #33254, #24253 ),
 ( #23619, #38907 ),
 ( #53562, #54540 ) ),
 .UNSPECIFIED., .F., .F., .F. ) 
 B_SPLINE_SURFACE_WITH_KNOTS ( ( 4, 4 ),
 ( 2, 2 ),
 ( 0.000000000000000000, 1.000000000000000000 ),
 ( 0.000000000000000000, 1.000000000000000000 ),
 .UNSPECIFIED. ) 
 GEOMETRIC_REPRESENTATION_ITEM ( )  RATIONAL_B_SPLINE_SURFACE ( (
 ( 1.000000000000000000, 1.000000000000000000),
 ( 0.6933888150995267674, 0.9895912004443193632),
 ( 0.6933888150995267674, 0.9895912004443193632),
 ( 1.000000000000000000, 1.000000000000000000) ) ) 
 REPRESENTATION_ITEM ( '' )  SURFACE ( )  );
#13759=ORIENTED_EDGE ( 'NONE', *, *, #52998, .F. ) ;
#13766=AXIS2_PLACEMENT_3D ( 'NONE', #50864, #1317, #16267 ) ;
#13771=CARTESIAN_POINT ( 'NONE',  ( 0.2648978790185584908, 6.237101853238694815, -10.53870023327857197 ) ) ;
#13772=CARTESIAN_POINT ( 'NONE',  ( 0.2833330754217364689, -6.300330022379283079, 10.50818856955516090 ) ) ;
#13776=CARTESIAN_POINT ( 'NONE',  ( 0.9296196016818646379, 7.691217109781894656, 9.812579935704260237 ) ) ;
#13777=VERTEX_POINT ( 'NONE', #57097 ) ;
#13790=CARTESIAN_POINT ( 'NONE',  ( 2.941278708680199916, 1.972702289976003165, 5.814102272488595347 ) ) ;
#13794=EDGE_LOOP ( 'NONE', ( #43085, #43749, #31786, #10449 ) ) ;
#13795=CARTESIAN_POINT ( 'NONE',  ( 1.452237505248552996, 1.611965288198731194, 12.55261342181975870 ) ) ;
#13798=CARTESIAN_POINT ( 'NONE',  ( 2.241506898688419458, -1.286963596520043440, 7.525229609709739087 ) ) ;
#13799=CARTESIAN_POINT ( 'NONE',  ( 0.3675815128205912052, -10.50067073900647330, -6.367184624550275451 ) ) ;
#13805=CARTESIAN_POINT ( 'NONE',  ( 2.251139882113959878, 3.925854078924309043, -6.551456272498855427 ) ) ;
#13813=ORIENTED_EDGE ( 'NONE', *, *, #15629, .F. ) ;
#13830=EDGE_LOOP ( 'NONE', ( #25668, #42877, #16349, #17233 ) ) ;
#13832=CARTESIAN_POINT ( 'NONE',  ( 0.2655924914740778187, 2.083162675473614112, 12.06787830249865756 ) ) ;
#13850=CARTESIAN_POINT ( 'NONE',  ( 2.253265082352434945, 7.543541742286983265, -1.199885753716548598 ) ) ;
#13855=ORIENTED_EDGE ( 'NONE', *, *, #54500, .T. ) ;
#13858=( NAMED_UNIT ( * ) SI_UNIT ( $, .STERADIAN. ) SOLID_ANGLE_UNIT ( ) );
#13867=CARTESIAN_POINT ( 'NONE',  ( 2.256373768223947085, -5.011614056002601458, -5.765785888498891509 ) ) ;
#13875=ORIENTED_EDGE ( 'NONE', *, *, #32557, .F. ) ;
#13884=DIRECTION ( 'NONE',  ( -0.3939253465568944290, -0.009718094113426823527, -0.9190910618577645685 ) ) ;
#13892=B_SPLINE_CURVE_WITH_KNOTS ( 'NONE', 3,
 ( #52615, #7039, #53256, #7703, #17688, #48602, #2052, #2742, #42256, #22316, #42586, #62888, #32609, #17353, #57930, #43581, #23000, #12344, #3056 ),
 .UNSPECIFIED., .F., .F.,
 ( 4, 3, 3, 3, 3, 3, 4 ),
 ( 8.641030098560686409E-18, 2.825908398991792413E-05, 4.208813692702779546E-05, 5.591713747221096955E-05, 6.279584083537769477E-05, 9.105792820727356767E-05, 0.0001153131102486933926 ),
 .UNSPECIFIED. ) ;
#13897=CARTESIAN_POINT ( 'NONE',  ( 1.198791140417499124, 5.826488554586223501, 11.12379938352617081 ) ) ;
#13904=CARTESIAN_POINT ( 'NONE',  ( 2.665405856346775959, 7.981834391067746282, 5.274989403260939902 ) ) ;
#13922=AXIS2_PLACEMENT_3D ( 'NONE', #60314, #54997, #19102 ) ;
#13930=EDGE_CURVE ( 'NONE', #12898, #14666, #1278, .T. ) ;
#13931=EDGE_LOOP ( 'NONE', ( #23076, #61260, #46859, #56038 ) ) ;
#13935=CARTESIAN_POINT ( 'NONE',  ( 2.241352910868908310, -5.901537464758421336, -4.843133558968188979 ) ) ;
#13936=CARTESIAN_POINT ( 'NONE',  ( 0.3002738374340830907, 12.25576345519757915, 0.2255758963751899049 ) ) ;
#13937=CARTESIAN_POINT ( 'NONE',  ( 0.3057689695767515370, 9.241339546505193070, -8.055876362038247862 ) ) ;
#13949=CARTESIAN_POINT ( 'NONE',  ( 2.241352910868908310, -3.744764251556946366, -6.652881166698550786 ) ) ;
#13961=CARTESIAN_POINT ( 'NONE',  ( 2.249013661412228693, 2.498855301843084131, 7.216565855998264389 ) ) ;
#13973=CARTESIAN_POINT ( 'NONE',  ( 2.241352910868908754, -7.202080440908725123, -2.532612177304514933 ) ) ;
#13977=CARTESIAN_POINT ( 'NONE',  ( 1.104777566491145002, 11.07886329447276808, 5.844728374724304842 ) ) ;
#13979=ORIENTED_EDGE ( 'NONE', *, *, #9915, .T. ) ;
#13983=ADVANCED_FACE ( 'NONE', ( #7870 ), #42508, .F. ) ;
#13985=VERTEX_POINT ( 'NONE', #2890 ) ;
#13986=CARTESIAN_POINT ( 'NONE',  ( 0.3537226245948357772, -10.75912040401513359, 5.910416419900492713 ) ) ;
#13991=VECTOR ( 'NONE', #31958, 1000.000000000000000 ) ;
#14000=CARTESIAN_POINT ( 'NONE',  ( 0.7400311444011713480, -9.270387619166385207, 8.241979373543633969 ) ) ;
#14003=CARTESIAN_POINT ( 'NONE',  ( 1.020182472822224851, 1.729367949134763771, 12.37761526492745112 ) ) ;
#14009=CARTESIAN_POINT ( 'NONE',  ( 2.573738926104375047, -5.156412073069320812, 5.779258037546994409 ) ) ;
#14015=ORIENTED_EDGE ( 'NONE', *, *, #59667, .F. ) ;
#14018=VERTEX_POINT ( 'NONE', #28788 ) ;
#14020=CARTESIAN_POINT ( 'NONE',  ( 2.770579946183332254, -7.437949029067708828, 2.384572752174059396 ) ) ;
#14025=EDGE_LOOP ( 'NONE', ( #29638, #15265, #14888, #23306 ) ) ;
#14026=ORIENTED_EDGE ( 'NONE', *, *, #31777, .F. ) ;
#14027=CARTESIAN_POINT ( 'NONE',  ( 0.2657645697724678180, -7.755260067564094584, -9.477802844074121325 ) ) ;
#14033=CARTESIAN_POINT ( 'NONE',  ( 0.2956976708475456683, 10.50256636126827203, 6.317697191869677376 ) ) ;
#14038=CARTESIAN_POINT ( 'NONE',  ( 2.259025283528087957, -1.461109758650511070, -7.499281868334255918 ) ) ;
#14039=CARTESIAN_POINT ( 'NONE',  ( 5.536195898058073439, 0.008323005098841094671, -0.001726268814999541799 ) ) ;
#14040=VERTEX_POINT ( 'NONE', #41053 ) ;
#14043=CARTESIAN_POINT ( 'NONE',  ( 0.2872850955227773118, -6.306790329742856471, -10.50585060073186483 ) ) ;
#14047=CARTESIAN_POINT ( 'NONE',  ( 0.3164563675027628475, 3.967501530099240448, -11.60369811966058862 ) ) ;
#14052=CARTESIAN_POINT ( 'NONE',  ( 0.2653519991613838003, -11.51519138201633474, 4.167757449530376412 ) ) ;
#14054=CARTESIAN_POINT ( 'NONE',  ( 0.2911222467163541716, -3.989243506922266924, -11.58731125337564016 ) ) ;
#14063=EDGE_CURVE ( 'NONE', #50365, #7766, #45334, .T. ) ;
#14066=CARTESIAN_POINT ( 'NONE',  ( 0.3665391374699472626, 10.76665847464312620, 5.911453292029639428 ) ) ;
#14068=CARTESIAN_POINT ( 'NONE',  ( 0.2671309869109479429, -10.52409658627921019, 6.263183022891143814 ) ) ;
#14072=CARTESIAN_POINT ( 'NONE',  ( 1.633930747252547055, -11.34237452761363585, -5.718685543473386090 ) ) ;
#14078=EDGE_LOOP ( 'NONE', ( #47435, #39265, #5826, #26596, #14015, #29916 ) ) ;
#14081=B_SPLINE_CURVE_WITH_KNOTS ( 'NONE', 3,
 ( #51448, #26157, #41418, #11185, #5560, #30783, #46428, #40444, #60741, #15183 ),
 .UNSPECIFIED., .F., .F.,
 ( 4, 3, 3, 4 ),
 ( 1.939479807224432123E-18, 6.607638129004473975E-05, 9.911389841680488377E-05, 0.0001667630577588610102 ),
 .UNSPECIFIED. ) ;
#14082=AXIS2_PLACEMENT_3D ( 'NONE', #6911, #31509, #41819 ) ;
#14084=ADVANCED_FACE ( 'NONE', ( #11767 ), #40792, .F. ) ;
#14085=CARTESIAN_POINT ( 'NONE',  ( 2.241528039335008327, -2.596349773934832683, -7.179411278563578414 ) ) ;
#14097=CARTESIAN_POINT ( 'NONE',  ( 0.2706063244538030044, -12.09107863371559155, 1.954041462022380049 ) ) ;
#14103=VERTEX_POINT ( 'NONE', #16766 ) ;
#14110=CARTESIAN_POINT ( 'NONE',  ( 0.3160775863651047457, -6.338373607799261400, 10.49803827792120714 ) ) ;
#14111=CARTESIAN_POINT ( 'NONE',  ( 2.305787727787084851, -7.566723232958062262, -1.164987321564809886 ) ) ;
#14112=CARTESIAN_POINT ( 'NONE',  ( 1.937114397841932290, -7.538912286488274717, -10.38782037574624262 ) ) ;
#14113=CARTESIAN_POINT ( 'NONE',  ( 2.241506898688418570, -7.634383346098566392, 0.03933068055388246748 ) ) ;
#14117=AXIS2_PLACEMENT_3D ( 'NONE', #25313, #55246, #14993 ) ;
#14129=CARTESIAN_POINT ( 'NONE',  ( 5.516018279890452902, 0.004525000489649935558, -0.005042957932159086720 ) ) ;
#14132=VERTEX_POINT ( 'NONE', #12419 ) ;
#14137=CARTESIAN_POINT ( 'NONE',  ( 2.655192694323660341, -8.010337395399627525, 5.293797899976080856 ) ) ;
#14142=CARTESIAN_POINT ( 'NONE',  ( 1.719304012338398469, 8.755325027793414705, 9.242227816402090568 ) ) ;
#14143=CARTESIAN_POINT ( 'NONE',  ( 2.903928887688295379, 0.9983813550132488723, -8.712847781149726245 ) ) ;
#14146=VERTEX_POINT ( 'NONE', #46382 ) ;
#14153=CARTESIAN_POINT ( 'NONE',  ( 5.520433897694421610, -0.007082458259338479320, 0.01329351892498011924 ) ) ;
#14169=CARTESIAN_POINT ( 'NONE',  ( 2.844750968615770148, -3.626176236708136713, 6.946006365803760296 ) ) ;
#14170=CARTESIAN_POINT ( 'NONE',  ( 0.3675815128205894289, -4.447030445008105737, -11.44679196252413789 ) ) ;
#14173=CARTESIAN_POINT ( 'NONE',  ( 2.835339799623878054, 6.612744557053422234, 4.197472173747671675 ) ) ;
#14177=CARTESIAN_POINT ( 'NONE',  ( 0.9296196016823387032, -6.590257778216964901, 10.58347995892855842 ) ) ;
#14185=CARTESIAN_POINT ( 'NONE',  ( 1.719304012342639965, 12.38166659047149487, -2.961219984262613458 ) ) ;
#14187=CARTESIAN_POINT ( 'NONE',  ( 2.241352910868909643, -6.569501556381414531, -3.889181972941518683 ) ) ;
#14191=CARTESIAN_POINT ( 'NONE',  ( 2.969415267405017822, -4.760005747566342649, 6.276215141898974892 ) ) ;
#14192=CARTESIAN_POINT ( 'NONE',  ( 2.255723233588951882, 7.544965460065586882, -1.196143347838635407 ) ) ;
#14196=CARTESIAN_POINT ( 'NONE',  ( 2.242418902651536428, 1.227462051875141569, -7.535443599794351854 ) ) ;
#14204=CARTESIAN_POINT ( 'NONE',  ( 1.452237505248552996, 3.767214359061125784, 12.08199618361514460 ) ) ;
#14206=CARTESIAN_POINT ( 'NONE',  ( 0.3632410797595245211, 5.910360611678975751, -10.76277061791634360 ) ) ;
#14208=CARTESIAN_POINT ( 'NONE',  ( 2.244591118396919605, -4.989853642776339804, -5.779440292195060280 ) ) ;
#14209=ORIENTED_EDGE ( 'NONE', *, *, #33503, .T. ) ;
#14210=VERTEX_POINT ( 'NONE', #32382 ) ;
#14211=CARTESIAN_POINT ( 'NONE',  ( 2.260457164927185847, -7.226149053012470347, -2.482766715766981935 ) ) ;
#14214=EDGE_CURVE ( 'NONE', #8323, #64016, #36279, .T. ) ;
#14227=CARTESIAN_POINT ( 'NONE',  ( 2.260457164927187179, 7.639515169785715543, -0.1384509728649304106 ) ) ;
#14236=B_SPLINE_CURVE_WITH_KNOTS ( 'NONE', 3,
 ( #21272, #31264, #62174, #41217, #61194, #15940, #16626, #35892, #56189, #56538, #47228, #51235, #10982, #51568, #62480, #6017 ),
 .UNSPECIFIED., .F., .F.,
 ( 4, 3, 3, 3, 3, 4 ),
 ( 0.000000000000000000, 0.0002176109881720252439, 0.0004352086762394603413, 0.0006528017811446877247, 0.0007615147961451705421, 0.0009453342004947429180 ),
 .UNSPECIFIED. ) ;
#14239=EDGE_CURVE ( 'NONE', #20746, #25736, #4008, .T. ) ;
#14240=ORIENTED_EDGE ( 'NONE', *, *, #37079, .F. ) ;
#14241=CARTESIAN_POINT ( 'NONE',  ( 0.3675815128205894289, 0.2638082659428422350, 12.27743992903066328 ) ) ;
#14242=EDGE_CURVE ( 'NONE', #61726, #14742, #64594, .T. ) ;
#14246=CARTESIAN_POINT ( 'NONE',  ( 2.255723233588948773, -7.499053486174012129, -1.456523090672685816 ) ) ;
#14248=CARTESIAN_POINT ( 'NONE',  ( 2.241537034860906275, -4.910958050585477963, 5.845308934728764783 ) ) ;
#14252=ORIENTED_EDGE ( 'NONE', *, *, #17190, .F. ) ;
#14256=CARTESIAN_POINT ( 'NONE',  ( 0.9232167919969133107, 2.570564963838149364, 12.19756235544080525 ) ) ;
#14257=ADVANCED_FACE ( 'NONE', ( #8770 ), #47583, .F. ) ;
#14263=CARTESIAN_POINT ( 'NONE',  ( 0.2915757698887299632, -0.2147157799033968251, -12.25305747416128099 ) ) ;
#14265=CIRCLE ( 'NONE', #43995, 7.938172270156617749 ) ;
#14274=CARTESIAN_POINT ( 'NONE',  ( 5.515188684475870851, -0.003709313826049772961, 0.003857086913166378472 ) ) ;
#14276=CARTESIAN_POINT ( 'NONE',  ( 2.941278708680199916, 3.185832147968446826, 5.248410529370236333 ) ) ;
#14277=CARTESIAN_POINT ( 'NONE',  ( 0.3223008802179246901, 9.236652594547246409, -8.069628056118025583 ) ) ;
#14291=CARTESIAN_POINT ( 'NONE',  ( 3.152665057736013132, 7.281573230473836311, -3.161213418915250095 ) ) ;
#14300=CARTESIAN_POINT ( 'NONE',  ( 0.2648978790185602672, 11.55204314799263798, 4.063980959785085112 ) ) ;
#14302=EDGE_CURVE ( 'NONE', #12134, #47920, #55596, .T. ) ;
#14305=CARTESIAN_POINT ( 'NONE',  ( 0.6511581176963763262, -0.3309006379877175164, 12.37037447926123868 ) ) ;
#14307=CARTESIAN_POINT ( 'NONE',  ( 2.276198483117257698, -7.130755363255148360, -2.759333101207220196 ) ) ;
#14308=VERTEX_POINT ( 'NONE', #10625 ) ;
#14314=CARTESIAN_POINT ( 'NONE',  ( 1.109979610372471059, 9.898186741523009147, -7.679283534372109976 ) ) ;
#14320=CARTESIAN_POINT ( 'NONE',  ( 1.104777566491138563, 6.672212870706200505, 10.60111489796736350 ) ) ;
#14334=CARTESIAN_POINT ( 'NONE',  ( 0.2801149460245161427, -12.09752788490056119, -1.933835447580753319 ) ) ;
#14336=CARTESIAN_POINT ( 'NONE',  ( 2.931247277082683844, -5.333206743525275684, 5.779735553870076536 ) ) ;
#14346=( BOUNDED_SURFACE ( )  B_SPLINE_SURFACE ( 3, 1, ( 
 ( #26993, #26014 ),
 ( #11357, #21993 ),
 ( #46947, #52607 ),
 ( #36948, #2042 ) ),
 .UNSPECIFIED., .F., .F., .F. ) 
 B_SPLINE_SURFACE_WITH_KNOTS ( ( 4, 4 ),
 ( 2, 2 ),
 ( 0.000000000000000000, 1.000000000000000000 ),
 ( 0.000000000000000000, 1.000000000000000000 ),
 .UNSPECIFIED. ) 
 GEOMETRIC_REPRESENTATION_ITEM ( )  RATIONAL_B_SPLINE_SURFACE ( (
 ( 1.000000000000000000, 1.000000000000000000),
 ( 0.9942764183789327692, 0.8450855930916585379),
 ( 0.9942764183789327692, 0.8450855930916585379),
 ( 1.000000000000000000, 1.000000000000000000) ) ) 
 REPRESENTATION_ITEM ( '' )  SURFACE ( )  );
#14348=CARTESIAN_POINT ( 'NONE',  ( 3.152665057734119536, 1.848755561852129858, -7.719888720907784219 ) ) ;
#14349=CYLINDRICAL_SURFACE ( 'NONE', #14117, 4.000000000000000000 ) ;
#14355=ORIENTED_EDGE ( 'NONE', *, *, #63485, .F. ) ;
#14356=ORIENTED_EDGE ( 'NONE', *, *, #53163, .T. ) ;
#14357=CARTESIAN_POINT ( 'NONE',  ( 2.963017218115628904, 3.051711603120633498, -7.259628195185902300 ) ) ;
#14361=DIRECTION ( 'NONE',  ( 0.3865475372811021937, 0.01937500237529058214, -0.9220659470476461061 ) ) ;
#14362=CARTESIAN_POINT ( 'NONE',  ( 0.3654063281920728601, -9.235228056823977738, 8.093076148786007451 ) ) ;
#14368=CARTESIAN_POINT ( 'NONE',  ( 2.305787727787083519, 7.135468203929983488, 2.774453000917173284 ) ) ;
#14371=CARTESIAN_POINT ( 'NONE',  ( 5.515539859299206427, -0.005751553894234964250, 0.001886660928063870184 ) ) ;
#14373=CARTESIAN_POINT ( 'NONE',  ( 0.3109076770649054633, -6.333869442011710760, -10.49874397806412141 ) ) ;
#14376=CARTESIAN_POINT ( 'NONE',  ( 2.941278708680199916, 5.721889327162181793, -2.226055275041733506 ) ) ;
#14383=CARTESIAN_POINT ( 'NONE',  ( 0.2676618633000454883, -4.037335446657164262, -11.56235835488944197 ) ) ;
#14384=CARTESIAN_POINT ( 'NONE',  ( 0.2648978790185602672, -0.1321385342561549048, -12.24533305150758267 ) ) ;
#14391=CARTESIAN_POINT ( 'NONE',  ( 0.5547464869798243159, 1.842327806480310137, -12.20441397277154572 ) ) ;
#14396=CARTESIAN_POINT ( 'NONE',  ( 2.297017764049619437, 7.246120070222534792, 2.462009443075805493 ) ) ;
#14397=CARTESIAN_POINT ( 'NONE',  ( 1.459561108993787659, -11.25243317554921063, -5.767168887069020755 ) ) ;
#14398=EDGE_LOOP ( 'NONE', ( #5319, #35576, #20039, #37696 ) ) ;
#14399=CARTESIAN_POINT ( 'NONE',  ( 2.350038591457826342, -7.710465783964407294, -7.305692696276328668 ) ) ;
#14410=CARTESIAN_POINT ( 'NONE',  ( 0.3665391374699472626, -11.44911061034389732, 4.447929964102808498 ) ) ;
#14411=DIRECTION ( 'NONE',  ( -0.3939253465568942625, 0.7103112711423451575, 0.5833358547425114837 ) ) ;
#14412=B_SPLINE_CURVE_WITH_KNOTS ( 'NONE', 3,
 ( #21278, #42522, #41554, #62821, #37568, #16307, #36584 ),
 .UNSPECIFIED., .F., .F.,
 ( 4, 3, 4 ),
 ( 4.926993459890410048E-15, 0.002398160485434636807, 0.005002426799381711787 ),
 .UNSPECIFIED. ) ;
#14415=EDGE_CURVE ( 'NONE', #16341, #11407, #16941, .T. ) ;
#14423=ADVANCED_FACE ( 'NONE', ( #58500 ), #8776, .T. ) ;
#14428=EDGE_LOOP ( 'NONE', ( #46046, #7699, #64238, #55860 ) ) ;
#14433=CARTESIAN_POINT ( 'NONE',  ( 0.3053067050349123623, -6.328522421120339914, 10.49978800868458961 ) ) ;
#14436=CARTESIAN_POINT ( 'NONE',  ( 2.241352910868908310, -7.633946224498473043, -0.08337961031712197435 ) ) ;
#14439=VERTEX_POINT ( 'NONE', #6655 ) ;
#14442=ORIENTED_EDGE ( 'NONE', *, *, #4830, .F. ) ;
#14449=CARTESIAN_POINT ( 'NONE',  ( 2.241352910868910531, 5.901537464758454199, 4.843133558968147234 ) ) ;
#14451=ADVANCED_FACE ( 'NONE', ( #32864 ), #65426, .F. ) ;
#14452=VECTOR ( 'NONE', #32710, 1000.000000000000114 ) ;
#14454=FACE_OUTER_BOUND ( 'NONE', #21714, .T. ) ;
#14455=ORIENTED_EDGE ( 'NONE', *, *, #39540, .F. ) ;
#14463=CARTESIAN_POINT ( 'NONE',  ( 2.406456491626523420, 7.176027849159630989, 7.573451137021355528 ) ) ;
#14469=EDGE_CURVE ( 'NONE', #18816, #43792, #34130, .T. ) ;
#14474=CARTESIAN_POINT ( 'NONE',  ( 1.719304012339867516, -12.38166659046446938, 2.961219984258617544 ) ) ;
#14476=FACE_OUTER_BOUND ( 'NONE', #63131, .T. ) ;
#14477=CARTESIAN_POINT ( 'NONE',  ( 2.305787727787084407, -5.047606869483016290, -5.756228004061508585 ) ) ;
#14486=CARTESIAN_POINT ( 'NONE',  ( 2.899286259009686617, -6.616268644969667712, -4.231523595108555469 ) ) ;
#14489=CARTESIAN_POINT ( 'NONE',  ( 2.241352910868908310, 7.633946224498473931, -0.08337961031706911386 ) ) ;
#14490=CARTESIAN_POINT ( 'NONE',  ( 2.573738926104320424, 6.586859681822653911, 4.074516960797377685 ) ) ;
#14493=CARTESIAN_POINT ( 'NONE',  ( 1.020182472821653974, -6.631405022219332146, 10.59341968305508708 ) ) ;
#14497=CARTESIAN_POINT ( 'NONE',  ( 2.406456491625218685, 9.571062220824229527, -4.152987573057118631 ) ) ;
#14498=B_SPLINE_CURVE_WITH_KNOTS ( 'NONE', 3,
 ( #41846, #10937, #57482, #47188, #52167, #46200, #645, #51840, #61457, #15902, #5976, #62135, #36855, #57155, #1633, #27526 ),
 .UNSPECIFIED., .F., .F.,
 ( 4, 3, 3, 3, 3, 4 ),
 ( 0.000000000000000000, 0.0002999043160757539290, 0.0005998071753051414413, 0.0008997092107375177696, 0.001204458948197544834, 0.001510329163480266142 ),
 .UNSPECIFIED. ) ;
#14499=CARTESIAN_POINT ( 'NONE',  ( 0.3675815128205894289, 1.872154644482084684, 12.13672785388550679 ) ) ;
#14504=CARTESIAN_POINT ( 'NONE',  ( 1.020182472824197495, -1.729367949134086979, -12.37761526492820785 ) ) ;
#14505=CARTESIAN_POINT ( 'NONE',  ( 2.276198483117262583, 7.555081843354708226, -1.175725118478776920 ) ) ;
#14508=CARTESIAN_POINT ( 'NONE',  ( 2.280717697722506099, 1.173604464352448806, -7.556934756534813502 ) ) ;
#14520=CARTESIAN_POINT ( 'NONE',  ( 2.242418902652064006, -4.983487297756227896, -5.783980263415513079 ) ) ;
#14523=CARTESIAN_POINT ( 'NONE',  ( 2.705197763288548884, 0.2797837188787443141, -7.783989928191459740 ) ) ;
#14525=AXIS2_PLACEMENT_3D ( 'NONE', #42848, #22241, #53164 ) ;
#14529=CARTESIAN_POINT ( 'NONE',  ( 2.266490820343225465, 7.130860233521887359, -2.750080098241445725 ) ) ;
#14530=CARTESIAN_POINT ( 'NONE',  ( 2.373367633546869193, -3.994744114396135526, 6.557448619657627376 ) ) ;
#14533=AXIS2_PLACEMENT_3D ( 'NONE', #12636, #52591, #13315 ) ;
#14536=( BOUNDED_SURFACE ( )  B_SPLINE_SURFACE ( 3, 1, ( 
 ( #39648, #3454 ),
 ( #28363, #3783 ),
 ( #24688, #18412 ),
 ( #14039, #48659 ) ),
 .UNSPECIFIED., .F., .F., .F. ) 
 B_SPLINE_SURFACE_WITH_KNOTS ( ( 4, 4 ),
 ( 2, 2 ),
 ( 0.000000000000000000, 1.000000000000000000 ),
 ( 0.000000000000000000, 1.000000000000000000 ),
 .UNSPECIFIED. ) 
 GEOMETRIC_REPRESENTATION_ITEM ( )  RATIONAL_B_SPLINE_SURFACE ( (
 ( 1.000000000000000000, 1.000000000000000000),
 ( 0.6933888150995267674, 0.9895912004443193632),
 ( 0.6933888150995267674, 0.9895912004443193632),
 ( 1.000000000000000000, 1.000000000000000000) ) ) 
 REPRESENTATION_ITEM ( '' )  SURFACE ( )  );
#14537=CARTESIAN_POINT ( 'NONE',  ( 1.634816307076173425, -12.16351623921533331, 3.661851000130821099 ) ) ;
#14538=CARTESIAN_POINT ( 'NONE',  ( 1.719304012341412724, 2.961219984259706450, -12.38166659046466300 ) ) ;
#14540=EDGE_CURVE ( 'NONE', #36604, #33098, #57954, .T. ) ;
#14547=EDGE_CURVE ( 'NONE', #43973, #56447, #13521, .T. ) ;
#14554=CARTESIAN_POINT ( 'NONE',  ( 1.719304012338836563, -2.961219984258077087, 12.38166659046417095 ) ) ;
#14555=DIRECTION ( 'NONE',  ( 0.000000000000000000, 0.000000000000000000, -1.000000000000000000 ) ) ;
#14556=CARTESIAN_POINT ( 'NONE',  ( 2.844750968616409637, 5.286885609675039177, 5.783165144077036857 ) ) ;
#14561=CARTESIAN_POINT ( 'NONE',  ( 0.5547464869798239828, 2.442933571354971356, 12.09851097165510403 ) ) ;
#14566=CARTESIAN_POINT ( 'NONE',  ( 0.2646305136544072623, -6.237419468587151350, 10.53923716745245009 ) ) ;
#14568=CARTESIAN_POINT ( 'NONE',  ( 0.3109076770649031873, -0.2359198520040302893, -12.25911371383827841 ) ) ;
#14571=CARTESIAN_POINT ( 'NONE',  ( 2.827825597296805604, 6.207590800588465463, -6.550135365664023546 ) ) ;
#14572=CARTESIAN_POINT ( 'NONE',  ( 20.00005080000000035, 5.400000000000000355, 1.000000000000000000 ) ) ;
#14579=CARTESIAN_POINT ( 'NONE',  ( 2.406456491626467020, 5.751891873090721141, 8.704497555691622424 ) ) ;
#14585=VERTEX_POINT ( 'NONE', #65096 ) ;
#14588=EDGE_LOOP ( 'NONE', ( #65282, #15086, #33836, #59808 ) ) ;
#14589=B_SPLINE_CURVE_WITH_KNOTS ( 'NONE', 3,
 ( #33143, #42441, #37144, #58106, #63391, #23171, #47158, #57448, #37482, #7211, #17859, #32152, #27181, #57790, #47793, #52475, #47475, #27836, #2247, #52136, #42788, #63084 ),
 .UNSPECIFIED., .F., .F.,
 ( 4, 3, 3, 3, 3, 3, 3, 4 ),
 ( 1.318988870012550679E-18, 4.449119708436826640E-05, 6.626296329540441862E-05, 8.803456484962596642E-05, 0.0001098060367612799996, 0.0001315774408628507465, 0.0001760698110411156123, 0.0001829697163287818842 ),
 .UNSPECIFIED. ) ;
#14600=CARTESIAN_POINT ( 'NONE',  ( 1.719304012340731269, -10.22720798541492826, -7.581471372739399861 ) ) ;
#14605=ORIENTED_EDGE ( 'NONE', *, *, #64698, .F. ) ;
#14606=CARTESIAN_POINT ( 'NONE',  ( 1.719304012339881282, -12.20344780066076318, 3.626341562669963992 ) ) ;
#14610=CARTESIAN_POINT ( 'NONE',  ( 0.2651627682582904932, 11.53745347823616285, 4.105539787731750323 ) ) ;
#14616=CARTESIAN_POINT ( 'NONE',  ( 1.547277799337432702, 11.29700934613254404, 5.744300480442556811 ) ) ;
#14618=ORIENTED_EDGE ( 'NONE', *, *, #29881, .F. ) ;
#14632=CARTESIAN_POINT ( 'NONE',  ( 0.7400311444011733464, 9.726551103566812628, 7.698344902199123041 ) ) ;
#14634=CARTESIAN_POINT ( 'NONE',  ( 3.152665057735448251, 0.9030954876725900693, -7.886634106564547331 ) ) ;
#14638=CARTESIAN_POINT ( 'NONE',  ( 0.5547464869798223175, 5.905377260991372168, -10.83828453080459120 ) ) ;
#14641=B_SPLINE_CURVE_WITH_KNOTS ( 'NONE', 3,
 ( #56970, #27031, #118, #31358, #35677, #20398, #5453 ),
 .UNSPECIFIED., .F., .F.,
 ( 4, 3, 4 ),
 ( 0.000000000000000000, 0.001700533616330539505, 0.005002426799371278293 ),
 .UNSPECIFIED. ) ;
#14642=CARTESIAN_POINT ( 'NONE',  ( 3.152665057735807075, 3.546019893115007537, -7.102135024646828221 ) ) ;
#14643=CARTESIAN_POINT ( 'NONE',  ( 3.152665057734113319, -5.461013642405577073, 5.761241965769066553 ) ) ;
#14644=CARTESIAN_POINT ( 'NONE',  ( 2.263328370261525890, -5.944174889971089115, -4.802372801874562391 ) ) ;
#14663=CARTESIAN_POINT ( 'NONE',  ( 2.507146904658100972, 2.843654641958985430, -7.180414359940920477 ) ) ;
#14664=CARTESIAN_POINT ( 'NONE',  ( 2.589278595513593739, 3.664724287895330335, -6.829211973730652474 ) ) ;
#14666=VERTEX_POINT ( 'NONE', #20201 ) ;
#14667=DIRECTION ( 'NONE',  ( 1.000000000000000000, 0.000000000000000000, 0.000000000000000000 ) ) ;
#14679=ORIENTED_EDGE ( 'NONE', *, *, #38418, .T. ) ;
#14680=CARTESIAN_POINT ( 'NONE',  ( 2.889800649504073782, 5.267262008933712991, -3.118861721612510518 ) ) ;
#14683=CARTESIAN_POINT ( 'NONE',  ( 0.2648978790185619880, 9.465406350830608773, 7.769924372105235122 ) ) ;
#14687=CARTESIAN_POINT ( 'NONE',  ( 0.2648978790185602672, -12.24533305150758267, 0.1321385342561976484 ) ) ;
#14698=ORIENTED_EDGE ( 'NONE', *, *, #9278, .F. ) ;
#14699=CARTESIAN_POINT ( 'NONE',  ( 0.2834382757447995171, 8.029794915379554254, 9.254160138068977304 ) ) ;
#14702=EDGE_CURVE ( 'NONE', #20748, #60151, #822, .T. ) ;
#14705=CARTESIAN_POINT ( 'NONE',  ( 2.259025283526328920, 7.225123487441466708, 2.484282765460346543 ) ) ;
#14711=CARTESIAN_POINT ( 'NONE',  ( 2.573738926104369718, -6.081632213771414719, 4.796056562246151955 ) ) ;
#14723=CARTESIAN_POINT ( 'NONE',  ( 2.241311220309555097, 6.657499176698838284, -3.736531646286193276 ) ) ;
#14736=ORIENTED_EDGE ( 'NONE', *, *, #59154, .T. ) ;
#14741=VERTEX_POINT ( 'NONE', #6568 ) ;
#14742=VERTEX_POINT ( 'NONE', #26836 ) ;
#14749=VECTOR ( 'NONE', #62840, 1000.000000000000114 ) ;
#14751=CARTESIAN_POINT ( 'NONE',  ( 0.2653141617321020385, 4.229807441322468442, -11.49253039221378003 ) ) ;
#14754=CARTESIAN_POINT ( 'NONE',  ( 1.634816307074677955, 7.601181930721248925, 10.17753964889715235 ) ) ;
#14760=CIRCLE ( 'NONE', #5205, 7.580821595991582562 ) ;
#14761=EDGE_LOOP ( 'NONE', ( #46192, #48304, #29337, #24691, #28025, #45171, #15252, #51935, #61347, #25500, #1877, #8662, #5342, #28111, #35561, #25902, #2708, #46365, #22507, #20006, #40569, #27039, #13855, #61926, #22606, #37326, #61120, #27770, #5966, #15391, #26276, #30557, #57608, #34496, #18721, #59474, #19731, #51278, #56618, #4099, #30385, #56676, #5664, #18140, #35146, #50716, #29657, #28392, #1707, #30057, #62207, #17054, #29197, #22317, #27279, #55779, #25558, #17830, #52601, #11552, #27359, #38717, #23893, #56233, #27447, #17747, #39532, #22613, #24693, #48718, #52329, #6294, #33414, #1007, #58673, #15041, #9625, #38526, #53139, #58113, #44409, #62349, #29838, #40498, #26679, #29971, #37588, #56237, #55284, #37223, #30755, #17093, #37531, #43530, #61325, #36647, #13654, #8720, #62344, #32461, #64660, #30216, #8761, #24256, #58923, #5677, #41666, #18312, #7953, #43067, #54547, #53567 ) ) ;
#14764=CARTESIAN_POINT ( 'NONE',  ( 3.100650473569754872, 7.866294126167277412, -0.9283202922944042701 ) ) ;
#14770=ORIENTED_EDGE ( 'NONE', *, *, #44399, .T. ) ;
#14774=CARTESIAN_POINT ( 'NONE',  ( 0.9232058338315058954, -3.908895078357600639, 11.84276737136199209 ) ) ;
#14777=EDGE_CURVE ( 'NONE', #49417, #1896, #39687, .T. ) ;
#14779=CARTESIAN_POINT ( 'NONE',  ( 1.948354844647019579, 8.228891433294911906, 8.685970062892966581 ) ) ;
#14788=CARTESIAN_POINT ( 'NONE',  ( 2.259025283528083516, 7.499281868334258583, -1.461109758650477541 ) ) ;
#14798=CARTESIAN_POINT ( 'NONE',  ( 0.2653141334712558197, 10.62748186152497176, 6.084912053827373768 ) ) ;
#14802=EDGE_CURVE ( 'NONE', #21790, #2995, #56405, .T. ) ;
#14808=CARTESIAN_POINT ( 'NONE',  ( 5.516018279890452902, 0.004525000489649771626, 0.005042957932158598396 ) ) ;
#14811=CARTESIAN_POINT ( 'NONE',  ( 1.109979610369611347, -6.674783385104200661, 10.60154531817194368 ) ) ;
#14813=CARTESIAN_POINT ( 'NONE',  ( 0.2655924914740778187, -12.24627751708824341, -0.04405032194315980365 ) ) ;
#14814=EDGE_CURVE ( 'NONE', #12988, #21262, #51365, .T. ) ;
#14815=CARTESIAN_POINT ( 'NONE',  ( 0.2648321136542693410, -7.979621084888171900, 9.289286523730396539 ) ) ;
#14830=EDGE_CURVE ( 'NONE', #5000, #47037, #26080, .T. ) ;
#14835=AXIS2_PLACEMENT_3D ( 'NONE', #62439, #6287, #46837 ) ;
#14836=CARTESIAN_POINT ( 'NONE',  ( 0.3401186441510198888, 11.44115600261391386, 4.436257390736866313 ) ) ;
#14843=ORIENTED_EDGE ( 'NONE', *, *, #5304, .F. ) ;
#14848=CARTESIAN_POINT ( 'NONE',  ( 0.3665391374699465965, 4.447929964102846689, 11.44911061034387956 ) ) ;
#14851=ADVANCED_FACE ( 'NONE', ( #55682 ), #11078, .F. ) ;
#14852=CARTESIAN_POINT ( 'NONE',  ( 2.276905613633651626, 7.130967020394731293, -2.759436818562420068 ) ) ;
#14853=CARTESIAN_POINT ( 'NONE',  ( 2.994568964204202821, -4.283796412555518351, 6.620406464816379177 ) ) ;
#14856=CARTESIAN_POINT ( 'NONE',  ( 0.3610902822527155553, 11.62472836966323442, 3.951920836718759489 ) ) ;
#14857=ORIENTED_EDGE ( 'NONE', *, *, #6729, .T. ) ;
#14858=CARTESIAN_POINT ( 'NONE',  ( 1.287602823386778228, -12.00540336274477049, 3.781900355162060468 ) ) ;
#14866=CARTESIAN_POINT ( 'NONE',  ( 2.889800649504073782, 3.002151847318916822, 5.334644486274205732 ) ) ;
#14871=CARTESIAN_POINT ( 'NONE',  ( 0.2739690278137263402, 0.1830199730327409235, 12.24770428423990687 ) ) ;
#14877=CARTESIAN_POINT ( 'NONE',  ( 2.259025283527873906, 2.484282765458685649, -7.225123487442588477 ) ) ;
#14880=CARTESIAN_POINT ( 'NONE',  ( 2.556980015513303783, 2.429125721802597226, -7.348538402679253956 ) ) ;
#14887=DIRECTION ( 'NONE',  ( 0.3939253465568944290, -0.009718094113445955792, 0.9190910618577643465 ) ) ;
#14888=ORIENTED_EDGE ( 'NONE', *, *, #59857, .F. ) ;
#14893=AXIS2_PLACEMENT_3D ( 'NONE', #47290, #1729, #27302 ) ;
#14894=B_SPLINE_CURVE_WITH_KNOTS ( 'NONE', 3,
 ( #61481, #45885, #1324, #21599, #35868, #12823, #40893, #984, #53070, #7507, #336, #51215, #56862, #12487, #53419, #58399 ),
 .UNSPECIFIED., .F., .F.,
 ( 4, 3, 3, 3, 3, 4 ),
 ( 6.505213034913026604E-19, 0.0003017745587525245423, 0.0006035491769808726563, 0.0009053241094668157060, 0.001207275924540510614, 0.001510325902534028712 ),
 .UNSPECIFIED. ) ;
#14906=CARTESIAN_POINT ( 'NONE',  ( 0.7400311444011685724, 9.270387619166440274, -8.241979373543562915 ) ) ;
#14916=CARTESIAN_POINT ( 'NONE',  ( 0.7400311444011702378, -2.502569705372887920, -12.14938086789864791 ) ) ;
#14917=EDGE_CURVE ( 'NONE', #35302, #32743, #3187, .T. ) ;
#14918=CONICAL_SURFACE ( 'NONE', #12848, 12.73084802173761787, 0.3217505529694027477 ) ;
#14919=CARTESIAN_POINT ( 'NONE',  ( 2.350038591457882298, 9.502240128959392962, -4.746773736939736921 ) ) ;
#14927=CARTESIAN_POINT ( 'NONE',  ( 5.530133899448235191, -0.006998616117863498513, -0.01437126147332041734 ) ) ;
#14935=ORIENTED_EDGE ( 'NONE', *, *, #9051, .F. ) ;
#14946=VERTEX_POINT ( 'NONE', #27693 ) ;
#14959=EDGE_CURVE ( 'NONE', #59854, #39489, #18371, .T. ) ;
#14965=CARTESIAN_POINT ( 'NONE',  ( 1.014383007554952032, 9.851867765302182889, 7.686901933424183042 ) ) ;
#14967=CARTESIAN_POINT ( 'NONE',  ( 2.556980015513417914, 4.067895092073379182, 6.584367695372176144 ) ) ;
#14972=CARTESIAN_POINT ( 'NONE',  ( 1.104777566491140783, 5.844728374724420306, -11.07886329447270235 ) ) ;
#14974=CARTESIAN_POINT ( 'NONE',  ( 3.152665057734040488, 0.000000000000000000, 0.000000000000000000 ) ) ;
#14988=VERTEX_POINT ( 'NONE', #16738 ) ;
#14993=DIRECTION ( 'NONE',  ( 0.000000000000000000, 0.000000000000000000, 1.000000000000000000 ) ) ;
#14996=CARTESIAN_POINT ( 'NONE',  ( 0.3040950598368144520, -0.2511348647276499535, 12.25911170648142878 ) ) ;
#15000=ORIENTED_EDGE ( 'NONE', *, *, #50812, .F. ) ;
#15002=CARTESIAN_POINT ( 'NONE',  ( 2.899286259009689282, 3.018334250363182925, -7.250549018622912456 ) ) ;
#15003=DIRECTION ( 'NONE',  ( 0.3865475372811021382, 0.8598319252293097348, 0.3335716741247277684 ) ) ;
#15004=ORIENTED_EDGE ( 'NONE', *, *, #41731, .F. ) ;
#15008=CARTESIAN_POINT ( 'NONE',  ( 2.827825597296804272, -8.965636292765729820, 1.027532345921656765 ) ) ;
#15009=ORIENTED_EDGE ( 'NONE', *, *, #17943, .T. ) ;
#15012=CARTESIAN_POINT ( 'NONE',  ( 5.516018279890452902, 0.005976902763918716562, 0.003191189039764460479 ) ) ;
#15019=CARTESIAN_POINT ( 'NONE',  ( 0.3632410797595255758, -6.365652464380835873, -10.49990774419908490 ) ) ;
#15020=B_SPLINE_CURVE_WITH_KNOTS ( 'NONE', 3,
 ( #59916, #39279, #59576, #29311, #14009, #54611, #9033, #24316, #44581, #64867, #14336, #9332, #65212, #55233, #39938, #14643 ),
 .UNSPECIFIED., .F., .F.,
 ( 4, 3, 3, 3, 3, 4 ),
 ( 0.000000000000000000, 0.0002176109881720223165, 0.0004352086762394594198, 0.0006528017811446865321, 0.0007615147961451690243, 0.0009453342004947184150 ),
 .UNSPECIFIED. ) ;
#15026=CARTESIAN_POINT ( 'NONE',  ( 1.633930747252548388, -6.963441708414224607, -10.62371422070959781 ) ) ;
#15032=CARTESIAN_POINT ( 'NONE',  ( 2.242418902651940549, 5.783980263416092171, -4.983487297755500478 ) ) ;
#15034=CARTESIAN_POINT ( 'NONE',  ( 0.2648978790185593790, -4.063980959784970537, -11.55204314799267884 ) ) ;
#15041=ORIENTED_EDGE ( 'NONE', *, *, #2939, .T. ) ;
#15042=CARTESIAN_POINT ( 'NONE',  ( 0.7400311444011692386, -12.39937114182725253, 0.3548322008126636451 ) ) ;
#15043=LINE ( 'NONE', #54332, #63374 ) ;
#15050=DIRECTION ( 'NONE',  ( -1.000000000000000000, -0.000000000000000000, -0.000000000000000000 ) ) ;
#15056=CARTESIAN_POINT ( 'NONE',  ( 0.7446945582509254535, 12.15064199164585546, 2.504154979875858000 ) ) ;
#15059=B_SPLINE_CURVE_WITH_KNOTS ( 'NONE', 3,
 ( #50063, #24792, #40061, #15458, #56019, #60350, #65652, #40386, #30736, #20780 ),
 .UNSPECIFIED., .F., .F.,
 ( 4, 3, 3, 4 ),
 ( 1.517883041479706208E-18, 6.607638129004506501E-05, 9.911389841680592731E-05, 0.0001667630577588618504 ),
 .UNSPECIFIED. ) ;
#15066=EDGE_CURVE ( 'NONE', #61002, #36996, #28681, .T. ) ;
#15067=ORIENTED_EDGE ( 'NONE', *, *, #9295, .T. ) ;
#15068=CARTESIAN_POINT ( 'NONE',  ( 2.255723233588952770, 6.680843247642368254, -3.704537245404970314 ) ) ;
#15082=ORIENTED_EDGE ( 'NONE', *, *, #47164, .T. ) ;
#15086=ORIENTED_EDGE ( 'NONE', *, *, #41142, .F. ) ;
#15093=CARTESIAN_POINT ( 'NONE',  ( 0.2869720083484325057, -6.306330337780580386, 10.50600528807145118 ) ) ;
#15107=CARTESIAN_POINT ( 'NONE',  ( 0.3002738374340929162, 9.533456882268753318, -7.705051734330175428 ) ) ;
#15110=CARTESIAN_POINT ( 'NONE',  ( 2.770579946183334918, 7.739026583264748460, -1.056759439485493335 ) ) ;
#15115=ORIENTED_EDGE ( 'NONE', *, *, #15204, .T. ) ;
#15118=ORIENTED_EDGE ( 'NONE', *, *, #1523, .F. ) ;
#15121=LINE ( 'NONE', #33845, #56477 ) ;
#15124=CARTESIAN_POINT ( 'NONE',  ( 2.241352910868908310, 7.633946224498473931, 0.08337961031706864201 ) ) ;
#15131=( BOUNDED_SURFACE ( )  B_SPLINE_SURFACE ( 3, 1, ( 
 ( #58457, #49147 ),
 ( #53478, #3913 ),
 ( #23534, #43460 ),
 ( #18870, #18569 ) ),
 .UNSPECIFIED., .F., .F., .F. ) 
 B_SPLINE_SURFACE_WITH_KNOTS ( ( 4, 4 ),
 ( 2, 2 ),
 ( 0.000000000000000000, 1.000000000000000000 ),
 ( 0.000000000000000000, 1.000000000000000000 ),
 .UNSPECIFIED. ) 
 GEOMETRIC_REPRESENTATION_ITEM ( )  RATIONAL_B_SPLINE_SURFACE ( (
 ( 1.000000000000000000, 1.000000000000000000),
 ( 0.6933888150995267674, 0.9895912004443193632),
 ( 0.6933888150995267674, 0.9895912004443193632),
 ( 1.000000000000000000, 1.000000000000000000) ) ) 
 REPRESENTATION_ITEM ( '' )  SURFACE ( )  );
#15144=CARTESIAN_POINT ( 'NONE',  ( 2.717984159219211104, 6.148373979318834337, 4.788867404453586829 ) ) ;
#15150=B_SPLINE_CURVE_WITH_KNOTS ( 'NONE', 3,
 ( #41249, #11652, #15973, #1035, #21305, #52246, #6687, #31293, #16972, #17313, #57894, #37246, #26958 ),
 .UNSPECIFIED., .F., .F.,
 ( 4, 3, 3, 3, 4 ),
 ( 2.602085213965210642E-18, 6.607593386745474117E-05, 0.0001321518677373518646, 0.0001982171734706210224, 0.0002642860854759482834 ),
 .UNSPECIFIED. ) ;
#15152=FACE_OUTER_BOUND ( 'NONE', #63189, .T. ) ;
#15154=DIRECTION ( 'NONE',  ( -1.000000000000000000, -0.000000000000000000, -0.000000000000000000 ) ) ;
#15155=CARTESIAN_POINT ( 'NONE',  ( 2.507146904658057451, 6.577532285019759506, 4.047319006787481577 ) ) ;
#15169=VECTOR ( 'NONE', #11554, 1000.000000000000227 ) ;
#15175=CARTESIAN_POINT ( 'NONE',  ( 0.3675815128205912052, 7.689697408877274931, 9.574637318041988365 ) ) ;
#15179=CARTESIAN_POINT ( 'NONE',  ( 0.2956976708475453908, -11.44006538352183533, -4.397965666276546060 ) ) ;
#15183=CARTESIAN_POINT ( 'NONE',  ( 2.241352910868908754, 2.689314586382447914, -7.145045428366549878 ) ) ;
#15185=ORIENTED_EDGE ( 'NONE', *, *, #51663, .T. ) ;
#15190=CARTESIAN_POINT ( 'NONE',  ( 0.2956976708475421711, 11.44006538352186020, 4.397965666276463459 ) ) ;
#15199=CARTESIAN_POINT ( 'NONE',  ( 0.3675815128205912052, -12.27743992903065973, -0.2638082659429707988 ) ) ;
#15202=CARTESIAN_POINT ( 'NONE',  ( 5.516018279890452902, 0.004180585980734530596, -0.005331956019561480582 ) ) ;
#15203=CARTESIAN_POINT ( 'NONE',  ( 2.280717697723838366, 7.131299706077064648, -2.762096098144267042 ) ) ;
#15204=EDGE_CURVE ( 'NONE', #14946, #4245, #60699, .T. ) ;
#15209=CARTESIAN_POINT ( 'NONE',  ( 2.276198483117261695, -1.479169956994117241, 7.501576331167729705 ) ) ;
#15211=CARTESIAN_POINT ( 'NONE',  ( 3.152665057735716037, -2.258875078500806044, 7.609997527621833235 ) ) ;
#15221=B_SPLINE_CURVE_WITH_KNOTS ( 'NONE', 3,
 ( #15820, #56403, #31139, #51449, #46429, #874, #21147, #41419, #27779, #48413, #3184, #33432, #32103, #57739, #58054, #52421 ),
 .UNSPECIFIED., .F., .F.,
 ( 4, 3, 3, 3, 3, 4 ),
 ( 0.000000000000000000, 0.0003017745587525252470, 0.0006035491769808760173, 0.0009053241094668197176, 0.001207275924539396922, 0.001510325902531781811 ),
 .UNSPECIFIED. ) ;
#15229=CARTESIAN_POINT ( 'NONE',  ( 2.717984159219388740, -7.719081760284177030, -1.073093837952627361 ) ) ;
#15234=LINE ( 'NONE', #6257, #37776 ) ;
#15241=ORIENTED_EDGE ( 'NONE', *, *, #11700, .T. ) ;
#15243=CARTESIAN_POINT ( 'NONE',  ( 1.937114397841932290, 12.76557247859000555, -1.334979369128294291 ) ) ;
#15245=CARTESIAN_POINT ( 'NONE',  ( 0.2651627923886309968, 12.24583724871548540, 0.08809136839520097240 ) ) ;
#15252=ORIENTED_EDGE ( 'NONE', *, *, #32394, .F. ) ;
#15254=CARTESIAN_POINT ( 'NONE',  ( 0.2646305136544065406, -1.996350543472912076, -12.08286001766537510 ) ) ;
#15257=CARTESIAN_POINT ( 'NONE',  ( 2.249013661412228249, -6.552953334857887668, -3.921976945965406358 ) ) ;
#15261=CARTESIAN_POINT ( 'NONE',  ( 0.4613984246114886667, 9.246873830556006979, -8.128335150814411492 ) ) ;
#15263=CARTESIAN_POINT ( 'NONE',  ( 0.2646305136544065406, -7.770320294339109424, -9.465888453933038349 ) ) ;
#15264=CARTESIAN_POINT ( 'NONE',  ( 1.109979610370706027, -12.51859925746133051, -0.4797593171730065165 ) ) ;
#15265=ORIENTED_EDGE ( 'NONE', *, *, #56521, .F. ) ;
#15268=CARTESIAN_POINT ( 'NONE',  ( 1.634816307076136122, -11.34285134320839816, 5.718391684266176611 ) ) ;
#15270=CARTESIAN_POINT ( 'NONE',  ( 1.948354844646524642, -9.612178954896725358, -7.125078658759304240 ) ) ;
#15278=FACE_OUTER_BOUND ( 'NONE', #49319, .T. ) ;
#15281=ORIENTED_EDGE ( 'NONE', *, *, #26804, .F. ) ;
#15290=CARTESIAN_POINT ( 'NONE',  ( 2.653899356899400264, -5.782420802795832593, 5.192946150929120819 ) ) ;
#15306=CARTESIAN_POINT ( 'NONE',  ( 0.3053067050349138056, -10.73055518945191800, 5.928821939311894162 ) ) ;
#15307=CARTESIAN_POINT ( 'NONE',  ( 5.520433897694421610, 0.01120198501134884658, -0.01006947824912454194 ) ) ;
#15314=CARTESIAN_POINT ( 'NONE',  ( 0.2872850955227753134, 10.71476594226533763, 5.944938343726287933 ) ) ;
#15317=CARTESIAN_POINT ( 'NONE',  ( 2.261269890821706596, -3.699080366006974874, -6.685978463721846232 ) ) ;
#15326=CARTESIAN_POINT ( 'NONE',  ( 2.705197763288543999, 3.649695155981514727, 6.881024880055361947 ) ) ;
#15330=CARTESIAN_POINT ( 'NONE',  ( 0.2653141617321010393, -2.169890202573276472, 12.05243138604825148 ) ) ;
#15331=CARTESIAN_POINT ( 'NONE',  ( 5.516018279890452902, -0.006440244342253015342, -0.002104829434640740401 ) ) ;
#15340=( BOUNDED_SURFACE ( )  B_SPLINE_SURFACE ( 3, 1, ( 
 ( #28632, #48937 ),
 ( #9012, #55554 ),
 ( #19658, #55211 ),
 ( #54586, #9997 ) ),
 .UNSPECIFIED., .F., .F., .F. ) 
 B_SPLINE_SURFACE_WITH_KNOTS ( ( 4, 4 ),
 ( 2, 2 ),
 ( 0.000000000000000000, 1.000000000000000000 ),
 ( 0.000000000000000000, 1.000000000000000000 ),
 .UNSPECIFIED. ) 
 GEOMETRIC_REPRESENTATION_ITEM ( )  RATIONAL_B_SPLINE_SURFACE ( (
 ( 1.000000000000000000, 1.000000000000000000),
 ( 0.9942764183789327692, 0.8450855930916585379),
 ( 0.9942764183789327692, 0.8450855930916585379),
 ( 1.000000000000000000, 1.000000000000000000) ) ) 
 REPRESENTATION_ITEM ( '' )  SURFACE ( )  );
#15341=CARTESIAN_POINT ( 'NONE',  ( 5.515188684475870851, 0.0005703990286342820910, 0.005320786921497272677 ) ) ;
#15343=CONICAL_SURFACE ( 'NONE', #23859, 7.580821595991582562, 0.3217505529694035249 ) ;
#15348=CARTESIAN_POINT ( 'NONE',  ( 0.3040950598368144520, 8.072385578287596175, -9.229598020917608281 ) ) ;
#15350=CARTESIAN_POINT ( 'NONE',  ( 2.305787727787083519, -6.545285700970500109, -3.971363876084033961 ) ) ;
#15352=DIRECTION ( 'NONE',  ( 0.000000000000000000, 0.000000000000000000, 1.000000000000000000 ) ) ;
#15354=CARTESIAN_POINT ( 'NONE',  ( 2.034671305879984349, -11.60021725667404624, 1.331347915349250233 ) ) ;
#15356=CARTESIAN_POINT ( 'NONE',  ( 2.260457164927716978, 4.804526096742694818, -5.941202713844608851 ) ) ;
#15367=B_SPLINE_CURVE_WITH_KNOTS ( 'NONE', 3,
 ( #42292, #46655, #16411, #46340, #16059, #780, #31674 ),
 .UNSPECIFIED., .F., .F.,
 ( 4, 3, 4 ),
 ( 9.707054739159190006E-15, 0.002398160485435410494, 0.005002426799386534319 ),
 .UNSPECIFIED. ) ;
#15370=CARTESIAN_POINT ( 'NONE',  ( 2.263328370261531219, 5.761609105518052942, -5.019946231381251067 ) ) ;
#15372=CARTESIAN_POINT ( 'NONE',  ( 0.3053067050349155820, -3.975408458060438299, -11.59706307017086857 ) ) ;
#15379=CARTESIAN_POINT ( 'NONE',  ( 0.3675815128205894289, -4.447030445008257615, 11.44679196252407927 ) ) ;
#15384=CARTESIAN_POINT ( 'NONE',  ( 1.194176325881337597, -12.54527478469375801, 0.5141316333310796960 ) ) ;
#15385=CARTESIAN_POINT ( 'NONE',  ( 0.3040950598368152291, 10.74226959800791370, 5.912066680610649883 ) ) ;
#15390=EDGE_CURVE ( 'NONE', #14439, #6208, #42028, .T. ) ;
#15391=ORIENTED_EDGE ( 'NONE', *, *, #62654, .T. ) ;
#15392=CARTESIAN_POINT ( 'NONE',  ( 1.547277799339151105, -11.29700934613339669, -5.744300480442161572 ) ) ;
#15397=ORIENTED_EDGE ( 'NONE', *, *, #35011, .T. ) ;
#15408=CARTESIAN_POINT ( 'NONE',  ( 1.462291587750753630, -3.724645088506430834, -12.08418494300916279 ) ) ;
#15411=CARTESIAN_POINT ( 'NONE',  ( 0.3665391374699472626, -10.76665847464308534, -5.911453292029715811 ) ) ;
#15416=CARTESIAN_POINT ( 'NONE',  ( 0.3665391374699465965, 5.911453292029754003, -10.76665847464306403 ) ) ;
#15421=VERTEX_POINT ( 'NONE', #32224 ) ;
#15434=EDGE_LOOP ( 'NONE', ( #21529, #24201, #35116, #3694 ) ) ;
#15437=DIRECTION ( 'NONE',  ( -0.3865475372811021937, 0.6075346789811162385, 0.6938894834606063045 ) ) ;
#15449=EDGE_CURVE ( 'NONE', #38095, #5162, #53105, .T. ) ;
#15452=VERTEX_POINT ( 'NONE', #64437 ) ;
#15455=ORIENTED_EDGE ( 'NONE', *, *, #18326, .T. ) ;
#15458=CARTESIAN_POINT ( 'NONE',  ( 2.241526690369555208, 1.342748965918883597, 7.515450538999841612 ) ) ;
#15460=CARTESIAN_POINT ( 'NONE',  ( 2.251139882113959434, 7.636654603229073857, 0.1241612276496930622 ) ) ;
#15464=EDGE_CURVE ( 'NONE', #20267, #19209, #61817, .T. ) ;
#15467=CARTESIAN_POINT ( 'NONE',  ( 2.305787727787085295, 7.508843116234176662, -1.493241775258346227 ) ) ;
#15474=CARTESIAN_POINT ( 'NONE',  ( 1.549075743846762387, 2.862200647102950857, -12.34675572956577660 ) ) ;
#15479=CARTESIAN_POINT ( 'NONE',  ( 3.152665057736245391, 2.258875078500370837, -7.609997527622033076 ) ) ;
#15480=CARTESIAN_POINT ( 'NONE',  ( 5.514624014163232779, 0.004137701579365773812, -0.0001700579043838819533 ) ) ;
#15484=CARTESIAN_POINT ( 'NONE',  ( 5.514970785353741078, 0.004324946436530184915, 0.001897634820904495461 ) ) ;
#15485=CARTESIAN_POINT ( 'NONE',  ( 2.242819959140645025, 1.224821922055974177, 7.536009875295339278 ) ) ;
#15487=CARTESIAN_POINT ( 'NONE',  ( 0.3675815128205912052, -6.367184624550238148, 10.50067073900649461 ) ) ;
#15490=CARTESIAN_POINT ( 'NONE',  ( 2.994568964204208594, 0.9739368093814753102, 7.825096839971880769 ) ) ;
#15494=CARTESIAN_POINT ( 'NONE',  ( 2.589278595513413439, -7.361833592938442195, -2.423168677231957613 ) ) ;
#15500=CARTESIAN_POINT ( 'NONE',  ( 0.7446945582528449181, -1.802628359587426621, -12.27434006248856235 ) ) ;
#15503=CARTESIAN_POINT ( 'NONE',  ( 0.3632410797595273522, 11.44577450250092632, -4.445654054452411685 ) ) ;
#15506=ORIENTED_EDGE ( 'NONE', *, *, #9156, .F. ) ;
#15507=( NAMED_UNIT ( * ) SI_UNIT ( $, .STERADIAN. ) SOLID_ANGLE_UNIT ( ) );
#15509=CARTESIAN_POINT ( 'NONE',  ( 2.781367136452630451, 1.659348694504713562, 7.636197200465927537 ) ) ;
#15520=CARTESIAN_POINT ( 'NONE',  ( 2.273267844204863941, -7.234348261136791969, -2.472013099045105022 ) ) ;
#15524=CARTESIAN_POINT ( 'NONE',  ( 1.937114397841935398, 5.226660192101590496, 11.72279974487465459 ) ) ;
#15526=LINE ( 'NONE', #591, #53919 ) ;
#15539=CARTESIAN_POINT ( 'NONE',  ( 2.350038591458241566, 9.744161863086068465, 4.227970903880576614 ) ) ;
#15552=CARTESIAN_POINT ( 'NONE',  ( 0.2648978790185584908, -12.08224454301450201, 1.996248716311589400 ) ) ;
#15553=LINE ( 'NONE', #10557, #41375 ) ;
#15556=CARTESIAN_POINT ( 'NONE',  ( 0.3040950598368152291, 9.552450779732110320, 7.687624643091462318 ) ) ;
#15558=CARTESIAN_POINT ( 'NONE',  ( 0.9232167919969122005, -1.756271097262150027, 12.34114433434356961 ) ) ;
#15560=CARTESIAN_POINT ( 'NONE',  ( 5.530133899448235191, 0.001124651387254991695, 0.01594518557925637264 ) ) ;
#15565=CARTESIAN_POINT ( 'NONE',  ( 0.3164563675027623479, -0.2404665832030537798, -12.26087493884172019 ) ) ;
#15570=ORIENTED_EDGE ( 'NONE', *, *, #20445, .F. ) ;
#15572=CARTESIAN_POINT ( 'NONE',  ( 5.514970785353741078, -0.004532877335078326457, 0.001326349372336564462 ) ) ;
#15575=CARTESIAN_POINT ( 'NONE',  ( 0.2638984909335720941, -0.1991813963113141794, -12.24571285024409129 ) ) ;
#15576=FACE_OUTER_BOUND ( 'NONE', #11986, .T. ) ;
#15583=CARTESIAN_POINT ( 'NONE',  ( 1.719304012341584365, 10.22720798541559439, -7.581471372738991299 ) ) ;
#15587=CARTESIAN_POINT ( 'NONE',  ( 0.3665391374699464300, 9.576575648339126445, -7.691255657244195909 ) ) ;
#15607=VERTEX_POINT ( 'NONE', #52036 ) ;
#15610=DIRECTION ( 'NONE',  ( 1.000000000000000000, 0.000000000000000000, 0.000000000000000000 ) ) ;
#15611=CARTESIAN_POINT ( 'NONE',  ( 2.253265082352433613, 2.732639326785903489, -7.132841660187132504 ) ) ;
#15619=CARTESIAN_POINT ( 'NONE',  ( 1.462291587751620714, 10.08151577215017447, -7.633056170897675408 ) ) ;
#15627=CARTESIAN_POINT ( 'NONE',  ( 0.2717059086739003759, 10.69429229731978026, 5.971041827598861040 ) ) ;
#15629=EDGE_CURVE ( 'NONE', #19799, #31314, #32057, .T. ) ;
#15630=CARTESIAN_POINT ( 'NONE',  ( 2.242819959140599284, -3.728423299585179151, -6.662619100654629811 ) ) ;
#15631=CARTESIAN_POINT ( 'NONE',  ( 2.241536586108912488, 7.519576125149805002, 1.319514354261222211 ) ) ;
#15632=ORIENTED_EDGE ( 'NONE', *, *, #35470, .F. ) ;
#15633=CARTESIAN_POINT ( 'NONE',  ( 1.948354844646327688, 5.347695345042151160, -10.70340528295104399 ) ) ;
#15637=CARTESIAN_POINT ( 'NONE',  ( 2.770579946183327813, 3.639932028439821998, 6.910873157406250300 ) ) ;
#15640=CARTESIAN_POINT ( 'NONE',  ( 1.452237505248555660, -4.880303821310934431, -11.67686475128084567 ) ) ;
#15641=CARTESIAN_POINT ( 'NONE',  ( 2.276905613633648517, -5.955225895210555009, -4.795880183929630114 ) ) ;
#15654=FACE_OUTER_BOUND ( 'NONE', #33888, .T. ) ;
#15657=VERTEX_POINT ( 'NONE', #28391 ) ;
#15668=CARTESIAN_POINT ( 'NONE',  ( 0.2958664285830455154, -6.318165763623551534, -10.50235171906346388 ) ) ;
#15686=CARTESIAN_POINT ( 'NONE',  ( 3.100650473569726007, -5.767490999797071360, -5.429218121582424672 ) ) ;
#15688=CARTESIAN_POINT ( 'NONE',  ( 0.2739690278137239532, 8.012873994335690142, 9.264642836915861324 ) ) ;
#15707=( BOUNDED_SURFACE ( )  B_SPLINE_SURFACE ( 3, 1, ( 
 ( #39774, #9833 ),
 ( #38800, #19825 ),
 ( #39435, #28815 ),
 ( #44412, #30125 ) ),
 .UNSPECIFIED., .F., .F., .F. ) 
 B_SPLINE_SURFACE_WITH_KNOTS ( ( 4, 4 ),
 ( 2, 2 ),
 ( 0.000000000000000000, 1.000000000000000000 ),
 ( 0.000000000000000000, 1.000000000000000000 ),
 .UNSPECIFIED. ) 
 GEOMETRIC_REPRESENTATION_ITEM ( )  RATIONAL_B_SPLINE_SURFACE ( (
 ( 1.000000000000000000, 1.000000000000000000),
 ( 0.6933888150995267674, 0.9895912004443193632),
 ( 0.6933888150995267674, 0.9895912004443193632),
 ( 1.000000000000000000, 1.000000000000000000) ) ) 
 REPRESENTATION_ITEM ( '' )  SURFACE ( )  );
#15714=DIRECTION ( 'NONE',  ( -1.000000000000000000, -0.000000000000000000, -0.000000000000000000 ) ) ;
#15718=CARTESIAN_POINT ( 'NONE',  ( 0.2646305136544072623, 9.296005949277228453, 7.972778379581582975 ) ) ;
#15722=CARTESIAN_POINT ( 'NONE',  ( 0.5572780756278413739, 10.53376864352694042, 6.434474476007812527 ) ) ;
#15726=CARTESIAN_POINT ( 'NONE',  ( 5.515539859299206427, -0.005618668168217476680, 0.002251761459665986825 ) ) ;
#15735=CARTESIAN_POINT ( 'NONE',  ( 0.3665391374699472626, -7.691255657244357558, 9.576575648338993219 ) ) ;
#15739=CARTESIAN_POINT ( 'NONE',  ( 0.2646305136544065406, 4.064188116014548768, 11.55263159009959750 ) ) ;
#15748=ORIENTED_EDGE ( 'NONE', *, *, #64353, .F. ) ;
#15756=CARTESIAN_POINT ( 'NONE',  ( 3.152665057736003362, 6.378477742801834438, 4.725420687649379836 ) ) ;
#15757=CARTESIAN_POINT ( 'NONE',  ( 2.963017218115625795, 7.812878240621082604, -0.9869543242667312422 ) ) ;
#15758=CARTESIAN_POINT ( 'NONE',  ( 0.7446945582511041994, -2.504154979875959253, 12.15064199164589986 ) ) ;
#15764=EDGE_LOOP ( 'NONE', ( #45911, #41756, #9342, #59868 ) ) ;
#15768=CARTESIAN_POINT ( 'NONE',  ( 0.3675815128205894289, -10.50067073900656212, 6.367184624550128014 ) ) ;
#15771=CARTESIAN_POINT ( 'NONE',  ( 1.547277799338578230, -12.34637640861317820, 2.861188171558898929 ) ) ;
#15779=CARTESIAN_POINT ( 'NONE',  ( 2.305787727787083519, 2.461236246751071555, 7.249469779319919205 ) ) ;
#15780=EDGE_CURVE ( 'NONE', #54088, #14585, #46000, .T. ) ;
#15787=CARTESIAN_POINT ( 'NONE',  ( 3.152665057734095555, 3.546019893116337141, 7.102135024645864547 ) ) ;
#15789=CARTESIAN_POINT ( 'NONE',  ( 0.2648978790185593790, 10.67083876753491900, 6.008231198269021078 ) ) ;
#15793=CARTESIAN_POINT ( 'NONE',  ( 2.705197763288547996, -6.601241161176654160, -4.134294772209995195 ) ) ;
#15796=EDGE_CURVE ( 'NONE', #55428, #6208, #4732, .T. ) ;
#15800=CARTESIAN_POINT ( 'NONE',  ( 2.249013661412229581, 1.207748565003235575, 7.540851674528672888 ) ) ;
#15812=CARTESIAN_POINT ( 'NONE',  ( 2.368238019615253709, -7.273245349264763071, -2.455958560214716258 ) ) ;
#15818=CARTESIAN_POINT ( 'NONE',  ( -14.47334165536100059, 0.000000000000000000, -1.000000000000000000 ) ) ;
#15820=CARTESIAN_POINT ( 'NONE',  ( 0.3675815128205894289, 0.2638082659428422350, 12.27743992903066328 ) ) ;
#15823=CARTESIAN_POINT ( 'NONE',  ( 2.241352910868908310, -4.970878533273800137, 5.794346703933830334 ) ) ;
#15825=CARTESIAN_POINT ( 'NONE',  ( 1.719304012340734822, -5.690355757825686922, -11.38834240361529737 ) ) ;
#15837=VERTEX_POINT ( 'NONE', #34361 ) ;
#15838=CARTESIAN_POINT ( 'NONE',  ( 5.515539859299206427, 0.004037661319610825333, -0.004509673239148351796 ) ) ;
#15844=CARTESIAN_POINT ( 'NONE',  ( 2.963017218115628015, -7.812878240621079051, 0.9869543242667844218 ) ) ;
#15853=FACE_OUTER_BOUND ( 'NONE', #33754, .T. ) ;
#15857=ORIENTED_EDGE ( 'NONE', *, *, #38292, .T. ) ;
#15859=ORIENTED_EDGE ( 'NONE', *, *, #5267, .F. ) ;
#15865=LINE ( 'NONE', #31506, #20319 ) ;
#15870=CARTESIAN_POINT ( 'NONE',  ( 1.462291587749843691, -12.54737685278368353, 1.569662666436692389 ) ) ;
#15895=( BOUNDED_SURFACE ( )  B_SPLINE_SURFACE ( 3, 1, ( 
 ( #42273, #32317 ),
 ( #42957, #42604 ),
 ( #53274, #7057 ),
 ( #28009, #37650 ) ),
 .UNSPECIFIED., .F., .F., .F. ) 
 B_SPLINE_SURFACE_WITH_KNOTS ( ( 4, 4 ),
 ( 2, 2 ),
 ( 0.000000000000000000, 1.000000000000000000 ),
 ( 0.000000000000000000, 1.000000000000000000 ),
 .UNSPECIFIED. ) 
 GEOMETRIC_REPRESENTATION_ITEM ( )  RATIONAL_B_SPLINE_SURFACE ( (
 ( 1.000000000000000000, 1.000000000000000000),
 ( 0.9942764183789327692, 0.8450855930916580938),
 ( 0.9942764183789327692, 0.8450855930916580938),
 ( 1.000000000000000000, 1.000000000000000000) ) ) 
 REPRESENTATION_ITEM ( '' )  SURFACE ( )  );
#15897=DIRECTION ( 'NONE',  ( 0.000000000000000000, 0.000000000000000000, 1.000000000000000000 ) ) ;
#15902=CARTESIAN_POINT ( 'NONE',  ( 0.9296196016868064627, 12.34355205587819171, -1.754499435239005756 ) ) ;
#15907=CARTESIAN_POINT ( 'NONE',  ( 0.5572780756290103277, 4.507550621618655384, -11.49107179558557412 ) ) ;
#15909=CARTESIAN_POINT ( 'NONE',  ( 3.152665057736163678, 7.923639299009212600, -0.4801242025614006481 ) ) ;
#15918=EDGE_LOOP ( 'NONE', ( #33634, #6064, #55265, #8498, #35976, #60986, #15009, #18954, #8622, #64024, #62458, #37604, #21436, #36469, #19400, #61395, #22549, #46026, #10348, #18723, #26863, #44141, #59583, #37096, #4980, #6135, #51696, #57669, #37134, #59769, #57565, #43975, #61575, #970, #35394, #7348, #13337, #41342, #23921, #45987, #21744, #7660, #24998, #35222, #22216, #55719, #20763, #26934, #712, #32925, #7634, #51045, #23977, #43364, #55688, #52426, #12315, #8647, #11420, #28487, #8068, #10085, #27066, #40216, #54465, #32521, #28848, #49600, #56517, #9307, #35055, #62459, #49439, #5125, #37282, #57370, #51226, #55176, #62444, #20934, #2964, #16772, #18121, #13875, #19919, #33433, #64833, #26803, #53808, #23018, #38684, #8778, #58365, #42815, #3450, #25751, #14857, #61513, #6453, #36320, #35023, #28143, #55107, #56503, #24160, #45248, #29643, #59238, #53186, #63257, #3395, #39713 ) ) ;
#15929=DIRECTION ( 'NONE',  ( 0.3939253465568944290, -0.4679616473074953431, 0.7910971609033152774 ) ) ;
#15930=CARTESIAN_POINT ( 'NONE',  ( 2.249013661412229581, 2.724484898587385739, -7.134443398813845150 ) ) ;
#15937=CARTESIAN_POINT ( 'NONE',  ( 5.514970785353741078, 0.0005190732562558549642, 0.004694330894494371832 ) ) ;
#15939=CARTESIAN_POINT ( 'NONE',  ( 2.827825597296807381, -4.031992772938934877, -8.073505504738399452 ) ) ;
#15940=CARTESIAN_POINT ( 'NONE',  ( 2.639814597422738718, -7.763021810282388913, -0.2564041122425915198 ) ) ;
#15941=B_SPLINE_CURVE_WITH_KNOTS ( 'NONE', 3,
 ( #6739, #63231, #62558, #52932, #7366, #27014, #42267 ),
 .UNSPECIFIED., .F., .F.,
 ( 4, 3, 4 ),
 ( 5.151706802971572009E-15, 0.002398160485434644180, 0.005002426799381929495 ),
 .UNSPECIFIED. ) ;
#15949=CARTESIAN_POINT ( 'NONE',  ( 2.305787727787085295, 5.970480882365287734, -4.792270232040832134 ) ) ;
#15950=CARTESIAN_POINT ( 'NONE',  ( 2.653899356899655171, 4.109946795501193684, 6.596318473603771437 ) ) ;
#15955=CARTESIAN_POINT ( 'NONE',  ( 0.8320506296491554377, 5.883188144889929916, -10.95539209551940907 ) ) ;
#15961=CARTESIAN_POINT ( 'NONE',  ( 0.2739690278137261736, 12.24770428423990687, -0.1830199730327832508 ) ) ;
#15963=AXIS2_PLACEMENT_3D ( 'NONE', #58460, #23536, #17888 ) ;
#15973=CARTESIAN_POINT ( 'NONE',  ( 0.2651627923886306082, 2.039714259676174812, 12.07509237025071691 ) ) ;
#15983=ADVANCED_FACE ( 'NONE', ( #42264 ), #56928, .F. ) ;
#15996=CARTESIAN_POINT ( 'NONE',  ( 2.242819959140781805, 7.138786956203901468, 2.707278038035910939 ) ) ;
#16012=CARTESIAN_POINT ( 'NONE',  ( 1.719304012338199517, 0.000000000000000000, 0.000000000000000000 ) ) ;
#16015=CARTESIAN_POINT ( 'NONE',  ( 2.903928887688777660, 8.407112942775256670, 2.496183838365350738 ) ) ;
#16016=ORIENTED_EDGE ( 'NONE', *, *, #54064, .F. ) ;
#16018=CARTESIAN_POINT ( 'NONE',  ( 2.835339799623989521, -5.783398714696522447, -5.281994181469054972 ) ) ;
#16019=EDGE_LOOP ( 'NONE', ( #26921, #60652, #51691, #9545 ) ) ;
#16021=CARTESIAN_POINT ( 'NONE',  ( 0.5572780756290403037, 11.70006938410089248, -3.933334466452371725 ) ) ;
#16052=EDGE_CURVE ( 'NONE', #63452, #13640, #28637, .T. ) ;
#16056=DIRECTION ( 'NONE',  ( -0.3865475372811021382, 0.7187975063895682970, 0.5778504531711067260 ) ) ;
#16059=CARTESIAN_POINT ( 'NONE',  ( 2.655192694323234459, -5.716669423976344255, 7.714239566602159037 ) ) ;
#16063=CARTESIAN_POINT ( 'NONE',  ( 3.152665057734040488, 0.000000000000000000, 0.000000000000000000 ) ) ;
#16064=AXIS2_PLACEMENT_3D ( 'NONE', #41497, #60478, #35199 ) ;
#16067=CARTESIAN_POINT ( 'NONE',  ( 0.2671309869109492752, -5.982543484153297619, 10.68612389951475627 ) ) ;
#16068=EDGE_LOOP ( 'NONE', ( #46409, #33013, #35515, #5660 ) ) ;
#16076=EDGE_CURVE ( 'NONE', #59854, #23038, #42798, .T. ) ;
#16085=CARTESIAN_POINT ( 'NONE',  ( 0.2652384529303126182, -12.07141085622971843, -2.061422456317149265 ) ) ;
#16088=CARTESIAN_POINT ( 'NONE',  ( 5.520433897694421610, -0.003119431460922313538, -0.01473594271720287882 ) ) ;
#16098=ORIENTED_EDGE ( 'NONE', *, *, #13278, .T. ) ;
#16114=CARTESIAN_POINT ( 'NONE',  ( 1.719304012340549859, -10.62216384465898500, -7.017415949616274240 ) ) ;
#16121=( BOUNDED_SURFACE ( )  B_SPLINE_SURFACE ( 3, 1, ( 
 ( #4885, #24830 ),
 ( #25150, #220 ),
 ( #60390, #14813 ),
 ( #10495, #49770 ) ),
 .UNSPECIFIED., .F., .F., .F. ) 
 B_SPLINE_SURFACE_WITH_KNOTS ( ( 4, 4 ),
 ( 2, 2 ),
 ( 0.000000000000000000, 1.000000000000000000 ),
 ( 0.000000000000000000, 1.000000000000000000 ),
 .UNSPECIFIED. ) 
 GEOMETRIC_REPRESENTATION_ITEM ( )  RATIONAL_B_SPLINE_SURFACE ( (
 ( 1.000000000000000000, 1.000000000000000000),
 ( 0.9856612449720755231, 0.9999558406602322425),
 ( 0.9856612449720755231, 0.9999558406602322425),
 ( 1.000000000000000000, 1.000000000000000000) ) ) 
 REPRESENTATION_ITEM ( '' )  SURFACE ( )  );
#16131=B_SPLINE_CURVE_WITH_KNOTS ( 'NONE', 3,
 ( #33022, #63948, #54656, #64276, #38011, #14052, #13721, #48359, #33687, #44310, #54321, #3468, #59295 ),
 .UNSPECIFIED., .F., .F.,
 ( 4, 3, 3, 3, 4 ),
 ( 1.734723475976807094E-18, 6.607593386745445657E-05, 0.0001321518677373518917, 0.0001982171734706195316, 0.0002642860854759485545 ),
 .UNSPECIFIED. ) ;
#16148=ORIENTED_EDGE ( 'NONE', *, *, #38025, .T. ) ;
#16149=CARTESIAN_POINT ( 'NONE',  ( 2.241451721903217731, 7.634225434981125602, 0.06083185034798754831 ) ) ;
#16152=CARTESIAN_POINT ( 'NONE',  ( 2.255723233588952326, 1.196143347838711790, 7.544965460065571783 ) ) ;
#16160=CARTESIAN_POINT ( 'NONE',  ( 2.889800649504073782, 2.156828754871467968, 5.728825117897715202 ) ) ;
#16180=B_SPLINE_CURVE_WITH_KNOTS ( 'NONE', 3,
 ( #44265, #59911, #3749, #39274, #60219, #8370, #43954 ),
 .UNSPECIFIED., .F., .F.,
 ( 4, 3, 4 ),
 ( 5.561277602346480916E-15, 0.002398160485434703160, 0.005002426799382430830 ),
 .UNSPECIFIED. ) ;
#16181=DIRECTION ( 'NONE',  ( 0.000000000000000000, 0.000000000000000000, 1.000000000000000000 ) ) ;
#16183=CARTESIAN_POINT ( 'NONE',  ( 0.3040950598368144520, -10.49113473328026380, -6.347045025870875712 ) ) ;
#16186=ORIENTED_EDGE ( 'NONE', *, *, #16552, .T. ) ;
#16187=ORIENTED_EDGE ( 'NONE', *, *, #28893, .T. ) ;
#16200=VERTEX_POINT ( 'NONE', #40238 ) ;
#16204=EDGE_CURVE ( 'NONE', #60647, #8323, #27730, .T. ) ;
#16205=CARTESIAN_POINT ( 'NONE',  ( 2.573738926104378155, 4.074516960797472720, -6.586859681822621937 ) ) ;
#16208=CARTESIAN_POINT ( 'NONE',  ( 1.452237505248552996, 7.672309600508697258, 10.06489946308204786 ) ) ;
#16212=EDGE_CURVE ( 'NONE', #59842, #49890, #60233, .T. ) ;
#16218=CARTESIAN_POINT ( 'NONE',  ( 2.259830038565016963, 4.804964945109173158, 5.940579220577212105 ) ) ;
#16223=VECTOR ( 'NONE', #53948, 1000.000000000000114 ) ;
#16226=CARTESIAN_POINT ( 'NONE',  ( 1.719304012338836563, -1.452142814150213734, 12.64775761152536759 ) ) ;
#16227=DIRECTION ( 'NONE',  ( 0.000000000000000000, 0.000000000000000000, 1.000000000000000000 ) ) ;
#16230=CARTESIAN_POINT ( 'NONE',  ( 0.2759803524722200252, 6.288205958087932146, -10.51260004517005875 ) ) ;
#16231=CARTESIAN_POINT ( 'NONE',  ( 2.297017764050092392, 2.771707546665591604, 7.133399178907324334 ) ) ;
#16245=VERTEX_POINT ( 'NONE', #29944 ) ;
#16259=EDGE_CURVE ( 'NONE', #20729, #1896, #54253, .T. ) ;
#16267=DIRECTION ( 'NONE',  ( 0.000000000000000000, 0.000000000000000000, 1.000000000000000000 ) ) ;
#16269=ORIENTED_EDGE ( 'NONE', *, *, #15066, .T. ) ;
#16285=LINE ( 'NONE', #62803, #44413 ) ;
#16296=CARTESIAN_POINT ( 'NONE',  ( 0.4626703367448973814, 9.611037151103600351, -7.694993290995405744 ) ) ;
#16299=CARTESIAN_POINT ( 'NONE',  ( 0.9296196016852520394, -10.58347995892885862, -6.590257778218327367 ) ) ;
#16301=VERTEX_POINT ( 'NONE', #16303 ) ;
#16303=CARTESIAN_POINT ( 'NONE',  ( 0.2648978790185593790, -2.256510822326224464, 12.03635331166811540 ) ) ;
#16304=AXIS2_PLACEMENT_3D ( 'NONE', #22375, #17062, #41682 ) ;
#16307=CARTESIAN_POINT ( 'NONE',  ( 2.903928887688531191, 3.491800274468411569, 8.044738195288426041 ) ) ;
#16309=CIRCLE ( 'NONE', #366, 12.73084802173761787 ) ;
#16315=CARTESIAN_POINT ( 'NONE',  ( 0.2759803524722195811, 2.313459762622696925, -12.02930579076647000 ) ) ;
#16325=CARTESIAN_POINT ( 'NONE',  ( 2.262775599886254874, 0.1412024122916927804, -7.640237753423678058 ) ) ;
#16326=B_SPLINE_CURVE_WITH_KNOTS ( 'NONE', 3,
 ( #37890, #46893, #1352, #57205, #62489, #7292, #16634 ),
 .UNSPECIFIED., .F., .F.,
 ( 4, 3, 4 ),
 ( 7.634253333962453795E-15, 0.002398160485434851479, 0.005002426799384450916 ),
 .UNSPECIFIED. ) ;
#16337=ORIENTED_EDGE ( 'NONE', *, *, #16076, .F. ) ;
#16339=B_SPLINE_CURVE_WITH_KNOTS ( 'NONE', 3,
 ( #9602, #22723, #53644, #12711, #42985, #32995, #29900, #50208, #4665, #37678, #37990, #52307, #7722, #17029, #1758, #23339, #23020, #27653, #48622 ),
 .UNSPECIFIED., .F., .F.,
 ( 4, 3, 3, 3, 3, 3, 4 ),
 ( 8.523235939525396438E-18, 4.457896483014765320E-05, 6.639290541542085754E-05, 8.820687556478969962E-05, 0.0001100173248778915706, 0.0001545671401658112892, 0.0001830328308068612602 ),
 .UNSPECIFIED. ) ;
#16341=VERTEX_POINT ( 'NONE', #31576 ) ;
#16349=ORIENTED_EDGE ( 'NONE', *, *, #62032, .T. ) ;
#16353=ORIENTED_EDGE ( 'NONE', *, *, #32193, .T. ) ;
#16356=CARTESIAN_POINT ( 'NONE',  ( 1.719304012341583476, 7.581471372739232883, -10.22720798541541498 ) ) ;
#16365=CARTESIAN_POINT ( 'NONE',  ( 0.8375941296816619142, 6.548446001456726506, -10.57337970710577224 ) ) ;
#16376=CARTESIAN_POINT ( 'NONE',  ( 2.717984159219859475, 7.415470774237106433, 2.397195612260604403 ) ) ;
#16378=CARTESIAN_POINT ( 'NONE',  ( 0.9296196016851566712, 11.85136013469101890, -3.871279966919404458 ) ) ;
#16381=DIRECTION ( 'NONE',  ( -1.000000000000000000, -0.000000000000000000, -0.000000000000000000 ) ) ;
#16397=CARTESIAN_POINT ( 'NONE',  ( 2.655192694323989411, 0.5793947661801427396, 9.584054627287489581 ) ) ;
#16401=CARTESIAN_POINT ( 'NONE',  ( 0.2759803524722218571, -5.960075719898764390, -10.70204612651783549 ) ) ;
#16402=CARTESIAN_POINT ( 'NONE',  ( 0.2655924914740778187, 4.147079829127255479, 11.52280271232872089 ) ) ;
#16403=CARTESIAN_POINT ( 'NONE',  ( 2.266490820343223245, -5.760233951938548813, 5.023127813992176449 ) ) ;
#16411=CARTESIAN_POINT ( 'NONE',  ( 2.177405672430794414, -6.668684901900762796, 8.997150696571290851 ) ) ;
#16414=ORIENTED_EDGE ( 'NONE', *, *, #49142, .F. ) ;
#16419=CARTESIAN_POINT ( 'NONE',  ( 0.2915757698887287419, -5.940579417090853021, 10.71881693660620094 ) ) ;
#16423=ADVANCED_FACE ( 'NONE', ( #11310 ), #31459, .F. ) ;
#16426=CARTESIAN_POINT ( 'NONE',  ( 0.6511581176968108675, -11.51117493088908361, -4.541862140119740765 ) ) ;
#16431=CARTESIAN_POINT ( 'NONE',  ( 2.889800649504073782, -3.986129653162616471, -4.645655809191405083 ) ) ;
#16438=CARTESIAN_POINT ( 'NONE',  ( 0.2648978790185593790, 9.465406350830713578, -7.769924372105106336 ) ) ;
#16444=CARTESIAN_POINT ( 'NONE',  ( 2.245754705088394143, -7.635057163463319974, -0.1113317465207585011 ) ) ;
#16450=ORIENTED_EDGE ( 'NONE', *, *, #1091, .F. ) ;
#16452=CARTESIAN_POINT ( 'NONE',  ( 0.2657645697724694833, 12.03308811492268759, 2.275433120353130612 ) ) ;
#16456=B_SPLINE_CURVE_WITH_KNOTS ( 'NONE', 3,
 ( #5210, #559, #45763, #65693, #45426, #20500, #40784, #866, #61065, #15494, #51753, #35760, #41089, #61368, #15812, #56394 ),
 .UNSPECIFIED., .F., .F.,
 ( 4, 3, 3, 3, 3, 4 ),
 ( 2.948971425439945768E-15, 0.0002126834539179795619, 0.0004253519300366472239, 0.0006380165497224497828, 0.0007442707582428645472, 0.0009453531351415651613 ),
 .UNSPECIFIED. ) ;
#16466=CARTESIAN_POINT ( 'NONE',  ( 5.516018279890452902, 0.003191189039764439229, -0.005976902763918727837 ) ) ;
#16470=CARTESIAN_POINT ( 'NONE',  ( 0.3218525148189834151, 4.423735011438986398, -11.43947393562872605 ) ) ;
#16471=CARTESIAN_POINT ( 'NONE',  ( 1.937114397841935398, -9.228205347192510288, 8.920887662793440143 ) ) ;
#16491=CARTESIAN_POINT ( 'NONE',  ( 2.556980015513956150, 6.815084337351906107, 3.668282146013149170 ) ) ;
#16492=CARTESIAN_POINT ( 'NONE',  ( 5.515188684475870851, 0.003857086913166444826, -0.003709313826050250878 ) ) ;
#16494=CARTESIAN_POINT ( 'NONE',  ( 2.931247277082679847, 0.9994150891046325036, 7.800615791174658753 ) ) ;
#16502=EDGE_CURVE ( 'NONE', #3105, #62664, #40728, .T. ) ;
#16515=SHAPE_REPRESENTATION_RELATIONSHIP ( 'NONE' , 'NONE' ,  #39018, #28612 ) ;
#16517=CARTESIAN_POINT ( 'NONE',  ( 0.9232058338315048962, -9.791640253608198563, 7.723624854284683927 ) ) ;
#16518=CARTESIAN_POINT ( 'NONE',  ( 0.2655924914740778742, 4.147079829127409134, -11.52280271232866582 ) ) ;
#16519=ORIENTED_EDGE ( 'NONE', *, *, #58437, .F. ) ;
#16520=CARTESIAN_POINT ( 'NONE',  ( 1.719304012338199517, 0.000000000000000000, 0.000000000000000000 ) ) ;
#16528=EDGE_CURVE ( 'NONE', #60783, #39489, #11818, .T. ) ;
#16537=CARTESIAN_POINT ( 'NONE',  ( 2.899286259009688838, -7.788326766693359104, 1.011320371384315298 ) ) ;
#16545=CARTESIAN_POINT ( 'NONE',  ( 2.241311220309555097, -3.897297589552028096, 6.564680916077786144 ) ) ;
#16546=CARTESIAN_POINT ( 'NONE',  ( 0.2648978790185619880, -10.67083876753487637, -6.008231198269095685 ) ) ;
#16552=EDGE_CURVE ( 'NONE', #55547, #14742, #26099, .T. ) ;
#16553=B_SPLINE_CURVE_WITH_KNOTS ( 'NONE', 3,
 ( #9660, #60882, #34290, #35263, #24984, #54604, #9027 ),
 .UNSPECIFIED., .F., .F.,
 ( 4, 3, 4 ),
 ( 7.780893502321468812E-16, 0.002398160485434359685, 0.005002426799377646463 ),
 .UNSPECIFIED. ) ;
#16554=ORIENTED_EDGE ( 'NONE', *, *, #30700, .F. ) ;
#16555=CARTESIAN_POINT ( 'NONE',  ( 0.2653519890538384995, 1.477274386607676477E-15, 12.24619734961521189 ) ) ;
#16556=DIRECTION ( 'NONE',  ( 0.000000000000000000, 0.000000000000000000, 1.000000000000000000 ) ) ;
#16558=CARTESIAN_POINT ( 'NONE',  ( 2.298277635560284082, 1.491234112749290963, -7.506689984432308727 ) ) ;
#16587=CARTESIAN_POINT ( 'NONE',  ( 2.653899356898011153, 7.767552767343518738, -0.2611590963040564817 ) ) ;
#16591=CARTESIAN_POINT ( 'NONE',  ( 0.9232167919969161973, -5.871274944231774207, 10.99620217063213623 ) ) ;
#16600=CARTESIAN_POINT ( 'NONE',  ( 2.889800649504073782, -4.645655809191337582, -3.986129653162696407 ) ) ;
#16610=CARTESIAN_POINT ( 'NONE',  ( 0.3223008802179245791, 4.423848692584686937, 11.43958962819733571 ) ) ;
#16618=CARTESIAN_POINT ( 'NONE',  ( 2.080613030138688480, 0.000000000000000000, 4.000000000000000000 ) ) ;
#16624=CARTESIAN_POINT ( 'NONE',  ( 0.5572780756290603987, 9.649189244958913392, -7.697784780878635935 ) ) ;
#16625=CARTESIAN_POINT ( 'NONE',  ( 5.515539859299206427, -0.001886660928063928948, -0.005751553894234946035 ) ) ;
#16626=CARTESIAN_POINT ( 'NONE',  ( 2.705197763288547552, -7.783989928191463292, -0.2797837188787176133 ) ) ;
#16627=ADVANCED_FACE ( 'NONE', ( #29224 ), #33973, .F. ) ;
#16629=CARTESIAN_POINT ( 'NONE',  ( 5.514624014163232779, -0.004137701579365678402, -0.0001700579043834388670 ) ) ;
#16633=CARTESIAN_POINT ( 'NONE',  ( 0.3675815128205912052, 7.689697408877274931, 9.574637318041988365 ) ) ;
#16634=CARTESIAN_POINT ( 'NONE',  ( 3.152665057735760445, 4.725420687649616092, -6.378477742801607953 ) ) ;
#16642=CARTESIAN_POINT ( 'NONE',  ( 5.516018279890452902, 0.0002248006052446666569, -0.006771744149385742172 ) ) ;
#16643=CARTESIAN_POINT ( 'NONE',  ( 2.241528039335008327, 2.596349773934880201, 7.179411278563565091 ) ) ;
#16647=EDGE_LOOP ( 'NONE', ( #41592, #9049, #49556, #16414 ) ) ;
#16672=LINE ( 'NONE', #41611, #30521 ) ;
#16673=CARTESIAN_POINT ( 'NONE',  ( 2.241352910868908310, 4.843133558968128582, 5.901537464758471074 ) ) ;
#16679=CARTESIAN_POINT ( 'NONE',  ( 0.2648978790185584908, 4.063980959785046032, 11.55204314799265042 ) ) ;
#16683=ORIENTED_EDGE ( 'NONE', *, *, #4959, .T. ) ;
#16685=FACE_OUTER_BOUND ( 'NONE', #28661, .T. ) ;
#16691=B_SPLINE_CURVE_WITH_KNOTS ( 'NONE', 3,
 ( #28116, #37757, #33427, #2184, #54035, #42384, #58050, #37421, #48409, #12465 ),
 .UNSPECIFIED., .F., .F.,
 ( 4, 3, 3, 4 ),
 ( 8.673617379884035472E-19, 6.607638129004486172E-05, 9.911389841680541231E-05, 0.0001667630577588623383 ),
 .UNSPECIFIED. ) ;
#16694=VERTEX_POINT ( 'NONE', #62101 ) ;
#16700=CARTESIAN_POINT ( 'NONE',  ( 5.530133899448235191, 0.01594518557925582100, 0.001124651387255043086 ) ) ;
#16706=B_SPLINE_CURVE_WITH_KNOTS ( 'NONE', 3,
 ( #30152, #45122, #41095, #65384, #45434, #65699, #20170, #40442, #60740, #15179, #52418, #57068, #11819, #31767, #46427, #52738, #7162, #11184, #1213 ),
 .UNSPECIFIED., .F., .F.,
 ( 4, 3, 3, 3, 3, 3, 4 ),
 ( 9.899098333708122648E-18, 4.457896483014865609E-05, 6.639290541542039676E-05, 8.820687556478868318E-05, 0.0001100173248778915164, 0.0001545671401658093647, 0.0001830328308068584413 ),
 .UNSPECIFIED. ) ;
#16711=CARTESIAN_POINT ( 'NONE',  ( 0.2648978790185602672, 7.972372351883029395, 9.295532325666474804 ) ) ;
#16725=CARTESIAN_POINT ( 'NONE',  ( 0.2717059086739035401, -5.971041827598893903, 10.69429229731975894 ) ) ;
#16736=CARTESIAN_POINT ( 'NONE',  ( 1.014383007554946037, -0.4441500209062191895, -12.48801387563329790 ) ) ;
#16738=CARTESIAN_POINT ( 'NONE',  ( 1.719304012340734378, -7.017415949613340587, -10.62216384465587282 ) ) ;
#16751=CARTESIAN_POINT ( 'NONE',  ( 1.549075743844138042, -4.962709020479777244, 11.66216484053746427 ) ) ;
#16766=CARTESIAN_POINT ( 'NONE',  ( 3.152665057734004073, 7.102135024645805039, -3.546019893116331811 ) ) ;
#16767=CARTESIAN_POINT ( 'NONE',  ( 2.941278708680199916, 0.9331242451664990556, 6.068329152486379385 ) ) ;
#16772=ORIENTED_EDGE ( 'NONE', *, *, #10420, .T. ) ;
#16778=CARTESIAN_POINT ( 'NONE',  ( 0.2869720083484372797, 4.386174336869755663, -11.44147823180126977 ) ) ;
#16779=EDGE_CURVE ( 'NONE', #38095, #35612, #16860, .T. ) ;
#16782=CARTESIAN_POINT ( 'NONE',  ( 2.080613030138687591, 0.000000000000000000, 0.000000000000000000 ) ) ;
#16788=LINE ( 'NONE', #42699, #2546 ) ;
#16791=FACE_OUTER_BOUND ( 'NONE', #62288, .T. ) ;
#16794=FACE_OUTER_BOUND ( 'NONE', #2816, .T. ) ;
#16798=ORIENTED_EDGE ( 'NONE', *, *, #39196, .F. ) ;
#16799=CARTESIAN_POINT ( 'NONE',  ( 2.524535260912660561, 6.801151891677185368, 3.671333852642844064 ) ) ;
#16811=CARTESIAN_POINT ( 'NONE',  ( 0.2652384529303112304, -7.820949643217205427, 9.423437232855640389 ) ) ;
#16822=ORIENTED_EDGE ( 'NONE', *, *, #15780, .T. ) ;
#16828=ADVANCED_FACE ( 'NONE', ( #22518 ), #61187, .F. ) ;
#16829=CARTESIAN_POINT ( 'NONE',  ( 5.514970785353741078, -0.003805873180274332770, 0.002796696073589857289 ) ) ;
#16841=CARTESIAN_POINT ( 'NONE',  ( 0.7400311444011722362, 12.27261279799597737, 1.803686700615449112 ) ) ;
#16846=VERTEX_POINT ( 'NONE', #33136 ) ;
#16852=CARTESIAN_POINT ( 'NONE',  ( 5.514970785353741078, 0.001897634820904955163, 0.004324946436530311550 ) ) ;
#16853=CARTESIAN_POINT ( 'NONE',  ( 2.368238019615144907, -2.793778585134617742, -7.150288915654806843 ) ) ;
#16855=CARTESIAN_POINT ( 'NONE',  ( 0.2638984909335720941, 4.375449752477134524, 11.43908195192331334 ) ) ;
#16860=LINE ( 'NONE', #7536, #55647 ) ;
#16864=VERTEX_POINT ( 'NONE', #45088 ) ;
#16866=CARTESIAN_POINT ( 'NONE',  ( 5.514970785353741078, -0.002619824551223247366, 0.003929719953530060386 ) ) ;
#16868=CARTESIAN_POINT ( 'NONE',  ( 2.242819959140648134, 4.828731837260225923, 5.913965034148179534 ) ) ;
#16871=CARTESIAN_POINT ( 'NONE',  ( 3.047904605210420836, 2.299870214474541541, 7.561255571389395413 ) ) ;
#16878=LINE ( 'NONE', #52790, #40371 ) ;
#16879=( BOUNDED_SURFACE ( )  B_SPLINE_SURFACE ( 3, 1, ( 
 ( #56511, #57838 ),
 ( #6636, #62790 ),
 ( #981, #6955 ),
 ( #11284, #6303 ) ),
 .UNSPECIFIED., .F., .F., .F. ) 
 B_SPLINE_SURFACE_WITH_KNOTS ( ( 4, 4 ),
 ( 2, 2 ),
 ( 0.000000000000000000, 1.000000000000000000 ),
 ( 0.000000000000000000, 1.000000000000000000 ),
 .UNSPECIFIED. ) 
 GEOMETRIC_REPRESENTATION_ITEM ( )  RATIONAL_B_SPLINE_SURFACE ( (
 ( 1.000000000000000000, 1.000000000000000000),
 ( 0.9942764183789327692, 0.8450855930916585379),
 ( 0.9942764183789327692, 0.8450855930916585379),
 ( 1.000000000000000000, 1.000000000000000000) ) ) 
 REPRESENTATION_ITEM ( '' )  SURFACE ( )  );
#16882=ORIENTED_EDGE ( 'NONE', *, *, #23246, .F. ) ;
#16885=CARTESIAN_POINT ( 'NONE',  ( 0.2655924914740778187, 12.24627751708824341, 0.04405032194307429566 ) ) ;
#16888=ADVANCED_FACE ( 'NONE', ( #49747 ), #63681, .F. ) ;
#16893=CARTESIAN_POINT ( 'NONE',  ( 0.3537226245948366654, 1.874138792913011553, 12.13174752084887054 ) ) ;
#16899=CARTESIAN_POINT ( 'NONE',  ( 0.6473888112830272767, 3.920507224439243377, -11.73602097806015720 ) ) ;
#16901=CARTESIAN_POINT ( 'NONE',  ( 2.491965175172130120, 7.715025372670220705, -0.2120508241292647922 ) ) ;
#16902=CARTESIAN_POINT ( 'NONE',  ( 2.253265082353315130, 5.768060979106778063, 5.007416537587866756 ) ) ;
#16912=CARTESIAN_POINT ( 'NONE',  ( 1.634816307077934461, 8.702988562441301923, -9.253014110594602215 ) ) ;
#16933=CARTESIAN_POINT ( 'NONE',  ( 0.9232058338315048962, 5.905985151448150283, 10.98407661738930763 ) ) ;
#16940=CARTESIAN_POINT ( 'NONE',  ( 3.047904605210329798, 4.747272783555662734, 6.318654123925870891 ) ) ;
#16941=LINE ( 'NONE', #27246, #35278 ) ;
#16942=CARTESIAN_POINT ( 'NONE',  ( 0.3109076770649044086, -8.060731492642734253, -9.239379580302180983 ) ) ;
#16943=DIRECTION ( 'NONE',  ( 0.000000000000000000, 0.000000000000000000, -1.000000000000000000 ) ) ;
#16946=ORIENTED_EDGE ( 'NONE', *, *, #49342, .F. ) ;
#16951=CARTESIAN_POINT ( 'NONE',  ( 5.515539859299206427, -0.003193223631739290028, -0.005142293699651858188 ) ) ;
#16955=CARTESIAN_POINT ( 'NONE',  ( 2.255723233588950105, -6.680843247642341609, 3.704537245405018275 ) ) ;
#16957=CARTESIAN_POINT ( 'NONE',  ( 0.6473888112830219477, 10.54705164520787442, -6.470260187014609699 ) ) ;
#16965=CARTESIAN_POINT ( 'NONE',  ( 0.2655924914740778742, 7.905499957109238807, 9.352877839710629360 ) ) ;
#16966=CARTESIAN_POINT ( 'NONE',  ( 0.2650492433740064269, -2.017984765249154488, 12.07870441534855743 ) ) ;
#16970=VERTEX_POINT ( 'NONE', #49446 ) ;
#16972=CARTESIAN_POINT ( 'NONE',  ( 0.2653141334712580401, 2.169900597054518432, 12.05242949860144286 ) ) ;
#16974=FACE_OUTER_BOUND ( 'NONE', #34485, .T. ) ;
#16979=DIRECTION ( 'NONE',  ( -1.000000000000000000, -0.000000000000000000, -0.000000000000000000 ) ) ;
#16985=DIRECTION ( 'NONE',  ( -1.000000000000000000, -0.000000000000000000, -0.000000000000000000 ) ) ;
#16995=CARTESIAN_POINT ( 'NONE',  ( 2.241537034860907607, 4.903726641589524426, 5.851376807350157527 ) ) ;
#16999=CARTESIAN_POINT ( 'NONE',  ( 2.241352910868909643, -6.569501556381469598, 3.889181972941426313 ) ) ;
#17001=CARTESIAN_POINT ( 'NONE',  ( 0.3040950598368144520, -6.347045025870841073, 10.49113473328028867 ) ) ;
#17007=CARTESIAN_POINT ( 'NONE',  ( 5.530133899448235191, 0.001661287012794044910, 0.01589823604557701400 ) ) ;
#17009=B_SPLINE_CURVE_WITH_KNOTS ( 'NONE', 3,
 ( #51498, #12204, #32473, #56812, #62736, #37478, #52782, #27494, #5945, #2244, #21195, #41466, #61762, #11234, #51806, #28168 ),
 .UNSPECIFIED., .F., .F.,
 ( 4, 3, 3, 3, 3, 4 ),
 ( 5.963111948670274387E-19, 0.0003017745587525257349, 0.0006035491769808738489, 0.0009053241094668159229, 0.001207275924540508662, 0.001510325902534021556 ),
 .UNSPECIFIED. ) ;
#17017=CARTESIAN_POINT ( 'NONE',  ( 5.520433897694421610, 0.01278034823631963093, 0.007971295965052456120 ) ) ;
#17018=B_SPLINE_CURVE_WITH_KNOTS ( 'NONE', 3,
 ( #8418, #43005, #54315, #12733, #34338, #58988, #48355, #2805, #18074, #3463, #63600, #8755, #59292, #9070, #14047, #63280, #38337, #64272, #54652, #29036, #3791, #48011 ),
 .UNSPECIFIED., .F., .F.,
 ( 4, 3, 3, 3, 3, 3, 3, 4 ),
 ( 1.764953265579307567E-18, 4.449119708436945902E-05, 6.626296329540647860E-05, 8.803456484962896152E-05, 0.0001098060367612814227, 0.0001315774408628525083, 0.0001760698110411161544, 0.0001829697163287809084 ),
 .UNSPECIFIED. ) ;
#17021=ORIENTED_EDGE ( 'NONE', *, *, #22722, .F. ) ;
#17022=CARTESIAN_POINT ( 'NONE',  ( 3.152665057734129750, 3.161213418913565221, -7.281573230474259972 ) ) ;
#17025=CARTESIAN_POINT ( 'NONE',  ( 3.152665057734087117, 7.886634106564184954, -0.9030954876737516956 ) ) ;
#17027=DIRECTION ( 'NONE',  ( 0.3939253465568943735, -0.9068155327749454209, 0.1500280335741383531 ) ) ;
#17029=CARTESIAN_POINT ( 'NONE',  ( 0.2759803524722191925, -12.02930579076649131, -2.313459762622668947 ) ) ;
#17038=CARTESIAN_POINT ( 'NONE',  ( 0.2655924914740778742, 4.229867354073558516, 11.49267051747969681 ) ) ;
#17040=CARTESIAN_POINT ( 'NONE',  ( 0.7400311444011685724, 4.574267895796849892, 11.53023780418227950 ) ) ;
#17041=CARTESIAN_POINT ( 'NONE',  ( 2.994568964204221473, 5.368337437440340310, -5.775954174106879613 ) ) ;
#17042=B_SPLINE_CURVE_WITH_KNOTS ( 'NONE', 3,
 ( #4814, #65612, #44355, #39707, #20412, #60985, #24093, #20083, #59674, #35687 ),
 .UNSPECIFIED., .F., .F.,
 ( 4, 3, 3, 4 ),
 ( 8.673617379884035472E-19, 6.607638129004594592E-05, 9.911389841680703862E-05, 0.0001667630577588622570 ),
 .UNSPECIFIED. ) ;
#17043=ORIENTED_EDGE ( 'NONE', *, *, #1312, .T. ) ;
#17050=CARTESIAN_POINT ( 'NONE',  ( 2.251139882114759239, 6.551456272498336730, 3.925854078925700374 ) ) ;
#17054=ORIENTED_EDGE ( 'NONE', *, *, #21244, .T. ) ;
#17057=VERTEX_POINT ( 'NONE', #6169 ) ;
#17062=DIRECTION ( 'NONE',  ( -1.000000000000000000, 0.000000000000000000, 0.000000000000000000 ) ) ;
#17064=CARTESIAN_POINT ( 'NONE',  ( 0.3223008802179215260, -7.695050880595557530, 9.550960164375572603 ) ) ;
#17073=CARTESIAN_POINT ( 'NONE',  ( 0.2651627682582927692, 9.324228491541633801, -7.938957913267660871 ) ) ;
#17077=CARTESIAN_POINT ( 'NONE',  ( 0.9296196016823148334, -4.652334946094635271, 11.56707937094485139 ) ) ;
#17085=B_SPLINE_CURVE_WITH_KNOTS ( 'NONE', 3,
 ( #13486, #3559, #33770, #38103, #63695, #53433, #13805, #2224, #54416, #22841, #18173, #29135, #22504, #43096, #42764, #7876, #32773, #39088, #28151 ),
 .UNSPECIFIED., .F., .F.,
 ( 4, 3, 3, 3, 3, 3, 4 ),
 ( 1.226634733346699349E-18, 2.831840207499513698E-05, 4.217266859840391790E-05, 5.602024318395954422E-05, 6.290810167969108978E-05, 9.120440630945299103E-05, 0.0001153103026479744092 ),
 .UNSPECIFIED. ) ;
#17087=VERTEX_POINT ( 'NONE', #20796 ) ;
#17088=( BOUNDED_SURFACE ( )  B_SPLINE_SURFACE ( 3, 1, ( 
 ( #22879, #53123 ),
 ( #38140, #32491 ),
 ( #28190, #48478 ),
 ( #63409, #58450 ) ),
 .UNSPECIFIED., .F., .F., .F. ) 
 B_SPLINE_SURFACE_WITH_KNOTS ( ( 4, 4 ),
 ( 2, 2 ),
 ( 0.000000000000000000, 1.000000000000000000 ),
 ( 0.000000000000000000, 1.000000000000000000 ),
 .UNSPECIFIED. ) 
 GEOMETRIC_REPRESENTATION_ITEM ( )  RATIONAL_B_SPLINE_SURFACE ( (
 ( 1.000000000000000000, 1.000000000000000000),
 ( 0.6933888150995267674, 0.9895912004443193632),
 ( 0.6933888150995267674, 0.9895912004443193632),
 ( 1.000000000000000000, 1.000000000000000000) ) ) 
 REPRESENTATION_ITEM ( '' )  SURFACE ( )  );
#17089=EDGE_LOOP ( 'NONE', ( #31705, #29164, #52254, #47482 ) ) ;
#17093=ORIENTED_EDGE ( 'NONE', *, *, #35702, .T. ) ;
#17096=CARTESIAN_POINT ( 'NONE',  ( 1.719304012341432264, 5.066286238787408358, -11.67935079956426847 ) ) ;
#17098=CARTESIAN_POINT ( 'NONE',  ( 5.515188684475870851, -0.001283816547384759822, 0.005194992164431476087 ) ) ;
#17099=VECTOR ( 'NONE', #60413, 1000.000000000000000 ) ;
#17116=CARTESIAN_POINT ( 'NONE',  ( 1.719304012340653998, -9.242227816403676854, -8.755325027797448811 ) ) ;
#17123=CARTESIAN_POINT ( 'NONE',  ( 2.844750968616420739, -1.686994672842389242, -7.651810733888938287 ) ) ;
#17127=EDGE_CURVE ( 'NONE', #59321, #6328, #50418, .T. ) ;
#17131=DIRECTION ( 'NONE',  ( -1.000000000000000000, -0.000000000000000000, -0.000000000000000000 ) ) ;
#17132=CARTESIAN_POINT ( 'NONE',  ( 0.3675815128205894289, 2.391755495700764289, -12.04510820461657161 ) ) ;
#17134=CARTESIAN_POINT ( 'NONE',  ( 1.547277799339153104, -12.58038279313752739, -1.534072017332470450 ) ) ;
#17138=CARTESIAN_POINT ( 'NONE',  ( 0.2651627923886338833, -12.24583724871547474, -0.08809136839528641794 ) ) ;
#17146=CARTESIAN_POINT ( 'NONE',  ( 0.3278977287071203062, -9.554671284920345897, 7.693417476735495697 ) ) ;
#17149=DIRECTION ( 'NONE',  ( -0.3939253465568943735, 0.8603393047165004415, -0.3234796780324220578 ) ) ;
#17152=CARTESIAN_POINT ( 'NONE',  ( 0.7400311444011719031, 11.77295732453934640, 3.907401494354961979 ) ) ;
#17157=CARTESIAN_POINT ( 'NONE',  ( 1.719304012338836563, -1.452142814150213734, 12.64775761152536759 ) ) ;
#17170=CARTESIAN_POINT ( 'NONE',  ( 2.907497136250630554, 7.666666002096657273, -1.716624290781218809 ) ) ;
#17178=CARTESIAN_POINT ( 'NONE',  ( 1.104777566491141672, 12.40974092093472514, 1.703053712365368177 ) ) ;
#17190=EDGE_CURVE ( 'NONE', #6215, #23985, #42045, .T. ) ;
#17192=CARTESIAN_POINT ( 'NONE',  ( 2.249013661412229137, -3.921976945965382377, 6.552953334857902767 ) ) ;
#17194=ORIENTED_EDGE ( 'NONE', *, *, #29215, .F. ) ;
#17197=CARTESIAN_POINT ( 'NONE',  ( 0.2655924914740778187, 11.49267051747968438, 4.229867354073594043 ) ) ;
#17204=CARTESIAN_POINT ( 'NONE',  ( 5.514970785353741078, 0.003805873180274783798, 0.002796696073589750170 ) ) ;
#17205=CARTESIAN_POINT ( 'NONE',  ( 0.2648978790185602672, -0.1321385342561549048, -12.24533305150758267 ) ) ;
#17208=CARTESIAN_POINT ( 'NONE',  ( 2.573738926104369718, 2.426778239006456062, 7.355212866432303542 ) ) ;
#17211=CARTESIAN_POINT ( 'NONE',  ( 0.2653519890518156177, -10.60552241699063103, -6.123091032184257543 ) ) ;
#17220=CARTESIAN_POINT ( 'NONE',  ( 5.514970785353741078, 0.0003039746380528312057, 0.004713149585127536512 ) ) ;
#17224=CARTESIAN_POINT ( 'NONE',  ( 0.3675815128205912052, 9.574637318042068301, -7.689697408877177232 ) ) ;
#17232=CARTESIAN_POINT ( 'NONE',  ( 0.2706063244538048362, 1.954041462022419573, 12.09107863371558089 ) ) ;
#17233=ORIENTED_EDGE ( 'NONE', *, *, #64979, .F. ) ;
#17237=CARTESIAN_POINT ( 'NONE',  ( 0.3675815128205894289, 3.951233083390626177, -11.62724744438061641 ) ) ;
#17239=CARTESIAN_POINT ( 'NONE',  ( 2.256373768223415066, 7.545294827890042022, 1.195444820369703232 ) ) ;
#17243=CARTESIAN_POINT ( 'NONE',  ( 2.827825597296808269, -6.207590800588422830, 6.550135365664063514 ) ) ;
#17258=ORIENTED_EDGE ( 'NONE', *, *, #32557, .T. ) ;
#17260=VERTEX_POINT ( 'NONE', #12432 ) ;
#17263=ADVANCED_FACE ( 'NONE', ( #43033 ), #8941, .F. ) ;
#17264=ORIENTED_EDGE ( 'NONE', *, *, #3843, .F. ) ;
#17270=CARTESIAN_POINT ( 'NONE',  ( 1.937114397841935398, -5.620553190833057045, 11.53912442307253450 ) ) ;
#17283=ORIENTED_EDGE ( 'NONE', *, *, #37826, .T. ) ;
#17288=CARTESIAN_POINT ( 'NONE',  ( 2.255723233588949661, 5.936060085173614276, -4.808373255828823467 ) ) ;
#17291=CARTESIAN_POINT ( 'NONE',  ( 2.770579946183333586, -4.784693811915849970, -6.173813901927596604 ) ) ;
#17299=EDGE_CURVE ( 'NONE', #43792, #43254, #46694, .T. ) ;
#17301=EDGE_CURVE ( 'NONE', #41809, #15421, #16553, .T. ) ;
#17304=B_SPLINE_CURVE_WITH_KNOTS ( 'NONE', 3,
 ( #1804, #62297, #16751, #37024, #22389, #57327, #11749, #32036, #6796, #17077, #27070, #47361, #37357, #57668, #12090, #32368 ),
 .UNSPECIFIED., .F., .F.,
 ( 4, 3, 3, 3, 3, 4 ),
 ( 0.000000000000000000, 0.0002999043160757280165, 0.0005998071753050859302, 0.0008997092107374342861, 0.001204458948194992189, 0.001510329163475222867 ),
 .UNSPECIFIED. ) ;
#17309=CARTESIAN_POINT ( 'NONE',  ( 0.2648978790185619880, -1.996248716311710414, 12.08224454301447892 ) ) ;
#17312=CARTESIAN_POINT ( 'NONE',  ( 0.2646305136544065406, 10.53923716745246608, 6.237419468587114935 ) ) ;
#17313=CARTESIAN_POINT ( 'NONE',  ( 0.2652384529303146166, 2.191562200667183546, 12.04846370803829103 ) ) ;
#17316=LINE ( 'NONE', #8316, #34966 ) ;
#17321=ORIENTED_EDGE ( 'NONE', *, *, #12758, .T. ) ;
#17330=VERTEX_POINT ( 'NONE', #29308 ) ;
#17342=CARTESIAN_POINT ( 'NONE',  ( 2.665405856346790614, -2.723742051529387975, -9.171500569027763561 ) ) ;
#17353=CARTESIAN_POINT ( 'NONE',  ( 2.251152103361936163, 6.676162264138683966, 3.709836606815780424 ) ) ;
#17354=EDGE_CURVE ( 'NONE', #35137, #3903, #40250, .T. ) ;
#17357=CARTESIAN_POINT ( 'NONE',  ( 1.719304012339893051, -12.70777170743898310, 0.7661785589588769874 ) ) ;
#17359=CARTESIAN_POINT ( 'NONE',  ( 0.2739690278137246748, -2.307031017960371688, -12.02985305092653334 ) ) ;
#17365=ORIENTED_EDGE ( 'NONE', *, *, #62921, .F. ) ;
#17370=VERTEX_POINT ( 'NONE', #44926 ) ;
#17396=CARTESIAN_POINT ( 'NONE',  ( 2.284126774969133855, 6.543266298866131869, 3.960764882115977770 ) ) ;
#17417=CARTESIAN_POINT ( 'NONE',  ( 0.2646305136544072623, 6.237419468587079407, 10.53923716745249095 ) ) ;
#17419=ORIENTED_EDGE ( 'NONE', *, *, #57768, .T. ) ;
#17427=CARTESIAN_POINT ( 'NONE',  ( 5.515188684475870851, -0.004442604682416460317, -0.002983184900674899515 ) ) ;
#17428=CARTESIAN_POINT ( 'NONE',  ( 2.241537034860906719, -5.851376807350176179, 4.903726641589506663 ) ) ;
#17431=ORIENTED_EDGE ( 'NONE', *, *, #36328, .F. ) ;
#17447=CARTESIAN_POINT ( 'NONE',  ( 0.3675815128205912052, 12.04510820461662668, -2.391755495700480516 ) ) ;
#17450=CARTESIAN_POINT ( 'NONE',  ( 2.297017764050095057, -4.791851130936013448, 5.967068736727098255 ) ) ;
#17467=CARTESIAN_POINT ( 'NONE',  ( 2.903928887688250970, 6.365315087929518612, -6.032681461746785878 ) ) ;
#17481=CARTESIAN_POINT ( 'NONE',  ( 0.2648321136542702292, -9.471460387169321038, 7.762514728658064911 ) ) ;
#17486=( BOUNDED_SURFACE ( )  B_SPLINE_SURFACE ( 3, 1, ( 
 ( #6448, #52668 ),
 ( #17742, #12723 ),
 ( #1793, #38000 ),
 ( #11423, #42314 ) ),
 .UNSPECIFIED., .F., .F., .F. ) 
 B_SPLINE_SURFACE_WITH_KNOTS ( ( 4, 4 ),
 ( 2, 2 ),
 ( 0.000000000000000000, 1.000000000000000000 ),
 ( 0.000000000000000000, 1.000000000000000000 ),
 .UNSPECIFIED. ) 
 GEOMETRIC_REPRESENTATION_ITEM ( )  RATIONAL_B_SPLINE_SURFACE ( (
 ( 1.000000000000000000, 1.000000000000000000),
 ( 0.6933888150995267674, 0.9895912004443193632),
 ( 0.6933888150995267674, 0.9895912004443193632),
 ( 1.000000000000000000, 1.000000000000000000) ) ) 
 REPRESENTATION_ITEM ( '' )  SURFACE ( )  );
#17488=CARTESIAN_POINT ( 'NONE',  ( 0.2706063244538030044, 5.971590789837518898, 10.69357582853948863 ) ) ;
#17496=ORIENTED_EDGE ( 'NONE', *, *, #24914, .T. ) ;
#17498=CARTESIAN_POINT ( 'NONE',  ( 1.014383007554949367, -11.58298623339617706, 4.688516792764573893 ) ) ;
#17511=CARTESIAN_POINT ( 'NONE',  ( 5.520433897694421610, -0.01329351892498009322, -0.007082458259338525290 ) ) ;
#17516=CARTESIAN_POINT ( 'NONE',  ( 5.516018279890452902, 0.006629829924290471695, -0.001397286410094441449 ) ) ;
#17519=FACE_OUTER_BOUND ( 'NONE', #45189, .T. ) ;
#17524=CIRCLE ( 'NONE', #54690, 7.938172270156617749 ) ;
#17526=ORIENTED_EDGE ( 'NONE', *, *, #42176, .F. ) ;
#17528=CARTESIAN_POINT ( 'NONE',  ( 0.2653519789438738008, -6.104019611498650910, 10.61653328464225687 ) ) ;
#17536=CARTESIAN_POINT ( 'NONE',  ( 5.514970785353741078, -0.002796696073589895887, -0.003805873180274304147 ) ) ;
#17541=CARTESIAN_POINT ( 'NONE',  ( 2.253265082352432724, 1.452519439326557249, -7.498995607278123643 ) ) ;
#17542=ORIENTED_EDGE ( 'NONE', *, *, #832, .T. ) ;
#17543=CARTESIAN_POINT ( 'NONE',  ( 0.2648978790185584908, -6.008231198268910056, -10.67083876753498117 ) ) ;
#17545=CARTESIAN_POINT ( 'NONE',  ( 0.2651627923886310523, -10.56116046379969653, -6.199207987242205675 ) ) ;
#17547=EDGE_CURVE ( 'NONE', #24896, #29925, #22773, .T. ) ;
#17548=VECTOR ( 'NONE', #44649, 1000.000000000000114 ) ;
#17549=CARTESIAN_POINT ( 'NONE',  ( 0.2676618633000443781, 6.262131165853879189, -10.52491907319755526 ) ) ;
#17553=CARTESIAN_POINT ( 'NONE',  ( 2.245754705088395031, 0.1113317465207851603, -7.635057163463313756 ) ) ;
#17559=( GEOMETRIC_REPRESENTATION_CONTEXT ( 3 ) GLOBAL_UNCERTAINTY_ASSIGNED_CONTEXT ( ( #11970 ) ) GLOBAL_UNIT_ASSIGNED_CONTEXT ( ( #60747, #10512, #15507 ) ) REPRESENTATION_CONTEXT ( 'NONE', 'WORKASPACE' ) );
#17564=ORIENTED_EDGE ( 'NONE', *, *, #40213, .F. ) ;
#17566=ORIENTED_EDGE ( 'NONE', *, *, #63502, .F. ) ;
#17568=CARTESIAN_POINT ( 'NONE',  ( 2.705197763288546664, 7.410249563424458508, -2.399370654839196870 ) ) ;
#17571=CARTESIAN_POINT ( 'NONE',  ( 1.459561108994223533, 3.725588117663211740, -12.08294179906978272 ) ) ;
#17572=CARTESIAN_POINT ( 'NONE',  ( 0.4626703367447423387, -7.694993290995431501, -9.611037151103516862 ) ) ;
#17574=CARTESIAN_POINT ( 'NONE',  ( 2.269879328256728002, -1.181008584586007659, 7.552124491910168658 ) ) ;
#17579=CARTESIAN_POINT ( 'NONE',  ( 1.194176325881342704, -5.827386336992954163, 11.12159247766670767 ) ) ;
#17583=CARTESIAN_POINT ( 'NONE',  ( 0.3665391374699467075, 0.2638605131388869762, -12.27992639892678106 ) ) ;
#17591=ORIENTED_EDGE ( 'NONE', *, *, #35927, .T. ) ;
#17605=CARTESIAN_POINT ( 'NONE',  ( 5.514624014163232779, -0.0001700579043834244742, 0.004137701579365677534 ) ) ;
#17607=EDGE_CURVE ( 'NONE', #61407, #7317, #8298, .T. ) ;
#17609=B_SPLINE_CURVE_WITH_KNOTS ( 'NONE', 3,
 ( #63298, #17769, #58333, #12751, #2824, #49365, #18442, #25049, #38704, #19073 ),
 .UNSPECIFIED., .F., .F.,
 ( 4, 3, 3, 4 ),
 ( 1.084202172485504241E-18, 6.607638129004478041E-05, 9.911389841680565626E-05, 0.0001667630577588619589 ),
 .UNSPECIFIED. ) ;
#17617=CARTESIAN_POINT ( 'NONE',  ( 2.907497136250764225, -4.235253383576185193, -6.617189382231105199 ) ) ;
#17618=CARTESIAN_POINT ( 'NONE',  ( 0.3654063281920759687, -11.62642356802259513, -3.951404032559384216 ) ) ;
#17620=B_SPLINE_CURVE_WITH_KNOTS ( 'NONE', 3,
 ( #3916, #48813, #59763, #49151, #33513, #60086, #33815, #13850, #14192, #54783, #65058, #44441, #44135, #64092, #14505, #18874, #39134, #34144, #54113 ),
 .UNSPECIFIED., .F., .F.,
 ( 4, 3, 3, 3, 3, 3, 4 ),
 ( 2.168404344971008868E-19, 2.831840207499647868E-05, 4.217266859840459553E-05, 5.602024318396018118E-05, 6.290810167969207911E-05, 9.120440630945170354E-05, 0.0001153103026479764556 ),
 .UNSPECIFIED. ) ;
#17629=CARTESIAN_POINT ( 'NONE',  ( 2.305787727787084407, -4.792270232040854339, -5.970480882365271746 ) ) ;
#17639=CARTESIAN_POINT ( 'NONE',  ( 5.514624014163232779, -0.001921576324372477156, -0.003668383633201366227 ) ) ;
#17650=DIRECTION ( 'NONE',  ( 0.3939253465568944290, -0.1500280335741476234, -0.9068155327749437555 ) ) ;
#17652=ADVANCED_FACE ( 'NONE', ( #27582 ), #27974, .T. ) ;
#17653=ORIENTED_EDGE ( 'NONE', *, *, #56920, .F. ) ;
#17657=CARTESIAN_POINT ( 'NONE',  ( 0.2646305136544072623, -1.996350543473075945, 12.08286001766534845 ) ) ;
#17661=CARTESIAN_POINT ( 'NONE',  ( 2.305787727787083519, -7.566723232958080914, 1.164987321564707967 ) ) ;
#17670=CARTESIAN_POINT ( 'NONE',  ( 2.258463476536644698, 2.484972401833245748, 7.224688073723612547 ) ) ;
#17673=B_SPLINE_CURVE_WITH_KNOTS ( 'NONE', 3,
 ( #39059, #14754, #39726, #29414, #8478, #34712, #49709, #4157, #18494, #13776, #29106, #34067, #19784, #29729, #28762, #39386 ),
 .UNSPECIFIED., .F., .F.,
 ( 4, 3, 3, 3, 3, 4 ),
 ( 0.000000000000000000, 0.0002999043160757236797, 0.0005998071753050783408, 0.0008997092107374227935, 0.001204458948194733715, 0.001510329163474712858 ),
 .UNSPECIFIED. ) ;
#17674=CARTESIAN_POINT ( 'NONE',  ( 2.262775599886258870, 3.697834000591639914, 6.687241191563670917 ) ) ;
#17685=( BOUNDED_SURFACE ( )  B_SPLINE_SURFACE ( 3, 1, ( 
 ( #10866, #41775 ),
 ( #1879, #62072 ),
 ( #57406, #26479 ),
 ( #57754, #2209 ) ),
 .UNSPECIFIED., .F., .F., .F. ) 
 B_SPLINE_SURFACE_WITH_KNOTS ( ( 4, 4 ),
 ( 2, 2 ),
 ( 0.000000000000000000, 1.000000000000000000 ),
 ( 0.000000000000000000, 1.000000000000000000 ),
 .UNSPECIFIED. ) 
 GEOMETRIC_REPRESENTATION_ITEM ( )  RATIONAL_B_SPLINE_SURFACE ( (
 ( 1.000000000000000000, 1.000000000000000000),
 ( 0.9856612449720755231, 0.9999558406602322425),
 ( 0.9856612449720755231, 0.9999558406602322425),
 ( 1.000000000000000000, 1.000000000000000000) ) ) 
 REPRESENTATION_ITEM ( '' )  SURFACE ( )  );
#17688=CARTESIAN_POINT ( 'NONE',  ( 2.276905613632194569, 6.697548486789856703, 3.688905863353881376 ) ) ;
#17693=CARTESIAN_POINT ( 'NONE',  ( 0.2648978790185619880, -9.465406350830555482, -7.769924372105300847 ) ) ;
#17700=CARTESIAN_POINT ( 'NONE',  ( 5.514624014163232779, 0.002529391395135306177, 0.003278974416024616270 ) ) ;
#17701=CARTESIAN_POINT ( 'NONE',  ( 2.034671305879538483, 11.60021725667554371, -1.331347915349341049 ) ) ;
#17703=ORIENTED_EDGE ( 'NONE', *, *, #50955, .F. ) ;
#17705=FACE_OUTER_BOUND ( 'NONE', #507, .T. ) ;
#17717=CARTESIAN_POINT ( 'NONE',  ( 2.268878695253352618, -0.1481365927654071657, 7.642144312464380640 ) ) ;
#17725=EDGE_LOOP ( 'NONE', ( #11455, #51832, #8806, #14252 ) ) ;
#17728=ORIENTED_EDGE ( 'NONE', *, *, #56882, .F. ) ;
#17733=B_SPLINE_CURVE_WITH_KNOTS ( 'NONE', 3,
 ( #47302, #1741, #40653, #33629, #13342, #12667, #3060, #37293, #8046, #32949, #23003, #22680, #43260, #37636, #53260, #2747, #28312, #7356, #43585, #42945, #27993, #18009 ),
 .UNSPECIFIED., .F., .F.,
 ( 4, 3, 3, 3, 3, 3, 3, 4 ),
 ( 1.755771606739170543E-18, 4.449119708436529840E-05, 6.626296329539953971E-05, 8.803456484962175158E-05, 0.0001098060367612756628, 0.0001315774408628470331, 0.0001760698110411152600, 0.0001829697163287826703 ),
 .UNSPECIFIED. ) ;
#17738=CARTESIAN_POINT ( 'NONE',  ( -14.47334165536099881, 4.898587196589412829E-16, -4.000000000000000000 ) ) ;
#17742=CARTESIAN_POINT ( 'NONE',  ( 5.520433897694421610, -0.01186170453199867497, -0.009283255140285580700 ) ) ;
#17743=ORIENTED_EDGE ( 'NONE', *, *, #42753, .F. ) ;
#17747=ORIENTED_EDGE ( 'NONE', *, *, #30700, .T. ) ;
#17754=CARTESIAN_POINT ( 'NONE',  ( 0.2739690278137235091, 9.499928778897116288, 7.732471127692628343 ) ) ;
#17755=CARTESIAN_POINT ( 'NONE',  ( 1.948354844646963180, -11.88693049004113611, -1.364409644999339255 ) ) ;
#17766=CARTESIAN_POINT ( 'NONE',  ( 5.536195898058073439, -0.008323005098840522212, -0.001726268814999801574 ) ) ;
#17767=CARTESIAN_POINT ( 'NONE',  ( 0.3474126878361749604, -10.49748369253935998, 6.359473273659659753 ) ) ;
#17769=CARTESIAN_POINT ( 'NONE',  ( 2.241449424704146764, -7.528892370271783818, -1.265244293929165709 ) ) ;
#17772=CARTESIAN_POINT ( 'NONE',  ( 2.276198483117261251, -5.756970692722241267, -5.031786924855536469 ) ) ;
#17781=LINE ( 'NONE', #52050, #26112 ) ;
#17786=B_SPLINE_CURVE_WITH_KNOTS ( 'NONE', 3,
 ( #57414, #57094, #37784, #47124, #11519, #31790, #1577, #27465, #21850, #53076 ),
 .UNSPECIFIED., .F., .F.,
 ( 4, 3, 3, 4 ),
 ( 1.301042606982605321E-18, 6.607638129004456357E-05, 9.911389841680489732E-05, 0.0001667630577588619318 ),
 .UNSPECIFIED. ) ;
#17792=CARTESIAN_POINT ( 'NONE',  ( 2.305787727787084407, -4.792270232040854339, -5.970480882365271746 ) ) ;
#17794=CARTESIAN_POINT ( 'NONE',  ( 0.3474126878361818438, 2.385599230262039239, 12.03947592323247306 ) ) ;
#17795=CARTESIAN_POINT ( 'NONE',  ( 1.452237505248552996, 12.08199618361518013, -3.767214359061005435 ) ) ;
#17798=ORIENTED_EDGE ( 'NONE', *, *, #22087, .F. ) ;
#17806=CARTESIAN_POINT ( 'NONE',  ( 2.269879328256731554, -7.552124491910167770, -1.181008584586032306 ) ) ;
#17815=EDGE_LOOP ( 'NONE', ( #62563, #26879, #33484, #51560 ) ) ;
#17818=EDGE_CURVE ( 'NONE', #3364, #29286, #34627, .T. ) ;
#17826=CARTESIAN_POINT ( 'NONE',  ( 0.2833330754217401881, 11.58086621621913359, -3.999965385632473946 ) ) ;
#17829=CARTESIAN_POINT ( 'NONE',  ( 5.536195898058073439, -0.008496323383586770056, 0.0002547682446684717324 ) ) ;
#17830=ORIENTED_EDGE ( 'NONE', *, *, #2199, .T. ) ;
#17833=CARTESIAN_POINT ( 'NONE',  ( 0.2956976708475410054, -10.50256636126823473, -6.317697191869750206 ) ) ;
#17853=CARTESIAN_POINT ( 'NONE',  ( 0.3109076770649009669, 7.699281309344454982, -9.542672295796739590 ) ) ;
#17855=CARTESIAN_POINT ( 'NONE',  ( 2.280717697723836146, 1.481796453660317425, 7.502592193582054314 ) ) ;
#17859=CARTESIAN_POINT ( 'NONE',  ( 0.2958664285830424623, 12.10650684287254286, 1.910785783655619241 ) ) ;
#17864=EDGE_CURVE ( 'NONE', #32570, #38861, #47389, .T. ) ;
#17865=CARTESIAN_POINT ( 'NONE',  ( 3.152665057735843490, -3.546019893114926713, 7.102135024646879735 ) ) ;
#17882=CARTESIAN_POINT ( 'NONE',  ( 0.2834382757447999057, -11.44241760114838691, 4.380429851625286197 ) ) ;
#17887=CARTESIAN_POINT ( 'NONE',  ( 0.2801149460245153100, -9.509848747524133117, -7.723514566794077219 ) ) ;
#17888=DIRECTION ( 'NONE',  ( 0.000000000000000000, 0.000000000000000000, 1.000000000000000000 ) ) ;
#17891=CARTESIAN_POINT ( 'NONE',  ( 2.260457164927185847, 7.547495527593559572, 1.190240296002696541 ) ) ;
#17899=CARTESIAN_POINT ( 'NONE',  ( 0.4626703367449477300, 8.128802338754596235, -9.247028139127518642 ) ) ;
#17902=ORIENTED_EDGE ( 'NONE', *, *, #22107, .F. ) ;
#17903=CARTESIAN_POINT ( 'NONE',  ( 0.3006302518452036443, 5.932248915294314529, -10.72687985734936333 ) ) ;
#17904=CARTESIAN_POINT ( 'NONE',  ( 3.100650473569749543, 1.818095316078704560, -7.709402782713593361 ) ) ;
#17906=CARTESIAN_POINT ( 'NONE',  ( 2.994568964204212591, -1.761139509856882945, 7.686291764591503650 ) ) ;
#17912=ORIENTED_EDGE ( 'NONE', *, *, #60809, .T. ) ;
#17917=EDGE_CURVE ( 'NONE', #14308, #49252, #55816, .T. ) ;
#17919=CARTESIAN_POINT ( 'NONE',  ( 0.2956976708475479443, 8.045468685197048941, -9.245952174682468439 ) ) ;
#17921=CARTESIAN_POINT ( 'NONE',  ( 0.3164563675027571854, 11.60369811966062770, 3.967501530099125873 ) ) ;
#17933=CARTESIAN_POINT ( 'NONE',  ( 0.000000000000000000, 0.000000000000000000, 0.000000000000000000 ) ) ;
#17937=ORIENTED_EDGE ( 'NONE', *, *, #58173, .F. ) ;
#17938=EDGE_CURVE ( 'NONE', #28876, #6075, #10242, .T. ) ;
#17943=EDGE_CURVE ( 'NONE', #11296, #64733, #46546, .T. ) ;
#17944=CARTESIAN_POINT ( 'NONE',  ( 2.556980015512939186, 7.658710847181238179, 1.116161541731872653 ) ) ;
#17949=CARTESIAN_POINT ( 'NONE',  ( 0.2653519991613831897, -2.104847849998778830, -12.06397323649778031 ) ) ;
#17955=CARTESIAN_POINT ( 'NONE',  ( 2.524535260911985102, -0.2211075636758263463, -7.725637239510234622 ) ) ;
#17957=CARTESIAN_POINT ( 'NONE',  ( 2.288423627607477862, -3.963881558061918664, -6.543055113184263583 ) ) ;
#17962=EDGE_CURVE ( 'NONE', #35534, #24646, #28293, .T. ) ;
#17963=AXIS2_PLACEMENT_3D ( 'NONE', #65445, #4642, #19908 ) ;
#17975=CARTESIAN_POINT ( 'NONE',  ( 0.2646305136544065406, 11.46223899740605923, -4.312539723326019647 ) ) ;
#17990=CARTESIAN_POINT ( 'NONE',  ( 0.3665391374699464300, 0.2638605131388880864, -12.27992639892677929 ) ) ;
#17996=CARTESIAN_POINT ( 'NONE',  ( 2.889800649504073782, -4.645655809191389984, 3.986129653162632902 ) ) ;
#17997=CARTESIAN_POINT ( 'NONE',  ( 1.634816307074789865, -0.7191532042403158131, 12.68239325670730544 ) ) ;
#18004=B_SPLINE_CURVE_WITH_KNOTS ( 'NONE', 3,
 ( #4770, #55273, #24357, #25030, #39658, #9713, #9376, #29662, #49968, #60588, #45301, #20030, #40296, #25339, #15026, #35308 ),
 .UNSPECIFIED., .F., .F.,
 ( 4, 3, 3, 3, 3, 4 ),
 ( 5.421010862427522170E-19, 0.0003017745587525283912, 0.0006035491769808814383, 0.0009053241094668286080, 0.001207275924540519938, 0.001510325902534030013 ),
 .UNSPECIFIED. ) ;
#18005=CARTESIAN_POINT ( 'NONE',  ( 1.937114397841935398, -12.45230409340483391, 3.111612666690036999 ) ) ;
#18008=CARTESIAN_POINT ( 'NONE',  ( 0.2646305136544065406, -6.008537389229341663, -10.67138229758235646 ) ) ;
#18009=CARTESIAN_POINT ( 'NONE',  ( 0.3675815128205894289, 6.367184624550164429, 10.50067073900654080 ) ) ;
#18010=CARTESIAN_POINT ( 'NONE',  ( 2.907497136250194902, -7.666666002096546251, 1.716624290781062712 ) ) ;
#18019=CARTESIAN_POINT ( 'NONE',  ( 2.241509619876139059, -1.287997509666521045, -7.525055189891920904 ) ) ;
#18021=EDGE_CURVE ( 'NONE', #63698, #18517, #65596, .T. ) ;
#18027=ADVANCED_FACE ( 'NONE', ( #65361 ), #15707, .F. ) ;
#18029=CARTESIAN_POINT ( 'NONE',  ( 5.515188684475870851, 0.004322737127823480206, -0.003154373509839912288 ) ) ;
#18031=CARTESIAN_POINT ( 'NONE',  ( 0.2650492594609233921, 7.786980091309454011, 9.451471004987361368 ) ) ;
#18037=ORIENTED_EDGE ( 'NONE', *, *, #54266, .T. ) ;
#18041=ORIENTED_EDGE ( 'NONE', *, *, #14214, .F. ) ;
#18042=CARTESIAN_POINT ( 'NONE',  ( 0.3610902822527229938, 1.873269382026155228, -12.13436647668548929 ) ) ;
#18044=CARTESIAN_POINT ( 'NONE',  ( 1.109979610372368919, -9.281420052101120532, -8.414317452283038179 ) ) ;
#18047=CARTESIAN_POINT ( 'NONE',  ( 2.253265082353314686, 6.549959928642921980, 3.929729351084445099 ) ) ;
#18069=ORIENTED_EDGE ( 'NONE', *, *, #41184, .T. ) ;
#18074=CARTESIAN_POINT ( 'NONE',  ( 0.2872850955227758685, 3.994021792079249789, -11.58431228138434932 ) ) ;
#18076=CARTESIAN_POINT ( 'NONE',  ( 0.3675815128205894289, -3.951233083390547129, 11.62724744438064306 ) ) ;
#18078=CARTESIAN_POINT ( 'NONE',  ( 0.3610902822527287670, 9.572034936626899082, 7.689482111308885592 ) ) ;
#18085=EDGE_CURVE ( 'NONE', #65715, #10582, #21940, .T. ) ;
#18086=CARTESIAN_POINT ( 'NONE',  ( 1.372161826076905289, 1.607409531431637673, -12.51237317864402954 ) ) ;
#18109=CARTESIAN_POINT ( 'NONE',  ( 5.514970785353741078, 0.004588761610584827719, 0.001117786416802128355 ) ) ;
#18111=AXIS2_PLACEMENT_3D ( 'NONE', #46611, #36949, #26994 ) ;
#18119=CARTESIAN_POINT ( 'NONE',  ( 2.255723233588630361, -4.808373255829151205, -5.936060085173213707 ) ) ;
#18121=ORIENTED_EDGE ( 'NONE', *, *, #18360, .T. ) ;
#18126=ORIENTED_EDGE ( 'NONE', *, *, #62596, .T. ) ;
#18133=CARTESIAN_POINT ( 'NONE',  ( 1.462291587749892319, -12.32753368892837642, -2.816455204776596499 ) ) ;
#18138=CARTESIAN_POINT ( 'NONE',  ( 1.372161826075801283, 12.04315837901262221, 3.755740169579934840 ) ) ;
#18140=ORIENTED_EDGE ( 'NONE', *, *, #23367, .T. ) ;
#18142=ORIENTED_EDGE ( 'NONE', *, *, #1379, .F. ) ;
#18163=CARTESIAN_POINT ( 'NONE',  ( 0.9232058338315048962, -4.617996777200650271, 11.58467545991552328 ) ) ;
#18173=CARTESIAN_POINT ( 'NONE',  ( 2.259830038564998311, 3.938923657569498360, -6.546987858513332093 ) ) ;
#18180=CARTESIAN_POINT ( 'NONE',  ( 0.3675815128205912052, 3.951233083390468526, 11.62724744438066971 ) ) ;
#18185=VERTEX_POINT ( 'NONE', #15479 ) ;
#18194=ORIENTED_EDGE ( 'NONE', *, *, #19776, .T. ) ;
#18195=CARTESIAN_POINT ( 'NONE',  ( 2.373367633546869193, 2.455525055524889755, 7.275198254387420072 ) ) ;
#18197=CARTESIAN_POINT ( 'NONE',  ( 2.556980015514224824, -1.116161541731589102, 7.658710847181716019 ) ) ;
#18202=CARTESIAN_POINT ( 'NONE',  ( 2.257661810676422576, -0.1348365785570478925, -7.638648121130928281 ) ) ;
#18210=CARTESIAN_POINT ( 'NONE',  ( 1.198791140418975054, -8.460175745278220916, 9.279671759317787760 ) ) ;
#18224=CARTESIAN_POINT ( 'NONE',  ( 2.263328370261526334, -1.186889399881243978, 7.548992860189811971 ) ) ;
#18225=CARTESIAN_POINT ( 'NONE',  ( 0.3665391374699464300, 7.691255657244292721, 9.576575648339046509 ) ) ;
#18228=ORIENTED_EDGE ( 'NONE', *, *, #43745, .T. ) ;
#18229=CARTESIAN_POINT ( 'NONE',  ( 5.515188684475870851, -0.003154373509839893206, 0.004322737127823964194 ) ) ;
#18235=AXIS2_PLACEMENT_3D ( 'NONE', #16012, #20696, #21001 ) ;
#18239=CARTESIAN_POINT ( 'NONE',  ( 0.2872850955227734815, 5.944938343726402508, -10.71476594226527190 ) ) ;
#18241=CARTESIAN_POINT ( 'NONE',  ( 2.440552418640496768, 1.531218882877394050, -7.547055375260044663 ) ) ;
#18242=CARTESIAN_POINT ( 'NONE',  ( 3.100650473569749987, -1.818095316078653267, 7.709402782713603131 ) ) ;
#18243=EDGE_LOOP ( 'NONE', ( #62608, #36504, #31835, #26174 ) ) ;
#18245=FACE_OUTER_BOUND ( 'NONE', #25124, .T. ) ;
#18249=B_SPLINE_CURVE_WITH_KNOTS ( 'NONE', 3,
 ( #42476, #42154, #17243, #62443, #64099, #13540, #54789 ),
 .UNSPECIFIED., .F., .F.,
 ( 4, 3, 4 ),
 ( 0.000000000000000000, 0.001700533616330525194, 0.005002426799371280895 ),
 .UNSPECIFIED. ) ;
#18259=AXIS2_PLACEMENT_3D ( 'NONE', #38205, #22946, #29229 ) ;
#18263=PLANE ( 'NONE',  #42195 ) ;
#18266=CARTESIAN_POINT ( 'NONE',  ( 2.288423627607770960, 3.684511167348237581, -6.704349683466525711 ) ) ;
#18277=CARTESIAN_POINT ( 'NONE',  ( 3.100650473569752652, -7.276570693048392435, -3.129198107108044802 ) ) ;
#18284=CARTESIAN_POINT ( 'NONE',  ( 2.245754705088394587, -6.667819336165968558, 3.721112460996998994 ) ) ;
#18293=CARTESIAN_POINT ( 'NONE',  ( 2.305787727787084407, -3.682701754025465846, -6.711944854845862451 ) ) ;
#18297=CARTESIAN_POINT ( 'NONE',  ( 2.241352910868908754, -3.889181972941404553, -6.569501556381482921 ) ) ;
#18303=ORIENTED_EDGE ( 'NONE', *, *, #32927, .F. ) ;
#18306=CARTESIAN_POINT ( 'NONE',  ( 5.515188684475870851, 0.002166413411657797106, 0.004893136156458006460 ) ) ;
#18309=CARTESIAN_POINT ( 'NONE',  ( 0.2958664285830451823, 9.245659426743992881, -8.045892866065264215 ) ) ;
#18312=ORIENTED_EDGE ( 'NONE', *, *, #25770, .T. ) ;
#18318=EDGE_CURVE ( 'NONE', #15421, #27180, #51268, .T. ) ;
#18322=CARTESIAN_POINT ( 'NONE',  ( 2.253265082352431836, -7.543541742286985041, 1.199885753716602999 ) ) ;
#18323=EDGE_LOOP ( 'NONE', ( #34424, #14605, #50224, #37504 ) ) ;
#18326=EDGE_CURVE ( 'NONE', #52979, #64920, #16788, .T. ) ;
#18337=CARTESIAN_POINT ( 'NONE',  ( 0.2653519991613819129, -4.209134909048826145, 11.50013121838206764 ) ) ;
#18338=CARTESIAN_POINT ( 'NONE',  ( 0.2653519890518172830, 11.50766430042468969, 4.188437879978292422 ) ) ;
#18347=CARTESIAN_POINT ( 'NONE',  ( 0.3675815128205894289, 10.76447900494940235, 5.910255304480483751 ) ) ;
#18351=CARTESIAN_POINT ( 'NONE',  ( 5.536195898058073439, -0.001726268814999772300, 0.008323005098840527416 ) ) ;
#18354=CARTESIAN_POINT ( 'NONE',  ( 0.3057689695767480398, 12.03117299329039369, -2.355923806019077915 ) ) ;
#18355=CARTESIAN_POINT ( 'NONE',  ( 0.3341166715381371222, -2.378838837789017280, -12.03629799686217616 ) ) ;
#18360=EDGE_CURVE ( 'NONE', #43566, #27530, #32971, .T. ) ;
#18366=CARTESIAN_POINT ( 'NONE',  ( 2.241352910868908310, -1.407733736974815963, -7.503490710578247125 ) ) ;
#18371=CIRCLE ( 'NONE', #28846, 7.938172270156617749 ) ;
#18377=CARTESIAN_POINT ( 'NONE',  ( 2.770579946183340248, 5.249166435139440701, -5.784075095088735630 ) ) ;
#18381=ADVANCED_FACE ( 'NONE', ( #16685 ), #39689, .T. ) ;
#18384=CARTESIAN_POINT ( 'NONE',  ( 2.258463476536644254, -0.1358786215988691815, 7.638896687393373242 ) ) ;
#18388=CARTESIAN_POINT ( 'NONE',  ( 2.941278708680199916, -1.198640839021349436, 6.021511413163959325 ) ) ;
#18403=CARTESIAN_POINT ( 'NONE',  ( 3.152665057734036491, 7.923639299009025194, 0.4801242025592407647 ) ) ;
#18404=CARTESIAN_POINT ( 'NONE',  ( 0.2647959493198551173, -9.285851961022009604, 7.983607158780296587 ) ) ;
#18412=CARTESIAN_POINT ( 'NONE',  ( 1.452237505248552996, 2.778494755359218971, -12.34692280296789235 ) ) ;
#18424=CARTESIAN_POINT ( 'NONE',  ( 0.3164563675027678991, 9.546944054903095278, 7.696930404785069513 ) ) ;
#18432=CIRCLE ( 'NONE', #49191, 12.73084802173761787 ) ;
#18433=VERTEX_POINT ( 'NONE', #31334 ) ;
#18438=CARTESIAN_POINT ( 'NONE',  ( 0.3057689695767462079, -10.49983108339464266, 6.328747727191149863 ) ) ;
#18440=CARTESIAN_POINT ( 'NONE',  ( 5.520433897694421610, -0.005630909886752966977, 0.01397038704729857209 ) ) ;
#18442=CARTESIAN_POINT ( 'NONE',  ( 2.241528039335008771, -7.515727438419991024, -1.341200777944226097 ) ) ;
#18443=B_SPLINE_CURVE_WITH_KNOTS ( 'NONE', 3,
 ( #1558, #6529, #21832, #36778, #52078, #25485, #47103, #31463, #6205, #62059, #25829, #26158, #42079, #61073, #55760, #10192, #56765, #30472, #235, #15503, #35770, #46121 ),
 .UNSPECIFIED., .F., .F.,
 ( 4, 3, 3, 3, 3, 3, 3, 4 ),
 ( 8.741117365843378158E-19, 4.449119708436879495E-05, 6.626296329540436441E-05, 8.803456484962602063E-05, 0.0001098060367612803520, 0.0001315774408628526981, 0.0001760698110411182686, 0.0001829697163287819926 ),
 .UNSPECIFIED. ) ;
#18444=CARTESIAN_POINT ( 'NONE',  ( 1.283627346226762889, -11.16434663959575957, -5.810034161408871967 ) ) ;
#18446=B_SPLINE_CURVE_WITH_KNOTS ( 'NONE', 3,
 ( #14142, #14779, #34433, #14463, #29133, #9469, #35063 ),
 .UNSPECIFIED., .F., .F.,
 ( 4, 3, 4 ),
 ( 4.722362119209427361E-15, 0.002398160485434635940, 0.005002426799381492345 ),
 .UNSPECIFIED. ) ;
#18454=CIRCLE ( 'NONE', #56714, 12.73084802173761787 ) ;
#18455=B_SPLINE_CURVE_WITH_KNOTS ( 'NONE', 3,
 ( #59847, #29556, #3988, #59196, #9596, #43889, #39547, #54852, #13936, #34230, #40187, #44210, #35200, #3689, #24252, #18646, #49864, #54199, #8641 ),
 .UNSPECIFIED., .F., .F.,
 ( 4, 3, 3, 3, 3, 3, 4 ),
 ( 6.023423705678515846E-18, 4.457896483014980128E-05, 6.639290541542210437E-05, 8.820687556479006554E-05, 0.0001100173248778921805, 0.0001545671401658128613, 0.0001830328308068609349 ),
 .UNSPECIFIED. ) ;
#18476=CARTESIAN_POINT ( 'NONE',  ( 0.2648978790185593790, -4.063980959784970537, -11.55204314799267884 ) ) ;
#18485=ORIENTED_EDGE ( 'NONE', *, *, #2264, .F. ) ;
#18489=CARTESIAN_POINT ( 'NONE',  ( 1.719304012338833676, 3.626341562670448493, 12.20344780066006152 ) ) ;
#18492=CARTESIAN_POINT ( 'NONE',  ( 1.633930747250414317, 12.16309769563548393, 3.662223193116243891 ) ) ;
#18494=CARTESIAN_POINT ( 'NONE',  ( 1.020182472821183683, 7.686484208905105753, 9.854645283129331190 ) ) ;
#18517=VERTEX_POINT ( 'NONE', #27309 ) ;
#18518=CARTESIAN_POINT ( 'NONE',  ( 2.241451721903216399, -1.385577012535806229, 7.507681056655371776 ) ) ;
#18519=CARTESIAN_POINT ( 'NONE',  ( 0.3002738374340788163, -10.50101454678641133, -6.323236184341234356 ) ) ;
#18530=EDGE_CURVE ( 'NONE', #11089, #44680, #13892, .T. ) ;
#18531=CARTESIAN_POINT ( 'NONE',  ( 1.109979610369598912, 3.830786822173106732, 11.92772269523320716 ) ) ;
#18545=CARTESIAN_POINT ( 'NONE',  ( 2.941278708680199916, -5.814102272488603340, 1.972702289975983625 ) ) ;
#18546=CARTESIAN_POINT ( 'NONE',  ( 3.152665057735933640, -5.461013642407022139, -5.761241965768077122 ) ) ;
#18552=CARTESIAN_POINT ( 'NONE',  ( 2.249013661412228693, -5.926694833810643992, 4.816366775941328449 ) ) ;
#18554=CARTESIAN_POINT ( 'NONE',  ( 2.280717697723835702, -2.468022724683509583, 7.238333660707031214 ) ) ;
#18561=CARTESIAN_POINT ( 'NONE',  ( 3.152665057734128862, 5.461013642405629476, -5.761241965769021256 ) ) ;
#18564=CARTESIAN_POINT ( 'NONE',  ( 2.903928887688111526, 8.044738195289742322, -3.491800274468887189 ) ) ;
#18569=CARTESIAN_POINT ( 'NONE',  ( 1.937114397841932290, -3.111612666690160456, 12.45230409340480371 ) ) ;
#18570=CARTESIAN_POINT ( 'NONE',  ( 2.639814597422737386, 7.382549681340947245, -2.414168779979510848 ) ) ;
#18574=CARTESIAN_POINT ( 'NONE',  ( 2.241352910868908754, 7.532448145350508995, 1.243507963608119438 ) ) ;
#18577=ADVANCED_FACE ( 'NONE', ( #38614 ), #42917, .F. ) ;
#18581=ORIENTED_EDGE ( 'NONE', *, *, #54044, .F. ) ;
#18590=CARTESIAN_POINT ( 'NONE',  ( 2.305787727787084407, -5.047606869483016290, -5.756228004061508585 ) ) ;
#18594=CONICAL_SURFACE ( 'NONE', #47254, 7.938172270156617749, 1.280189991382167047 ) ;
#18599=EDGE_CURVE ( 'NONE', #60970, #4245, #23659, .T. ) ;
#18602=CARTESIAN_POINT ( 'NONE',  ( 0.2671309869109501078, 10.52409658627924571, -6.263183022891068319 ) ) ;
#18604=CARTESIAN_POINT ( 'NONE',  ( 0.9232058338315058954, -5.905985151448226667, 10.98407661738926677 ) ) ;
#18606=DIRECTION ( 'NONE',  ( 0.000000000000000000, 0.000000000000000000, 1.000000000000000000 ) ) ;
#18608=CARTESIAN_POINT ( 'NONE',  ( 2.247206125382828379, -1.439877054338154050, 7.499376972323892332 ) ) ;
#18609=CARTESIAN_POINT ( 'NONE',  ( 0.2653141334712560973, 7.837911425448908176, -9.409392642815664232 ) ) ;
#18610=CARTESIAN_POINT ( 'NONE',  ( 0.2653519890538382775, -0.02202236966336145602, 12.24619734961521544 ) ) ;
#18627=CARTESIAN_POINT ( 'NONE',  ( 1.719304012341273724, 0.7661785589598685275, -12.70777170743938456 ) ) ;
#18636=CARTESIAN_POINT ( 'NONE',  ( 2.524535260911804802, 5.776056274541051749, -5.135322114975449104 ) ) ;
#18646=CARTESIAN_POINT ( 'NONE',  ( 0.2676618633000457659, 12.24591287309139354, 0.1607051348608056485 ) ) ;
#18647=CARTESIAN_POINT ( 'NONE',  ( 0.3109076770649061849, 9.239379580302207629, -8.060731492642700502 ) ) ;
#18649=EDGE_LOOP ( 'NONE', ( #10336, #33586, #27253, #48587 ) ) ;
#18651=VERTEX_POINT ( 'NONE', #9639 ) ;
#18658=CARTESIAN_POINT ( 'NONE',  ( 2.305787727787085295, -3.971363876084009537, 6.545285700970515208 ) ) ;
#18659=CARTESIAN_POINT ( 'NONE',  ( 2.261269890822073414, -7.547924622047981202, 1.189259211195918375 ) ) ;
#18661=( BOUNDED_SURFACE ( )  B_SPLINE_SURFACE ( 3, 1, ( 
 ( #21535, #6572 ),
 ( #11223, #51142 ),
 ( #51796, #16208 ),
 ( #62396, #36489 ) ),
 .UNSPECIFIED., .F., .F., .F. ) 
 B_SPLINE_SURFACE_WITH_KNOTS ( ( 4, 4 ),
 ( 2, 2 ),
 ( 0.000000000000000000, 1.000000000000000000 ),
 ( 0.000000000000000000, 1.000000000000000000 ),
 .UNSPECIFIED. ) 
 GEOMETRIC_REPRESENTATION_ITEM ( )  RATIONAL_B_SPLINE_SURFACE ( (
 ( 1.000000000000000000, 1.000000000000000000),
 ( 0.6933888150995267674, 0.9895912004443193632),
 ( 0.6933888150995267674, 0.9895912004443193632),
 ( 1.000000000000000000, 1.000000000000000000) ) ) 
 REPRESENTATION_ITEM ( '' )  SURFACE ( )  );
#18662=CARTESIAN_POINT ( 'NONE',  ( 2.241451721903215955, 6.641849090085004903, -3.764430789729908522 ) ) ;
#18663=CARTESIAN_POINT ( 'NONE',  ( 2.251152103363646795, -2.729599998984361786, -7.133254101175212192 ) ) ;
#18673=CARTESIAN_POINT ( 'NONE',  ( 2.665405856346775071, 7.686816759402975485, -5.696318245876773823 ) ) ;
#18679=CARTESIAN_POINT ( 'NONE',  ( 1.287602823386882367, -0.5522659225150480244, 12.57487505104553804 ) ) ;
#18685=CARTESIAN_POINT ( 'NONE',  ( 20.00005080000000035, 4.898587196589412829E-16, -4.000000000000000000 ) ) ;
#18687=CARTESIAN_POINT ( 'NONE',  ( 0.3401186441510235525, -10.75260364139049329, 5.912862694513676409 ) ) ;
#18689=CARTESIAN_POINT ( 'NONE',  ( 2.491965175173618707, -7.560994562509134376, 1.548529392253887416 ) ) ;
#18699=CARTESIAN_POINT ( 'NONE',  ( 1.194176325881340039, -9.279760592562150023, 8.457794872459091451 ) ) ;
#18703=B_SPLINE_CURVE_WITH_KNOTS ( 'NONE', 3,
 ( #8030, #28297, #13642, #43569, #63853, #18337, #38602, #58915, #13328, #28614, #32597, #64202, #23645 ),
 .UNSPECIFIED., .F., .F.,
 ( 4, 3, 3, 3, 4 ),
 ( 3.878959614448864246E-18, 6.607593386745498512E-05, 0.0001321518677373512412, 0.0001982171734706196671, 0.0002642860854759480666 ),
 .UNSPECIFIED. ) ;
#18705=CARTESIAN_POINT ( 'NONE',  ( 2.373367633546871858, -7.528269033630144769, -1.511052049479995718 ) ) ;
#18715=VECTOR ( 'NONE', #23771, 1000.000000000000114 ) ;
#18720=CARTESIAN_POINT ( 'NONE',  ( 0.2653519991613825790, -12.24619736885323995, -0.02201648635055044115 ) ) ;
#18721=ORIENTED_EDGE ( 'NONE', *, *, #7329, .T. ) ;
#18723=ORIENTED_EDGE ( 'NONE', *, *, #61672, .T. ) ;
#18728=CARTESIAN_POINT ( 'NONE',  ( 2.440552418640495880, 5.770332237304444334, 5.099602138956223385 ) ) ;
#18730=CARTESIAN_POINT ( 'NONE',  ( 5.515188684475870851, -0.0005703990286340425908, 0.005320786921497679470 ) ) ;
#18739=VERTEX_POINT ( 'NONE', #38381 ) ;
#18743=DIRECTION ( 'NONE',  ( -1.000000000000000000, -0.000000000000000000, -0.000000000000000000 ) ) ;
#18751=VERTEX_POINT ( 'NONE', #8454 ) ;
#18753=CARTESIAN_POINT ( 'NONE',  ( 0.2648978790185619880, -9.295532325666501450, 7.972372351882998309 ) ) ;
#18757=CARTESIAN_POINT ( 'NONE',  ( 3.152665057734040488, 0.000000000000000000, 0.000000000000000000 ) ) ;
#18758=EDGE_CURVE ( 'NONE', #5369, #20748, #4125, .T. ) ;
#18759=CARTESIAN_POINT ( 'NONE',  ( 0.3160775863651080764, 10.73821170199163078, -5.922381034681481360 ) ) ;
#18760=VECTOR ( 'NONE', #37681, 1000.000000000000000 ) ;
#18764=CARTESIAN_POINT ( 'NONE',  ( 2.827825597296807825, -6.550135365664038645, -6.207590800588439706 ) ) ;
#18765=CARTESIAN_POINT ( 'NONE',  ( 2.245754705088395475, -5.777230445738506859, -4.993005209687642498 ) ) ;
#18779=VERTEX_POINT ( 'NONE', #23421 ) ;
#18780=CARTESIAN_POINT ( 'NONE',  ( 5.514970785353741078, 0.002093325033903811663, -0.004233694591582961957 ) ) ;
#18782=CARTESIAN_POINT ( 'NONE',  ( 0.2911222467163570027, -12.10399882413660855, 1.916522451062495414 ) ) ;
#18785=CARTESIAN_POINT ( 'NONE',  ( 0.2767916011545370480, 2.313848297676449839, 12.02950149294534654 ) ) ;
#18805=ORIENTED_EDGE ( 'NONE', *, *, #54129, .T. ) ;
#18807=B_SPLINE_CURVE_WITH_KNOTS ( 'NONE', 3,
 ( #5835, #20770, #41040, #55358, #21427, #20443, #31403, #61323, #21081, #40374, #10447, #15758, #30726, #46373, #61012, #6145 ),
 .UNSPECIFIED., .F., .F.,
 ( 4, 3, 3, 3, 3, 4 ),
 ( 0.000000000000000000, 0.0002999043160757283960, 0.0005998071753050876649, 0.0008997092107374375387, 0.001204458948194999561, 0.001510329163475231107 ),
 .UNSPECIFIED. ) ;
#18816=VERTEX_POINT ( 'NONE', #24392 ) ;
#18822=DIRECTION ( 'NONE',  ( 0.000000000000000000, 0.000000000000000000, 1.000000000000000000 ) ) ;
#18824=ADVANCED_FACE ( 'NONE', ( #39035, #48703 ), #59659, .F. ) ;
#18825=ADVANCED_FACE ( 'NONE', ( #59326 ), #56530, .F. ) ;
#18832=EDGE_CURVE ( 'NONE', #14741, #61553, #22638, .T. ) ;
#18835=B_SPLINE_CURVE_WITH_KNOTS ( 'NONE', 3,
 ( #37732, #62650, #36748, #58027, #38043, #52712, #7135, #58348, #47711, #27105, #26772, #22104, #12770, #47070, #37060, #33058, #57042, #42697, #42358 ),
 .UNSPECIFIED., .F., .F.,
 ( 4, 3, 3, 3, 3, 3, 4 ),
 ( 9.072543920006869694E-18, 4.457896483014687393E-05, 6.639290541542043741E-05, 8.820687556478911686E-05, 0.0001100173248778932783, 0.0001545671401658158157, 0.0001830328308068589834 ),
 .UNSPECIFIED. ) ;
#18839=( BOUNDED_SURFACE ( )  B_SPLINE_SURFACE ( 3, 1, ( 
 ( #46342, #4811 ),
 ( #60982, #65300 ),
 ( #45672, #55325 ),
 ( #20080, #15416 ) ),
 .UNSPECIFIED., .F., .F., .F. ) 
 B_SPLINE_SURFACE_WITH_KNOTS ( ( 4, 4 ),
 ( 2, 2 ),
 ( 0.000000000000000000, 1.000000000000000000 ),
 ( 0.000000000000000000, 1.000000000000000000 ),
 .UNSPECIFIED. ) 
 GEOMETRIC_REPRESENTATION_ITEM ( )  RATIONAL_B_SPLINE_SURFACE ( (
 ( 1.000000000000000000, 1.000000000000000000),
 ( 0.6933888150995267674, 0.9895912004443193632),
 ( 0.6933888150995267674, 0.9895912004443193632),
 ( 1.000000000000000000, 1.000000000000000000) ) ) 
 REPRESENTATION_ITEM ( '' )  SURFACE ( )  );
#18842=CARTESIAN_POINT ( 'NONE',  ( 2.247112776671467582, 1.440655381229470233, 7.499199956301994874 ) ) ;
#18848=CARTESIAN_POINT ( 'NONE',  ( 1.948354844646123629, -8.228891433296906754, -8.685970062895197685 ) ) ;
#18849=CARTESIAN_POINT ( 'NONE',  ( 2.273267844204867938, -0.1513603614829975852, -7.643541951623947561 ) ) ;
#18850=CARTESIAN_POINT ( 'NONE',  ( 1.372161826076866653, -4.864129100816962925, -11.63973780005257019 ) ) ;
#18852=CARTESIAN_POINT ( 'NONE',  ( 0.2655924914740778187, -7.905499957109299203, 9.352877839710574293 ) ) ;
#18853=CARTESIAN_POINT ( 'NONE',  ( 0.9232058338315058954, 10.98407661738928631, 5.905985151448186699 ) ) ;
#18859=FACE_OUTER_BOUND ( 'NONE', #63851, .T. ) ;
#18861=CARTESIAN_POINT ( 'NONE',  ( 0.3278977287071183633, -8.073566434006636428, 9.235688435081703673 ) ) ;
#18862=CARTESIAN_POINT ( 'NONE',  ( 1.719304012341202004, 11.67935079956989775, -5.066286238790292273 ) ) ;
#18863=EDGE_CURVE ( 'NONE', #3903, #6328, #36150, .T. ) ;
#18867=B_SPLINE_CURVE_WITH_KNOTS ( 'NONE', 3,
 ( #10375, #744, #35959, #50322, #39078, #16015, #5087 ),
 .UNSPECIFIED., .F., .F.,
 ( 4, 3, 4 ),
 ( 2.185848306064139164E-15, 0.002398160485434442518, 0.005002426799378964853 ),
 .UNSPECIFIED. ) ;
#18870=CARTESIAN_POINT ( 'NONE',  ( 5.536195898058073439, -0.008323005098841084262, 0.001726268814999596442 ) ) ;
#18873=CARTESIAN_POINT ( 'NONE',  ( 2.990245332647798016, -6.814589384234918334, 5.049055049623243363 ) ) ;
#18874=CARTESIAN_POINT ( 'NONE',  ( 2.284126774967664808, 7.558363379199202647, -1.171808575345546721 ) ) ;
#18877=CARTESIAN_POINT ( 'NONE',  ( 2.242418902651939216, 7.535443599794976244, 1.227462051872167725 ) ) ;
#18879=ORIENTED_EDGE ( 'NONE', *, *, #8539, .F. ) ;
#18881=( LENGTH_UNIT ( ) NAMED_UNIT ( * ) SI_UNIT ( .MILLI., .METRE. ) );
#18889=CARTESIAN_POINT ( 'NONE',  ( 0.2915757698887277427, 5.940579417090927627, -10.71881693660615475 ) ) ;
#18895=CARTESIAN_POINT ( 'NONE',  ( 0.3665391374699467075, 9.237363111276769345, 8.095513416941262363 ) ) ;
#18908=CARTESIAN_POINT ( 'NONE',  ( 0.2648978790185584908, 7.972372351883154629, -9.295532325666371776 ) ) ;
#18909=CARTESIAN_POINT ( 'NONE',  ( 0.2651627923886356042, -9.437479615842690350, 7.803990550466266995 ) ) ;
#18921=CARTESIAN_POINT ( 'NONE',  ( 0.9232058338315058954, 8.301689855530167250, 9.306586124266621241 ) ) ;
#18922=CARTESIAN_POINT ( 'NONE',  ( 2.290907136833250757, -7.504812001538596178, -1.488079974905019309 ) ) ;
#18938=CARTESIAN_POINT ( 'NONE',  ( 2.781367136451633471, 5.783466416658805009, -5.255136723410042343 ) ) ;
#18951=CARTESIAN_POINT ( 'NONE',  ( 5.516018279890452902, 0.005331956019561711300, -0.004180585980734999839 ) ) ;
#18954=ORIENTED_EDGE ( 'NONE', *, *, #22087, .T. ) ;
#18955=ORIENTED_EDGE ( 'NONE', *, *, #64047, .T. ) ;
#18957=CARTESIAN_POINT ( 'NONE',  ( 2.253265082352433168, 7.220580418434058068, -2.491579069691517656 ) ) ;
#18959=DIRECTION ( 'NONE',  ( 0.3865475372811021382, -0.6075346789811253423, 0.6938894834605981998 ) ) ;
#18964=AXIS2_PLACEMENT_3D ( 'NONE', #9028, #49924, #8706 ) ;
#18973=CARTESIAN_POINT ( 'NONE',  ( 2.247206125382828823, 2.502718378778807207, 7.214589497757592618 ) ) ;
#18980=CARTESIAN_POINT ( 'NONE',  ( 0.2648978790185584908, 11.46165506714228322, 4.312320170909275774 ) ) ;
#18983=CARTESIAN_POINT ( 'NONE',  ( 1.719304012339844867, -10.62216384465586216, 7.017415949612814785 ) ) ;
#18985=EDGE_LOOP ( 'NONE', ( #64427, #57665, #63118, #48631 ) ) ;
#18986=CARTESIAN_POINT ( 'NONE',  ( 0.7400311444011711259, 10.91558650018042620, 5.892391870929054143 ) ) ;
#18993=CARTESIAN_POINT ( 'NONE',  ( 2.276905613633645853, -6.697548486790738664, -3.688905863353284520 ) ) ;
#18997=CARTESIAN_POINT ( 'NONE',  ( 2.276905613633652070, -7.644700064315451904, 0.1540880535620714475 ) ) ;
#19005=ADVANCED_FACE ( 'NONE', ( #6103 ), #60787, .F. ) ;
#19019=VECTOR ( 'NONE', #27090, 1000.000000000000114 ) ;
#19025=CARTESIAN_POINT ( 'NONE',  ( 0.2801149460245166978, 1.933835447580789957, -12.09752788490055053 ) ) ;
#19027=CARTESIAN_POINT ( 'NONE',  ( 2.573738926104375935, -7.355212866432314200, 2.426778239006430304 ) ) ;
#19028=CARTESIAN_POINT ( 'NONE',  ( 0.3675815128205894289, 3.951233083390626177, -11.62724744438061641 ) ) ;
#19031=EDGE_LOOP ( 'NONE', ( #5689, #35053, #52510, #21801 ) ) ;
#19038=CARTESIAN_POINT ( 'NONE',  ( 0.2648321136542712284, 10.53380804838497475, 6.245325033825767314 ) ) ;
#19039=CARTESIAN_POINT ( 'NONE',  ( 2.305787727787083519, -2.461236246751120849, 7.249469779319902329 ) ) ;
#19047=CARTESIAN_POINT ( 'NONE',  ( 0.2648978790185602672, -6.237101853238473659, -10.53870023327869987 ) ) ;
#19050=B_SPLINE_CURVE_WITH_KNOTS ( 'NONE', 3,
 ( #41415, #51101, #31134, #47098, #46117, #26797, #31457, #46749, #1553, #16811, #10846, #5557, #6859 ),
 .UNSPECIFIED., .F., .F.,
 ( 4, 3, 3, 3, 4 ),
 ( 2.453269466693398698E-18, 6.607593386745200356E-05, 0.0001321518677373506177, 0.0001982171734706192877, 0.0002642860854759468197 ),
 .UNSPECIFIED. ) ;
#19055=CARTESIAN_POINT ( 'NONE',  ( 0.3654063281920786332, 9.573804659448660104, 7.689576266239694924 ) ) ;
#19057=CARTESIAN_POINT ( 'NONE',  ( 2.350038591458106119, -4.227970903880792441, 9.744161863086473474 ) ) ;
#19073=CARTESIAN_POINT ( 'NONE',  ( 2.241352910868909643, -7.503490710578223144, -1.407733736974942973 ) ) ;
#19091=LINE ( 'NONE', #59993, #50275 ) ;
#19094=CARTESIAN_POINT ( 'NONE',  ( 3.152665057734121756, -0.4801242025592447060, 7.923639299008720549 ) ) ;
#19100=ORIENTED_EDGE ( 'NONE', *, *, #60975, .F. ) ;
#19102=DIRECTION ( 'NONE',  ( 0.000000000000000000, 0.000000000000000000, 1.000000000000000000 ) ) ;
#19124=DIRECTION ( 'NONE',  ( 0.000000000000000000, 0.000000000000000000, 1.000000000000000000 ) ) ;
#19137=CARTESIAN_POINT ( 'NONE',  ( 2.177405672431479644, -9.343720763424588682, 6.173731551723741440 ) ) ;
#19146=ADVANCED_FACE ( 'NONE', ( #58952 ), #46797, .F. ) ;
#19153=CARTESIAN_POINT ( 'NONE',  ( 5.530133899448235191, -0.004396748047611511757, 0.01536822665454945329 ) ) ;
#19154=EDGE_CURVE ( 'NONE', #28687, #62520, #56518, .T. ) ;
#19155=CONICAL_SURFACE ( 'NONE', #61625, 7.938172270156617749, 1.280189991382167047 ) ;
#19162=CARTESIAN_POINT ( 'NONE',  ( 0.2653519991613847440, 12.05632699103097494, 2.148211862902952074 ) ) ;
#19163=CARTESIAN_POINT ( 'NONE',  ( 5.515188684475870851, -0.005194992164431471750, -0.001283816547384778904 ) ) ;
#19164=CARTESIAN_POINT ( 'NONE',  ( 2.655192694323472047, -6.604353705985011480, -6.969384012965773145 ) ) ;
#19168=CARTESIAN_POINT ( 'NONE',  ( 2.373367633546871414, -6.557448619657612277, -3.994744114396157286 ) ) ;
#19169=CARTESIAN_POINT ( 'NONE',  ( 1.104777566491150553, -4.729982681549460999, -11.59867774809549701 ) ) ;
#19171=FACE_OUTER_BOUND ( 'NONE', #37070, .T. ) ;
#19172=CARTESIAN_POINT ( 'NONE',  ( 0.3665391374699467075, -0.2638605131388012115, 12.27992639892678284 ) ) ;
#19182=CARTESIAN_POINT ( 'NONE',  ( 1.104777566491141449, 12.24382064406183268, -2.644034362100568192 ) ) ;
#19185=CARTESIAN_POINT ( 'NONE',  ( 2.242819959140646358, -7.208832857235893954, 2.514828506625046423 ) ) ;
#19191=CARTESIAN_POINT ( 'NONE',  ( 3.152665057734127529, -7.281573230474269742, -3.161213418913537687 ) ) ;
#19194=CARTESIAN_POINT ( 'NONE',  ( 2.247112776669946133, 1.211104213049043032, -7.539676020704888515 ) ) ;
#19199=ORIENTED_EDGE ( 'NONE', *, *, #42241, .F. ) ;
#19200=DIRECTION ( 'NONE',  ( -0.3865475372811021937, 0.9114221272958270559, 0.1410344188397433807 ) ) ;
#19201=ADVANCED_FACE ( 'NONE', ( #59918 ), #60015, .F. ) ;
#19202=FACE_OUTER_BOUND ( 'NONE', #38041, .T. ) ;
#19204=VECTOR ( 'NONE', #53902, 999.9999999999998863 ) ;
#19205=CARTESIAN_POINT ( 'NONE',  ( 3.152665057734126197, -1.848755561852092333, 7.719888720907804647 ) ) ;
#19206=CARTESIAN_POINT ( 'NONE',  ( 3.152665057734119536, 1.848755561852129858, -7.719888720907784219 ) ) ;
#19209=VERTEX_POINT ( 'NONE', #29312 ) ;
#19211=CARTESIAN_POINT ( 'NONE',  ( 2.269879328256730222, -7.232310762824150530, -2.474479066008294037 ) ) ;
#19213=EDGE_CURVE ( 'NONE', #14308, #45693, #12105, .T. ) ;
#19226=CARTESIAN_POINT ( 'NONE',  ( 2.256373768223414622, 7.638251659827605344, -0.1329433694244546993 ) ) ;
#19227=VECTOR ( 'NONE', #61022, 1000.000000000000114 ) ;
#19229=CARTESIAN_POINT ( 'NONE',  ( 0.2653519789438759102, 7.854827495960937433, -9.395292406847850941 ) ) ;
#19230=CARTESIAN_POINT ( 'NONE',  ( 0.2653519890518156177, -9.381125756446625275, 7.871710682401878323 ) ) ;
#19232=DIRECTION ( 'NONE',  ( -0.3865475372811021382, -0.4442537292684440309, 0.8082200352954602707 ) ) ;
#19234=CARTESIAN_POINT ( 'NONE',  ( 0.7446945582528475827, 0.3561743995939678498, -12.40088838630016888 ) ) ;
#19235=CARTESIAN_POINT ( 'NONE',  ( 1.719304012338199517, 12.70777170743846796, 0.7661785589580254463 ) ) ;
#19240=AXIS2_PLACEMENT_3D ( 'NONE', #48391, #43358, #54683 ) ;
#19245=AXIS2_PLACEMENT_3D ( 'NONE', #13082, #18743, #34002 ) ;
#19249=CARTESIAN_POINT ( 'NONE',  ( 5.515539859299206427, -0.005142293699651846045, 0.003193223631739306942 ) ) ;
#19252=CARTESIAN_POINT ( 'NONE',  ( 0.2652384770603654629, 9.338499095996429133, 7.922175044417011591 ) ) ;
#19254=VERTEX_POINT ( 'NONE', #30606 ) ;
#19266=CARTESIAN_POINT ( 'NONE',  ( 2.907497136250074554, 5.781215374755592329, -5.319973245618017543 ) ) ;
#19269=FACE_OUTER_BOUND ( 'NONE', #55831, .T. ) ;
#19271=EDGE_CURVE ( 'NONE', #16301, #25549, #19308, .T. ) ;
#19273=ORIENTED_EDGE ( 'NONE', *, *, #21341, .F. ) ;
#19278=DIRECTION ( 'NONE',  ( 0.3939253465568944290, 0.7103112711423489323, -0.5833358547425069318 ) ) ;
#19279=CARTESIAN_POINT ( 'NONE',  ( 2.969415267405009384, 6.619534278261656191, -4.269695207293545458 ) ) ;
#19281=CARTESIAN_POINT ( 'NONE',  ( 0.9296196016834407105, -12.46069139398445103, -0.4155906739600075950 ) ) ;
#19284=EDGE_LOOP ( 'NONE', ( #60584, #6041, #29875, #58984 ) ) ;
#19286=CARTESIAN_POINT ( 'NONE',  ( 2.177405672431599992, -8.997150696569100603, -6.668684901899186279 ) ) ;
#19289=CARTESIAN_POINT ( 'NONE',  ( 2.903928887688913107, 8.753847148604096517, -0.5297564406060942810 ) ) ;
#19294=CARTESIAN_POINT ( 'NONE',  ( 3.152665057734119536, 7.281573230474295499, 3.161213418913482620 ) ) ;
#19295=FACE_OUTER_BOUND ( 'NONE', #13393, .T. ) ;
#19299=VERTEX_POINT ( 'NONE', #36915 ) ;
#19308=B_SPLINE_CURVE_WITH_KNOTS ( 'NONE', 3,
 ( #20313, #40598, #50917, #40933, #15330, #5362, #47253, #30944, #21295, #31593, #32252, #16966, #17309 ),
 .UNSPECIFIED., .F., .F.,
 ( 4, 3, 3, 3, 4 ),
 ( 2.168404344971008868E-18, 6.607593386745438881E-05, 0.0001321518677373503738, 0.0001982171734706192063, 0.0002642860854759491508 ),
 .UNSPECIFIED. ) ;
#19309=CARTESIAN_POINT ( 'NONE',  ( 0.2653141334712562083, 11.52266042163707560, 4.147025708564464175 ) ) ;
#19314=CARTESIAN_POINT ( 'NONE',  ( 2.253265082352433168, -7.132841660187145827, -2.732639326785877731 ) ) ;
#19316=EDGE_LOOP ( 'NONE', ( #32143, #61466, #62175, #14355 ) ) ;
#19324=DIRECTION ( 'NONE',  ( -1.000000000000000000, -0.000000000000000000, -0.000000000000000000 ) ) ;
#19325=ADVANCED_FACE ( 'NONE', ( #56562 ), #23498, .F. ) ;
#19326=VERTEX_POINT ( 'NONE', #31918 ) ;
#19330=ORIENTED_EDGE ( 'NONE', *, *, #32193, .F. ) ;
#19331=CARTESIAN_POINT ( 'NONE',  ( 2.242418902651940549, -7.634109827927228586, 0.09970190380430356270 ) ) ;
#19333=ORIENTED_EDGE ( 'NONE', *, *, #54609, .T. ) ;
#19338=CARTESIAN_POINT ( 'NONE',  ( 0.2648978790185584908, -9.295532325666394868, -7.972372351883127095 ) ) ;
#19339=CARTESIAN_POINT ( 'NONE',  ( 0.8320506296491624321, -9.275353261146591421, 8.282532257448787405 ) ) ;
#19341=CARTESIAN_POINT ( 'NONE',  ( 2.241537034860907163, 3.821322318518465266, -6.609284473755296929 ) ) ;
#19342=CARTESIAN_POINT ( 'NONE',  ( 0.9296196016828991437, 1.754499435240217453, 12.34355205587671200 ) ) ;
#19353=B_SPLINE_CURVE_WITH_KNOTS ( 'NONE', 3,
 ( #48009, #44307, #27704, #43004, #63279, #28370, #3121, #43653, #38685, #8416 ),
 .UNSPECIFIED., .F., .F.,
 ( 4, 3, 3, 4 ),
 ( 0.000000000000000000, 6.607638129004453646E-05, 9.911389841680473469E-05, 0.0001667630577588630702 ),
 .UNSPECIFIED. ) ;
#19354=ORIENTED_EDGE ( 'NONE', *, *, #21724, .T. ) ;
#19357=EDGE_CURVE ( 'NONE', #44256, #5538, #52644, .T. ) ;
#19359=CARTESIAN_POINT ( 'NONE',  ( 0.2834382757448032919, 1.927645269571043984, -12.09963924911732391 ) ) ;
#19362=CARTESIAN_POINT ( 'NONE',  ( 2.284126774969132523, -1.171808575344847503, -7.558363379199810161 ) ) ;
#19365=ORIENTED_EDGE ( 'NONE', *, *, #42176, .T. ) ;
#19373=CARTESIAN_POINT ( 'NONE',  ( 2.899286259009677291, 5.780956296532521854, 5.316140236670786834 ) ) ;
#19374=CARTESIAN_POINT ( 'NONE',  ( 2.241352910868909643, 3.744764251557084922, -6.652881166698471738 ) ) ;
#19376=CARTESIAN_POINT ( 'NONE',  ( 2.589278595513357484, -2.423168677231944734, 7.361833592938436865 ) ) ;
#19384=EDGE_CURVE ( 'NONE', #31007, #62530, #9746, .T. ) ;
#19387=ORIENTED_EDGE ( 'NONE', *, *, #13417, .F. ) ;
#19389=STYLED_ITEM ( 'NONE', ( #63749 ), #29035 ) ;
#19392=FACE_OUTER_BOUND ( 'NONE', #6944, .T. ) ;
#19397=CARTESIAN_POINT ( 'NONE',  ( 0.3218525148189793628, -3.964374483810575445, -11.60666749448228607 ) ) ;
#19400=ORIENTED_EDGE ( 'NONE', *, *, #51870, .T. ) ;
#19405=CARTESIAN_POINT ( 'NONE',  ( 1.194176325881338263, 1.672143286119727179, -12.44396189284383070 ) ) ;
#19406=DIRECTION ( 'NONE',  ( -1.000000000000000000, -0.000000000000000000, -0.000000000000000000 ) ) ;
#19408=CARTESIAN_POINT ( 'NONE',  ( 0.2651627923886311078, 0.08809136839532921703, -12.24583724871548540 ) ) ;
#19418=CARTESIAN_POINT ( 'NONE',  ( 1.634816307074518305, 12.36483956257112204, 2.910502128620317208 ) ) ;
#19434=CARTESIAN_POINT ( 'NONE',  ( 2.665405856346786173, -0.5773576323838383040, 9.549966053095403140 ) ) ;
#19440=DIRECTION ( 'NONE',  ( 0.000000000000000000, 0.000000000000000000, 1.000000000000000000 ) ) ;
#19451=CARTESIAN_POINT ( 'NONE',  ( 0.2653519991613820794, 6.142165520908316800, -10.59450977800975480 ) ) ;
#19453=CARTESIAN_POINT ( 'NONE',  ( 0.2648978790185593790, 4.312320170909392125, -11.46165506714223703 ) ) ;
#19454=CARTESIAN_POINT ( 'NONE',  ( 0.3223008802179273546, -10.74209118105752658, -5.919638939520693199 ) ) ;
#19455=CARTESIAN_POINT ( 'NONE',  ( 2.241534463349553086, 0.005768439177839456040, 7.634462073473345711 ) ) ;
#19458=CARTESIAN_POINT ( 'NONE',  ( 5.516018279890452902, -0.006440244342253398716, 0.002104829434641079973 ) ) ;
#19463=ORIENTED_EDGE ( 'NONE', *, *, #64171, .T. ) ;
#19464=CARTESIAN_POINT ( 'NONE',  ( 0.3675815128205912052, 9.574637318042068301, -7.689697408877177232 ) ) ;
#19479=CARTESIAN_POINT ( 'NONE',  ( 2.241537034860907163, -1.330359961362336696, 7.517665055736002522 ) ) ;
#19481=CARTESIAN_POINT ( 'NONE',  ( 1.719304012339867516, -12.38166659046446938, 2.961219984258617544 ) ) ;
#19486=ORIENTED_EDGE ( 'NONE', *, *, #47038, .F. ) ;
#19490=CARTESIAN_POINT ( 'NONE',  ( 0.5572780756280654169, 3.933334466452599987, 11.70006938410048036 ) ) ;
#19503=CARTESIAN_POINT ( 'NONE',  ( 5.514970785353741078, -0.004713149585127258956, -0.0003039746380524797073 ) ) ;
#19504=B_SPLINE_CURVE_WITH_KNOTS ( 'NONE', 3,
 ( #4371, #40921, #15630, #55223, #4718, #24979, #25288, #30929, #5695, #45252, #55565, #15317, #35901, #10006, #5025, #20303, #40585, #60877, #35593 ),
 .UNSPECIFIED., .F., .F.,
 ( 4, 3, 3, 3, 3, 3, 4 ),
 ( 4.336808689942017736E-19, 2.831840207457924380E-05, 4.217266859783480663E-05, 5.602024318339633507E-05, 6.290810167913046238E-05, 9.120440630890213501E-05, 0.0001153103026480247297 ),
 .UNSPECIFIED. ) ;
#19508=B_SPLINE_CURVE_WITH_KNOTS ( 'NONE', 3,
 ( #59821, #24898, #4636, #25211, #60456, #4949, #55143, #45173, #19901, #65751, #14880, #35171, #55478, #55815, #30840, #39522 ),
 .UNSPECIFIED., .F., .F.,
 ( 4, 3, 3, 3, 3, 4 ),
 ( 1.669781113969282313E-15, 0.0002126834539180026825, 0.0004253519300366890199, 0.0006380165497225110402, 0.0007442707582429369719, 0.0009453531351410801977 ),
 .UNSPECIFIED. ) ;
#19521=CARTESIAN_POINT ( 'NONE',  ( 2.241534463349552198, -1.511811348926356884E-18, -7.634462073473343935 ) ) ;
#19528=CARTESIAN_POINT ( 'NONE',  ( 1.372161826078031277, 12.30755118281487981, -2.769012792637354003 ) ) ;
#19532=CARTESIAN_POINT ( 'NONE',  ( 0.3474126878361833981, -9.566300984424350062, -7.689340002166830779 ) ) ;
#19536=CARTESIAN_POINT ( 'NONE',  ( 1.719304012338398469, 8.755325027793414705, 9.242227816402090568 ) ) ;
#19539=EDGE_CURVE ( 'NONE', #11247, #38647, #29243, .T. ) ;
#19543=B_SPLINE_CURVE_WITH_KNOTS ( 'NONE', 3,
 ( #1178, #26121, #15474, #10477, #41067, #50738, #56728, #5527, #845, #5864, #41387, #46084, #31429, #41728, #198, #11462 ),
 .UNSPECIFIED., .F., .F.,
 ( 4, 3, 3, 3, 3, 4 ),
 ( 0.000000000000000000, 0.0002999043160757425448, 0.0005998071753051165047, 0.0008997092107374801478, 0.001204458948196538044, 0.001510329163478281618 ),
 .UNSPECIFIED. ) ;
#19547=DIRECTION ( 'NONE',  ( -1.000000000000000000, -0.000000000000000000, -0.000000000000000000 ) ) ;
#19548=ORIENTED_EDGE ( 'NONE', *, *, #14540, .F. ) ;
#19554=CARTESIAN_POINT ( 'NONE',  ( 3.152665057734023613, 0.4801242025591827001, -7.923639299008664594 ) ) ;
#19561=CARTESIAN_POINT ( 'NONE',  ( 2.305787727787083519, 7.135468203930020792, -2.774453000917077805 ) ) ;
#19563=CARTESIAN_POINT ( 'NONE',  ( 2.241352910868908310, -7.633946224498474820, 0.08337961031701579540 ) ) ;
#19567=CARTESIAN_POINT ( 'NONE',  ( 2.241317068080781905, 7.633845645378814382, -0.09149433816018485988 ) ) ;
#19572=CARTESIAN_POINT ( 'NONE',  ( 1.109979610372149761, 0.4797593171736048157, -12.51859925746178703 ) ) ;
#19579=CARTESIAN_POINT ( 'NONE',  ( 5.530133899448235191, 0.006998616117863598260, 0.01437126147332036877 ) ) ;
#19584=CARTESIAN_POINT ( 'NONE',  ( 2.241536586108912932, -4.902521014023369261, 5.852386772940055160 ) ) ;
#19590=CARTESIAN_POINT ( 'NONE',  ( 2.257661810676417691, -3.702552158175651087, 6.682681612748201161 ) ) ;
#19612=CARTESIAN_POINT ( 'NONE',  ( 2.259830038564996979, -6.546987858513350744, -3.938923657569476600 ) ) ;
#19619=CARTESIAN_POINT ( 'NONE',  ( 0.8375941296801611147, -12.43103843094034389, -0.3844307390187421403 ) ) ;
#19621=CARTESIAN_POINT ( 'NONE',  ( 2.241352910868909643, -7.145045428366594287, 2.689314586382326677 ) ) ;
#19631=ORIENTED_EDGE ( 'NONE', *, *, #23754, .T. ) ;
#19632=CARTESIAN_POINT ( 'NONE',  ( 2.241352910868908310, 6.652881166698564108, -3.744764251556923274 ) ) ;
#19633=( BOUNDED_SURFACE ( )  B_SPLINE_SURFACE ( 3, 1, ( 
 ( #14129, #54723 ),
 ( #24434, #9144 ),
 ( #29426, #33752 ),
 ( #44707, #49722 ) ),
 .UNSPECIFIED., .F., .F., .F. ) 
 B_SPLINE_SURFACE_WITH_KNOTS ( ( 4, 4 ),
 ( 2, 2 ),
 ( 0.000000000000000000, 1.000000000000000000 ),
 ( 0.000000000000000000, 1.000000000000000000 ),
 .UNSPECIFIED. ) 
 GEOMETRIC_REPRESENTATION_ITEM ( )  RATIONAL_B_SPLINE_SURFACE ( (
 ( 1.000000000000000000, 1.000000000000000000),
 ( 0.6933888150995267674, 0.9895912004443193632),
 ( 0.6933888150995267674, 0.9895912004443193632),
 ( 1.000000000000000000, 1.000000000000000000) ) ) 
 REPRESENTATION_ITEM ( '' )  SURFACE ( )  );
#19635=CARTESIAN_POINT ( 'NONE',  ( 2.781367136452162825, 7.232043329634170625, -2.960151187464861611 ) ) ;
#19636=ORIENTED_EDGE ( 'NONE', *, *, #15780, .F. ) ;
#19637=ORIENTED_EDGE ( 'NONE', *, *, #7908, .T. ) ;
#19642=B_SPLINE_CURVE_WITH_KNOTS ( 'NONE', 3,
 ( #61690, #61055, #15485, #35751, #56384, #15800, #30766, #51086, #16152, #36078, #36431, #31443, #51430, #11168, #11800, #36758, #43048, #32083, #2522 ),
 .UNSPECIFIED., .F., .F.,
 ( 4, 3, 3, 3, 3, 3, 4 ),
 ( 0.000000000000000000, 2.831840207499679716E-05, 4.217266859840589657E-05, 5.602024318396098078E-05, 6.290810167969312265E-05, 9.120440630945326208E-05, 0.0001153103026479758322 ),
 .UNSPECIFIED. ) ;
#19657=CARTESIAN_POINT ( 'NONE',  ( 0.6511581176972706109, 9.688955459275215176, -7.698038847496603054 ) ) ;
#19658=CARTESIAN_POINT ( 'NONE',  ( 5.515188684475870851, 0.003154373509839897977, 0.004322737127823491482 ) ) ;
#19659=CARTESIAN_POINT ( 'NONE',  ( 2.241317068080794783, -6.656851426547295780, -3.737686401540284198 ) ) ;
#19660=VERTEX_POINT ( 'NONE', #628 ) ;
#19662=EDGE_CURVE ( 'NONE', #49910, #63048, #63671, .T. ) ;
#19664=CARTESIAN_POINT ( 'NONE',  ( 1.459561108992809331, 6.861308540877414153, 10.62073135189154272 ) ) ;
#19668=CARTESIAN_POINT ( 'NONE',  ( 1.459561108992595502, 10.08002506399508214, 7.633517148169521427 ) ) ;
#19671=CARTESIAN_POINT ( 'NONE',  ( 0.6473888112830242791, -9.263269341114842348, 8.203438694127630271 ) ) ;
#19679=B_SPLINE_CURVE_WITH_KNOTS ( 'NONE', 3,
 ( #43783, #34110, #29155, #19823, #65030, #28477, #29773, #8211, #28813, #34454, #4202, #48784, #50089, #8863, #4548, #33485 ),
 .UNSPECIFIED., .F., .F.,
 ( 4, 3, 3, 3, 3, 4 ),
 ( 2.158593104248768223E-15, 0.0002126834539180167500, 0.0004253519300367212207, 0.0006380165497225577693, 0.0007442707582429906399, 0.0009453531351407485402 ),
 .UNSPECIFIED. ) ;
#19685=CARTESIAN_POINT ( 'NONE',  ( 2.406456491626453698, -1.188938370543003442, 10.36527681095974707 ) ) ;
#19696=ORIENTED_EDGE ( 'NONE', *, *, #46160, .F. ) ;
#19698=EDGE_LOOP ( 'NONE', ( #25274, #21418, #24847, #45505 ) ) ;
#19700=CARTESIAN_POINT ( 'NONE',  ( 2.573738926104377711, 2.868819712476807560, -7.194322927777922594 ) ) ;
#19707=CARTESIAN_POINT ( 'NONE',  ( 0.3040950598368144520, 9.552450779732218678, -7.687624643091335308 ) ) ;
#19708=CARTESIAN_POINT ( 'NONE',  ( 2.781367136452256084, -2.381060477055441549, 7.442815111163296748 ) ) ;
#19719=CARTESIAN_POINT ( 'NONE',  ( 0.4626703367446075021, -9.611037151103436926, 7.694993290995456370 ) ) ;
#19720=VERTEX_POINT ( 'NONE', #32164 ) ;
#19731=ORIENTED_EDGE ( 'NONE', *, *, #36834, .F. ) ;
#19735=CARTESIAN_POINT ( 'NONE',  ( 0.9232167919969115344, -12.45862789703290652, 0.4134278310082598606 ) ) ;
#19746=CARTESIAN_POINT ( 'NONE',  ( 1.719304012338201737, 9.242227816402087015, 8.755325027793320558 ) ) ;
#19747=CARTESIAN_POINT ( 'NONE',  ( 0.6511581176956539041, 12.12498040206523875, 2.473966499147935760 ) ) ;
#19757=CARTESIAN_POINT ( 'NONE',  ( 2.298277635560276533, 6.709004959608422247, -3.682855706290065090 ) ) ;
#19764=ORIENTED_EDGE ( 'NONE', *, *, #25770, .F. ) ;
#19766=CARTESIAN_POINT ( 'NONE',  ( 0.2869720083484353368, -12.10169797402142500, 1.922200714744121575 ) ) ;
#19774=EDGE_CURVE ( 'NONE', #24593, #29718, #10563, .T. ) ;
#19776=EDGE_CURVE ( 'NONE', #19299, #20746, #32489, .T. ) ;
#19777=FACE_OUTER_BOUND ( 'NONE', #4276, .T. ) ;
#19778=CARTESIAN_POINT ( 'NONE',  ( 0.2651627682582892720, 6.046625184671136743, -10.64925413290587919 ) ) ;
#19784=CARTESIAN_POINT ( 'NONE',  ( 0.6511581176955547612, 7.698038847496699866, 9.688955459274410487 ) ) ;
#19789=LINE ( 'NONE', #60330, #31659 ) ;
#19799=VERTEX_POINT ( 'NONE', #17224 ) ;
#19807=CARTESIAN_POINT ( 'NONE',  ( 2.290907136833256086, 7.649199419879180617, 0.1622757685885358181 ) ) ;
#19810=EDGE_CURVE ( 'NONE', #646, #14018, #27068, .T. ) ;
#19820=CARTESIAN_POINT ( 'NONE',  ( 5.516018279890452902, 0.002527316374434305981, 0.006286471671801938804 ) ) ;
#19822=ORIENTED_EDGE ( 'NONE', *, *, #54136, .F. ) ;
#19823=CARTESIAN_POINT ( 'NONE',  ( 2.969415267403833880, -6.276215141898326522, -4.760005747566549594 ) ) ;
#19825=CARTESIAN_POINT ( 'NONE',  ( 1.452237505248555660, 12.64182585313126062, -0.5922625322517459656 ) ) ;
#19830=CARTESIAN_POINT ( 'NONE',  ( 0.5547464869798252041, -4.506704303875380013, -11.49049644196207964 ) ) ;
#19843=ORIENTED_EDGE ( 'NONE', *, *, #4786, .T. ) ;
#19853=CARTESIAN_POINT ( 'NONE',  ( 2.262775599886257094, -5.019217486251079663, 5.761998514039110120 ) ) ;
#19862=AXIS2_PLACEMENT_3D ( 'NONE', #39674, #45637, #44321 ) ;
#19865=ORIENTED_EDGE ( 'NONE', *, *, #55879, .F. ) ;
#19868=B_SPLINE_CURVE_WITH_KNOTS ( 'NONE', 3,
 ( #15124, #65342, #29752, #46070, #10148, #24445, #15460, #41054, #44724, #9808, #516, #30426, #49737, #25778, #25437, #60043, #19807, #30099, #25121 ),
 .UNSPECIFIED., .F., .F.,
 ( 4, 3, 3, 3, 3, 3, 4 ),
 ( 0.000000000000000000, 2.831840207499482866E-05, 4.217266859840272528E-05, 5.602024318395762653E-05, 6.290810167968828440E-05, 9.120440630944945382E-05, 0.0001153103026479763201 ),
 .UNSPECIFIED. ) ;
#19873=CARTESIAN_POINT ( 'NONE',  ( 2.241352910868909643, 7.145045428366612050, -2.689314586382279604 ) ) ;
#19874=CARTESIAN_POINT ( 'NONE',  ( 2.639814597422733833, -4.103563379978059977, 6.594772041715924793 ) ) ;
#19880=CARTESIAN_POINT ( 'NONE',  ( 1.719304012338836563, -2.961219984258077087, 12.38166659046417095 ) ) ;
#19891=CARTESIAN_POINT ( 'NONE',  ( 0.3610902822527202183, 0.2623004149194609336, 12.27530799859938071 ) ) ;
#19899=VERTEX_POINT ( 'NONE', #49138 ) ;
#19901=CARTESIAN_POINT ( 'NONE',  ( 2.653899356899545037, 2.411250235128249653, -7.388433688587198844 ) ) ;
#19908=DIRECTION ( 'NONE',  ( 0.000000000000000000, 0.000000000000000000, 1.000000000000000000 ) ) ;
#19919=ORIENTED_EDGE ( 'NONE', *, *, #58883, .T. ) ;
#19926=CARTESIAN_POINT ( 'NONE',  ( 3.152665057733834431, -3.161213418913157991, 7.281573230474281289 ) ) ;
#19928=CARTESIAN_POINT ( 'NONE',  ( 0.5572780756284301251, -10.83930267798907288, 5.905274004878299010 ) ) ;
#19933=CARTESIAN_POINT ( 'NONE',  ( 2.990245332647754051, 7.587819667496316534, -3.789007530133582602 ) ) ;
#19942=ORIENTED_EDGE ( 'NONE', *, *, #39476, .F. ) ;
#19949=CARTESIAN_POINT ( 'NONE',  ( 2.491965175173544100, -5.773748672881963806, 5.121563073453287096 ) ) ;
#19953=CARTESIAN_POINT ( 'NONE',  ( 2.835339799623985968, -1.035140033449997388, -7.763739326985123590 ) ) ;
#19957=CARTESIAN_POINT ( 'NONE',  ( 2.242819959140598840, -2.514828506625285787, -7.208832857235797142 ) ) ;
#19965=CARTESIAN_POINT ( 'NONE',  ( 0.2676618633000425462, -10.68562420805846891, 5.983781707237577407 ) ) ;
#19966=CARTESIAN_POINT ( 'NONE',  ( 0.2911222467163552818, 3.989243506922341531, 11.58731125337560997 ) ) ;
#19971=DIRECTION ( 'NONE',  ( -0.3939253465568943180, -0.4511294145502819930, 0.8008152550167551009 ) ) ;
#19977=CARTESIAN_POINT ( 'NONE',  ( 2.491965175173810998, 4.041154086925143218, 6.575382551509535212 ) ) ;
#19980=CARTESIAN_POINT ( 'NONE',  ( 2.266490820343232127, -4.800466063945415307, 5.947069344280080827 ) ) ;
#19989=CARTESIAN_POINT ( 'NONE',  ( 5.516018279890452902, -0.005331956019561440684, -0.004180585980734585240 ) ) ;
#20000=CARTESIAN_POINT ( 'NONE',  ( 3.152665057734062248, -7.609997527621111146, 2.258875078502258216 ) ) ;
#20006=ORIENTED_EDGE ( 'NONE', *, *, #39789, .T. ) ;
#20008=ADVANCED_FACE ( 'NONE', ( #42973 ), #40002, .F. ) ;
#20015=CARTESIAN_POINT ( 'NONE',  ( 2.257661810676953262, 4.806737555285070407, -5.938215228163155501 ) ) ;
#20023=CARTESIAN_POINT ( 'NONE',  ( 0.3474126878361845638, -6.359473273659631332, -10.49748369253938307 ) ) ;
#20030=CARTESIAN_POINT ( 'NONE',  ( 1.372161826076679469, -6.811451307636759545, -10.61825687422748388 ) ) ;
#20039=ORIENTED_EDGE ( 'NONE', *, *, #20655, .T. ) ;
#20057=CARTESIAN_POINT ( 'NONE',  ( 2.835339799623973089, -6.206025468804385881, 4.778327228934561965 ) ) ;
#20062=AXIS2_PLACEMENT_3D ( 'NONE', #24802, #50729, #34742 ) ;
#20069=LINE ( 'NONE', #48468, #34873 ) ;
#20075=CARTESIAN_POINT ( 'NONE',  ( 5.515188684475870851, 0.001485678338381713100, 0.005140903460551141980 ) ) ;
#20080=CARTESIAN_POINT ( 'NONE',  ( 5.516018279890452902, -0.006771744149385265123, 0.0002248006052448276067 ) ) ;
#20083=CARTESIAN_POINT ( 'NONE',  ( 2.241509619876139059, 6.592435552901117823, 3.850348903238736131 ) ) ;
#20085=ORIENTED_EDGE ( 'NONE', *, *, #40467, .T. ) ;
#20090=DIRECTION ( 'NONE',  ( 0.000000000000000000, 0.000000000000000000, 1.000000000000000000 ) ) ;
#20097=CARTESIAN_POINT ( 'NONE',  ( 0.2648978790185593790, -12.03635331166810651, -2.256510822326266652 ) ) ;
#20103=EDGE_CURVE ( 'NONE', #61553, #39884, #1760, .T. ) ;
#20105=VERTEX_POINT ( 'NONE', #28662 ) ;
#20108=FACE_OUTER_BOUND ( 'NONE', #12053, .T. ) ;
#20116=B_SPLINE_CURVE_WITH_KNOTS ( 'NONE', 3,
 ( #56506, #10951, #5311, #57169, #51544, #21243, #46215, #30888, #31550, #26563, #51207, #657, #20916, #37185, #51852, #41190 ),
 .UNSPECIFIED., .F., .F.,
 ( 4, 3, 3, 3, 3, 4 ),
 ( 2.342674890740637216E-15, 0.0002126834539179767430, 0.0004253519300366382250, 0.0006380165497224343871, 0.0007442707582428458989, 0.0009453531351416440912 ),
 .UNSPECIFIED. ) ;
#20129=EDGE_LOOP ( 'NONE', ( #24095, #53322, #18303, #58086 ) ) ;
#20132=DIRECTION ( 'NONE',  ( 0.000000000000000000, 0.000000000000000000, 1.000000000000000000 ) ) ;
#20139=DIRECTION ( 'NONE',  ( -1.000000000000000000, -0.000000000000000000, -0.000000000000000000 ) ) ;
#20143=CARTESIAN_POINT ( 'NONE',  ( 3.100650473569728671, -0.4517506188708464432, 7.907988569972077997 ) ) ;
#20148=CARTESIAN_POINT ( 'NONE',  ( 2.717984159219867468, -7.221467817271594036, 2.930214355830794037 ) ) ;
#20150=CARTESIAN_POINT ( 'NONE',  ( 2.241537034860906275, 7.634469414369386087, 0.004719967007703176898 ) ) ;
#20158=ORIENTED_EDGE ( 'NONE', *, *, #14547, .T. ) ;
#20165=CARTESIAN_POINT ( 'NONE',  ( 0.3537226245948358883, 7.688925565305018139, 9.569332148897489176 ) ) ;
#20169=CARTESIAN_POINT ( 'NONE',  ( 1.634816307077574971, -1.494046826341809853, -12.61459884933005782 ) ) ;
#20170=CARTESIAN_POINT ( 'NONE',  ( 0.3106921474978483477, -11.43920276778354328, -4.414111574791946602 ) ) ;
#20179=CARTESIAN_POINT ( 'NONE',  ( 5.520433897694421610, -0.01473594271720286668, 0.003119431460922364278 ) ) ;
#20182=CARTESIAN_POINT ( 'NONE',  ( 0.2646305136544065406, -10.53923716745242345, -6.237419468587189542 ) ) ;
#20186=ORIENTED_EDGE ( 'NONE', *, *, #15449, .T. ) ;
#20195=CARTESIAN_POINT ( 'NONE',  ( 2.263328370261530331, 7.131064289852376170, -2.746620058315224711 ) ) ;
#20197=CARTESIAN_POINT ( 'NONE',  ( 0.2651627682582926582, -10.56115808354087093, 6.199212018117401968 ) ) ;
#20200=CARTESIAN_POINT ( 'NONE',  ( 2.273267844204862609, 7.643541951623948449, -0.1513603614830752175 ) ) ;
#20201=CARTESIAN_POINT ( 'NONE',  ( 3.152665057734119536, 7.281573230474295499, 3.161213418913482620 ) ) ;
#20219=CARTESIAN_POINT ( 'NONE',  ( 2.844750968615706199, -7.767336242080769004, -1.031816958530684891 ) ) ;
#20220=CARTESIAN_POINT ( 'NONE',  ( 2.241317068080789898, 2.524952427345916739, -7.204761327832042817 ) ) ;
#20225=CARTESIAN_POINT ( 'NONE',  ( 2.241537034860906275, -6.609284473755313805, -3.821322318518443506 ) ) ;
#20232=CARTESIAN_POINT ( 'NONE',  ( 0.2717059086739043727, -0.1760722388997017218, -12.24704971877459592 ) ) ;
#20235=CARTESIAN_POINT ( 'NONE',  ( 0.2648978790185584908, 7.769924372105204036, 9.465406350830633642 ) ) ;
#20238=ORIENTED_EDGE ( 'NONE', *, *, #64750, .T. ) ;
#20240=ORIENTED_EDGE ( 'NONE', *, *, #65210, .F. ) ;
#20242=CARTESIAN_POINT ( 'NONE',  ( 2.261269890822070749, -6.546486799463086648, -3.940687015735715892 ) ) ;
#20245=CARTESIAN_POINT ( 'NONE',  ( 1.719304012338199517, 0.000000000000000000, 0.000000000000000000 ) ) ;
#20246=CARTESIAN_POINT ( 'NONE',  ( 2.827825597296806492, -4.975864478227457255, 7.528560921609606993 ) ) ;
#20251=CARTESIAN_POINT ( 'NONE',  ( 2.573738926104379043, -2.426778239006406324, -7.355212866432320418 ) ) ;
#20252=ORIENTED_EDGE ( 'NONE', *, *, #28831, .F. ) ;
#20253=CARTESIAN_POINT ( 'NONE',  ( 1.719304012341273280, -2.961219984259375160, -12.38166659046469675 ) ) ;
#20267=VERTEX_POINT ( 'NONE', #14348 ) ;
#20275=ORIENTED_EDGE ( 'NONE', *, *, #9811, .F. ) ;
#20286=CARTESIAN_POINT ( 'NONE',  ( 2.241352910868909643, -2.532612177304395029, -7.202080440908765979 ) ) ;
#20299=VERTEX_POINT ( 'NONE', #20322 ) ;
#20302=CARTESIAN_POINT ( 'NONE',  ( 2.440552418640497212, 6.765628357760830269, -3.678171968408256998 ) ) ;
#20303=CARTESIAN_POINT ( 'NONE',  ( 2.284126774967170537, -3.686252397487239651, -6.701756155761708911 ) ) ;
#20304=CARTESIAN_POINT ( 'NONE',  ( 2.305787727787084407, 2.774453000917148415, 7.135468203929992370 ) ) ;
#20313=CARTESIAN_POINT ( 'NONE',  ( 0.2648978790185593790, -2.256510822326224464, 12.03635331166811540 ) ) ;
#20319=VECTOR ( 'NONE', #31193, 1000.000000000000000 ) ;
#20322=CARTESIAN_POINT ( 'NONE',  ( 2.305787727787084407, -5.047606869483016290, -5.756228004061508585 ) ) ;
#20325=CARTESIAN_POINT ( 'NONE',  ( 2.276198483118644145, -1.175725118477902287, -7.555081843355313076 ) ) ;
#20326=ADVANCED_FACE ( 'NONE', ( #34622 ), #62511, .F. ) ;
#20330=CARTESIAN_POINT ( 'NONE',  ( 2.305787727787084407, 2.774453000917245671, -7.135468203929955067 ) ) ;
#20336=CARTESIAN_POINT ( 'NONE',  ( 2.844750968615921582, -2.364925124214038998, 7.470159816919260010 ) ) ;
#20339=B_SPLINE_CURVE_WITH_KNOTS ( 'NONE', 3,
 ( #51185, #46193, #50527, #4970, #25233, #15257, #5636, #30863, #56483, #65456, #19612, #20242, #60818, #25905, #35537, #20896, #10929, #24920, #29890 ),
 .UNSPECIFIED., .F., .F.,
 ( 4, 3, 3, 3, 3, 3, 4 ),
 ( 0.000000000000000000, 2.831840207499450679E-05, 4.217266859840506987E-05, 5.602024318395848712E-05, 6.290810167968935505E-05, 9.120440630944629608E-05, 0.0001153103026479747480 ),
 .UNSPECIFIED. ) ;
#20347=CARTESIAN_POINT ( 'NONE',  ( 0.3675815128205894289, -6.367184624550092487, -10.50067073900658521 ) ) ;
#20349=ORIENTED_EDGE ( 'NONE', *, *, #39590, .F. ) ;
#20353=CARTESIAN_POINT ( 'NONE',  ( 2.241352910868909643, -1.407733736974916772, 7.503490710578227585 ) ) ;
#20361=CARTESIAN_POINT ( 'NONE',  ( 2.990245332647579524, -3.377079998295319907, 7.779904630197314930 ) ) ;
#20365=DIRECTION ( 'NONE',  ( -1.000000000000000000, -0.000000000000000000, -0.000000000000000000 ) ) ;
#20366=ORIENTED_EDGE ( 'NONE', *, *, #53754, .F. ) ;
#20371=CARTESIAN_POINT ( 'NONE',  ( 0.2872850955227739256, 8.035297825011367578, 9.251080475901380495 ) ) ;
#20382=CARTESIAN_POINT ( 'NONE',  ( 2.430348790456773767, 0.1949172018038413667, 7.694949746373610289 ) ) ;
#20390=AXIS2_PLACEMENT_3D ( 'NONE', #36402, #42034, #2135 ) ;
#20396=CARTESIAN_POINT ( 'NONE',  ( 0.2653519789438741339, 2.104833950422741129, -12.06397564829375568 ) ) ;
#20398=CARTESIAN_POINT ( 'NONE',  ( 2.034671305879974135, -11.65517003033971122, -0.7032348381693538375 ) ) ;
#20404=CARTESIAN_POINT ( 'NONE',  ( 5.515539859299206427, 0.0008592514567754854947, 0.005991790098943841278 ) ) ;
#20406=EDGE_CURVE ( 'NONE', #56858, #53890, #15150, .T. ) ;
#20412=CARTESIAN_POINT ( 'NONE',  ( 2.241536586108913820, 6.614789707676462349, 3.811784405792373764 ) ) ;
#20413=EDGE_CURVE ( 'NONE', #11115, #24280, #8117, .T. ) ;
#20422=LINE ( 'NONE', #40702, #32231 ) ;
#20426=EDGE_CURVE ( 'NONE', #59359, #54096, #33421, .T. ) ;
#20443=CARTESIAN_POINT ( 'NONE',  ( 1.287602823385630479, -2.727479899220070170, 12.28793447239686287 ) ) ;
#20444=CARTESIAN_POINT ( 'NONE',  ( 0.3057689695767489280, -12.03117299329037593, 2.355923806019164957 ) ) ;
#20445=EDGE_CURVE ( 'NONE', #21752, #14146, #12624, .T. ) ;
#20451=EDGE_CURVE ( 'NONE', #45693, #45313, #39775, .T. ) ;
#20458=CARTESIAN_POINT ( 'NONE',  ( 0.8320506296491581022, -12.17395768195217975, 2.535206712041412569 ) ) ;
#20463=VERTEX_POINT ( 'NONE', #23277 ) ;
#20465=CARTESIAN_POINT ( 'NONE',  ( 2.251152103363643242, 7.498874008626774668, -1.449454666117645507 ) ) ;
#20480=EDGE_CURVE ( 'NONE', #36604, #22476, #49231, .T. ) ;
#20486=CARTESIAN_POINT ( 'NONE',  ( 2.241528039335008327, 7.634443721858077403, 0.01573255094244493946 ) ) ;
#20495=CARTESIAN_POINT ( 'NONE',  ( 3.100650473569713128, 0.9283202922945034130, 7.866294126167251655 ) ) ;
#20497=FACE_OUTER_BOUND ( 'NONE', #47763, .T. ) ;
#20500=CARTESIAN_POINT ( 'NONE',  ( 2.844750968615974873, -7.470159816919274220, -2.364925124214049212 ) ) ;
#20506=LINE ( 'NONE', #15818, #11890 ) ;
#20510=VERTEX_POINT ( 'NONE', #3015 ) ;
#20518=CARTESIAN_POINT ( 'NONE',  ( 2.907497136251038228, 1.716624290781495699, 7.666666002096734545 ) ) ;
#20520=CARTESIAN_POINT ( 'NONE',  ( 0.2646305136544072623, 4.312539723326286989, -11.46223899740595797 ) ) ;
#20530=EDGE_LOOP ( 'NONE', ( #12564, #10257, #28164, #22682 ) ) ;
#20533=CARTESIAN_POINT ( 'NONE',  ( 5.516018279890452902, -0.002104829434641057422, -0.006440244342253404787 ) ) ;
#20534=CARTESIAN_POINT ( 'NONE',  ( 2.269879328256731110, 7.130835954829884749, -2.753278809616039879 ) ) ;
#20540=CARTESIAN_POINT ( 'NONE',  ( 1.547277799337429594, 12.65564732076229681, -0.6737945300318757269 ) ) ;
#20562=CARTESIAN_POINT ( 'NONE',  ( 2.280717697723675386, 2.468022724683634372, -7.238333660706929074 ) ) ;
#20568=CARTESIAN_POINT ( 'NONE',  ( 2.941278708680199916, 6.068329152486391820, -0.9331242451664371051 ) ) ;
#20569=CARTESIAN_POINT ( 'NONE',  ( 2.241506898688418126, -6.631235260227141382, -3.783130304541498123 ) ) ;
#20572=CARTESIAN_POINT ( 'NONE',  ( 2.257661810676420355, 2.739276463085679403, 7.131864446283232795 ) ) ;
#20579=CARTESIAN_POINT ( 'NONE',  ( 2.241536586108912932, 7.176205604390212045, 2.605228657247374180 ) ) ;
#20582=ADVANCED_FACE ( 'NONE', ( #40524 ), #48958, .F. ) ;
#20590=( BOUNDED_SURFACE ( )  B_SPLINE_SURFACE ( 3, 1, ( 
 ( #37920, #17657 ),
 ( #63192, #58213 ),
 ( #32911, #4324 ),
 ( #39557, #64490 ) ),
 .UNSPECIFIED., .F., .F., .F. ) 
 B_SPLINE_SURFACE_WITH_KNOTS ( ( 4, 4 ),
 ( 2, 2 ),
 ( 0.000000000000000000, 1.000000000000000000 ),
 ( 0.000000000000000000, 1.000000000000000000 ),
 .UNSPECIFIED. ) 
 GEOMETRIC_REPRESENTATION_ITEM ( )  RATIONAL_B_SPLINE_SURFACE ( (
 ( 1.000000000000000000, 1.000000000000000000),
 ( 0.9856612449720755231, 0.9999558406602322425),
 ( 0.9856612449720755231, 0.9999558406602322425),
 ( 1.000000000000000000, 1.000000000000000000) ) ) 
 REPRESENTATION_ITEM ( '' )  SURFACE ( )  );
#20592=CARTESIAN_POINT ( 'NONE',  ( 0.9232058338315048962, 10.60677148422244365, 6.559496812049697034 ) ) ;
#20593=CARTESIAN_POINT ( 'NONE',  ( 2.655192694323794456, -8.807900729500619974, 3.822392723567597628 ) ) ;
#20594=CARTESIAN_POINT ( 'NONE',  ( 1.547277799339725757, 9.261681528764395210, -8.651049845884754674 ) ) ;
#20595=CARTESIAN_POINT ( 'NONE',  ( 5.515188684475870851, 0.005320786921497679470, 0.0005703990286340230751 ) ) ;
#20597=VERTEX_POINT ( 'NONE', #40867 ) ;
#20598=CARTESIAN_POINT ( 'NONE',  ( 0.7446945582518260665, -10.91757157182789051, 5.891988114924179065 ) ) ;
#20613=CARTESIAN_POINT ( 'NONE',  ( 2.507146904658097863, -6.793847219607473953, 3.672650549645643636 ) ) ;
#20615=CARTESIAN_POINT ( 'NONE',  ( 0.2706063244538062795, 11.56807224179758720, -4.023948952279145175 ) ) ;
#20619=B_SPLINE_CURVE_WITH_KNOTS ( 'NONE', 3,
 ( #46884, #684, #45903, #20941, #357, #10628, #20637, #30919, #36229, #16299, #40913, #21622, #6325, #1341, #31573, #6658 ),
 .UNSPECIFIED., .F., .F.,
 ( 4, 3, 3, 3, 3, 4 ),
 ( 0.000000000000000000, 0.0002999043160758303110, 0.0005998071753052896518, 0.0008997092107377380795, 0.001204458948196922069, 0.001510329163478790109 ),
 .UNSPECIFIED. ) ;
#20622=AXIS2_PLACEMENT_3D ( 'NONE', #53145, #7591, #27877 ) ;
#20624=CARTESIAN_POINT ( 'NONE',  ( 0.2655924914740778187, -4.229867354073634012, 11.49267051747967017 ) ) ;
#20636=CARTESIAN_POINT ( 'NONE',  ( 1.452237505248552996, -9.303501428255968264, -8.579708443906842064 ) ) ;
#20637=CARTESIAN_POINT ( 'NONE',  ( 1.198791140420903512, -10.60778679489422949, -6.720248575444034422 ) ) ;
#20645=CARTESIAN_POINT ( 'NONE',  ( 3.152665057734004073, 7.102135024645805039, -3.546019893116331811 ) ) ;
#20647=CARTESIAN_POINT ( 'NONE',  ( 2.889800649504073782, -0.9965440656174132661, 6.039722463373535355 ) ) ;
#20654=DIRECTION ( 'NONE',  ( 0.000000000000000000, 0.000000000000000000, 1.000000000000000000 ) ) ;
#20655=EDGE_CURVE ( 'NONE', #52583, #62889, #39875, .T. ) ;
#20657=FACE_OUTER_BOUND ( 'NONE', #34691, .T. ) ;
#20658=CARTESIAN_POINT ( 'NONE',  ( 2.259025283528082628, -5.939720477913319918, -4.805599953367722499 ) ) ;
#20661=CARTESIAN_POINT ( 'NONE',  ( -14.47334165536099881, 3.872983346207417021, 1.000000000000000000 ) ) ;
#20663=EDGE_CURVE ( 'NONE', #33180, #42715, #59845, .T. ) ;
#20667=CARTESIAN_POINT ( 'NONE',  ( 0.3040950598368152291, -9.552450779732055253, -7.687624643091528931 ) ) ;
#20669=CARTESIAN_POINT ( 'NONE',  ( 2.241451721903216399, 3.764430789729979132, 6.641849090084966711 ) ) ;
#20673=LINE ( 'NONE', #25007, #5781 ) ;
#20682=CARTESIAN_POINT ( 'NONE',  ( 0.3040950598368152291, -10.49113473328035084, 6.347045025870730939 ) ) ;
#20686=CARTESIAN_POINT ( 'NONE',  ( 1.634816307076161879, -10.17753964889841711, 7.601181930721068625 ) ) ;
#20687=VERTEX_POINT ( 'NONE', #25562 ) ;
#20693=CARTESIAN_POINT ( 'NONE',  ( 0.3006302518452020900, -12.25587491745529967, 0.2259616664571819644 ) ) ;
#20696=DIRECTION ( 'NONE',  ( -1.000000000000000000, -0.000000000000000000, -0.000000000000000000 ) ) ;
#20697=LINE ( 'NONE', #40177, #23563 ) ;
#20702=CARTESIAN_POINT ( 'NONE',  ( 0.3106921474978441844, -4.414111574791904857, 11.43920276778355927 ) ) ;
#20703=ORIENTED_EDGE ( 'NONE', *, *, #43095, .F. ) ;
#20708=CARTESIAN_POINT ( 'NONE',  ( 0.6511581176972393026, 11.73752429815159815, -3.919972364658484754 ) ) ;
#20726=CARTESIAN_POINT ( 'NONE',  ( 2.305787727787083519, 5.047606869483132641, -5.756228004061408221 ) ) ;
#20728=CARTESIAN_POINT ( 'NONE',  ( 0.2648978790185584908, -6.008231198268910056, -10.67083876753498117 ) ) ;
#20729=VERTEX_POINT ( 'NONE', #25906 ) ;
#20740=CARTESIAN_POINT ( 'NONE',  ( 5.516018279890452902, 0.005042957932158584518, -0.004525000489649788973 ) ) ;
#20744=CARTESIAN_POINT ( 'NONE',  ( 1.719304012340733934, -11.67935079956419031, -5.066286238786891438 ) ) ;
#20746=VERTEX_POINT ( 'NONE', #11576 ) ;
#20748=VERTEX_POINT ( 'NONE', #46831 ) ;
#20751=CARTESIAN_POINT ( 'NONE',  ( 2.903928887688637328, 7.845932231840992088, 3.918141038919173536 ) ) ;
#20753=CARTESIAN_POINT ( 'NONE',  ( 3.152665057734131526, -0.9030954876737319337, -7.886634106564212487 ) ) ;
#20755=CARTESIAN_POINT ( 'NONE',  ( 1.948354844646335460, 9.982942661982825427, -6.595573209516024882 ) ) ;
#20762=FACE_OUTER_BOUND ( 'NONE', #34806, .T. ) ;
#20763=ORIENTED_EDGE ( 'NONE', *, *, #38799, .T. ) ;
#20770=CARTESIAN_POINT ( 'NONE',  ( 1.634816307075119601, -2.910502128620189310, 12.36483956257006511 ) ) ;
#20773=( BOUNDED_SURFACE ( )  B_SPLINE_SURFACE ( 3, 1, ( 
 ( #65368, #30133 ),
 ( #4210, #25806 ),
 ( #4879, #35441 ),
 ( #65681, #546 ) ),
 .UNSPECIFIED., .F., .F., .F. ) 
 B_SPLINE_SURFACE_WITH_KNOTS ( ( 4, 4 ),
 ( 2, 2 ),
 ( 0.000000000000000000, 1.000000000000000000 ),
 ( 0.000000000000000000, 1.000000000000000000 ),
 .UNSPECIFIED. ) 
 GEOMETRIC_REPRESENTATION_ITEM ( )  RATIONAL_B_SPLINE_SURFACE ( (
 ( 1.000000000000000000, 1.000000000000000000),
 ( 0.6933888150995267674, 0.9895912004443193632),
 ( 0.6933888150995267674, 0.9895912004443193632),
 ( 1.000000000000000000, 1.000000000000000000) ) ) 
 REPRESENTATION_ITEM ( '' )  SURFACE ( )  );
#20775=CARTESIAN_POINT ( 'NONE',  ( 0.3106921474978469599, 12.03191800497307895, 2.360654586927831478 ) ) ;
#20780=CARTESIAN_POINT ( 'NONE',  ( 2.241352910868908754, 1.243507963608094347, 7.532448145350512547 ) ) ;
#20787=( BOUNDED_SURFACE ( )  B_SPLINE_SURFACE ( 3, 1, ( 
 ( #24480, #44757 ),
 ( #65367, #38807 ),
 ( #29782, #18852 ),
 ( #9841, #23857 ) ),
 .UNSPECIFIED., .F., .F., .F. ) 
 B_SPLINE_SURFACE_WITH_KNOTS ( ( 4, 4 ),
 ( 2, 2 ),
 ( 0.000000000000000000, 1.000000000000000000 ),
 ( 0.000000000000000000, 1.000000000000000000 ),
 .UNSPECIFIED. ) 
 GEOMETRIC_REPRESENTATION_ITEM ( )  RATIONAL_B_SPLINE_SURFACE ( (
 ( 1.000000000000000000, 1.000000000000000000),
 ( 0.9856612449720755231, 0.9999558406602322425),
 ( 0.9856612449720755231, 0.9999558406602322425),
 ( 1.000000000000000000, 1.000000000000000000) ) ) 
 REPRESENTATION_ITEM ( '' )  SURFACE ( )  );
#20790=ADVANCED_FACE ( 'NONE', ( #6282 ), #50292, .T. ) ;
#20794=AXIS2_PLACEMENT_3D ( 'NONE', #6799, #2122, #22748 ) ;
#20796=CARTESIAN_POINT ( 'NONE',  ( 1.719304012339893939, -12.38166659046436457, -2.961219984258754767 ) ) ;
#20803=CARTESIAN_POINT ( 'NONE',  ( 0.2651627682582901602, 10.64925413290593603, 6.046625184671022168 ) ) ;
#20804=CARTESIAN_POINT ( 'NONE',  ( 5.515188684475870851, 0.003857086913166391916, 0.003709313826049759084 ) ) ;
#20808=CARTESIAN_POINT ( 'NONE',  ( 0.3675815128205894289, 12.13672785388550324, 1.872154644482125763 ) ) ;
#20823=CARTESIAN_POINT ( 'NONE',  ( 3.152665057735546839, 0.4801242025606423658, 7.923639299008859105 ) ) ;
#20831=CARTESIAN_POINT ( 'NONE',  ( 2.889800649504073782, -5.728825117897692998, -2.156828754871525256 ) ) ;
#20838=B_SPLINE_CURVE_WITH_KNOTS ( 'NONE', 3,
 ( #9465, #59376, #13798, #8182, #28786, #19479, #39748, #24442, #18518, #49097 ),
 .UNSPECIFIED., .F., .F.,
 ( 4, 3, 3, 4 ),
 ( 8.673617379884035472E-19, 6.607638129004427896E-05, 9.911389841680530389E-05, 0.0001667630577588622028 ),
 .UNSPECIFIED. ) ;
#20841=CARTESIAN_POINT ( 'NONE',  ( 5.515539859299206427, 0.005618668168217494027, -0.002251761459665947360 ) ) ;
#20848=ORIENTED_EDGE ( 'NONE', *, *, #53780, .F. ) ;
#20855=EDGE_CURVE ( 'NONE', #48474, #54096, #43872, .T. ) ;
#20856=CARTESIAN_POINT ( 'NONE',  ( 2.298277635560284082, 7.506689984432329155, 1.491234112749218355 ) ) ;
#20864=CARTESIAN_POINT ( 'NONE',  ( 0.3164563675027660117, -10.73846246126245063, -5.922187299605745636 ) ) ;
#20866=CARTESIAN_POINT ( 'NONE',  ( 5.514970785353741078, 0.001117786416802112525, -0.004588761610584830321 ) ) ;
#20871=CARTESIAN_POINT ( 'NONE',  ( 0.2653141435805182469, 0.04404957080779424439, 12.24612531649369274 ) ) ;
#20874=CARTESIAN_POINT ( 'NONE',  ( 0.3675815128205894289, 4.447030445008336663, -11.44679196252404729 ) ) ;
#20879=CARTESIAN_POINT ( 'NONE',  ( 1.283627346226434263, -1.641214790178027405, 12.47820286973605342 ) ) ;
#20887=EDGE_CURVE ( 'NONE', #14210, #58632, #23900, .T. ) ;
#20889=CARTESIAN_POINT ( 'NONE',  ( 0.2834382757448011270, -0.2027202995056148482, -12.25055062943084927 ) ) ;
#20890=CARTESIAN_POINT ( 'NONE',  ( 0.3040950598368152291, -9.229598020917739731, 8.072385578287439856 ) ) ;
#20896=CARTESIAN_POINT ( 'NONE',  ( 2.284126774967656370, -6.543266298866105224, -3.960764882115069607 ) ) ;
#20899=CARTESIAN_POINT ( 'NONE',  ( 1.462291587748165700, 9.267729738232345582, 8.602888600420595111 ) ) ;
#20900=CARTESIAN_POINT ( 'NONE',  ( 0.9232167919969100911, 9.278116382137485019, -8.324955738482373135 ) ) ;
#20904=CARTESIAN_POINT ( 'NONE',  ( 2.994568964204218364, -2.317954327151173555, -7.537093683963818513 ) ) ;
#20908=CARTESIAN_POINT ( 'NONE',  ( 0.3632410797595237995, -9.235006602299407064, 8.092233745354604935 ) ) ;
#20915=CARTESIAN_POINT ( 'NONE',  ( 1.452237505248555660, 10.65201107290477012, -6.833827325205206193 ) ) ;
#20916=CARTESIAN_POINT ( 'NONE',  ( 2.491965175174298608, 2.837956678388472653, 7.177226758613711510 ) ) ;
#20918=VERTEX_POINT ( 'NONE', #8552 ) ;
#20926=VERTEX_POINT ( 'NONE', #8234 ) ;
#20927=DIRECTION ( 'NONE',  ( -0.3939253465568944290, -0.5833358547425138152, 0.7103112711423431591 ) ) ;
#20928=CARTESIAN_POINT ( 'NONE',  ( 0.7446945582506530048, 11.53120448859746539, 4.576048078258359020 ) ) ;
#20930=CARTESIAN_POINT ( 'NONE',  ( 5.530133899448235191, -0.01324661008606583569, 0.008946569461392389275 ) ) ;
#20932=ORIENTED_EDGE ( 'NONE', *, *, #11523, .T. ) ;
#20934=ORIENTED_EDGE ( 'NONE', *, *, #19213, .T. ) ;
#20938=EDGE_CURVE ( 'NONE', #53897, #49252, #1638, .T. ) ;
#20941=CARTESIAN_POINT ( 'NONE',  ( 1.462291587751777033, -10.62080802716771721, -6.862867011843016840 ) ) ;
#20953=CARTESIAN_POINT ( 'NONE',  ( 0.7400311444011689055, 5.892391870929167830, -10.91558650018036225 ) ) ;
#20959=( BOUNDED_SURFACE ( )  B_SPLINE_SURFACE ( 3, 1, ( 
 ( #6761, #469 ),
 ( #56973, #11716 ),
 ( #62580, #61287 ),
 ( #21383, #15718 ) ),
 .UNSPECIFIED., .F., .F., .F. ) 
 B_SPLINE_SURFACE_WITH_KNOTS ( ( 4, 4 ),
 ( 2, 2 ),
 ( 0.000000000000000000, 1.000000000000000000 ),
 ( 0.000000000000000000, 1.000000000000000000 ),
 .UNSPECIFIED. ) 
 GEOMETRIC_REPRESENTATION_ITEM ( )  RATIONAL_B_SPLINE_SURFACE ( (
 ( 1.000000000000000000, 1.000000000000000000),
 ( 0.9856612449720755231, 0.9999558406602322425),
 ( 0.9856612449720755231, 0.9999558406602322425),
 ( 1.000000000000000000, 1.000000000000000000) ) ) 
 REPRESENTATION_ITEM ( '' )  SURFACE ( )  );
#20960=CARTESIAN_POINT ( 'NONE',  ( 5.520433897694421610, -0.01329351892497966821, 0.007082458259338164468 ) ) ;
#20974=EDGE_LOOP ( 'NONE', ( #4364, #45871, #61485, #47335 ) ) ;
#20975=CARTESIAN_POINT ( 'NONE',  ( 2.440552418640498544, 7.698292014589401155, 0.1974238147509528030 ) ) ;
#20982=AXIS2_PLACEMENT_3D ( 'NONE', #33315, #6744, #2070 ) ;
#20990=CARTESIAN_POINT ( 'NONE',  ( 1.372161826076962132, 7.648244077827059506, -10.03232826862097760 ) ) ;
#20994=CARTESIAN_POINT ( 'NONE',  ( 0.2646305136544072623, -11.55263159009956020, -4.064188116014665120 ) ) ;
#20995=CARTESIAN_POINT ( 'NONE',  ( 2.241317068080781461, 3.896159243838555941, 6.565357088387183460 ) ) ;
#21001=DIRECTION ( 'NONE',  ( 0.000000000000000000, 0.000000000000000000, 1.000000000000000000 ) ) ;
#21006=CARTESIAN_POINT ( 'NONE',  ( 5.520433897694421610, 0.01505375422439067870, 0.0005131706886599866424 ) ) ;
#21017=CARTESIAN_POINT ( 'NONE',  ( 5.514624014163232779, -0.003060352188290566856, 0.002789935220458457377 ) ) ;
#21022=CARTESIAN_POINT ( 'NONE',  ( 2.368238019614975709, 0.1797502808085061909, 7.674602282635966333 ) ) ;
#21033=CARTESIAN_POINT ( 'NONE',  ( 0.2869720083484383899, -5.945302302873177958, -10.71444492121024616 ) ) ;
#21043=EDGE_LOOP ( 'NONE', ( #3178, #5211, #62676, #50587 ) ) ;
#21044=FACE_OUTER_BOUND ( 'NONE', #7667, .T. ) ;
#21046=CARTESIAN_POINT ( 'NONE',  ( 2.889800649504073782, 2.156828754871545240, -5.728825117897685004 ) ) ;
#21048=CARTESIAN_POINT ( 'NONE',  ( 2.241317068080774355, -6.565357088387212769, 3.896159243838545283 ) ) ;
#21052=ORIENTED_EDGE ( 'NONE', *, *, #50429, .F. ) ;
#21057=CARTESIAN_POINT ( 'NONE',  ( 1.719304012338200849, 11.38834240361387096, 5.690355757826642602 ) ) ;
#21058=CARTESIAN_POINT ( 'NONE',  ( 0.4626703367447407289, -11.46957824750463217, -4.475905684073936186 ) ) ;
#21060=CARTESIAN_POINT ( 'NONE',  ( 0.5547464869798232057, -0.3049355384528142365, -12.33891836761636540 ) ) ;
#21063=CARTESIAN_POINT ( 'NONE',  ( 2.655192694323322389, 8.010337395400600968, -5.293797899976643073 ) ) ;
#21066=CARTESIAN_POINT ( 'NONE',  ( 0.2653141617321017054, -12.05243138604824260, -2.169890202573318216 ) ) ;
#21069=CARTESIAN_POINT ( 'NONE',  ( 0.3665391374699467075, -11.62960183138730130, 3.952034409876258092 ) ) ;
#21072=ORIENTED_EDGE ( 'NONE', *, *, #9051, .T. ) ;
#21077=CARTESIAN_POINT ( 'NONE',  ( 2.258463476536644254, -7.638896687393373242, -0.1358786215988950219 ) ) ;
#21081=CARTESIAN_POINT ( 'NONE',  ( 1.020182472821638431, -2.608319446514638873, 12.22263240120507355 ) ) ;
#21085=CIRCLE ( 'NONE', #58263, 7.938172270156617749 ) ;
#21089=ORIENTED_EDGE ( 'NONE', *, *, #58278, .F. ) ;
#21090=B_SPLINE_CURVE_WITH_KNOTS ( 'NONE', 3,
 ( #11100, #37675, #16067, #16725, #31373, #6435, #51676, #6118, #26377, #16419, #56984, #57304, #31679, #21742, #22043, #46662, #47339, #1780, #52960, #51990, #47647, #47006 ),
 .UNSPECIFIED., .F., .F.,
 ( 4, 3, 3, 3, 3, 3, 3, 4 ),
 ( 5.421010862427521568E-20, 4.449119708437187815E-05, 6.626296329540798293E-05, 8.803456484962904284E-05, 0.0001098060367612821951, 0.0001315774408628530776, 0.0001760698110411187565, 0.0001829697163287827787 ),
 .UNSPECIFIED. ) ;
#21093=ORIENTED_EDGE ( 'NONE', *, *, #54296, .F. ) ;
#21094=FACE_OUTER_BOUND ( 'NONE', #7427, .T. ) ;
#21099=CARTESIAN_POINT ( 'NONE',  ( 0.3040950598368152291, -6.347045025870692747, -10.49113473328036861 ) ) ;
#21109=CARTESIAN_POINT ( 'NONE',  ( 0.3040950598368144520, -9.229598020917633150, -8.072385578287565977 ) ) ;
#21113=EDGE_CURVE ( 'NONE', #56624, #35302, #19050, .T. ) ;
#21114=CARTESIAN_POINT ( 'NONE',  ( 2.963017218115626239, -0.3847317984105863009, 7.865565884553442189 ) ) ;
#21124=CARTESIAN_POINT ( 'NONE',  ( 2.241537034860906275, -3.813147095850935919, -6.614004440763081583 ) ) ;
#21131=VECTOR ( 'NONE', #22771, 1000.000000000000227 ) ;
#21147=CARTESIAN_POINT ( 'NONE',  ( 0.9232167919969119785, 0.4134278310083039920, 12.45862789703291185 ) ) ;
#21151=CARTESIAN_POINT ( 'NONE',  ( 2.253265082352432280, -5.007416537586561134, 5.768060979107519692 ) ) ;
#21162=( BOUNDED_SURFACE ( )  B_SPLINE_SURFACE ( 3, 1, ( 
 ( #58698, #14410 ),
 ( #59327, #34040 ),
 ( #28404, #64950 ),
 ( #18109, #54983 ) ),
 .UNSPECIFIED., .F., .F., .F. ) 
 B_SPLINE_SURFACE_WITH_KNOTS ( ( 4, 4 ),
 ( 2, 2 ),
 ( 0.000000000000000000, 1.000000000000000000 ),
 ( 0.000000000000000000, 1.000000000000000000 ),
 .UNSPECIFIED. ) 
 GEOMETRIC_REPRESENTATION_ITEM ( )  RATIONAL_B_SPLINE_SURFACE ( (
 ( 1.000000000000000000, 1.000000000000000000),
 ( 0.9942764183789327692, 0.8450855930916585379),
 ( 0.9942764183789327692, 0.8450855930916585379),
 ( 1.000000000000000000, 1.000000000000000000) ) ) 
 REPRESENTATION_ITEM ( '' )  SURFACE ( )  );
#21175=CARTESIAN_POINT ( 'NONE',  ( 2.835339799623985968, -7.763739326985120925, 1.035140033450024699 ) ) ;
#21179=VERTEX_POINT ( 'NONE', #7160 ) ;
#21180=CARTESIAN_POINT ( 'NONE',  ( 0.4626703367445959003, -11.66326339726744976, 3.943760108616771287 ) ) ;
#21183=CARTESIAN_POINT ( 'NONE',  ( 2.241537034860906275, 5.845308934728780770, 4.910958050585458423 ) ) ;
#21191=CARTESIAN_POINT ( 'NONE',  ( 0.9232058338315058954, -10.60677148422248983, 6.559496812049624204 ) ) ;
#21192=ORIENTED_EDGE ( 'NONE', *, *, #39590, .T. ) ;
#21195=CARTESIAN_POINT ( 'NONE',  ( 1.283627346226763999, -9.985833283678418937, -7.660435136228953112 ) ) ;
#21196=FACE_OUTER_BOUND ( 'NONE', #33167, .T. ) ;
#21199=CARTESIAN_POINT ( 'NONE',  ( 2.241534463349552198, -0.005768439177821054094, -7.634462073473343935 ) ) ;
#21201=CARTESIAN_POINT ( 'NONE',  ( 2.241352910868908754, -6.652881166698485949, -3.744764251557062718 ) ) ;
#21204=CARTESIAN_POINT ( 'NONE',  ( 2.889800649504073782, -0.9965440656173316647, -6.039722463373548678 ) ) ;
#21219=CARTESIAN_POINT ( 'NONE',  ( 1.719304012339844867, -11.38834240361479644, 5.690355757826019989 ) ) ;
#21225=CARTESIAN_POINT ( 'NONE',  ( 0.3675815128205912052, 9.235491948680007113, 8.093875121226108860 ) ) ;
#21240=ORIENTED_EDGE ( 'NONE', *, *, #2823, .T. ) ;
#21243=CARTESIAN_POINT ( 'NONE',  ( 2.844750968616052145, 2.990088422897422049, 7.242618984642885671 ) ) ;
#21244=EDGE_CURVE ( 'NONE', #29440, #36589, #16691, .T. ) ;
#21251=ORIENTED_EDGE ( 'NONE', *, *, #35626, .F. ) ;
#21255=CARTESIAN_POINT ( 'NONE',  ( 0.2671309869109498303, 4.340541005679527942, 11.45180222993656294 ) ) ;
#21262=VERTEX_POINT ( 'NONE', #43724 ) ;
#21271=CARTESIAN_POINT ( 'NONE',  ( 2.305787727787083519, 6.711944854845874886, -3.682701754025442753 ) ) ;
#21272=CARTESIAN_POINT ( 'NONE',  ( 2.305787727787083519, -7.654065630109506913, -0.1666591538753489643 ) ) ;
#21277=EDGE_LOOP ( 'NONE', ( #407, #23384, #33075, #58846 ) ) ;
#21278=CARTESIAN_POINT ( 'NONE',  ( 1.719304012338833676, 5.066286238785588480, 11.67935079956406597 ) ) ;
#21287=B_SPLINE_CURVE_WITH_KNOTS ( 'NONE', 3,
 ( #26321, #11353, #36944, #46291, #31624, #62221, #21329, #11673, #1060, #61897, #52603, #20990, #41272, #7026, #1401, #16356 ),
 .UNSPECIFIED., .F., .F.,
 ( 4, 3, 3, 3, 3, 4 ),
 ( 0.000000000000000000, 0.0003017745587525229160, 0.0006035491769808713552, 0.0009053241094668132124, 0.001207275924541012383, 0.001510325902535034634 ),
 .UNSPECIFIED. ) ;
#21288=CARTESIAN_POINT ( 'NONE',  ( 2.655192694323996072, 2.234846078477681353, 9.337840456948278245 ) ) ;
#21292=CARTESIAN_POINT ( 'NONE',  ( 0.3675815128205894289, 12.27743992903066328, -0.2638082659428851451 ) ) ;
#21293=CARTESIAN_POINT ( 'NONE',  ( 0.3665391374699465965, -4.447929964102771194, -11.44911061034390976 ) ) ;
#21295=CARTESIAN_POINT ( 'NONE',  ( 0.2653141334712576516, -2.083134085643126188, 12.06772877558522516 ) ) ;
#21297=CARTESIAN_POINT ( 'NONE',  ( 2.298277635560277865, 0.1650558796845167375, -7.651596582281724679 ) ) ;
#21303=ORIENTED_EDGE ( 'NONE', *, *, #14302, .F. ) ;
#21305=CARTESIAN_POINT ( 'NONE',  ( 0.2653141617321003176, 2.083144498805272526, 12.06772699408309535 ) ) ;
#21307=CARTESIAN_POINT ( 'NONE',  ( 2.305787727787084407, -4.792270232040933386, 5.970480882365206909 ) ) ;
#21324=CARTESIAN_POINT ( 'NONE',  ( 2.253265082353312021, 7.132841660186906019, 2.732639326787329903 ) ) ;
#21329=CARTESIAN_POINT ( 'NONE',  ( 0.9232167919969098691, 7.691547553333252019, -9.809608956680790470 ) ) ;
#21333=CARTESIAN_POINT ( 'NONE',  ( 0.2646305136544072623, -11.46223899740597396, -4.312539723326246133 ) ) ;
#21338=CARTESIAN_POINT ( 'NONE',  ( 0.2652384529303112304, 4.250461213012543205, 11.48485968917275279 ) ) ;
#21341=EDGE_CURVE ( 'NONE', #46591, #43331, #18454, .T. ) ;
#21345=FACE_OUTER_BOUND ( 'NONE', #60022, .T. ) ;
#21351=CARTESIAN_POINT ( 'NONE',  ( 0.7446945582530255514, 11.77484212699407884, -3.906659168236647606 ) ) ;
#21352=CARTESIAN_POINT ( 'NONE',  ( 3.152665057734040488, 0.000000000000000000, 0.000000000000000000 ) ) ;
#21359=( BOUNDED_SURFACE ( )  B_SPLINE_SURFACE ( 3, 1, ( 
 ( #61013, #46692 ),
 ( #11129, #62303 ),
 ( #37028, #11437 ),
 ( #50711, #10137 ) ),
 .UNSPECIFIED., .F., .F., .F. ) 
 B_SPLINE_SURFACE_WITH_KNOTS ( ( 4, 4 ),
 ( 2, 2 ),
 ( 0.000000000000000000, 1.000000000000000000 ),
 ( 0.000000000000000000, 1.000000000000000000 ),
 .UNSPECIFIED. ) 
 GEOMETRIC_REPRESENTATION_ITEM ( )  RATIONAL_B_SPLINE_SURFACE ( (
 ( 1.000000000000000000, 1.000000000000000000),
 ( 0.9942764183789327692, 0.8450855930916580938),
 ( 0.9942764183789327692, 0.8450855930916580938),
 ( 1.000000000000000000, 1.000000000000000000) ) ) 
 REPRESENTATION_ITEM ( '' )  SURFACE ( )  );
#21371=EDGE_CURVE ( 'NONE', #27786, #49417, #10326, .T. ) ;
#21383=CARTESIAN_POINT ( 'NONE',  ( 5.514970785353741078, -0.004694330894494713573, -0.0005190732562554920817 ) ) ;
#21384=CARTESIAN_POINT ( 'NONE',  ( 0.3675815128205912052, -12.27743992903065973, -0.2638082659429707988 ) ) ;
#21387=CARTESIAN_POINT ( 'NONE',  ( 5.536195898058073439, 0.008323005098840532620, 0.001726268814999744761 ) ) ;
#21406=CARTESIAN_POINT ( 'NONE',  ( 1.287602823387594020, -11.62763122279993233, -4.819820779360301621 ) ) ;
#21408=CYLINDRICAL_SURFACE ( 'NONE', #16304, 4.000000000000000000 ) ;
#21413=CARTESIAN_POINT ( 'NONE',  ( 2.941278708680199916, -4.048809123187903758, -4.615461433467297425 ) ) ;
#21414=EDGE_LOOP ( 'NONE', ( #35786, #27169, #16098, #32344 ) ) ;
#21418=ORIENTED_EDGE ( 'NONE', *, *, #57887, .T. ) ;
#21422=EDGE_CURVE ( 'NONE', #62530, #20687, #21750, .T. ) ;
#21427=CARTESIAN_POINT ( 'NONE',  ( 1.375507693217718597, -2.770709900325616371, 12.30831170622558446 ) ) ;
#21432=VERTEX_POINT ( 'NONE', #45684 ) ;
#21436=ORIENTED_EDGE ( 'NONE', *, *, #4315, .T. ) ;
#21439=CARTESIAN_POINT ( 'NONE',  ( 0.8320506296491625431, -10.57268643647778639, 6.546053790694139174 ) ) ;
#21441=B_SPLINE_CURVE_WITH_KNOTS ( 'NONE', 3,
 ( #58405, #64035, #19137, #38437, #14137, #58753, #33458 ),
 .UNSPECIFIED., .F., .F.,
 ( 4, 3, 4 ),
 ( 7.013569501285946009E-15, 0.002398160485434967272, 0.005002426799383816874 ),
 .UNSPECIFIED. ) ;
#21447=VERTEX_POINT ( 'NONE', #20753 ) ;
#21456=CARTESIAN_POINT ( 'NONE',  ( 0.2638984909335716500, -9.252728947331023690, -8.023974293733274976 ) ) ;
#21476=CARTESIAN_POINT ( 'NONE',  ( 2.781367136452438604, 6.916275212954706042, 3.637318098960494073 ) ) ;
#21478=CARTESIAN_POINT ( 'NONE',  ( 5.530133899448235191, 0.006510401266731618425, 0.01459891979722881261 ) ) ;
#21481=VERTEX_POINT ( 'NONE', #46353 ) ;
#21484=EDGE_CURVE ( 'NONE', #28445, #45757, #20422, .T. ) ;
#21485=B_SPLINE_CURVE_WITH_KNOTS ( 'NONE', 3,
 ( #26943, #42203, #62186, #26286, #52562, #56554, #52230, #31905, #46898, #26605, #57540, #56894, #7296, #16315, #36593, #10996, #31586, #41564, #61854 ),
 .UNSPECIFIED., .F., .F.,
 ( 4, 3, 3, 3, 3, 3, 4 ),
 ( 9.619659766987995311E-18, 4.457896483015182738E-05, 6.639290541542450317E-05, 8.820687556479344011E-05, 0.0001100173248778969103, 0.0001545671401658147586, 0.0001830328308068583057 ),
 .UNSPECIFIED. ) ;
#21488=CARTESIAN_POINT ( 'NONE',  ( 0.3053067050349154155, -9.538004819224397579, 7.702091166065980765 ) ) ;
#21505=CARTESIAN_POINT ( 'NONE',  ( 5.520433897694421610, -0.007971295965052688573, -0.01278034823632013400 ) ) ;
#21506=AXIS2_PLACEMENT_3D ( 'NONE', #17933, #22601, #28887 ) ;
#21520=CARTESIAN_POINT ( 'NONE',  ( 0.6473888112830253894, 12.23851338376148412, 1.823007254466997074 ) ) ;
#21528=CARTESIAN_POINT ( 'NONE',  ( 0.3675815128205912052, -11.62724744438068569, 3.951233083390429446 ) ) ;
#21529=ORIENTED_EDGE ( 'NONE', *, *, #58231, .T. ) ;
#21530=AXIS2_PLACEMENT_3D ( 'NONE', #4917, #40461, #35787 ) ;
#21535=CARTESIAN_POINT ( 'NONE',  ( 5.516018279890452902, -0.006707902355169293243, 0.0009545156522407741585 ) ) ;
#21540=VECTOR ( 'NONE', #56677, 1000.000000000000000 ) ;
#21545=CARTESIAN_POINT ( 'NONE',  ( 0.3665391374699464300, -3.952034409876219012, -11.62960183138731018 ) ) ;
#21547=CARTESIAN_POINT ( 'NONE',  ( 2.290907136833252533, 1.488079974905042180, -7.504812001538589961 ) ) ;
#21550=CARTESIAN_POINT ( 'NONE',  ( 2.241449424704145876, -0.06135604983222692904, -7.634218943782393296 ) ) ;
#21552=CARTESIAN_POINT ( 'NONE',  ( 0.3675815128205894289, -1.872154644482166397, 12.13672785388549613 ) ) ;
#21556=B_SPLINE_CURVE_WITH_KNOTS ( 'NONE', 3,
 ( #5014, #61192, #29598, #15619, #30916, #39592, #59891, #14314, #49905, #24630, #44907, #65190, #19657, #16624, #16296, #1340 ),
 .UNSPECIFIED., .F., .F.,
 ( 4, 3, 3, 3, 3, 4 ),
 ( 0.000000000000000000, 0.0002999043160757455806, 0.0005998071753051214920, 0.0008997092107374869783, 0.001204458948196641694, 0.001510329163478484364 ),
 .UNSPECIFIED. ) ;
#21569=B_SPLINE_CURVE_WITH_KNOTS ( 'NONE', 3,
 ( #13747, #44336, #49040, #44031, #38715, #13429, #14085, #39031, #38375, #8786 ),
 .UNSPECIFIED., .F., .F.,
 ( 4, 3, 3, 4 ),
 ( 1.563658610346375187E-18, 6.607638129004402147E-05, 9.911389841680390798E-05, 0.0001667630577588619318 ),
 .UNSPECIFIED. ) ;
#21572=VERTEX_POINT ( 'NONE', #51999 ) ;
#21581=CARTESIAN_POINT ( 'NONE',  ( 2.781367136450317634, 7.808329083462971276, -0.3081277311318336154 ) ) ;
#21585=CARTESIAN_POINT ( 'NONE',  ( 0.8320506296491628762, -5.883188144889849980, 10.95539209551944815 ) ) ;
#21599=CARTESIAN_POINT ( 'NONE',  ( 0.6473888112830222807, -11.73602097806018030, -3.920507224439204297 ) ) ;
#21605=CARTESIAN_POINT ( 'NONE',  ( 2.298277635560100229, 5.044791616846937110, -5.755367168477931727 ) ) ;
#21610=CARTESIAN_POINT ( 'NONE',  ( 3.152665057734040488, 0.000000000000000000, 0.000000000000000000 ) ) ;
#21621=CARTESIAN_POINT ( 'NONE',  ( 5.516018279890452902, -0.001397286410094463784, -0.006629829924290467358 ) ) ;
#21622=CARTESIAN_POINT ( 'NONE',  ( 0.7446945582530906105, -10.56139717223442354, -6.508900271376202085 ) ) ;
#21627=B_SPLINE_CURVE_WITH_KNOTS ( 'NONE', 3,
 ( #47462, #16545, #42426, #57776, #47140, #17192, #38110, #57430, #1592, #26839, #52117, #12194, #41800, #48453, #42773, #52772, #58421, #7199, #12506 ),
 .UNSPECIFIED., .F., .F.,
 ( 4, 3, 3, 3, 3, 3, 4 ),
 ( 4.336808689942017255E-19, 2.831840207499562487E-05, 4.217266859840527316E-05, 5.602024318396039802E-05, 6.290810167969274318E-05, 9.120440630945197459E-05, 0.0001153103026479775127 ),
 .UNSPECIFIED. ) ;
#21632=CARTESIAN_POINT ( 'NONE',  ( 2.994568964204208150, 6.289764245798291853, -4.756002438591006687 ) ) ;
#21637=CARTESIAN_POINT ( 'NONE',  ( 2.177405672431328210, 5.005033771132237241, -10.01846874165100409 ) ) ;
#21640=CARTESIAN_POINT ( 'NONE',  ( 0.2653141334712571520, -2.169900597054437608, -12.05242949860146418 ) ) ;
#21652=B_SPLINE_CURVE_WITH_KNOTS ( 'NONE', 3,
 ( #48578, #3029, #38588, #22292, #58904, #62864, #37606 ),
 .UNSPECIFIED., .F., .F.,
 ( 4, 3, 4 ),
 ( 0.000000000000000000, 0.001700533616330529530, 0.005002426799371274824 ),
 .UNSPECIFIED. ) ;
#21656=CARTESIAN_POINT ( 'NONE',  ( 2.653899356900291107, -6.596318473603853150, 4.109946795501455696 ) ) ;
#21662=CARTESIAN_POINT ( 'NONE',  ( 0.2717059086739007645, -1.953280559502777347, 12.09156413799790286 ) ) ;
#21671=CARTESIAN_POINT ( 'NONE',  ( 0.2648978790185584908, -9.465406350830660287, 7.769924372105172949 ) ) ;
#21677=CARTESIAN_POINT ( 'NONE',  ( 0.2646305136544065406, -10.53923716745251049, 6.237419468587042992 ) ) ;
#21679=CARTESIAN_POINT ( 'NONE',  ( 0.2956976708475498317, 12.10637007622315409, -1.911282699793599660 ) ) ;
#21687=CARTESIAN_POINT ( 'NONE',  ( 2.034671305879856895, -10.71175679137336445, -4.647127512369300106 ) ) ;
#21689=CARTESIAN_POINT ( 'NONE',  ( 5.515539859299206427, -0.005336559634876962034, -0.002856745161749523441 ) ) ;
#21692=ORIENTED_EDGE ( 'NONE', *, *, #17962, .T. ) ;
#21693=CARTESIAN_POINT ( 'NONE',  ( 0.2869720083484325057, -4.386174336869667734, 11.44147823180129464 ) ) ;
#21695=AXIS2_PLACEMENT_3D ( 'NONE', #51897, #6338, #12288 ) ;
#21704=CARTESIAN_POINT ( 'NONE',  ( 3.031336079629464830, -4.304138522350336338, -6.621879275826748845 ) ) ;
#21714=EDGE_LOOP ( 'NONE', ( #34963, #47551, #39965, #19764 ) ) ;
#21716=CARTESIAN_POINT ( 'NONE',  ( 0.3341166715381321817, -4.432780143632420788, -11.44035855572979976 ) ) ;
#21720=AXIS2_PLACEMENT_3D ( 'NONE', #21974, #16979, #57233 ) ;
#21724=EDGE_CURVE ( 'NONE', #56447, #24195, #8689, .T. ) ;
#21725=CARTESIAN_POINT ( 'NONE',  ( 5.514970785353741078, 0.001117786416802112525, -0.004588761610584830321 ) ) ;
#21726=CARTESIAN_POINT ( 'NONE',  ( 2.269879328256729334, -5.759117113708034807, 5.026125315665188609 ) ) ;
#21732=DIRECTION ( 'NONE',  ( 0.000000000000000000, 0.000000000000000000, 1.000000000000000000 ) ) ;
#21733=CARTESIAN_POINT ( 'NONE',  ( 0.2911222467163550598, -12.25291251554515704, -0.2144311696656930888 ) ) ;
#21735=CARTESIAN_POINT ( 'NONE',  ( 0.3665391374699465965, 2.392238720110458239, 12.04754782681758130 ) ) ;
#21738=ADVANCED_FACE ( 'NONE', ( #33670 ), #30297, .F. ) ;
#21742=CARTESIAN_POINT ( 'NONE',  ( 0.3109076770649071841, -5.925244271826518805, 10.73466383006819136 ) ) ;
#21744=ORIENTED_EDGE ( 'NONE', *, *, #52657, .T. ) ;
#21750=LINE ( 'NONE', #51015, #401 ) ;
#21751=CARTESIAN_POINT ( 'NONE',  ( 0.3675815128205894289, -0.2638082659427565813, -12.27743992903066328 ) ) ;
#21752=VERTEX_POINT ( 'NONE', #28678 ) ;
#21762=CARTESIAN_POINT ( 'NONE',  ( 3.152665057734062248, -7.609997527621111146, 2.258875078502258216 ) ) ;
#21767=CARTESIAN_POINT ( 'NONE',  ( 2.305787727787083519, -7.654065630109506913, -0.1666591538753489643 ) ) ;
#21769=EDGE_CURVE ( 'NONE', #33142, #41836, #31626, .T. ) ;
#21772=CARTESIAN_POINT ( 'NONE',  ( 0.3109076770649032984, -12.03190317807025878, 2.361108455562804576 ) ) ;
#21777=CARTESIAN_POINT ( 'NONE',  ( 3.047904605210369322, 7.698174516567099168, 1.788881754552535286 ) ) ;
#21778=EDGE_LOOP ( 'NONE', ( #6119, #27121, #39263, #1318 ) ) ;
#21782=CARTESIAN_POINT ( 'NONE',  ( 0.5547464869798247600, -10.53334899235175470, 6.433541106625056294 ) ) ;
#21788=B_SPLINE_CURVE_WITH_KNOTS ( 'NONE', 3,
 ( #39460, #8553, #28841, #14191, #23875, #3263, #2935, #43810, #59762, #48486, #13226, #34479, #4230, #44134, #38824, #33170 ),
 .UNSPECIFIED., .F., .F.,
 ( 4, 3, 3, 3, 3, 4 ),
 ( 2.636225826258666826E-15, 0.0002126834539179618623, 0.0004253519300366071084, 0.0006380165497223882001, 0.0007442707582427911467, 0.0009453531351419972159 ),
 .UNSPECIFIED. ) ;
#21790=VERTEX_POINT ( 'NONE', #37179 ) ;
#21791=CARTESIAN_POINT ( 'NONE',  ( 0.3040950598368152291, 6.347045025870766466, 10.49113473328032775 ) ) ;
#21795=B_SPLINE_CURVE_WITH_KNOTS ( 'NONE', 3,
 ( #3600, #23866, #34470, #18861, #33805, #55411, #59114, #64081, #4563, #8543, #44127, #24832, #60391, #34133, #24165, #54451, #54773, #14815, #64393 ),
 .UNSPECIFIED., .F., .F.,
 ( 4, 3, 3, 3, 3, 3, 4 ),
 ( 1.039534490390255771E-17, 4.457896483015144114E-05, 6.639290541542309371E-05, 8.820687556479193578E-05, 0.0001100173248778926413, 0.0001545671401658163036, 0.0001830328308068566252 ),
 .UNSPECIFIED. ) ;
#21796=CARTESIAN_POINT ( 'NONE',  ( 0.3537226245948369985, 4.442821955543956314, -11.44347094181047453 ) ) ;
#21801=ORIENTED_EDGE ( 'NONE', *, *, #54959, .F. ) ;
#21803=LINE ( 'NONE', #47400, #14452 ) ;
#21804=CARTESIAN_POINT ( 'NONE',  ( 5.515539859299206427, 0.003740028639278282496, 0.004759416711441693572 ) ) ;
#21805=CARTESIAN_POINT ( 'NONE',  ( 2.491965175174698288, -1.548529392254218040, -7.560994562509435468 ) ) ;
#21812=CARTESIAN_POINT ( 'NONE',  ( 2.655192694323436964, 6.969384012965880615, -6.604353705985066547 ) ) ;
#21814=CARTESIAN_POINT ( 'NONE',  ( 0.4613984246114888887, -12.17044190070616061, -1.858723191796595842 ) ) ;
#21825=ORIENTED_EDGE ( 'NONE', *, *, #52989, .F. ) ;
#21831=CARTESIAN_POINT ( 'NONE',  ( 0.2657645697724688172, 5.991637049003244009, 10.68050050043093258 ) ) ;
#21832=CARTESIAN_POINT ( 'NONE',  ( 0.2671309869109514956, 11.45180222993660379, -4.340541005679410702 ) ) ;
#21839=CARTESIAN_POINT ( 'NONE',  ( 2.350038591458109227, 1.210550722321025452, 10.55267716396076239 ) ) ;
#21848=CARTESIAN_POINT ( 'NONE',  ( 2.368238019615220402, 7.526794520527660737, -1.509700170844529232 ) ) ;
#21850=CARTESIAN_POINT ( 'NONE',  ( 2.241451721903216399, 1.385577012535855523, -7.507681056655362895 ) ) ;
#21856=CARTESIAN_POINT ( 'NONE',  ( 2.305787727787083519, -7.566723232958080914, 1.164987321564707967 ) ) ;
#21859=CARTESIAN_POINT ( 'NONE',  ( 1.459561108992491807, 12.62847742794652106, -0.6317018236570858258 ) ) ;
#21866=CARTESIAN_POINT ( 'NONE',  ( 0.2767916011545370480, -10.70244578860291718, -5.959903879715701791 ) ) ;
#21867=CARTESIAN_POINT ( 'NONE',  ( 0.2650492594609235031, -11.46945808033130909, -4.291723947796430849 ) ) ;
#21869=EDGE_LOOP ( 'NONE', ( #30268, #37403, #11527, #5553 ) ) ;
#21871=DIRECTION ( 'NONE',  ( 0.3939253465568944290, -0.5982248387291289049, 0.6978179301705699222 ) ) ;
#21873=CARTESIAN_POINT ( 'NONE',  ( 0.2767916011545404897, 7.727819755721592188, -9.504925141026269841 ) ) ;
#21875=CARTESIAN_POINT ( 'NONE',  ( 2.305787727787084851, -7.566723232958062262, -1.164987321564809886 ) ) ;
#21878=CARTESIAN_POINT ( 'NONE',  ( 0.2651627923886334393, -6.046629261473261963, -10.64925183219499694 ) ) ;
#21880=CARTESIAN_POINT ( 'NONE',  ( 0.6511581176963316953, -12.23990098761621326, 1.822219471614201725 ) ) ;
#21884=CARTESIAN_POINT ( 'NONE',  ( 0.3401186441510231639, 6.355596563012454681, -10.49699112323336259 ) ) ;
#21887=CARTESIAN_POINT ( 'NONE',  ( 0.2646305136544065406, 6.237419468587226845, -10.53923716745240036 ) ) ;
#21890=CARTESIAN_POINT ( 'NONE',  ( 2.241509619876136838, 7.160887714159624551, 2.647089031563595540 ) ) ;
#21892=CARTESIAN_POINT ( 'NONE',  ( 5.516018279890452902, 0.006440244342253029219, 0.002104829434640694864 ) ) ;
#21898=CARTESIAN_POINT ( 'NONE',  ( 0.3278977287071232483, 1.885359334311965895, 12.12129679591847164 ) ) ;
#21903=CARTESIAN_POINT ( 'NONE',  ( 2.241352910868908310, 0.08337961031714861970, -7.633946224498473043 ) ) ;
#21904=CARTESIAN_POINT ( 'NONE',  ( 1.462291587750753852, -7.633056170897860149, -10.08151577214967709 ) ) ;
#21908=CARTESIAN_POINT ( 'NONE',  ( 5.514624014163232779, 0.003946330869975002258, -0.001255375129358090409 ) ) ;
#21922=ORIENTED_EDGE ( 'NONE', *, *, #64055, .F. ) ;
#21927=CARTESIAN_POINT ( 'NONE',  ( 2.259830038564650589, 5.015955067335593043, -5.763537486834822587 ) ) ;
#21929=CARTESIAN_POINT ( 'NONE',  ( 2.242819959140644137, 2.707278038035169310, -7.138786956204133283 ) ) ;
#21930=EDGE_CURVE ( 'NONE', #18816, #61317, #49160, .T. ) ;
#21938=CARTESIAN_POINT ( 'NONE',  ( 2.269879328257217832, 3.692763753156445894, -6.692746930935887129 ) ) ;
#21940=B_SPLINE_CURVE_WITH_KNOTS ( 'NONE', 3,
 ( #23852, #24817, #40085, #44110, #34456, #64379, #29456 ),
 .UNSPECIFIED., .F., .F.,
 ( 4, 3, 4 ),
 ( 0.000000000000000000, 0.001700533616330535819, 0.005002426799371217578 ),
 .UNSPECIFIED. ) ;
#21941=CARTESIAN_POINT ( 'NONE',  ( 0.2958664285830405194, -8.045892866065303295, -9.245659426743973341 ) ) ;
#21942=PLANE ( 'NONE',  #33382 ) ;
#21950=CARTESIAN_POINT ( 'NONE',  ( 2.827825597296800719, 8.650999012440216518, -2.568788224597678305 ) ) ;
#21952=CARTESIAN_POINT ( 'NONE',  ( 2.253265082352431836, -6.678225412356971091, 3.707567016433793938 ) ) ;
#21960=CARTESIAN_POINT ( 'NONE',  ( 5.514970785353741078, -0.0005190732562558867313, -0.004694330894494369230 ) ) ;
#21974=CARTESIAN_POINT ( 'NONE',  ( 3.152665057734040488, 0.000000000000000000, 0.000000000000000000 ) ) ;
#21976=EDGE_CURVE ( 'NONE', #14585, #42516, #22764, .T. ) ;
#21980=VERTEX_POINT ( 'NONE', #53492 ) ;
#21981=CARTESIAN_POINT ( 'NONE',  ( 0.2653141617321035928, 11.52265685897335068, -4.147035654172604779 ) ) ;
#21985=VERTEX_POINT ( 'NONE', #32399 ) ;
#21991=CARTESIAN_POINT ( 'NONE',  ( 2.827825597296808269, -2.568788224597702730, -8.650999012440189873 ) ) ;
#21993=CARTESIAN_POINT ( 'NONE',  ( 0.3040950598368152291, 9.229598020917798351, -8.072385578287377683 ) ) ;
#21994=CARTESIAN_POINT ( 'NONE',  ( 2.827825597296804716, -8.278234963587674855, -3.592949031604497634 ) ) ;
#21997=CARTESIAN_POINT ( 'NONE',  ( 0.2648978790185602672, 4.312320170909236694, 11.46165506714229565 ) ) ;
#22005=ORIENTED_EDGE ( 'NONE', *, *, #23920, .T. ) ;
#22006=LINE ( 'NONE', #32303, #29649 ) ;
#22007=CARTESIAN_POINT ( 'NONE',  ( 0.3610902822527166656, 12.04327049858143539, -2.389900346487964899 ) ) ;
#22018=CARTESIAN_POINT ( 'NONE',  ( 0.2648978790185593790, -10.53870023327859151, -6.237101853238657512 ) ) ;
#22025=CARTESIAN_POINT ( 'NONE',  ( 0.3053067050349174139, -5.928821939311855083, -10.73055518945194819 ) ) ;
#22027=CARTESIAN_POINT ( 'NONE',  ( 1.283627346226426713, 4.817767733507119843, 11.62704807385632044 ) ) ;
#22028=CARTESIAN_POINT ( 'NONE',  ( 2.440552418640498988, 5.099602138956282893, -5.770332237304396372 ) ) ;
#22030=EDGE_CURVE ( 'NONE', #30538, #63048, #63313, .T. ) ;
#22032=DIRECTION ( 'NONE',  ( 0.3939253465568943735, 0.3052156353794266974, 0.8669868725995586445 ) ) ;
#22033=B_SPLINE_CURVE_WITH_KNOTS ( 'NONE', 3,
 ( #18347, #48291, #2738, #22997, #18986, #13010, #59546, #9004, #13977, #34268, #29287, #53596, #10621, #14616, #40564, #24622 ),
 .UNSPECIFIED., .F., .F.,
 ( 4, 3, 3, 3, 3, 4 ),
 ( 0.000000000000000000, 0.0003017745587525249760, 0.0006035491769808762341, 0.0009053241094668206933, 0.001207275924539024173, 0.001510325902531031326 ),
 .UNSPECIFIED. ) ;
#22035=ORIENTED_EDGE ( 'NONE', *, *, #921, .T. ) ;
#22037=CARTESIAN_POINT ( 'NONE',  ( 1.020182472820991837, 10.59341968305504089, 6.631405022218979539 ) ) ;
#22041=ORIENTED_EDGE ( 'NONE', *, *, #64055, .T. ) ;
#22043=CARTESIAN_POINT ( 'NONE',  ( 0.3164563675027631251, -5.922187299605712774, 10.73846246126247550 ) ) ;
#22050=ORIENTED_EDGE ( 'NONE', *, *, #22772, .F. ) ;
#22052=CARTESIAN_POINT ( 'NONE',  ( 0.9296196016843242260, -11.56707937094521732, -4.652334946095537660 ) ) ;
#22063=CARTESIAN_POINT ( 'NONE',  ( 0.2653141334712584287, 9.352759824582610904, -7.905403790036874767 ) ) ;
#22070=CARTESIAN_POINT ( 'NONE',  ( 2.177405672431969919, -11.12610351585405333, -1.276675186593726030 ) ) ;
#22071=CARTESIAN_POINT ( 'NONE',  ( 2.241451721903217731, -5.887257931662872146, 4.860585618235946370 ) ) ;
#22074=CARTESIAN_POINT ( 'NONE',  ( 2.963017218115620466, 7.679262289252045015, 1.744728040076931830 ) ) ;
#22081=CARTESIAN_POINT ( 'NONE',  ( 2.241352910868909643, 7.202080440908774861, -2.532612177304371048 ) ) ;
#22083=ADVANCED_FACE ( 'NONE', ( #12438 ), #55739, .F. ) ;
#22085=AXIS2_PLACEMENT_3D ( 'NONE', #33450, #4174, #23471 ) ;
#22087=EDGE_CURVE ( 'NONE', #64733, #28659, #6341, .T. ) ;
#22089=EDGE_CURVE ( 'NONE', #26102, #43663, #9477, .T. ) ;
#22091=ORIENTED_EDGE ( 'NONE', *, *, #38212, .F. ) ;
#22104=CARTESIAN_POINT ( 'NONE',  ( 0.2869720083484365580, -1.922200714744079164, -12.10169797402142500 ) ) ;
#22105=CARTESIAN_POINT ( 'NONE',  ( 0.2638984909335720941, -12.24571285024409129, 0.1991813963113568953 ) ) ;
#22107=EDGE_CURVE ( 'NONE', #281, #18433, #13378, .T. ) ;
#22112=CARTESIAN_POINT ( 'NONE',  ( 1.948354844646350115, 8.685970062895311372, -8.228891433297251368 ) ) ;
#22114=CARTESIAN_POINT ( 'NONE',  ( 2.241311220309522234, -4.835827934491081059, -5.907514893712877857 ) ) ;
#22115=CARTESIAN_POINT ( 'NONE',  ( 0.7400311444011719031, -12.27261279799597915, -1.803686700615534377 ) ) ;
#22118=CARTESIAN_POINT ( 'NONE',  ( 5.514624014163232779, 0.003060352188290776324, 0.002789935220458057957 ) ) ;
#22122=LINE ( 'NONE', #23112, #58637 ) ;
#22128=AXIS2_PLACEMENT_3D ( 'NONE', #31199, #56464, #16227 ) ;
#22131=LINE ( 'NONE', #62681, #47842 ) ;
#22134=CARTESIAN_POINT ( 'NONE',  ( 0.6473888112830245012, 11.73602097806020517, 3.920507224439127025 ) ) ;
#22137=CARTESIAN_POINT ( 'NONE',  ( 1.198791140420665702, 4.776130053253731411, -11.61358959650694089 ) ) ;
#22149=CARTESIAN_POINT ( 'NONE',  ( 0.4613984246114877785, -3.943860067443726525, 11.66278164635733461 ) ) ;
#22155=DIRECTION ( 'NONE',  ( -0.3865475372811021937, -0.8730852074079720193, -0.2971585806051939005 ) ) ;
#22160=CARTESIAN_POINT ( 'NONE',  ( 3.047904605210428386, -7.845751380824987464, 0.9519317672906529859 ) ) ;
#22169=CARTESIAN_POINT ( 'NONE',  ( 0.2648978790185593790, 9.465406350830713578, -7.769924372105106336 ) ) ;
#22171=CARTESIAN_POINT ( 'NONE',  ( 0.2648978790185584908, 10.67083876753500427, -6.008231198268870976 ) ) ;
#22174=ORIENTED_EDGE ( 'NONE', *, *, #41402, .T. ) ;
#22178=CARTESIAN_POINT ( 'NONE',  ( 0.3675815128205894289, 7.689697408877401941, -9.574637318041888889 ) ) ;
#22179=CARTESIAN_POINT ( 'NONE',  ( 0.3665391374699464300, 11.62960183138732440, -3.952034409876179932 ) ) ;
#22181=CARTESIAN_POINT ( 'NONE',  ( 2.251139882113970980, 4.813633939919418125, 5.929826121559315766 ) ) ;
#22184=CARTESIAN_POINT ( 'NONE',  ( 2.835339799623972645, 2.367573116406979317, 7.466040501142034991 ) ) ;
#22196=CARTESIAN_POINT ( 'NONE',  ( 2.665405856346786173, 9.304623509366205525, 2.226920474533411021 ) ) ;
#22211=CARTESIAN_POINT ( 'NONE',  ( 2.276905613633649406, 7.555317002492091483, 1.175741125184106339 ) ) ;
#22216=ORIENTED_EDGE ( 'NONE', *, *, #13488, .T. ) ;
#22217=CARTESIAN_POINT ( 'NONE',  ( 1.014383007554952254, -5.859361736620408045, 11.03701226956414239 ) ) ;
#22231=VERTEX_POINT ( 'NONE', #44778 ) ;
#22233=VERTEX_POINT ( 'NONE', #19536 ) ;
#22239=CARTESIAN_POINT ( 'NONE',  ( 0.3164563675027637912, 4.419430877662341217, 11.43920928915625623 ) ) ;
#22241=DIRECTION ( 'NONE',  ( -1.000000000000000000, -0.000000000000000000, -0.000000000000000000 ) ) ;
#22244=CARTESIAN_POINT ( 'NONE',  ( 5.536195898058073439, 0.005266167600747600520, 0.006672323185952732348 ) ) ;
#22249=CARTESIAN_POINT ( 'NONE',  ( 2.440552418640466126, 4.797131306497566250, 6.024135401262375566 ) ) ;
#22256=CARTESIAN_POINT ( 'NONE',  ( 1.719304012338199517, 0.000000000000000000, 0.000000000000000000 ) ) ;
#22259=CARTESIAN_POINT ( 'NONE',  ( 0.2759803524722198587, -0.1894460813476845917, 12.24828167798667877 ) ) ;
#22262=CARTESIAN_POINT ( 'NONE',  ( 2.268878695253353950, -6.692359410363624583, 3.692782103667259452 ) ) ;
#22265=CARTESIAN_POINT ( 'NONE',  ( 0.3675815128205894289, 11.44679196252409348, 4.447030445008218535 ) ) ;
#22272=ORIENTED_EDGE ( 'NONE', *, *, #33076, .T. ) ;
#22273=CARTESIAN_POINT ( 'NONE',  ( 0.2655924914740778742, -9.352877839710654229, 7.905499957109207720 ) ) ;
#22275=CARTESIAN_POINT ( 'NONE',  ( 5.530133899448235191, 0.004396748047611225528, 0.01536822665454896930 ) ) ;
#22279=CARTESIAN_POINT ( 'NONE',  ( 2.844750968616207576, -6.613363922490621327, 4.202329849280634910 ) ) ;
#22281=CARTESIAN_POINT ( 'NONE',  ( 0.9232167919969205272, -7.691547553333184517, 9.809608956680843761 ) ) ;
#22283=ORIENTED_EDGE ( 'NONE', *, *, #58315, .F. ) ;
#22286=CARTESIAN_POINT ( 'NONE',  ( 2.931247277082683844, 7.855653518374123401, 0.3703309885897093090 ) ) ;
#22287=B_SPLINE_CURVE_WITH_KNOTS ( 'NONE', 3,
 ( #1209, #52414, #12151, #17146, #33084, #37755, #28114, #21488, #37418, #32424, #42721, #63020, #57730, #41757, #47735, #2182, #22461, #17481, #12463 ),
 .UNSPECIFIED., .F., .F.,
 ( 4, 3, 3, 3, 3, 3, 4 ),
 ( 1.038473834433558171E-17, 4.457896483015033660E-05, 6.639290541542310726E-05, 8.820687556479056698E-05, 0.0001100173248778915164, 0.0001545671401658174149, 0.0001830328308068568150 ),
 .UNSPECIFIED. ) ;
#22292=CARTESIAN_POINT ( 'NONE',  ( 2.665405856346785729, -8.559192023451554832, 4.274976649834437481 ) ) ;
#22295=CARTESIAN_POINT ( 'NONE',  ( 2.242418902651938772, -2.704708480794760117, -7.139616612143416141 ) ) ;
#22303=CARTESIAN_POINT ( 'NONE',  ( 3.152665057734079568, -2.258875078502220024, -7.609997527621126245 ) ) ;
#22307=CARTESIAN_POINT ( 'NONE',  ( 2.990245332647881948, -7.779904630197274074, -3.377079998295690277 ) ) ;
#22308=CARTESIAN_POINT ( 'NONE',  ( 0.5572780756290600657, 6.434474476008377408, -10.53376864352708431 ) ) ;
#22313=( BOUNDED_SURFACE ( )  B_SPLINE_SURFACE ( 3, 1, ( 
 ( #42000, #15735 ),
 ( #37342, #26076 ),
 ( #57652, #794 ),
 ( #61623, #36365 ) ),
 .UNSPECIFIED., .F., .F., .F. ) 
 B_SPLINE_SURFACE_WITH_KNOTS ( ( 4, 4 ),
 ( 2, 2 ),
 ( 0.000000000000000000, 1.000000000000000000 ),
 ( 0.000000000000000000, 1.000000000000000000 ),
 .UNSPECIFIED. ) 
 GEOMETRIC_REPRESENTATION_ITEM ( )  RATIONAL_B_SPLINE_SURFACE ( (
 ( 1.000000000000000000, 1.000000000000000000),
 ( 0.9942764183789327692, 0.8450855930916585379),
 ( 0.9942764183789327692, 0.8450855930916585379),
 ( 1.000000000000000000, 1.000000000000000000) ) ) 
 REPRESENTATION_ITEM ( '' )  SURFACE ( )  );
#22314=ORIENTED_EDGE ( 'NONE', *, *, #17354, .T. ) ;
#22316=CARTESIAN_POINT ( 'NONE',  ( 2.260457164925429918, 6.685239696061921144, 3.699855525214781338 ) ) ;
#22317=ORIENTED_EDGE ( 'NONE', *, *, #54999, .T. ) ;
#22319=CARTESIAN_POINT ( 'NONE',  ( 0.2958664285830439056, 12.02992237133200071, -2.345117904768493577 ) ) ;
#22323=ORIENTED_EDGE ( 'NONE', *, *, #8149, .F. ) ;
#22324=CARTESIAN_POINT ( 'NONE',  ( 2.844750968616333697, -6.946006365804024973, -3.626176236708053224 ) ) ;
#22345=EDGE_CURVE ( 'NONE', #45562, #63445, #14081, .T. ) ;
#22348=CARTESIAN_POINT ( 'NONE',  ( 2.507146904658102304, 5.128007631637142794, -5.774795220010139118 ) ) ;
#22355=CONICAL_SURFACE ( 'NONE', #42519, 7.938172270156617749, 1.280189991382167047 ) ;
#22359=CARTESIAN_POINT ( 'NONE',  ( 2.177405672430581252, -6.173731551725364142, -9.343720763427118214 ) ) ;
#22361=AXIS2_PLACEMENT_3D ( 'NONE', #60441, #64760, #8934 ) ;
#22362=CARTESIAN_POINT ( 'NONE',  ( 2.241509619876138615, 4.936617871859581008, -5.823675573301023256 ) ) ;
#22372=CARTESIAN_POINT ( 'NONE',  ( 2.835339799623984192, -2.985412098050548746, 7.241165502254432340 ) ) ;
#22374=CIRCLE ( 'NONE', #40404, 12.73084802173761787 ) ;
#22375=CARTESIAN_POINT ( 'NONE',  ( 20.00005080000000035, 0.000000000000000000, 0.000000000000000000 ) ) ;
#22382=CARTESIAN_POINT ( 'NONE',  ( 5.530133899448235191, -0.006510401266731714702, -0.01459891979722877098 ) ) ;
#22389=CARTESIAN_POINT ( 'NONE',  ( 1.375507693217711713, -4.865932489130966765, 11.64019206974660214 ) ) ;
#22395=DIRECTION ( 'NONE',  ( -0.3865475372811021937, 0.9220659470476461061, -0.01937500237528741107 ) ) ;
#22403=CARTESIAN_POINT ( 'NONE',  ( 0.3675815128205894289, 1.872154644482245889, -12.13672785388548547 ) ) ;
#22433=CARTESIAN_POINT ( 'NONE',  ( 1.937114397841935398, -8.920887662793408168, -9.228205347192542263 ) ) ;
#22434=CARTESIAN_POINT ( 'NONE',  ( 2.430348790457659724, -1.528169972228470508, -7.544199152379142070 ) ) ;
#22440=CARTESIAN_POINT ( 'NONE',  ( 0.3665391374699465965, -6.368473106897055480, -10.50279796150443268 ) ) ;
#22444=EDGE_CURVE ( 'NONE', #22231, #53630, #8544, .T. ) ;
#22445=CARTESIAN_POINT ( 'NONE',  ( 2.247206125382657405, -4.819320926502908442, -5.923516414428318555 ) ) ;
#22459=AXIS2_PLACEMENT_3D ( 'NONE', #45827, #45169, #14555 ) ;
#22461=CARTESIAN_POINT ( 'NONE',  ( 0.2657645697724674849, -9.477802844074094679, 7.755260067564130111 ) ) ;
#22462=CARTESIAN_POINT ( 'NONE',  ( 5.515539859299206427, 0.005991790098943838676, -0.0008592514567755067450 ) ) ;
#22471=CARTESIAN_POINT ( 'NONE',  ( 0.9296196016850740707, 4.652334946095896484, -11.56707937094533634 ) ) ;
#22476=VERTEX_POINT ( 'NONE', #43064 ) ;
#22479=CARTESIAN_POINT ( 'NONE',  ( 2.827825597296809157, -5.372687261161216199, -7.250702617666037852 ) ) ;
#22485=CARTESIAN_POINT ( 'NONE',  ( 0.3040950598368152291, 1.881452845810536623, -12.11647736519418928 ) ) ;
#22486=CARTESIAN_POINT ( 'NONE',  ( 0.5547464869798236498, -3.933612953276315771, 11.69908463509555396 ) ) ;
#22497=EDGE_CURVE ( 'NONE', #19326, #46419, #25993, .T. ) ;
#22504=CARTESIAN_POINT ( 'NONE',  ( 2.262775599886257094, 3.942403752832098540, -6.546038779272000951 ) ) ;
#22506=CARTESIAN_POINT ( 'NONE',  ( 0.2648978790185584908, -11.46165506714225479, -4.312320170909353045 ) ) ;
#22507=ORIENTED_EDGE ( 'NONE', *, *, #52818, .F. ) ;
#22508=B_SPLINE_CURVE_WITH_KNOTS ( 'NONE', 3,
 ( #4736, #54498, #12592, #29221, #38194, #63461, #33221 ),
 .UNSPECIFIED., .F., .F.,
 ( 4, 3, 4 ),
 ( 5.216753085810794840E-15, 0.002398160485434687548, 0.005002426799382050059 ),
 .UNSPECIFIED. ) ;
#22509=CARTESIAN_POINT ( 'NONE',  ( 0.2653141617321017609, -6.161204121352767515, 10.58343467791294046 ) ) ;
#22511=CARTESIAN_POINT ( 'NONE',  ( 2.717984159219351437, -2.930214355830539574, -7.221467817271510548 ) ) ;
#22518=FACE_OUTER_BOUND ( 'NONE', #17089, .T. ) ;
#22519=( BOUNDED_SURFACE ( )  B_SPLINE_SURFACE ( 3, 1, ( 
 ( #22873, #27847 ),
 ( #8873, #53462 ),
 ( #38474, #13832 ),
 ( #23184, #33153 ) ),
 .UNSPECIFIED., .F., .F., .F. ) 
 B_SPLINE_SURFACE_WITH_KNOTS ( ( 4, 4 ),
 ( 2, 2 ),
 ( 0.000000000000000000, 1.000000000000000000 ),
 ( 0.000000000000000000, 1.000000000000000000 ),
 .UNSPECIFIED. ) 
 GEOMETRIC_REPRESENTATION_ITEM ( )  RATIONAL_B_SPLINE_SURFACE ( (
 ( 1.000000000000000000, 1.000000000000000000),
 ( 0.9856612449720755231, 0.9999558406602322425),
 ( 0.9856612449720755231, 0.9999558406602322425),
 ( 1.000000000000000000, 1.000000000000000000) ) ) 
 REPRESENTATION_ITEM ( '' )  SURFACE ( )  );
#22531=CARTESIAN_POINT ( 'NONE',  ( 0.2653519789438754106, -10.61653328464223023, -6.104019611498684661 ) ) ;
#22533=CARTESIAN_POINT ( 'NONE',  ( 0.2706063244538022272, 6.275112929891760061, -10.51833723927416031 ) ) ;
#22536=( BOUNDED_SURFACE ( )  B_SPLINE_SURFACE ( 3, 1, ( 
 ( #12494, #46777 ),
 ( #1578, #32767 ),
 ( #51782, #6226 ),
 ( #42097, #42757 ) ),
 .UNSPECIFIED., .F., .F., .F. ) 
 B_SPLINE_SURFACE_WITH_KNOTS ( ( 4, 4 ),
 ( 2, 2 ),
 ( 0.000000000000000000, 1.000000000000000000 ),
 ( 0.000000000000000000, 1.000000000000000000 ),
 .UNSPECIFIED. ) 
 GEOMETRIC_REPRESENTATION_ITEM ( )  RATIONAL_B_SPLINE_SURFACE ( (
 ( 1.000000000000000000, 1.000000000000000000),
 ( 0.9942764183789327692, 0.8450855930916580938),
 ( 0.9942764183789327692, 0.8450855930916580938),
 ( 1.000000000000000000, 1.000000000000000000) ) ) 
 REPRESENTATION_ITEM ( '' )  SURFACE ( )  );
#22541=CARTESIAN_POINT ( 'NONE',  ( 1.375507693218733563, -8.553661013312394701, 9.273955665125873438 ) ) ;
#22544=CARTESIAN_POINT ( 'NONE',  ( 0.2767916011545381583, -11.44495079483527711, 4.367596755337407544 ) ) ;
#22549=ORIENTED_EDGE ( 'NONE', *, *, #43628, .T. ) ;
#22550=B_SPLINE_CURVE_WITH_KNOTS ( 'NONE', 3,
 ( #58190, #7644, #57211, #27264, #27929, #17949, #7990, #2688, #21640, #47556, #33237, #57542, #1691 ),
 .UNSPECIFIED., .F., .F.,
 ( 4, 3, 3, 3, 4 ),
 ( 2.168404344971008868E-18, 6.607593386745501222E-05, 0.0001321518677373524609, 0.0001982171734706209411, 0.0002642860854759490423 ),
 .UNSPECIFIED. ) ;
#22551=FACE_OUTER_BOUND ( 'NONE', #27652, .T. ) ;
#22555=CARTESIAN_POINT ( 'NONE',  ( 3.152665057734130638, 7.609997527621177760, -2.258875078502145861 ) ) ;
#22557=CARTESIAN_POINT ( 'NONE',  ( 2.241528039335007438, 0.01573255094252495184, -7.634443721858079179 ) ) ;
#22558=CARTESIAN_POINT ( 'NONE',  ( 3.092491956583705015, 7.905533744257984274, -0.4473002062000842605 ) ) ;
#22559=ADVANCED_FACE ( 'NONE', ( #59048 ), #10279, .F. ) ;
#22560=CARTESIAN_POINT ( 'NONE',  ( 2.276198483118649030, 5.756970692721976590, 5.031786924856548104 ) ) ;
#22562=ORIENTED_EDGE ( 'NONE', *, *, #44875, .T. ) ;
#22571=CARTESIAN_POINT ( 'NONE',  ( 1.452237505248555660, -0.5922625322516135160, -12.64182585313126772 ) ) ;
#22574=VERTEX_POINT ( 'NONE', #59352 ) ;
#22581=ORIENTED_EDGE ( 'NONE', *, *, #14063, .F. ) ;
#22591=ORIENTED_EDGE ( 'NONE', *, *, #31777, .T. ) ;
#22594=CARTESIAN_POINT ( 'NONE',  ( 5.514970785353741078, -0.002619824551223729620, -0.003929719953530097683 ) ) ;
#22598=CARTESIAN_POINT ( 'NONE',  ( 0.2647959493198551173, -11.55693259385003735, -4.049980114636486661 ) ) ;
#22601=DIRECTION ( 'NONE',  ( -1.000000000000000000, -0.000000000000000000, -0.000000000000000000 ) ) ;
#22606=ORIENTED_EDGE ( 'NONE', *, *, #11523, .F. ) ;
#22607=DIRECTION ( 'NONE',  ( -1.000000000000000000, 0.000000000000000000, 0.000000000000000000 ) ) ;
#22608=CARTESIAN_POINT ( 'NONE',  ( 2.251139882113957658, 5.929826121559351293, -4.813633939919377269 ) ) ;
#22611=CARTESIAN_POINT ( 'NONE',  ( 2.507146904658097419, -4.796593924427943634, -6.052884339496478638 ) ) ;
#22612=EDGE_CURVE ( 'NONE', #52172, #7317, #45905, .T. ) ;
#22613=ORIENTED_EDGE ( 'NONE', *, *, #56617, .T. ) ;
#22615=CARTESIAN_POINT ( 'NONE',  ( 1.372161826076961022, 10.61825687422752473, -6.811451307636878560 ) ) ;
#22624=CARTESIAN_POINT ( 'NONE',  ( 2.844750968615479714, -0.3326424433130156788, -7.828506085988468755 ) ) ;
#22631=CARTESIAN_POINT ( 'NONE',  ( 2.297017764050092836, -6.543724852214706900, 3.968300849026735300 ) ) ;
#22632=CARTESIAN_POINT ( 'NONE',  ( 2.241352910868909643, -5.794346703933810794, -4.970878533273820565 ) ) ;
#22634=CARTESIAN_POINT ( 'NONE',  ( 1.633930747251776783, -7.601388527387466176, 10.17701904908730270 ) ) ;
#22638=B_SPLINE_CURVE_WITH_KNOTS ( 'NONE', 3,
 ( #64949, #43696, #38042, #63982, #51334, #40677, #56290, #20396, #45662, #5784, #46332, #26052, #35348 ),
 .UNSPECIFIED., .F., .F.,
 ( 4, 3, 3, 3, 4 ),
 ( 3.469446951953614189E-18, 6.607593386745428039E-05, 0.0001321518677373504551, 0.0001982171734706186642, 0.0002642860854759481750 ),
 .UNSPECIFIED. ) ;
#22643=CARTESIAN_POINT ( 'NONE',  ( 2.255723233588951437, 7.222632368701306760, -2.488140745365793105 ) ) ;
#22645=CARTESIAN_POINT ( 'NONE',  ( 3.152665057734040488, 0.000000000000000000, 0.000000000000000000 ) ) ;
#22653=CARTESIAN_POINT ( 'NONE',  ( 2.290907136834312130, 7.132394668149571793, 2.768669624189211032 ) ) ;
#22657=CARTESIAN_POINT ( 'NONE',  ( 0.2833330754217440739, 12.09951353627562298, -1.928200609300346091 ) ) ;
#22658=ORIENTED_EDGE ( 'NONE', *, *, #28831, .T. ) ;
#22662=CARTESIAN_POINT ( 'NONE',  ( 2.268878695253356170, 3.692782103667282101, 6.692359410363615702 ) ) ;
#22670=ORIENTED_EDGE ( 'NONE', *, *, #1312, .F. ) ;
#22672=EDGE_CURVE ( 'NONE', #64505, #45493, #60661, .T. ) ;
#22679=CARTESIAN_POINT ( 'NONE',  ( 2.430348790457469210, 7.297553103283551224, 2.448665558939112863 ) ) ;
#22680=CARTESIAN_POINT ( 'NONE',  ( 0.3006302518451994255, 6.323626002161084614, 10.50091819089218603 ) ) ;
#22681=CARTESIAN_POINT ( 'NONE',  ( 0.2648978790185610999, -2.256510822326061483, -12.03635331166814382 ) ) ;
#22682=ORIENTED_EDGE ( 'NONE', *, *, #54796, .F. ) ;
#22703=CARTESIAN_POINT ( 'NONE',  ( 2.259025283528082184, -5.764013728792217073, 5.014999102875841608 ) ) ;
#22716=VERTEX_POINT ( 'NONE', #36022 ) ;
#22717=CARTESIAN_POINT ( 'NONE',  ( 2.298277635560813437, 6.543949079924037626, 3.968740875991768835 ) ) ;
#22722=EDGE_CURVE ( 'NONE', #57595, #59842, #36341, .T. ) ;
#22723=CARTESIAN_POINT ( 'NONE',  ( 0.3537226245948383863, -12.04110684114371388, -2.388187631842642045 ) ) ;
#22726=CARTESIAN_POINT ( 'NONE',  ( 2.305787727787083519, -2.774453000917197265, 7.135468203929974607 ) ) ;
#22730=( BOUNDED_SURFACE ( )  B_SPLINE_SURFACE ( 3, 1, ( 
 ( #15572, #45504 ),
 ( #35838, #56833 ),
 ( #951, #41492 ),
 ( #61788, #52802 ) ),
 .UNSPECIFIED., .F., .F., .F. ) 
 B_SPLINE_SURFACE_WITH_KNOTS ( ( 4, 4 ),
 ( 2, 2 ),
 ( 0.000000000000000000, 1.000000000000000000 ),
 ( 0.000000000000000000, 1.000000000000000000 ),
 .UNSPECIFIED. ) 
 GEOMETRIC_REPRESENTATION_ITEM ( )  RATIONAL_B_SPLINE_SURFACE ( (
 ( 1.000000000000000000, 1.000000000000000000),
 ( 0.9856612449720755231, 0.9999558406602322425),
 ( 0.9856612449720755231, 0.9999558406602322425),
 ( 1.000000000000000000, 1.000000000000000000) ) ) 
 REPRESENTATION_ITEM ( '' )  SURFACE ( )  );
#22731=CARTESIAN_POINT ( 'NONE',  ( 0.2767916011545359933, -7.727819755721539785, 9.504925141026333790 ) ) ;
#22737=EDGE_LOOP ( 'NONE', ( #49460, #24426, #7704, #40194 ) ) ;
#22746=CARTESIAN_POINT ( 'NONE',  ( 0.2671309869109478319, -4.036029264453062204, 11.56263543972757368 ) ) ;
#22747=CARTESIAN_POINT ( 'NONE',  ( 1.104777566491145668, 8.411711248089098092, 9.281442536087510575 ) ) ;
#22748=DIRECTION ( 'NONE',  ( 0.000000000000000000, 0.000000000000000000, 1.000000000000000000 ) ) ;
#22751=ADVANCED_FACE ( 'NONE', ( #42996 ), #17486, .F. ) ;
#22763=DIRECTION ( 'NONE',  ( -1.000000000000000000, -0.000000000000000000, -0.000000000000000000 ) ) ;
#22764=CIRCLE ( 'NONE', #20622, 12.73084802173761787 ) ;
#22771=DIRECTION ( 'NONE',  ( -0.3865475372811021382, -0.1791957239473601637, -0.9046932595863066418 ) ) ;
#22772=EDGE_CURVE ( 'NONE', #56983, #39884, #58303, .T. ) ;
#22773=B_SPLINE_CURVE_WITH_KNOTS ( 'NONE', 3,
 ( #51581, #26944, #57541, #10644, #21288, #40928, #6339 ),
 .UNSPECIFIED., .F., .F.,
 ( 4, 3, 4 ),
 ( 4.934695962917737974E-15, 0.002398160485434642879, 0.005002426799381695308 ),
 .UNSPECIFIED. ) ;
#22774=CARTESIAN_POINT ( 'NONE',  ( 2.269879328256737772, -4.798845682294072823, 5.949827370243852442 ) ) ;
#22789=EDGE_LOOP ( 'NONE', ( #15570, #9869, #34281, #32508 ) ) ;
#22791=CARTESIAN_POINT ( 'NONE',  ( 5.536195898058073439, 0.007230647766619690241, -0.004468797463753810574 ) ) ;
#22805=CARTESIAN_POINT ( 'NONE',  ( 1.719304012341273724, 0.7661785589598685275, -12.70777170743938456 ) ) ;
#22807=CARTESIAN_POINT ( 'NONE',  ( 2.259025283528085737, -7.546748801935443396, -1.191911401085089750 ) ) ;
#22808=CARTESIAN_POINT ( 'NONE',  ( 2.430348790457457220, 3.678671624790124994, -6.761480562106341630 ) ) ;
#22819=CARTESIAN_POINT ( 'NONE',  ( 0.2648978790185593790, -4.063980959784970537, -11.55204314799267884 ) ) ;
#22830=ORIENTED_EDGE ( 'NONE', *, *, #14830, .T. ) ;
#22831=CARTESIAN_POINT ( 'NONE',  ( 5.516018279890452902, -0.004180585980735018921, -0.005331956019561697423 ) ) ;
#22841=CARTESIAN_POINT ( 'NONE',  ( 2.258463476536644254, 3.937122681832576188, -6.547539277367990351 ) ) ;
#22842=ORIENTED_EDGE ( 'NONE', *, *, #63502, .T. ) ;
#22844=B_SPLINE_CURVE_WITH_KNOTS ( 'NONE', 3,
 ( #8103, #7774, #22746, #24050, #48012, #2468, #3465, #43008, #33019, #39000, #38339, #8757, #33686, #63603, #29038, #59294, #64275, #38010, #58314, #28373, #28060, #18076 ),
 .UNSPECIFIED., .F., .F.,
 ( 4, 3, 3, 3, 3, 3, 3, 4 ),
 ( 8.741117365843378158E-19, 4.449119708437015698E-05, 6.626296329540635663E-05, 8.803456484963026257E-05, 0.0001098060367612851225, 0.0001315774408628581462, 0.0001760698110411260207, 0.0001829697163287835105 ),
 .UNSPECIFIED. ) ;
#22846=ORIENTED_EDGE ( 'NONE', *, *, #36174, .F. ) ;
#22849=CIRCLE ( 'NONE', #53616, 12.73084802173761787 ) ;
#22850=CARTESIAN_POINT ( 'NONE',  ( 2.556980015513487192, -2.862731173723767508, -7.190718924764468056 ) ) ;
#22860=EDGE_CURVE ( 'NONE', #27180, #32432, #5377, .T. ) ;
#22862=CARTESIAN_POINT ( 'NONE',  ( 1.719304012340733934, -12.20344780066092305, -3.626341562669774365 ) ) ;
#22864=CARTESIAN_POINT ( 'NONE',  ( 2.963017218115612028, 2.328652339224351664, 7.522800244854583873 ) ) ;
#22871=ORIENTED_EDGE ( 'NONE', *, *, #36241, .T. ) ;
#22873=CARTESIAN_POINT ( 'NONE',  ( 5.514970785353741078, 0.001897634820904481583, -0.004324946436530190987 ) ) ;
#22877=CARTESIAN_POINT ( 'NONE',  ( 3.152665057734126197, 7.719888720907812640, 1.848755561852068130 ) ) ;
#22879=CARTESIAN_POINT ( 'NONE',  ( 5.516018279890452902, -0.0002248006052447136570, 0.006771744149385739570 ) ) ;
#22880=CARTESIAN_POINT ( 'NONE',  ( 0.2648321136542715060, -11.55519783395230604, 4.054947570138854651 ) ) ;
#22884=CARTESIAN_POINT ( 'NONE',  ( 0.2657645697724703160, 1.977350809428533029, 12.08564806881062026 ) ) ;
#22886=FACE_OUTER_BOUND ( 'NONE', #12027, .T. ) ;
#22891=CARTESIAN_POINT ( 'NONE',  ( 2.251152103363646351, 7.542379262759450143, 1.202724109297105937 ) ) ;
#22893=VERTEX_POINT ( 'NONE', #29027 ) ;
#22900=CARTESIAN_POINT ( 'NONE',  ( 1.020182472824830988, 8.370187102470797669, -9.280950437305046208 ) ) ;
#22904=CARTESIAN_POINT ( 'NONE',  ( 5.520433897694421610, -0.01491416502703812180, 0.002108682515300225845 ) ) ;
#22905=CARTESIAN_POINT ( 'NONE',  ( 5.536195898058073439, -0.005656495196970933587, 0.006344799443923416181 ) ) ;
#22912=CARTESIAN_POINT ( 'NONE',  ( 2.288423627607478750, 3.963881558061958632, 6.543055113184225391 ) ) ;
#22916=CARTESIAN_POINT ( 'NONE',  ( 2.251139882113697865, 5.003859976902833573, -5.770207524086111484 ) ) ;
#22919=CARTESIAN_POINT ( 'NONE',  ( 0.2911222467163572247, 8.040284153519499100, -9.248441845564602914 ) ) ;
#22921=CARTESIAN_POINT ( 'NONE',  ( 0.3057689695767461524, 11.59726335252433316, 3.975296631252007717 ) ) ;
#22927=CARTESIAN_POINT ( 'NONE',  ( 2.305787727787084407, 3.682701754025606178, -6.711944854845784292 ) ) ;
#22930=CARTESIAN_POINT ( 'NONE',  ( 0.3675815128205894289, -8.093875121226016489, -9.235491948680088825 ) ) ;
#22931=CARTESIAN_POINT ( 'NONE',  ( 1.719304012341273724, 0.7661785589598685275, -12.70777170743938456 ) ) ;
#22934=CARTESIAN_POINT ( 'NONE',  ( 0.2648978790185584908, 7.972372351883154629, -9.295532325666371776 ) ) ;
#22941=ORIENTED_EDGE ( 'NONE', *, *, #36143, .F. ) ;
#22946=DIRECTION ( 'NONE',  ( -1.000000000000000000, -0.000000000000000000, -0.000000000000000000 ) ) ;
#22947=CARTESIAN_POINT ( 'NONE',  ( 2.241352910868908310, 2.689314586382351546, 7.145045428366586293 ) ) ;
#22951=CARTESIAN_POINT ( 'NONE',  ( 2.080613030138687147, 9.283828902438220978E-16, 7.580821595991582562 ) ) ;
#22958=CARTESIAN_POINT ( 'NONE',  ( 2.257661810676420799, -3.936095962955250993, -6.547845034191129621 ) ) ;
#22962=VERTEX_POINT ( 'NONE', #14368 ) ;
#22964=DIRECTION ( 'NONE',  ( 0.3865475372811021382, 0.1410344188397341658, 0.9114221272958283881 ) ) ;
#22970=ORIENTED_EDGE ( 'NONE', *, *, #16779, .F. ) ;
#22972=CARTESIAN_POINT ( 'NONE',  ( 2.241311220309555097, 7.205198716057821251, -2.523702734785272739 ) ) ;
#22988=CARTESIAN_POINT ( 'NONE',  ( 5.516018279890452902, 0.005752102158674347356, 0.003580555109620895717 ) ) ;
#22997=CARTESIAN_POINT ( 'NONE',  ( 0.6473888112830233910, 10.87693551365371292, 5.898884566269048335 ) ) ;
#22998=EDGE_LOOP ( 'NONE', ( #20275, #6455, #59146, #15241 ) ) ;
#22999=CARTESIAN_POINT ( 'NONE',  ( 2.251139882113958990, -2.728563091335203250, 7.133642337268851108 ) ) ;
#23000=CARTESIAN_POINT ( 'NONE',  ( 2.242418902651535095, 6.661183998166030129, 3.730710532465902229 ) ) ;
#23003=CARTESIAN_POINT ( 'NONE',  ( 0.2958664285830381879, 6.318165763623623477, 10.50235171906342657 ) ) ;
#23010=B_SPLINE_CURVE_WITH_KNOTS ( 'NONE', 3,
 ( #61155, #50211, #35548, #30552, #14916, #54548, #40534, #8978, #59856, #9282, #55177, #49873, #50539, #4322, #24594, #20253 ),
 .UNSPECIFIED., .F., .F.,
 ( 4, 3, 3, 3, 3, 4 ),
 ( 1.084202172485504434E-19, 0.0003017745587525236749, 0.0006035491769808723310, 0.0009053241094668153808, 0.001207275924540830887, 0.001510325902534668824 ),
 .UNSPECIFIED. ) ;
#23016=CARTESIAN_POINT ( 'NONE',  ( 0.3002738374340848670, -9.243462099800773046, -8.050654058169964600 ) ) ;
#23018=ORIENTED_EDGE ( 'NONE', *, *, #52910, .F. ) ;
#23020=CARTESIAN_POINT ( 'NONE',  ( 0.2657645697724709266, -12.03308811492267161, -2.275433120353216321 ) ) ;
#23021=B_SPLINE_CURVE_WITH_KNOTS ( 'NONE', 3,
 ( #21057, #5475, #25741, #41338, #486, #20751, #61302 ),
 .UNSPECIFIED., .F., .F.,
 ( 4, 3, 4 ),
 ( 3.553148716079863012E-15, 0.002398160485434544433, 0.005002426799380215588 ),
 .UNSPECIFIED. ) ;
#23023=CARTESIAN_POINT ( 'NONE',  ( 2.305787727787084851, -7.508843116234144688, -1.493241775258500770 ) ) ;
#23025=CARTESIAN_POINT ( 'NONE',  ( 5.514970785353741078, 0.003262412238248228995, -0.003415090918276198536 ) ) ;
#23029=B_SPLINE_CURVE_WITH_KNOTS ( 'NONE', 3,
 ( #17629, #7983, #48233, #22611, #52862, #47240, #33231, #17291, #1995, #47876, #53541, #28249, #42876, #6987, #63164, #2682 ),
 .UNSPECIFIED., .F., .F.,
 ( 4, 3, 3, 3, 3, 4 ),
 ( 8.673617379884035472E-19, 0.0002176109881720253794, 0.0004352086762394625640, 0.0006528017811446917363, 0.0007615147961451743368, 0.0009453342004947433517 ),
 .UNSPECIFIED. ) ;
#23035=CARTESIAN_POINT ( 'NONE',  ( 0.2717059086739036511, 1.953280559502855951, -12.09156413799788155 ) ) ;
#23038=VERTEX_POINT ( 'NONE', #29991 ) ;
#23048=CARTESIAN_POINT ( 'NONE',  ( 2.305787727787085295, 5.756228004061457959, 5.047606869483074910 ) ) ;
#23049=CARTESIAN_POINT ( 'NONE',  ( 2.639814597422737386, -2.896050884406582426, 7.207158938903940992 ) ) ;
#23053=CARTESIAN_POINT ( 'NONE',  ( 0.3006302518452007022, -7.704827863860860049, 9.533790235540713809 ) ) ;
#23056=CARTESIAN_POINT ( 'NONE',  ( 0.2648978790185619880, -12.08224454301447182, -1.996248716311752824 ) ) ;
#23058=CARTESIAN_POINT ( 'NONE',  ( 5.515539859299206427, 0.002856745161749541222, -0.005336559634876951626 ) ) ;
#23065=CARTESIAN_POINT ( 'NONE',  ( 2.241352910868908310, 6.652881166698511706, 3.744764251557016532 ) ) ;
#23070=CARTESIAN_POINT ( 'NONE',  ( 0.3109076770649057964, 9.542672295796823079, 7.699281309344357282 ) ) ;
#23071=LINE ( 'NONE', #57014, #29296 ) ;
#23072=CARTESIAN_POINT ( 'NONE',  ( 2.241352910868908310, -5.901537464758487062, 4.843133558968109043 ) ) ;
#23076=ORIENTED_EDGE ( 'NONE', *, *, #61195, .T. ) ;
#23082=ADVANCED_FACE ( 'NONE', ( #60577 ), #65037, .F. ) ;
#23088=EDGE_CURVE ( 'NONE', #63048, #22962, #6914, .T. ) ;
#23089=CARTESIAN_POINT ( 'NONE',  ( 2.260457164927193396, -4.804526096743045649, 5.941202713844093708 ) ) ;
#23104=CARTESIAN_POINT ( 'NONE',  ( 1.937114397841932290, -1.334979369128338922, -12.76557247858999844 ) ) ;
#23108=CARTESIAN_POINT ( 'NONE',  ( 0.2958664285830421292, 2.345117904768619699, 12.02992237133198472 ) ) ;
#23112=CARTESIAN_POINT ( 'NONE',  ( 2.889800649504073782, 3.002151847318991429, -5.334644486274164876 ) ) ;
#23116=CARTESIAN_POINT ( 'NONE',  ( 0.2650492594609225039, 6.218173512054911534, -10.54996119777439034 ) ) ;
#23120=CARTESIAN_POINT ( 'NONE',  ( 1.452237505248552996, -7.672309600508628868, -10.06489946308209760 ) ) ;
#23148=CARTESIAN_POINT ( 'NONE',  ( 0.2833330754217426306, 0.2021515668287386658, -12.25052326018166227 ) ) ;
#23163=CARTESIAN_POINT ( 'NONE',  ( 2.665405856346782620, -1.089747929268628068, -9.505137710817304963 ) ) ;
#23167=CARTESIAN_POINT ( 'NONE',  ( 0.2638984909335716500, 11.57533005135184645, -4.001111175853627522 ) ) ;
#23168=CARTESIAN_POINT ( 'NONE',  ( 2.259025283528085737, 1.461109758650560142, 7.499281868334248813 ) ) ;
#23171=CARTESIAN_POINT ( 'NONE',  ( 0.2767916011545390464, 12.09541651105896598, 1.940025653808885364 ) ) ;
#23178=CARTESIAN_POINT ( 'NONE',  ( 2.269879328256734219, -0.1483462450596719218, -7.642470739868882035 ) ) ;
#23184=CARTESIAN_POINT ( 'NONE',  ( 5.514970785353741078, -0.003262412238248734667, -0.003415090918276127846 ) ) ;
#23194=CARTESIAN_POINT ( 'NONE',  ( 0.2911222467163567251, -11.58731125337563128, 3.989243506922300231 ) ) ;
#23200=CARTESIAN_POINT ( 'NONE',  ( 2.963017218115626239, 7.522800244854608742, -2.328652339224271728 ) ) ;
#23201=DIRECTION ( 'NONE',  ( 0.000000000000000000, 0.000000000000000000, 1.000000000000000000 ) ) ;
#23202=CARTESIAN_POINT ( 'NONE',  ( 0.5547464869798263143, 3.933612953276393931, -11.69908463509552199 ) ) ;
#23203=DIRECTION ( 'NONE',  ( -0.3865475372811021937, 0.3335716741247191641, 0.8598319252293130655 ) ) ;
#23206=CARTESIAN_POINT ( 'NONE',  ( 2.276905613633648073, -1.175741125184132319, 7.555317002492079936 ) ) ;
#23217=CARTESIAN_POINT ( 'NONE',  ( 0.3109076770649042976, 5.925244271826596076, -10.73466383006815406 ) ) ;
#23218=CARTESIAN_POINT ( 'NONE',  ( 1.719304012340549859, -10.62216384465898500, -7.017415949616274240 ) ) ;
#23223=DIRECTION ( 'NONE',  ( -1.000000000000000000, -0.000000000000000000, -0.000000000000000000 ) ) ;
#23228=CARTESIAN_POINT ( 'NONE',  ( 0.2655924914740778742, -6.161287456391609574, -10.58356227062115806 ) ) ;
#23231=CARTESIAN_POINT ( 'NONE',  ( 0.2801149460245135336, 10.51028947658253010, -6.294737133725693212 ) ) ;
#23232=CARTESIAN_POINT ( 'NONE',  ( 0.2833330754217422420, 8.029341648258490949, -9.254504746325713072 ) ) ;
#23237=CARTESIAN_POINT ( 'NONE',  ( 2.245754705088395031, -1.435454129948258606, 7.499730934370272273 ) ) ;
#23239=CARTESIAN_POINT ( 'NONE',  ( 2.256373768223936871, 3.703993494727017666, -6.681391662622068850 ) ) ;
#23242=CARTESIAN_POINT ( 'NONE',  ( 1.462291587751302524, 0.6330131614661951289, -12.62932306616629141 ) ) ;
#23243=CARTESIAN_POINT ( 'NONE',  ( 2.969415267404644343, -4.269695207293366046, -6.619534278261627769 ) ) ;
#23244=CARTESIAN_POINT ( 'NONE',  ( 0.2915757698887299632, -11.58754481235184386, -3.989025639548751112 ) ) ;
#23246=EDGE_CURVE ( 'NONE', #13659, #32821, #43562, .T. ) ;
#23251=CARTESIAN_POINT ( 'NONE',  ( 0.3278977287071231372, -0.2481246099268901439, 12.26453627383315670 ) ) ;
#23254=CARTESIAN_POINT ( 'NONE',  ( 2.844750968615155085, 7.767336242080566500, 1.031816958530825001 ) ) ;
#23256=CARTESIAN_POINT ( 'NONE',  ( 1.283627346226907218, 10.61381050043341112, -6.763590725840940010 ) ) ;
#23267=CARTESIAN_POINT ( 'NONE',  ( 2.430348790456971386, -0.1949172018038362320, -7.694949746373680455 ) ) ;
#23270=CARTESIAN_POINT ( 'NONE',  ( 2.256373768223415510, -3.934258165100021909, -6.548448293197169257 ) ) ;
#23277=CARTESIAN_POINT ( 'NONE',  ( 2.305787727787085295, 7.508843116234176662, -1.493241775258346227 ) ) ;
#23297=CARTESIAN_POINT ( 'NONE',  ( 2.705197763288547552, 7.218866228162286625, 2.925192046931933465 ) ) ;
#23306=ORIENTED_EDGE ( 'NONE', *, *, #42555, .F. ) ;
#23307=CARTESIAN_POINT ( 'NONE',  ( 2.034671305879536263, 9.380408876024983300, -6.953089744305774644 ) ) ;
#23312=CARTESIAN_POINT ( 'NONE',  ( 0.9232167919969107572, 11.56588005394304020, -4.649596781010288282 ) ) ;
#23316=VERTEX_POINT ( 'NONE', #3035 ) ;
#23322=CARTESIAN_POINT ( 'NONE',  ( 0.3654063281920707507, 12.04448018134539744, -2.391195511198528134 ) ) ;
#23323=CARTESIAN_POINT ( 'NONE',  ( 0.3057689695767561444, -2.355923806019124100, -12.03117299329037415 ) ) ;
#23339=CARTESIAN_POINT ( 'NONE',  ( 0.2676618633000474867, -12.03196378632209118, -2.284744117040205413 ) ) ;
#23341=CARTESIAN_POINT ( 'NONE',  ( 3.047904605210315587, -7.698174516567070746, -1.788881754552557046 ) ) ;
#23342=CARTESIAN_POINT ( 'NONE',  ( 0.9232058338315048962, 4.617996777200729319, -11.58467545991549130 ) ) ;
#23343=CARTESIAN_POINT ( 'NONE',  ( 5.515539859299206427, 0.005336559634876441617, -0.002856745161749584157 ) ) ;
#23349=VERTEX_POINT ( 'NONE', #14600 ) ;
#23350=CARTESIAN_POINT ( 'NONE',  ( 2.298277635560272536, -0.1650558796844638076, 7.651596582281741554 ) ) ;
#23351=ORIENTED_EDGE ( 'NONE', *, *, #41718, .F. ) ;
#23367=EDGE_CURVE ( 'NONE', #25087, #15837, #26685, .T. ) ;
#23378=VERTEX_POINT ( 'NONE', #65477 ) ;
#23380=CARTESIAN_POINT ( 'NONE',  ( 5.515188684475870851, 0.003154373509839861981, -0.004322737127823984143 ) ) ;
#23382=CARTESIAN_POINT ( 'NONE',  ( 0.2648978790185610999, 9.295532325666560070, -7.972372351882934360 ) ) ;
#23384=ORIENTED_EDGE ( 'NONE', *, *, #7908, .F. ) ;
#23389=B_SPLINE_CURVE_WITH_KNOTS ( 'NONE', 3,
 ( #51978, #40679, #51662, #15408, #26363, #55972, #10406, #25718, #46008, #466, #41004, #56292, #10739, #31028, #2770, #7379 ),
 .UNSPECIFIED., .F., .F.,
 ( 4, 3, 3, 3, 3, 4 ),
 ( 0.000000000000000000, 0.0002999043160757392380, 0.0005998071753051102163, 0.0008997092107374701732, 0.001204458948196132986, 0.001510329163477478658 ),
 .UNSPECIFIED. ) ;
#23398=CARTESIAN_POINT ( 'NONE',  ( 5.516018279890452902, -0.002527316374434348482, -0.006286471671801920590 ) ) ;
#23400=CARTESIAN_POINT ( 'NONE',  ( 0.3109076770649005228, -10.49874397806409831, 6.333869442011739181 ) ) ;
#23406=CIRCLE ( 'NONE', #49989, 6.000000000000000888 ) ;
#23407=CARTESIAN_POINT ( 'NONE',  ( 1.014383007554949145, -11.03701226956412107, -5.859361736620448013 ) ) ;
#23415=CARTESIAN_POINT ( 'NONE',  ( 1.719304012341629884, 8.755325027796281745, -9.242227816402079910 ) ) ;
#23421=CARTESIAN_POINT ( 'NONE',  ( 0.2648978790185602672, -11.55204314799261311, -4.063980959785162383 ) ) ;
#23431=CARTESIAN_POINT ( 'NONE',  ( 0.2956976708475470561, 9.245952174682551927, 8.045468685196958347 ) ) ;
#23436=CARTESIAN_POINT ( 'NONE',  ( 0.2648978790185593790, -4.312320170909161199, -11.46165506714232762 ) ) ;
#23448=CARTESIAN_POINT ( 'NONE',  ( 2.276905613633650738, -7.555317002492078160, -1.175741125184157410 ) ) ;
#23450=CARTESIAN_POINT ( 'NONE',  ( 1.459561108992493361, 12.08294179906902954, 3.725588117663684695 ) ) ;
#23464=ADVANCED_FACE ( 'NONE', ( #59701 ), #19633, .F. ) ;
#23471=DIRECTION ( 'NONE',  ( 0.000000000000000000, 0.000000000000000000, 1.000000000000000000 ) ) ;
#23478=CARTESIAN_POINT ( 'NONE',  ( 0.3002738374340842564, 0.2255758963753189406, -12.25576345519757027 ) ) ;
#23489=CARTESIAN_POINT ( 'NONE',  ( 2.305787727787084407, -7.508843116234166004, 1.493241775258399073 ) ) ;
#23498=( BOUNDED_SURFACE ( )  B_SPLINE_SURFACE ( 3, 1, ( 
 ( #61523, #57216 ),
 ( #22275, #25979 ),
 ( #46262, #61864 ),
 ( #37583, #51257 ) ),
 .UNSPECIFIED., .F., .F., .F. ) 
 B_SPLINE_SURFACE_WITH_KNOTS ( ( 4, 4 ),
 ( 2, 2 ),
 ( 0.000000000000000000, 1.000000000000000000 ),
 ( 0.000000000000000000, 1.000000000000000000 ),
 .UNSPECIFIED. ) 
 GEOMETRIC_REPRESENTATION_ITEM ( )  RATIONAL_B_SPLINE_SURFACE ( (
 ( 1.000000000000000000, 1.000000000000000000),
 ( 0.6933888150995267674, 0.9895912004443193632),
 ( 0.6933888150995267674, 0.9895912004443193632),
 ( 1.000000000000000000, 1.000000000000000000) ) ) 
 REPRESENTATION_ITEM ( '' )  SURFACE ( )  );
#23499=VERTEX_POINT ( 'NONE', #59367 ) ;
#23503=CARTESIAN_POINT ( 'NONE',  ( 2.430348790457581565, -5.095533593439965259, -5.769383131055120906 ) ) ;
#23514=CARTESIAN_POINT ( 'NONE',  ( 2.276905613633652958, -0.1540880535620453018, -7.644700064315453680 ) ) ;
#23517=CARTESIAN_POINT ( 'NONE',  ( 2.241526690369557429, 7.634439869182790162, -0.01730530154279370444 ) ) ;
#23518=CARTESIAN_POINT ( 'NONE',  ( 5.520433897694421610, -0.01491416502703864569, -0.002108682515300430542 ) ) ;
#23522=CARTESIAN_POINT ( 'NONE',  ( 5.514624014163232779, -0.004137701579365772077, 0.0001700579043839103323 ) ) ;
#23526=B_SPLINE_CURVE_WITH_KNOTS ( 'NONE', 3,
 ( #6806, #47041, #41706, #1499, #37033, #27715, #62621, #27077, #27387, #47371, #12097, #22074, #47682, #21777, #2128, #32376 ),
 .UNSPECIFIED., .F., .F.,
 ( 4, 3, 3, 3, 3, 4 ),
 ( 0.000000000000000000, 0.0002176109881720229670, 0.0004352086762394590945, 0.0006528017811446854479, 0.0007615147961451684822, 0.0009453342004947398822 ),
 .UNSPECIFIED. ) ;
#23528=CARTESIAN_POINT ( 'NONE',  ( 0.2706063244538047807, -11.56807224179756233, 4.023948952279222446 ) ) ;
#23534=CARTESIAN_POINT ( 'NONE',  ( 5.530133899448235191, -0.01589823604557753789, -0.001661287012794294493 ) ) ;
#23535=CARTESIAN_POINT ( 'NONE',  ( 0.2915757698887291860, -9.524403232224818439, -7.711631695122943775 ) ) ;
#23536=DIRECTION ( 'NONE',  ( -1.000000000000000000, -0.000000000000000000, -0.000000000000000000 ) ) ;
#23544=ORIENTED_EDGE ( 'NONE', *, *, #47699, .F. ) ;
#23551=VECTOR ( 'NONE', #39362, 1000.000000000000114 ) ;
#23555=CARTESIAN_POINT ( 'NONE',  ( 2.260457164927182738, 6.546788723198603499, -3.939659644572469865 ) ) ;
#23556=CARTESIAN_POINT ( 'NONE',  ( 2.305787727787084851, -1.493241775258474124, 7.508843116234150905 ) ) ;
#23558=ORIENTED_EDGE ( 'NONE', *, *, #26804, .T. ) ;
#23561=VERTEX_POINT ( 'NONE', #59061 ) ;
#23563=VECTOR ( 'NONE', #44202, 1000.000000000000114 ) ;
#23570=CARTESIAN_POINT ( 'NONE',  ( 1.719304012338199517, 0.000000000000000000, 0.000000000000000000 ) ) ;
#23577=CARTESIAN_POINT ( 'NONE',  ( 0.2651627923886310523, -0.08809136839524371598, 12.24583724871548540 ) ) ;
#23588=CARTESIAN_POINT ( 'NONE',  ( 0.3164563675027619039, 0.2404665832031381567, 12.26087493884171664 ) ) ;
#23589=VECTOR ( 'NONE', #3809, 1000.000000000000114 ) ;
#23599=CARTESIAN_POINT ( 'NONE',  ( 2.269879328256729334, -3.692763753156697248, 6.692746930935561167 ) ) ;
#23609=CARTESIAN_POINT ( 'NONE',  ( 0.5547464869798240938, -8.164898018378748290, -9.256151063740635010 ) ) ;
#23616=CARTESIAN_POINT ( 'NONE',  ( 2.269879328256532158, 5.026125315665035842, 5.759117113708084545 ) ) ;
#23617=CARTESIAN_POINT ( 'NONE',  ( 2.241526690369557429, -5.859443871527007630, -4.894066724724313033 ) ) ;
#23619=CARTESIAN_POINT ( 'NONE',  ( 5.530133899448235191, 0.004396748047611614973, -0.01536822665454942727 ) ) ;
#23620=AXIS2_PLACEMENT_3D ( 'NONE', #2300, #23223, #23894 ) ;
#23621=CARTESIAN_POINT ( 'NONE',  ( 0.3665391374699465965, -9.576575648338966573, -7.691255657244391308 ) ) ;
#23623=ORIENTED_EDGE ( 'NONE', *, *, #57949, .F. ) ;
#23645=CARTESIAN_POINT ( 'NONE',  ( 0.2648978790185602672, -4.063980959785125080, 11.55204314799262555 ) ) ;
#23646=CARTESIAN_POINT ( 'NONE',  ( 0.2651627923886321070, 11.47719387551886427, 4.271101819784393072 ) ) ;
#23652=CARTESIAN_POINT ( 'NONE',  ( 1.372161826077490154, 11.63973780005268388, -4.864129100817252471 ) ) ;
#23657=CARTESIAN_POINT ( 'NONE',  ( 2.305787727787083519, -2.774453000917197265, 7.135468203929974607 ) ) ;
#23658=EDGE_CURVE ( 'NONE', #11179, #13729, #18807, .T. ) ;
#23659=LINE ( 'NONE', #18685, #64873 ) ;
#23663=CARTESIAN_POINT ( 'NONE',  ( 0.2676618633000464320, 4.037335446657237092, 11.56235835488941355 ) ) ;
#23664=CARTESIAN_POINT ( 'NONE',  ( 0.3654063281920748585, -2.391195511198570323, -12.04448018134538678 ) ) ;
#23670=CARTESIAN_POINT ( 'NONE',  ( 2.781367136452675304, -6.916275212954791307, -3.637318098960500290 ) ) ;
#23673=B_SPLINE_CURVE_WITH_KNOTS ( 'NONE', 3,
 ( #47752, #36787, #47113, #1565, #21839, #42086, #7173 ),
 .UNSPECIFIED., .F., .F.,
 ( 4, 3, 4 ),
 ( 0.000000000000000000, 0.001700533616330558370, 0.005002426799373359094 ),
 .UNSPECIFIED. ) ;
#23674=ADVANCED_FACE ( 'NONE', ( #10785 ), #8082, .T. ) ;
#23686=CARTESIAN_POINT ( 'NONE',  ( 2.655192694323995628, -2.733486750964454703, 9.204230091442163086 ) ) ;
#23688=CARTESIAN_POINT ( 'NONE',  ( 0.3665391374699467075, 9.576575648339128222, -7.691255657244196797 ) ) ;
#23699=CARTESIAN_POINT ( 'NONE',  ( 0.2648978790185602672, 1.996248716311790128, -12.08224454301446826 ) ) ;
#23701=CARTESIAN_POINT ( 'NONE',  ( 0.2648978790185602672, 6.237101853238547378, 10.53870023327865901 ) ) ;
#23703=ORIENTED_EDGE ( 'NONE', *, *, #39331, .F. ) ;
#23716=CARTESIAN_POINT ( 'NONE',  ( 0.2869720083484361695, 10.50600528807146894, 6.306330337780551076 ) ) ;
#23720=( BOUNDED_SURFACE ( )  B_SPLINE_SURFACE ( 3, 1, ( 
 ( #47726, #42374 ),
 ( #22118, #52063 ),
 ( #57057, #6512 ),
 ( #41749, #11481 ) ),
 .UNSPECIFIED., .F., .F., .T. ) 
 B_SPLINE_SURFACE_WITH_KNOTS ( ( 4, 4 ),
 ( 2, 2 ),
 ( 0.000000000000000000, 1.000000000000000000 ),
 ( 0.000000000000000000, 1.000000000000000000 ),
 .UNSPECIFIED. ) 
 GEOMETRIC_REPRESENTATION_ITEM ( )  RATIONAL_B_SPLINE_SURFACE ( (
 ( 1.000000000000000000, 1.000000000000000000),
 ( 0.9856612449720755231, 0.9999558406602322425),
 ( 0.9856612449720755231, 0.9999558406602322425),
 ( 1.000000000000000000, 1.000000000000000000) ) ) 
 REPRESENTATION_ITEM ( '' )  SURFACE ( )  );
#23729=EDGE_CURVE ( 'NONE', #23832, #47920, #23071, .T. ) ;
#23732=CARTESIAN_POINT ( 'NONE',  ( 0.2648978790185584908, -4.312320170909314854, 11.46165506714226900 ) ) ;
#23736=EDGE_CURVE ( 'NONE', #47135, #58095, #42659, .T. ) ;
#23740=CARTESIAN_POINT ( 'NONE',  ( 5.520433897694421610, -0.0005131706886599361186, -0.01505375422439122687 ) ) ;
#23746=CARTESIAN_POINT ( 'NONE',  ( 0.2638984909335720941, 12.09426044257624078, 1.930290337334096717 ) ) ;
#23754=EDGE_CURVE ( 'NONE', #15421, #43985, #11255, .T. ) ;
#23757=CARTESIAN_POINT ( 'NONE',  ( 2.247206125382828823, -5.774712443419418584, -4.996658593545119764 ) ) ;
#23761=ADVANCED_FACE ( 'NONE', ( #31707 ), #53622, .F. ) ;
#23763=CARTESIAN_POINT ( 'NONE',  ( 2.305787727787084407, -1.164987321564783684, 7.566723232958066703 ) ) ;
#23771=DIRECTION ( 'NONE',  ( -0.3939253465568944290, 0.4679616473074844074, 0.7910971609033218277 ) ) ;
#23775=CARTESIAN_POINT ( 'NONE',  ( 2.990245332647875287, -0.5125330575220037321, 8.465748356453847379 ) ) ;
#23790=CARTESIAN_POINT ( 'NONE',  ( 0.3675815128205912052, -12.04510820461657516, -2.391755495700727874 ) ) ;
#23793=CARTESIAN_POINT ( 'NONE',  ( 0.3537226245948340009, -6.362463382302340875, 10.49813096858607686 ) ) ;
#23821=EDGE_CURVE ( 'NONE', #37036, #35685, #25115, .T. ) ;
#23822=VERTEX_POINT ( 'NONE', #27382 ) ;
#23823=CARTESIAN_POINT ( 'NONE',  ( 2.269879328256732443, -7.500604381673471543, 1.473193649116112391 ) ) ;
#23832=VERTEX_POINT ( 'NONE', #29664 ) ;
#23835=CARTESIAN_POINT ( 'NONE',  ( 2.491965175174512659, 4.796682362486732742, -6.046355957631024403 ) ) ;
#23844=CARTESIAN_POINT ( 'NONE',  ( 2.241526690369557873, 5.837196604699912861, -4.920579984890902203 ) ) ;
#23852=CARTESIAN_POINT ( 'NONE',  ( 3.152665057734128862, 5.761241965769081652, 5.461013642405580626 ) ) ;
#23855=CARTESIAN_POINT ( 'NONE',  ( 1.633930747253003135, -5.012862767614699067, -11.67150509329692376 ) ) ;
#23857=CARTESIAN_POINT ( 'NONE',  ( 0.2646305136544072623, -7.972778379581612285, 9.296005949277201807 ) ) ;
#23859=AXIS2_PLACEMENT_3D ( 'NONE', #40721, #55357, #50709 ) ;
#23865=B_SPLINE_CURVE_WITH_KNOTS ( 'NONE', 3,
 ( #42784, #37141, #37479, #33141, #53448, #6585, #48136, #17541, #43111, #1269, #42439, #36826, #7893, #26851, #57123, #58431, #21547, #16558, #47791 ),
 .UNSPECIFIED., .F., .F.,
 ( 4, 3, 3, 3, 3, 3, 4 ),
 ( 0.000000000000000000, 2.831840207499449323E-05, 4.217266859840357231E-05, 5.602024318395839903E-05, 6.290810167969001913E-05, 9.120440630944526609E-05, 0.0001153103026479762659 ),
 .UNSPECIFIED. ) ;
#23866=CARTESIAN_POINT ( 'NONE',  ( 0.3537226245948352776, -8.088784578751358367, 9.233810598191753982 ) ) ;
#23867=CARTESIAN_POINT ( 'NONE',  ( 0.3654063281920737483, -11.44627072062582052, 4.446369912832466298 ) ) ;
#23874=CARTESIAN_POINT ( 'NONE',  ( 2.373367633546872302, 7.275198254387443164, -2.455525055524816480 ) ) ;
#23875=CARTESIAN_POINT ( 'NONE',  ( 2.907497136251146141, -4.769582063554104856, 6.243048412629086386 ) ) ;
#23888=CARTESIAN_POINT ( 'NONE',  ( 0.2648978790185619880, 6.008231198269132989, -10.67083876753485328 ) ) ;
#23890=CARTESIAN_POINT ( 'NONE',  ( 2.251152103363642354, 6.550893877460208792, -3.926807817126119371 ) ) ;
#23893=ORIENTED_EDGE ( 'NONE', *, *, #22107, .T. ) ;
#23894=DIRECTION ( 'NONE',  ( 0.000000000000000000, 0.000000000000000000, 1.000000000000000000 ) ) ;
#23900=B_SPLINE_CURVE_WITH_KNOTS ( 'NONE', 3,
 ( #63107, #23874, #12889, #2275, #2624, #18570, #17568, #13225, #48485, #2934, #58807, #23200, #27865, #42817, #64399, #22555 ),
 .UNSPECIFIED., .F., .F.,
 ( 4, 3, 3, 3, 3, 4 ),
 ( 4.336808689942017255E-19, 0.0002176109881720234007, 0.0004352086762394597992, 0.0006528017811446890258, 0.0007615147961451721684, 0.0009453342004947402075 ),
 .UNSPECIFIED. ) ;
#23905=CARTESIAN_POINT ( 'NONE',  ( 0.2647959493198558389, 10.53111783886899744, -6.249846955854157393 ) ) ;
#23906=CARTESIAN_POINT ( 'NONE',  ( 0.3160775863651102413, 8.065044686487434333, -9.237902461149165134 ) ) ;
#23909=EDGE_LOOP ( 'NONE', ( #56380, #29280, #46861, #14455 ) ) ;
#23910=( BOUNDED_SURFACE ( )  B_SPLINE_SURFACE ( 3, 1, ( 
 ( #30712, #5482 ),
 ( #6132, #26393 ),
 ( #51021, #36023 ),
 ( #36374, #25410 ) ),
 .UNSPECIFIED., .F., .F., .F. ) 
 B_SPLINE_SURFACE_WITH_KNOTS ( ( 4, 4 ),
 ( 2, 2 ),
 ( 0.000000000000000000, 1.000000000000000000 ),
 ( 0.000000000000000000, 1.000000000000000000 ),
 .UNSPECIFIED. ) 
 GEOMETRIC_REPRESENTATION_ITEM ( )  RATIONAL_B_SPLINE_SURFACE ( (
 ( 1.000000000000000000, 1.000000000000000000),
 ( 0.9942764183789327692, 0.8450855930916585379),
 ( 0.9942764183789327692, 0.8450855930916585379),
 ( 1.000000000000000000, 1.000000000000000000) ) ) 
 REPRESENTATION_ITEM ( '' )  SURFACE ( )  );
#23913=CARTESIAN_POINT ( 'NONE',  ( 0.2648978790185619880, -9.295532325666501450, 7.972372351882998309 ) ) ;
#23917=CARTESIAN_POINT ( 'NONE',  ( 3.092491956585653679, -4.340140213817308634, -6.622742949902657550 ) ) ;
#23919=CARTESIAN_POINT ( 'NONE',  ( 1.109979610369147274, 5.843815872356888264, 11.08130463534426902 ) ) ;
#23920=EDGE_CURVE ( 'NONE', #52172, #55547, #24052, .T. ) ;
#23921=ORIENTED_EDGE ( 'NONE', *, *, #55545, .T. ) ;
#23926=CARTESIAN_POINT ( 'NONE',  ( 2.305787727787084407, 6.711944854845823372, 3.682701754025536012 ) ) ;
#23928=CARTESIAN_POINT ( 'NONE',  ( 0.2638984909335720941, -4.375449752477059029, -11.43908195192333821 ) ) ;
#23929=ORIENTED_EDGE ( 'NONE', *, *, #18318, .F. ) ;
#23935=CARTESIAN_POINT ( 'NONE',  ( 2.080613030138687591, 5.400000000000000355, 0.000000000000000000 ) ) ;
#23940=CARTESIAN_POINT ( 'NONE',  ( 3.152665057736253829, 5.761241965767907480, -5.461013642407265500 ) ) ;
#23952=CARTESIAN_POINT ( 'NONE',  ( 3.092491956585968982, 6.622742949902548304, -4.340140213817556436 ) ) ;
#23956=ORIENTED_EDGE ( 'NONE', *, *, #35626, .T. ) ;
#23958=CARTESIAN_POINT ( 'NONE',  ( 2.245754705088395031, 7.212684575686813204, -2.506725724682591583 ) ) ;
#23965=CARTESIAN_POINT ( 'NONE',  ( 2.889800649504073782, -3.002151847318879518, -5.334644486274226161 ) ) ;
#23970=CARTESIAN_POINT ( 'NONE',  ( 2.255723233588950993, 2.488140745365865047, 7.222632368701277450 ) ) ;
#23977=ORIENTED_EDGE ( 'NONE', *, *, #24878, .T. ) ;
#23981=CARTESIAN_POINT ( 'NONE',  ( 0.3675815128205912052, 11.44679196252415210, -4.447030445008065769 ) ) ;
#23982=CARTESIAN_POINT ( 'NONE',  ( 0.8375941296801872049, -0.3844307390187073903, 12.43103843094035454 ) ) ;
#23985=VERTEX_POINT ( 'NONE', #50318 ) ;
#23995=CARTESIAN_POINT ( 'NONE',  ( 2.269879328256732887, -7.642470739868881147, 0.1483462450596979287 ) ) ;
#24000=CARTESIAN_POINT ( 'NONE',  ( 3.031336079629076696, 4.304138522350157814, 6.621879275826709765 ) ) ;
#24003=CARTESIAN_POINT ( 'NONE',  ( 0.6511581176960867801, 1.822219471614292763, 12.23990098761610490 ) ) ;
#24005=B_SPLINE_CURVE_WITH_KNOTS ( 'NONE', 3,
 ( #44607, #53, #15008, #55605, #60915, #15354, #6055 ),
 .UNSPECIFIED., .F., .F.,
 ( 4, 3, 4 ),
 ( 0.000000000000000000, 0.001700533616330540372, 0.005002426799371281763 ),
 .UNSPECIFIED. ) ;
#24006=CARTESIAN_POINT ( 'NONE',  ( 0.2834382757448029588, -12.09963924911733457, -1.927645269571007125 ) ) ;
#24010=CARTESIAN_POINT ( 'NONE',  ( 0.2648978790185602672, 7.972372351883029395, 9.295532325666474804 ) ) ;
#24023=CARTESIAN_POINT ( 'NONE',  ( 2.440552418640497212, -7.301551120181781762, 2.447453236303800406 ) ) ;
#24029=CARTESIAN_POINT ( 'NONE',  ( 0.3160775863651094642, -7.697077652699381822, -9.546663463486119383 ) ) ;
#24034=CARTESIAN_POINT ( 'NONE',  ( 0.3610902822527213840, -9.234828023175149170, 8.091349661862597742 ) ) ;
#24040=CARTESIAN_POINT ( 'NONE',  ( 2.247112776671470247, -1.440655381229420939, -7.499199956302001091 ) ) ;
#24047=CARTESIAN_POINT ( 'NONE',  ( 2.990245332647881060, 2.413832934171125100, 8.130497889782944299 ) ) ;
#24049=CARTESIAN_POINT ( 'NONE',  ( 3.152665057735509979, 7.102135024646700323, 3.546019893115181620 ) ) ;
#24050=CARTESIAN_POINT ( 'NONE',  ( 0.2717059086739018192, -4.023283916512504277, 11.56868249951480365 ) ) ;
#24052=LINE ( 'NONE', #39322, #47391 ) ;
#24060=ORIENTED_EDGE ( 'NONE', *, *, #34870, .F. ) ;
#24065=CARTESIAN_POINT ( 'NONE',  ( 0.2676618633000462100, 10.68562420805850621, -5.983781707237496583 ) ) ;
#24074=EDGE_CURVE ( 'NONE', #46959, #5369, #52080, .T. ) ;
#24079=CARTESIAN_POINT ( 'NONE',  ( 1.452237505248552996, -3.767214359061047180, -12.08199618361516592 ) ) ;
#24087=ADVANCED_FACE ( 'NONE', ( #62230 ), #28163, .F. ) ;
#24088=CARTESIAN_POINT ( 'NONE',  ( 2.280717697723837922, 0.1564731737570113912, 7.645922213779906329 ) ) ;
#24090=CARTESIAN_POINT ( 'NONE',  ( 3.152665057734040488, 0.000000000000000000, 0.000000000000000000 ) ) ;
#24091=ORIENTED_EDGE ( 'NONE', *, *, #65095, .T. ) ;
#24093=CARTESIAN_POINT ( 'NONE',  ( 2.241528039335009215, 6.603755931420482561, 3.830846649711536323 ) ) ;
#24095=ORIENTED_EDGE ( 'NONE', *, *, #58730, .T. ) ;
#24102=CARTESIAN_POINT ( 'NONE',  ( 5.515539859299206427, -0.0001942659352250951453, -0.006049968793488818240 ) ) ;
#24103=CARTESIAN_POINT ( 'NONE',  ( 0.2706063244538029489, -6.275112929891680125, 10.51833723927420472 ) ) ;
#24104=CARTESIAN_POINT ( 'NONE',  ( 2.241352910868909643, -7.532448145350499225, -1.243507963608171174 ) ) ;
#24106=CARTESIAN_POINT ( 'NONE',  ( 1.283627346226324351, 12.00363697230078408, 3.783098238613546993 ) ) ;
#24109=CARTESIAN_POINT ( 'NONE',  ( 0.3665391374699464300, 9.237363111276767569, 8.095513416941260587 ) ) ;
#24128=B_SPLINE_CURVE_WITH_KNOTS ( 'NONE', 3,
 ( #64940, #56278, #35666, #25056, #65587, #29687, #30029, #45327, #49671, #103, #9402, #4115, #61274 ),
 .UNSPECIFIED., .F., .F.,
 ( 4, 3, 3, 3, 4 ),
 ( 3.127317220692750759E-18, 6.607593386745476828E-05, 0.0001321518677373526235, 0.0001982171734706228384, 0.0002642860854759475787 ),
 .UNSPECIFIED. ) ;
#24129=ORIENTED_EDGE ( 'NONE', *, *, #40467, .F. ) ;
#24136=EDGE_LOOP ( 'NONE', ( #2337, #1711, #22050, #59136 ) ) ;
#24148=CARTESIAN_POINT ( 'NONE',  ( 5.536195898058073439, -0.004468797463753836595, 0.007230647766619077016 ) ) ;
#24153=ADVANCED_FACE ( 'NONE', ( #27981 ), #18594, .T. ) ;
#24157=CARTESIAN_POINT ( 'NONE',  ( 2.241352910868908310, -2.532612177304491397, 7.202080440908734005 ) ) ;
#24160=ORIENTED_EDGE ( 'NONE', *, *, #10804, .T. ) ;
#24161=CARTESIAN_POINT ( 'NONE',  ( 1.719304012338836563, -7.017415949612288095, 10.62216384465580710 ) ) ;
#24165=CARTESIAN_POINT ( 'NONE',  ( 0.2706063244538020052, -8.006269958070651782, 9.268878137104373138 ) ) ;
#24168=CARTESIAN_POINT ( 'NONE',  ( 0.7400311444011700157, 12.14938086789865856, -2.502569705372845288 ) ) ;
#24188=EDGE_CURVE ( 'NONE', #11102, #49132, #25951, .T. ) ;
#24195=VERTEX_POINT ( 'NONE', #3383 ) ;
#24201=ORIENTED_EDGE ( 'NONE', *, *, #29794, .F. ) ;
#24205=CARTESIAN_POINT ( 'NONE',  ( 5.530133899448235191, 0.01324661008606530140, 0.008946569461392205394 ) ) ;
#24206=B_SPLINE_CURVE_WITH_KNOTS ( 'NONE', 3,
 ( #26738, #62958, #42015, #47672, #57009, #51699, #27069, #12087, #57992, #36383 ),
 .UNSPECIFIED., .F., .F.,
 ( 4, 3, 3, 4 ),
 ( 2.453269466693398698E-18, 6.607638129004608145E-05, 9.911389841680660494E-05, 0.0001667630577588617149 ),
 .UNSPECIFIED. ) ;
#24207=CARTESIAN_POINT ( 'NONE',  ( 1.719304012338199517, 0.000000000000000000, 0.000000000000000000 ) ) ;
#24211=CARTESIAN_POINT ( 'NONE',  ( 0.2652384770603652409, -0.06606665821606472200, 12.24598129987882444 ) ) ;
#24212=CARTESIAN_POINT ( 'NONE',  ( 2.305787727787084407, 7.654065630109506913, -0.1666591538752953128 ) ) ;
#24216=CARTESIAN_POINT ( 'NONE',  ( 1.719304012341202004, 11.67935079956989775, -5.066286238790292273 ) ) ;
#24219=EDGE_CURVE ( 'NONE', #54308, #34453, #32361, .T. ) ;
#24221=CARTESIAN_POINT ( 'NONE',  ( 0.2767916011545367705, 0.1897947303542835418, 12.24854187541375161 ) ) ;
#24224=CARTESIAN_POINT ( 'NONE',  ( 2.350038591458163406, 8.861946706685587927, 5.855794476068265197 ) ) ;
#24225=CARTESIAN_POINT ( 'NONE',  ( 2.253265082352432724, -7.498995607278126307, -1.452519439326532824 ) ) ;
#24226=CARTESIAN_POINT ( 'NONE',  ( 2.241451721903216399, -4.953785420083449687, 5.809054012306841486 ) ) ;
#24229=ORIENTED_EDGE ( 'NONE', *, *, #4406, .F. ) ;
#24235=LINE ( 'NONE', #23935, #46741 ) ;
#24237=CARTESIAN_POINT ( 'NONE',  ( 5.514970785353741078, -0.0003039746380528621597, -0.004713149585127533910 ) ) ;
#24238=B_SPLINE_CURVE_WITH_KNOTS ( 'NONE', 3,
 ( #18862, #8881, #29173, #14497, #9853, #18564, #64711 ),
 .UNSPECIFIED., .F., .F.,
 ( 4, 3, 4 ),
 ( 3.571408088770477977E-15, 0.002398160485435184546, 0.005002426799386577687 ),
 .UNSPECIFIED. ) ;
#24244=CARTESIAN_POINT ( 'NONE',  ( 2.665405856346788838, 6.580881457836806447, -6.944580094494265943 ) ) ;
#24246=PLANE ( 'NONE',  #54319 ) ;
#24252=CARTESIAN_POINT ( 'NONE',  ( 0.2706063244538038925, 12.24670371972918481, 0.1752385892652434385 ) ) ;
#24253=CARTESIAN_POINT ( 'NONE',  ( 0.9232058338315048962, -11.58467545991550907, -4.617996777200689351 ) ) ;
#24255=CARTESIAN_POINT ( 'NONE',  ( 2.241352910868909643, -7.503490710578223144, -1.407733736974942973 ) ) ;
#24256=ORIENTED_EDGE ( 'NONE', *, *, #40771, .T. ) ;
#24260=EDGE_CURVE ( 'NONE', #37036, #44332, #22849, .T. ) ;
#24270=CARTESIAN_POINT ( 'NONE',  ( 2.507146904658097419, 7.180414359940957780, 2.843654641958914375 ) ) ;
#24271=( BOUNDED_SURFACE ( )  B_SPLINE_SURFACE ( 3, 1, ( 
 ( #22244, #17270 ),
 ( #24205, #33847 ),
 ( #38180, #18604 ),
 ( #49505, #44471 ) ),
 .UNSPECIFIED., .F., .F., .F. ) 
 B_SPLINE_SURFACE_WITH_KNOTS ( ( 4, 4 ),
 ( 2, 2 ),
 ( 0.000000000000000000, 1.000000000000000000 ),
 ( 0.000000000000000000, 1.000000000000000000 ),
 .UNSPECIFIED. ) 
 GEOMETRIC_REPRESENTATION_ITEM ( )  RATIONAL_B_SPLINE_SURFACE ( (
 ( 1.000000000000000000, 1.000000000000000000),
 ( 0.6933888150995267674, 0.9895912004443193632),
 ( 0.6933888150995267674, 0.9895912004443193632),
 ( 1.000000000000000000, 1.000000000000000000) ) ) 
 REPRESENTATION_ITEM ( '' )  SURFACE ( )  );
#24274=ORIENTED_EDGE ( 'NONE', *, *, #14469, .F. ) ;
#24277=CARTESIAN_POINT ( 'NONE',  ( 2.242819959140646802, 2.514828506625070403, 7.208832857235885072 ) ) ;
#24278=ORIENTED_EDGE ( 'NONE', *, *, #3945, .F. ) ;
#24280=VERTEX_POINT ( 'NONE', #61491 ) ;
#24294=ORIENTED_EDGE ( 'NONE', *, *, #58173, .T. ) ;
#24296=CARTESIAN_POINT ( 'NONE',  ( 3.152665057734086229, 4.725420687650732532, 6.378477742800449768 ) ) ;
#24306=CARTESIAN_POINT ( 'NONE',  ( 3.100650473569754872, 7.074394303868267286, -3.562766772868470877 ) ) ;
#24309=ORIENTED_EDGE ( 'NONE', *, *, #16259, .F. ) ;
#24315=CARTESIAN_POINT ( 'NONE',  ( 0.2648978790185619880, -12.08224454301447182, -1.996248716311752824 ) ) ;
#24316=CARTESIAN_POINT ( 'NONE',  ( 2.770579946183330922, -5.249166435139399844, 5.784075095088772045 ) ) ;
#24326=CARTESIAN_POINT ( 'NONE',  ( 0.3109076770649007448, 1.896437056876628446, -12.11383728282218897 ) ) ;
#24329=CARTESIAN_POINT ( 'NONE',  ( 2.245754705088790271, -1.216173395687026426, -7.538396044170202259 ) ) ;
#24338=CARTESIAN_POINT ( 'NONE',  ( 2.835339799623976198, 5.783398714696559750, 5.281994181469010563 ) ) ;
#24340=CARTESIAN_POINT ( 'NONE',  ( 0.3053067050349165812, 10.49978800868460915, 6.328522421120307939 ) ) ;
#24349=CARTESIAN_POINT ( 'NONE',  ( 3.152665057734040488, 0.000000000000000000, 0.000000000000000000 ) ) ;
#24351=CARTESIAN_POINT ( 'NONE',  ( 0.3610902822527257694, -6.364812822043094620, -10.49957835860569766 ) ) ;
#24357=CARTESIAN_POINT ( 'NONE',  ( 0.5547464869798260922, -6.433541106625019879, -10.53334899235177247 ) ) ;
#24359=CARTESIAN_POINT ( 'NONE',  ( 0.2671309869109471657, 9.484919892054820778, 7.747281147400578938 ) ) ;
#24361=CARTESIAN_POINT ( 'NONE',  ( 3.152665057733834431, -3.161213418913157991, 7.281573230474281289 ) ) ;
#24363=ORIENTED_EDGE ( 'NONE', *, *, #52989, .T. ) ;
#24369=CARTESIAN_POINT ( 'NONE',  ( 0.2646305136544072623, 6.237419468587225069, -10.53923716745240391 ) ) ;
#24371=AXIS2_PLACEMENT_3D ( 'NONE', #25925, #51206, #10950 ) ;
#24392=CARTESIAN_POINT ( 'NONE',  ( 2.305787727787084407, 3.682701754025606178, -6.711944854845784292 ) ) ;
#24403=CARTESIAN_POINT ( 'NONE',  ( 0.3675815128205894289, -12.13672785388551389, 1.872154644482044938 ) ) ;
#24412=CARTESIAN_POINT ( 'NONE',  ( 0.3675815128205894289, 5.910255304480596550, -10.76447900494934196 ) ) ;
#24420=CARTESIAN_POINT ( 'NONE',  ( 2.241509619876137283, -7.634391113243452764, -0.03828218718778049479 ) ) ;
#24424=CARTESIAN_POINT ( 'NONE',  ( 2.305787727787084407, -5.756228004061490822, 5.047606869483037606 ) ) ;
#24426=ORIENTED_EDGE ( 'NONE', *, *, #15449, .F. ) ;
#24429=DIRECTION ( 'NONE',  ( 0.000000000000000000, 0.000000000000000000, 1.000000000000000000 ) ) ;
#24434=CARTESIAN_POINT ( 'NONE',  ( 5.520433897694421610, 0.004666464468078328209, -0.01432141647227113193 ) ) ;
#24441=B_SPLINE_CURVE_WITH_KNOTS ( 'NONE', 3,
 ( #57054, #21814, #32723, #42711, #22115, #57716, #53033, #62038, #58360, #12780, #62343, #33071, #42371, #17134, #46733, #37408 ),
 .UNSPECIFIED., .F., .F.,
 ( 4, 3, 3, 3, 3, 4 ),
 ( 8.415671965864807093E-19, 0.0003017745587525263312, 0.0006035491769808766678, 0.0009053241094668192839, 0.001207275924540517119, 0.001510325902534023941 ),
 .UNSPECIFIED. ) ;
#24442=CARTESIAN_POINT ( 'NONE',  ( 2.241509619876138615, -1.363398699156099125, 7.511759925807393934 ) ) ;
#24443=CARTESIAN_POINT ( 'NONE',  ( 0.2759803524722239110, 0.1894460813477723549, -12.24828167798666456 ) ) ;
#24445=CARTESIAN_POINT ( 'NONE',  ( 2.249013661412229581, 7.636012530783587771, 0.1200550008339432706 ) ) ;
#24455=EDGE_CURVE ( 'NONE', #38649, #62456, #16285, .T. ) ;
#24464=CARTESIAN_POINT ( 'NONE',  ( 2.241449424704146320, 5.808712090826680274, -4.954182807723280568 ) ) ;
#24470=CARTESIAN_POINT ( 'NONE',  ( 5.516018279890452902, 0.004525000489649935558, -0.005042957932159086720 ) ) ;
#24478=CARTESIAN_POINT ( 'NONE',  ( 2.241311220309555097, -5.907514893712957793, 4.835827934491001123 ) ) ;
#24480=CARTESIAN_POINT ( 'NONE',  ( 5.514970785353741078, 0.004532877335078317783, -0.001326349372336594603 ) ) ;
#24481=CARTESIAN_POINT ( 'NONE',  ( 2.931247277082558611, 6.618030015945723044, 4.248542803114288446 ) ) ;
#24485=CARTESIAN_POINT ( 'NONE',  ( 2.305787727787084407, 7.249469779319909435, 2.461236246751095536 ) ) ;
#24490=VECTOR ( 'NONE', #56681, 1000.000000000000114 ) ;
#24494=VECTOR ( 'NONE', #50732, 1000.000000000000114 ) ;
#24495=CARTESIAN_POINT ( 'NONE',  ( 2.268878695253352618, -7.231932316093180546, 2.474564429974472901 ) ) ;
#24504=CARTESIAN_POINT ( 'NONE',  ( 2.288423627606496424, 1.169285315516220169, -7.560204962262810469 ) ) ;
#24526=CARTESIAN_POINT ( 'NONE',  ( 0.2646305136544072623, -6.237419468587005689, -10.53923716745253358 ) ) ;
#24531=CARTESIAN_POINT ( 'NONE',  ( 0.2651627923886329397, -10.64925183219497740, 6.046629261473301042 ) ) ;
#24536=CARTESIAN_POINT ( 'NONE',  ( 2.305787727787084851, -1.493241775258474124, 7.508843116234150905 ) ) ;
#24538=CARTESIAN_POINT ( 'NONE',  ( 0.2651627682582904932, 7.803986935114140877, -9.437482589529897936 ) ) ;
#24540=ADVANCED_FACE ( 'NONE', ( #47217 ), #24271, .F. ) ;
#24546=CARTESIAN_POINT ( 'NONE',  ( 0.3401186441510242187, 9.233880480307307792, 8.081824149807733448 ) ) ;
#24552=CARTESIAN_POINT ( 'NONE',  ( 0.2646305136544072623, -12.03696649559616283, 2.256625640822276235 ) ) ;
#24553=CARTESIAN_POINT ( 'NONE',  ( 2.276198483117255478, -7.501576331167725264, -1.479169956994139890 ) ) ;
#24563=CARTESIAN_POINT ( 'NONE',  ( 1.283627346226435373, 2.725559306498919643, 12.28700367512541014 ) ) ;
#24565=ADVANCED_FACE ( 'NONE', ( #54148 ), #48565, .F. ) ;
#24580=ORIENTED_EDGE ( 'NONE', *, *, #25110, .T. ) ;
#24584=CARTESIAN_POINT ( 'NONE',  ( 1.948354844646968731, 6.595573209513781343, 9.982942661979748777 ) ) ;
#24591=ORIENTED_EDGE ( 'NONE', *, *, #42228, .F. ) ;
#24593=VERTEX_POINT ( 'NONE', #33205 ) ;
#24594=CARTESIAN_POINT ( 'NONE',  ( 1.633930747253001581, -2.909970528251876853, -12.36466318969099198 ) ) ;
#24604=CARTESIAN_POINT ( 'NONE',  ( 2.241537034860906275, 6.614004440763098458, -3.813147095850915491 ) ) ;
#24606=CARTESIAN_POINT ( 'NONE',  ( 2.844750968615830100, 7.242618984642876789, -2.990088422897238196 ) ) ;
#24610=CARTESIAN_POINT ( 'NONE',  ( 2.899286259009682620, -6.972741252562078884, 3.614094927251911837 ) ) ;
#24614=ORIENTED_EDGE ( 'NONE', *, *, #64139, .F. ) ;
#24622=CARTESIAN_POINT ( 'NONE',  ( 1.719304012338200849, 11.38834240361387096, 5.690355757826642602 ) ) ;
#24630=CARTESIAN_POINT ( 'NONE',  ( 0.9296196016852207311, 9.812579935705901590, -7.691217109781619321 ) ) ;
#24638=ORIENTED_EDGE ( 'NONE', *, *, #22444, .T. ) ;
#24639=CARTESIAN_POINT ( 'NONE',  ( 2.259025283528086181, -7.639069972920485618, 0.1366755880739445317 ) ) ;
#24642=CARTESIAN_POINT ( 'NONE',  ( 1.633930747250580184, 10.17701904908664368, 7.601388527387680227 ) ) ;
#24644=CARTESIAN_POINT ( 'NONE',  ( 2.844750968615600506, 4.202329849280348029, 6.613363922490565372 ) ) ;
#24646=VERTEX_POINT ( 'NONE', #48845 ) ;
#24655=CARTESIAN_POINT ( 'NONE',  ( 0.3006302518452063088, -12.10891847026070245, -1.905681544119362636 ) ) ;
#24659=CARTESIAN_POINT ( 'NONE',  ( 5.520433897694421610, 0.0005131706886599361186, -0.01505375422439068044 ) ) ;
#24668=CARTESIAN_POINT ( 'NONE',  ( 0.2651627923886312188, 6.046629261473340122, 10.64925183219496319 ) ) ;
#24669=CARTESIAN_POINT ( 'NONE',  ( 2.241352910868908754, 3.744764251556992996, 6.652881166698525028 ) ) ;
#24673=ORIENTED_EDGE ( 'NONE', *, *, #47962, .T. ) ;
#24679=CARTESIAN_POINT ( 'NONE',  ( 3.152665057734128862, 5.761241965769081652, 5.461013642405580626 ) ) ;
#24688=CARTESIAN_POINT ( 'NONE',  ( 5.530133899448235191, 0.01589823604557752748, 0.001661287012794398143 ) ) ;
#24691=ORIENTED_EDGE ( 'NONE', *, *, #64261, .T. ) ;
#24692=CARTESIAN_POINT ( 'NONE',  ( 0.6511581176964164053, -9.688955459274794180, 7.698038847496666115 ) ) ;
#24693=ORIENTED_EDGE ( 'NONE', *, *, #50827, .T. ) ;
#24697=CARTESIAN_POINT ( 'NONE',  ( 2.241352910868908310, -7.633946224498473043, -0.08337961031712197435 ) ) ;
#24700=CARTESIAN_POINT ( 'NONE',  ( 0.3057689695767477067, -12.25749431726082506, 0.2309407641932320343 ) ) ;
#24701=CARTESIAN_POINT ( 'NONE',  ( 5.514624014163232779, 0.002216125254993666586, 0.003498325728817816473 ) ) ;
#24705=ORIENTED_EDGE ( 'NONE', *, *, #58640, .F. ) ;
#24731=CIRCLE ( 'NONE', #33223, 7.938172270156617749 ) ;
#24732=B_SPLINE_CURVE_WITH_KNOTS ( 'NONE', 3,
 ( #12273, #41545, #41884, #32537, #7282, #61836, #27565, #6323, #31262, #37556, #26588, #46882, #61500, #56879, #27247, #47538, #52544, #26270, #46547 ),
 .UNSPECIFIED., .F., .F.,
 ( 4, 3, 3, 3, 3, 3, 4 ),
 ( 9.619659766987995311E-18, 4.457896483015119041E-05, 6.639290541542508593E-05, 8.820687556479463274E-05, 0.0001100173248778967477, 0.0001545671401658198002, 0.0001830328308068606097 ),
 .UNSPECIFIED. ) ;
#24737=EDGE_LOOP ( 'NONE', ( #335, #58887, #49282, #50174 ) ) ;
#24744=LINE ( 'NONE', #45020, #23551 ) ;
#24745=FACE_OUTER_BOUND ( 'NONE', #13664, .T. ) ;
#24747=CARTESIAN_POINT ( 'NONE',  ( 2.247112776671469359, 0.1165461824817750069, 7.635437439951568095 ) ) ;
#24762=EDGE_CURVE ( 'NONE', #20510, #20746, #47266, .T. ) ;
#24769=ORIENTED_EDGE ( 'NONE', *, *, #38763, .F. ) ;
#24778=CARTESIAN_POINT ( 'NONE',  ( 2.406456491626625560, 8.382123850276952837, 6.212289237903838135 ) ) ;
#24791=CARTESIAN_POINT ( 'NONE',  ( 2.280717697723837922, -7.502592193582055202, 1.481796453660293222 ) ) ;
#24792=CARTESIAN_POINT ( 'NONE',  ( 2.241449424704146320, 1.386092121067206140, 7.507583637787353048 ) ) ;
#24800=ORIENTED_EDGE ( 'NONE', *, *, #2414, .F. ) ;
#24802=CARTESIAN_POINT ( 'NONE',  ( 1.719304012338199517, 0.000000000000000000, 0.000000000000000000 ) ) ;
#24803=CARTESIAN_POINT ( 'NONE',  ( 2.288423627607477417, 7.504187945869073673, -1.486973602181071552 ) ) ;
#24807=CARTESIAN_POINT ( 'NONE',  ( 1.452237505248552996, 11.67686475128079771, 4.880303821311048118 ) ) ;
#24810=CARTESIAN_POINT ( 'NONE',  ( 2.430348790457011798, 6.019963855523680962, 4.796903114819394354 ) ) ;
#24817=CARTESIAN_POINT ( 'NONE',  ( 2.990245332647882837, 6.155689586375199696, 5.834301250882226952 ) ) ;
#24820=CARTESIAN_POINT ( 'NONE',  ( 2.963017218115626683, -6.619413971958186593, -4.265970453343994606 ) ) ;
#24824=CARTESIAN_POINT ( 'NONE',  ( 2.770579946183238995, 6.607710183380625324, 4.165025702425821486 ) ) ;
#24828=CARTESIAN_POINT ( 'NONE',  ( 0.6511581176957980110, -6.471755598256246245, 10.54760823437298001 ) ) ;
#24830=CARTESIAN_POINT ( 'NONE',  ( 0.2646305136544072623, -12.24595685781654808, 0.1321451301297412451 ) ) ;
#24832=CARTESIAN_POINT ( 'NONE',  ( 0.2869720083484367801, -8.034871682535149162, 9.251312689958732349 ) ) ;
#24836=CARTESIAN_POINT ( 'NONE',  ( 1.014383007554945149, 12.22116704270661813, -2.605923236272006172 ) ) ;
#24840=CARTESIAN_POINT ( 'NONE',  ( 0.3341166715381310159, -9.559079491641819359, -7.691251065848441648 ) ) ;
#24841=CARTESIAN_POINT ( 'NONE',  ( 0.9296196016848911059, -1.754499435239580851, -12.34355205587747228 ) ) ;
#24846=CARTESIAN_POINT ( 'NONE',  ( 2.259025283526327588, 1.191911401087284217, -7.546748801934501927 ) ) ;
#24847=ORIENTED_EDGE ( 'NONE', *, *, #34916, .T. ) ;
#24853=AXIS2_PLACEMENT_3D ( 'NONE', #28386, #3140, #39012 ) ;
#24855=CARTESIAN_POINT ( 'NONE',  ( 5.530133899448235191, -0.01459891979722874843, 0.006510401266731764142 ) ) ;
#24869=ORIENTED_EDGE ( 'NONE', *, *, #2463, .T. ) ;
#24876=CARTESIAN_POINT ( 'NONE',  ( 2.276905613633648962, 7.644700064315451016, -0.1540880535621231562 ) ) ;
#24877=CARTESIAN_POINT ( 'NONE',  ( 0.2653519991613825235, 7.888569541500650040, -9.366979519113268537 ) ) ;
#24878=EDGE_CURVE ( 'NONE', #57898, #2022, #50438, .T. ) ;
#24880=FACE_OUTER_BOUND ( 'NONE', #21778, .T. ) ;
#24888=CARTESIAN_POINT ( 'NONE',  ( 0.2915757698887293525, 0.2147157799034817294, 12.25305747416127922 ) ) ;
#24894=FACE_OUTER_BOUND ( 'NONE', #62648, .T. ) ;
#24895=CARTESIAN_POINT ( 'NONE',  ( 2.781367136452752575, 5.255136723410658739, 5.783466416658742837 ) ) ;
#24896=VERTEX_POINT ( 'NONE', #36804 ) ;
#24898=CARTESIAN_POINT ( 'NONE',  ( 3.092491956585225577, 2.283527081234640654, -7.581757403488093239 ) ) ;
#24907=CARTESIAN_POINT ( 'NONE',  ( 0.3057689695767489280, -0.2309407641931890687, -12.25749431726082506 ) ) ;
#24913=B_SPLINE_CURVE_WITH_KNOTS ( 'NONE', 3,
 ( #63245, #2078, #22028, #22348, #62918, #28020, #37972, #18377, #12693, #7731, #12369, #8066, #17041, #32636, #48319, #52949 ),
 .UNSPECIFIED., .F., .F.,
 ( 4, 3, 3, 3, 3, 4 ),
 ( 8.673617379884035472E-19, 0.0002176109881720281712, 0.0004352086762394674971, 0.0006528017811446998678, 0.0007615147961451848536, 0.0009453342004947393401 ),
 .UNSPECIFIED. ) ;
#24914=EDGE_CURVE ( 'NONE', #11018, #14439, #47454, .T. ) ;
#24920=CARTESIAN_POINT ( 'NONE',  ( 2.298277635560274312, -6.543949079923912393, -3.968740875991624062 ) ) ;
#24923=CARTESIAN_POINT ( 'NONE',  ( 5.516018279890452902, -0.005976902763919015801, 0.003191189039764900665 ) ) ;
#24925=CARTESIAN_POINT ( 'NONE',  ( 2.665405856346790170, -5.274989403260943455, 7.981834391067692103 ) ) ;
#24931=CARTESIAN_POINT ( 'NONE',  ( 1.020182472822703801, -11.03967505355367607, 5.858468047365960274 ) ) ;
#24943=CARTESIAN_POINT ( 'NONE',  ( 2.430348790457227626, 7.164221884688219966, -2.814990071337918121 ) ) ;
#24946=CARTESIAN_POINT ( 'NONE',  ( 2.373367633546870525, -6.738274194514239923, 3.681545031436630033 ) ) ;
#24948=ORIENTED_EDGE ( 'NONE', *, *, #10396, .F. ) ;
#24949=CARTESIAN_POINT ( 'NONE',  ( 0.3160775863651100748, 11.60348481172941426, -3.967735865794236538 ) ) ;
#24954=CARTESIAN_POINT ( 'NONE',  ( 0.2650492594609225039, 11.46945808033133929, 4.291723947796354466 ) ) ;
#24958=ORIENTED_EDGE ( 'NONE', *, *, #38439, .T. ) ;
#24966=AXIS2_PLACEMENT_3D ( 'NONE', #10040, #15352, #14667 ) ;
#24967=ORIENTED_EDGE ( 'NONE', *, *, #65504, .F. ) ;
#24971=B_SPLINE_CURVE_WITH_KNOTS ( 'NONE', 3,
 ( #31222, #51528, #5642, #959, #65777, #40528, #25910, #51839, #6286, #60824, #55840, #61456, #46199, #40872, #10266, #45861 ),
 .UNSPECIFIED., .F., .F.,
 ( 4, 3, 3, 3, 3, 4 ),
 ( 0.000000000000000000, 0.0002999043160757438459, 0.0005998071753051191068, 0.0008997092107374842678, 0.001204458948196640827, 0.001510329163478487616 ),
 .UNSPECIFIED. ) ;
#24976=CARTESIAN_POINT ( 'NONE',  ( 0.3057689695767517035, 10.73077184758791702, 5.928746590069615685 ) ) ;
#24979=CARTESIAN_POINT ( 'NONE',  ( 2.249013661412013754, -3.714035584818559332, -6.673008335691601012 ) ) ;
#24984=CARTESIAN_POINT ( 'NONE',  ( 2.655192694324727487, -2.234846078477053410, -9.337840456945928125 ) ) ;
#24988=CARTESIAN_POINT ( 'NONE',  ( 0.3164563675027619039, -12.11636128244743027, -1.892265234253239115 ) ) ;
#24991=B_SPLINE_CURVE_WITH_KNOTS ( 'NONE', 3,
 ( #28601, #28940, #38922, #29267, #13319, #24604, #39230, #59210, #18662, #19632 ),
 .UNSPECIFIED., .F., .F.,
 ( 4, 3, 3, 4 ),
 ( 0.000000000000000000, 6.607638129004381818E-05, 9.911389841680568337E-05, 0.0001667630577588626094 ),
 .UNSPECIFIED. ) ;
#24992=CARTESIAN_POINT ( 'NONE',  ( 5.536195898058073439, -0.002666509901869554798, -0.008071068258923213418 ) ) ;
#24998=ORIENTED_EDGE ( 'NONE', *, *, #60031, .T. ) ;
#25000=CARTESIAN_POINT ( 'NONE',  ( 0.3665391374699472626, -9.576575648338968350, -7.691255657244390420 ) ) ;
#25002=CARTESIAN_POINT ( 'NONE',  ( 0.2638984909335716500, -0.1991813963114842101, 12.24571285024409129 ) ) ;
#25007=CARTESIAN_POINT ( 'NONE',  ( 2.889800649504073782, 0.9965440656174524570, -6.039722463373529138 ) ) ;
#25009=CARTESIAN_POINT ( 'NONE',  ( 3.031336079629583846, 3.582646412484484788, -7.038432939676037670 ) ) ;
#25010=ORIENTED_EDGE ( 'NONE', *, *, #18599, .F. ) ;
#25013=CARTESIAN_POINT ( 'NONE',  ( 2.368238019615237722, -2.455958560214692721, 7.273245349264759518 ) ) ;
#25016=CARTESIAN_POINT ( 'NONE',  ( 2.276905613634090386, 4.795880183929502216, -5.955225895210846332 ) ) ;
#25030=CARTESIAN_POINT ( 'NONE',  ( 0.6473888112830274988, -6.470260187014647890, -10.54705164520785132 ) ) ;
#25033=CARTESIAN_POINT ( 'NONE',  ( 0.2646305136544072623, -4.312539723326057839, -11.46223899740604502 ) ) ;
#25037=EDGE_LOOP ( 'NONE', ( #4903, #64487, #17496, #22846 ) ) ;
#25040=ORIENTED_EDGE ( 'NONE', *, *, #7397, .F. ) ;
#25045=CARTESIAN_POINT ( 'NONE',  ( 0.5547464869798220954, -12.33891836761637073, 0.3049355384528578683 ) ) ;
#25046=CARTESIAN_POINT ( 'NONE',  ( 5.516018279890452902, -0.0002248006052448983238, -0.006771744149385263388 ) ) ;
#25049=CARTESIAN_POINT ( 'NONE',  ( 2.241509619876138615, -7.511759925807386828, -1.363398699156125327 ) ) ;
#25053=VERTEX_POINT ( 'NONE', #1118 ) ;
#25054=CARTESIAN_POINT ( 'NONE',  ( 2.705197763288540003, -6.142723737672409534, 4.789125516644094915 ) ) ;
#25056=CARTESIAN_POINT ( 'NONE',  ( 0.2652384770603646302, -7.820955051613265319, -9.423432754625816088 ) ) ;
#25061=( BOUNDED_SURFACE ( )  B_SPLINE_SURFACE ( 3, 1, ( 
 ( #6396, #26666 ),
 ( #46961, #1419 ),
 ( #10711, #11689 ),
 ( #31971, #6732 ) ),
 .UNSPECIFIED., .F., .F., .F. ) 
 B_SPLINE_SURFACE_WITH_KNOTS ( ( 4, 4 ),
 ( 2, 2 ),
 ( 0.000000000000000000, 1.000000000000000000 ),
 ( 0.000000000000000000, 1.000000000000000000 ),
 .UNSPECIFIED. ) 
 GEOMETRIC_REPRESENTATION_ITEM ( )  RATIONAL_B_SPLINE_SURFACE ( (
 ( 1.000000000000000000, 1.000000000000000000),
 ( 0.6933888150995267674, 0.9895912004443193632),
 ( 0.6933888150995267674, 0.9895912004443193632),
 ( 1.000000000000000000, 1.000000000000000000) ) ) 
 REPRESENTATION_ITEM ( '' )  SURFACE ( )  );
#25076=CARTESIAN_POINT ( 'NONE',  ( 0.3106921474978477371, -12.11369598333778441, 1.896868624983024887 ) ) ;
#25087=VERTEX_POINT ( 'NONE', #36358 ) ;
#25097=ORIENTED_EDGE ( 'NONE', *, *, #10374, .F. ) ;
#25101=CARTESIAN_POINT ( 'NONE',  ( 0.3278977287071288549, 9.554671284920413399, -7.693417476735430860 ) ) ;
#25110=EDGE_CURVE ( 'NONE', #1896, #39587, #21090, .T. ) ;
#25115=B_SPLINE_CURVE_WITH_KNOTS ( 'NONE', 3,
 ( #7422, #17755, #22070, #27709, #48015, #57672, #12093 ),
 .UNSPECIFIED., .F., .F.,
 ( 4, 3, 4 ),
 ( 2.200004060863483116E-15, 0.002398160485434652853, 0.005002426799381861841 ),
 .UNSPECIFIED. ) ;
#25118=CARTESIAN_POINT ( 'NONE',  ( 0.3223008802179278542, 10.49760329338528386, -6.343104382804205521 ) ) ;
#25121=CARTESIAN_POINT ( 'NONE',  ( 2.305787727787084407, 7.654065630109506913, 0.1666591538752955071 ) ) ;
#25124=EDGE_LOOP ( 'NONE', ( #36357, #1110, #31974, #19843 ) ) ;
#25134=CARTESIAN_POINT ( 'NONE',  ( 0.9232058338315058954, -12.34162163148532798, -1.793035206307472151 ) ) ;
#25136=CARTESIAN_POINT ( 'NONE',  ( 2.899286259009687949, -0.3564726075923954629, 7.845618522360449987 ) ) ;
#25137=CARTESIAN_POINT ( 'NONE',  ( 0.3040950598368152291, 10.49113473328039170, -6.347045025870654555 ) ) ;
#25150=CARTESIAN_POINT ( 'NONE',  ( 5.514624014163232779, 0.004045310349816140343, 0.0008859786816842230061 ) ) ;
#25157=CARTESIAN_POINT ( 'NONE',  ( 0.2956976708475453353, 7.708404409946655989, 9.528782683728111991 ) ) ;
#25167=LINE ( 'NONE', #46435, #45995 ) ;
#25176=CARTESIAN_POINT ( 'NONE',  ( 2.305787727787084407, 0.1666591538753756929, -7.654065630109506024 ) ) ;
#25183=CARTESIAN_POINT ( 'NONE',  ( 2.251152103363647239, 7.133254101175224626, -2.729599998984340470 ) ) ;
#25187=B_SPLINE_CURVE_WITH_KNOTS ( 'NONE', 3,
 ( #52948, #26695, #27661, #56969, #17040, #37971, #11393, #51661, #42282, #31667, #22027, #62575, #51977, #6105, #26362, #6421 ),
 .UNSPECIFIED., .F., .F.,
 ( 4, 3, 3, 3, 3, 4 ),
 ( 2.710505431213761085E-19, 0.0003017745587525231328, 0.0006035491769808708131, 0.0009053241094668120197, 0.001207275924539391717, 0.001510325902531780510 ),
 .UNSPECIFIED. ) ;
#25190=CARTESIAN_POINT ( 'NONE',  ( 1.198791140419100287, -11.96656299555083613, 3.806343609711079434 ) ) ;
#25192=CARTESIAN_POINT ( 'NONE',  ( 2.241352910868909643, 5.794346703933845433, 4.970878533273779709 ) ) ;
#25211=CARTESIAN_POINT ( 'NONE',  ( 2.969415267404148739, 2.326350273511913258, -7.525730903320487108 ) ) ;
#25213=CARTESIAN_POINT ( 'NONE',  ( 2.665405856346785729, 5.274989403261000298, -7.981834391067653911 ) ) ;
#25225=CARTESIAN_POINT ( 'NONE',  ( 2.034671305879538483, 8.030508024280598178, -8.476347594674427555 ) ) ;
#25233=CARTESIAN_POINT ( 'NONE',  ( 2.247206125382826158, -6.554642244888441382, -3.917979829727982644 ) ) ;
#25237=CARTESIAN_POINT ( 'NONE',  ( 1.634816307074480779, 9.253014110594536490, 8.702988562438394027 ) ) ;
#25242=CARTESIAN_POINT ( 'NONE',  ( 0.2646305136544072623, -10.53923716745251404, 6.237419468587042104 ) ) ;
#25251=CARTESIAN_POINT ( 'NONE',  ( 5.514970785353741078, 0.001897634820904952127, 0.004324946436530311550 ) ) ;
#25252=CARTESIAN_POINT ( 'NONE',  ( 3.031336079629294744, 7.268683861177205330, -3.088871717871271461 ) ) ;
#25257=CARTESIAN_POINT ( 'NONE',  ( 0.3675815128205912052, 11.62724744438071056, -3.951233083390353062 ) ) ;
#25265=CARTESIAN_POINT ( 'NONE',  ( 2.573738926104376379, -1.112690714006486115, -7.664876274722925764 ) ) ;
#25274=ORIENTED_EDGE ( 'NONE', *, *, #47530, .F. ) ;
#25275=CARTESIAN_POINT ( 'NONE',  ( 0.3106921474978440734, -10.73438344699975389, 5.925601485921636602 ) ) ;
#25278=CARTESIAN_POINT ( 'NONE',  ( 2.260457164927179630, -6.685239696063459469, -3.699855525213223473 ) ) ;
#25282=CARTESIAN_POINT ( 'NONE',  ( 2.280717697723838810, -7.645922213779908994, 0.1564731737569851899 ) ) ;
#25288=CARTESIAN_POINT ( 'NONE',  ( 2.251139882113692536, -3.710800524305181369, -6.675617500148306682 ) ) ;
#25291=ORIENTED_EDGE ( 'NONE', *, *, #11842, .T. ) ;
#25303=LINE ( 'NONE', #45584, #28010 ) ;
#25309=CIRCLE ( 'NONE', #22128, 7.938172270156617749 ) ;
#25313=CARTESIAN_POINT ( 'NONE',  ( 20.00005080000000035, 0.000000000000000000, 0.000000000000000000 ) ) ;
#25321=ORIENTED_EDGE ( 'NONE', *, *, #60288, .F. ) ;
#25322=CARTESIAN_POINT ( 'NONE',  ( 3.047904605210376427, 3.098478597269376245, -7.270585891216581054 ) ) ;
#25326=CARTESIAN_POINT ( 'NONE',  ( 2.524535260912463386, -2.434550409953165850, 7.335347545455585205 ) ) ;
#25333=ORIENTED_EDGE ( 'NONE', *, *, #47515, .F. ) ;
#25339=CARTESIAN_POINT ( 'NONE',  ( 1.547277799339154214, -6.911346840320659268, -10.62321481610077178 ) ) ;
#25344=CARTESIAN_POINT ( 'NONE',  ( 0.2655924914740778742, -4.229867354073483021, -11.49267051747972523 ) ) ;
#25356=CARTESIAN_POINT ( 'NONE',  ( 0.3675815128205894289, 8.093875121226078662, 9.235491948680033758 ) ) ;
#25358=CARTESIAN_POINT ( 'NONE',  ( 5.515539859299206427, 0.005142293699651867729, -0.003193223631739272681 ) ) ;
#25367=CARTESIAN_POINT ( 'NONE',  ( 2.373367633546869193, -5.996611082971999629, 4.795703124519871352 ) ) ;
#25370=CARTESIAN_POINT ( 'NONE',  ( 0.3675815128205894289, 12.04510820461659293, 2.391755495700645273 ) ) ;
#25374=CARTESIAN_POINT ( 'NONE',  ( 0.3223008802179263554, -4.423848692584617659, -11.43958962819737124 ) ) ;
#25383=VECTOR ( 'NONE', #28442, 1000.000000000000114 ) ;
#25384=EDGE_CURVE ( 'NONE', #28435, #59321, #24971, .T. ) ;
#25394=DIRECTION ( 'NONE',  ( 0.000000000000000000, 0.000000000000000000, -1.000000000000000000 ) ) ;
#25410=CARTESIAN_POINT ( 'NONE',  ( 0.2646305136544065406, 7.972778379581551889, 9.296005949277249769 ) ) ;
#25418=ORIENTED_EDGE ( 'NONE', *, *, #1666, .F. ) ;
#25422=ADVANCED_FACE ( 'NONE', ( #30547 ), #26036, .F. ) ;
#25425=CARTESIAN_POINT ( 'NONE',  ( 0.3164563675027652345, -12.03284811452138747, 2.365891945210773173 ) ) ;
#25437=CARTESIAN_POINT ( 'NONE',  ( 2.276198483117260807, 7.644465698238550821, 0.1540629821338586058 ) ) ;
#25448=ADVANCED_FACE ( 'NONE', ( #11253 ), #6042, .F. ) ;
#25456=CARTESIAN_POINT ( 'NONE',  ( 1.719304012340749033, -5.066286238787660601, -11.67935079956571087 ) ) ;
#25462=CARTESIAN_POINT ( 'NONE',  ( 0.2655924914740778742, -12.06787830249863980, -2.083162675473735792 ) ) ;
#25466=CARTESIAN_POINT ( 'NONE',  ( 3.152665057733995191, 6.622010822086684456, 4.377619405892240856 ) ) ;
#25472=CARTESIAN_POINT ( 'NONE',  ( 2.440552418640495880, 1.142369876085324476, 7.615619946579172961 ) ) ;
#25475=AXIS2_PLACEMENT_3D ( 'NONE', #9031, #35268, #49607 ) ;
#25479=CARTESIAN_POINT ( 'NONE',  ( 0.3106921474978454056, 7.699584408545896430, 9.542334142800491747 ) ) ;
#25482=CARTESIAN_POINT ( 'NONE',  ( 1.287602823388152906, -1.639728374785596632, -12.47973441446222154 ) ) ;
#25485=CARTESIAN_POINT ( 'NONE',  ( 0.2767916011545413224, 11.44495079483529310, -4.367596755337330272 ) ) ;
#25488=EDGE_LOOP ( 'NONE', ( #51779, #33771, #29301, #62117 ) ) ;
#25491=CARTESIAN_POINT ( 'NONE',  ( 3.092491956585884161, 1.813286239165800451, 7.707758057368689464 ) ) ;
#25500=ORIENTED_EDGE ( 'NONE', *, *, #55879, .T. ) ;
#25501=CARTESIAN_POINT ( 'NONE',  ( 2.305787727787083519, -7.249469779319894336, -2.461236246751144829 ) ) ;
#25506=FACE_OUTER_BOUND ( 'NONE', #52743, .T. ) ;
#25507=CARTESIAN_POINT ( 'NONE',  ( 2.260457164927187623, 7.131443009846837988, -2.742969430850449086 ) ) ;
#25513=VERTEX_POINT ( 'NONE', #42139 ) ;
#25532=CARTESIAN_POINT ( 'NONE',  ( 0.9232058338315058954, 1.793035206307509677, -12.34162163148531732 ) ) ;
#25533=CARTESIAN_POINT ( 'NONE',  ( 2.368238019615157341, -7.589221137922671723, -1.155661230551862761 ) ) ;
#25534=DIRECTION ( 'NONE',  ( -0.3865475372811021382, -0.8598319252293142867, 0.3335716741247162220 ) ) ;
#25538=CARTESIAN_POINT ( 'NONE',  ( 1.547277799337861692, -1.534072017332991367, 12.58038279313703534 ) ) ;
#25549=VERTEX_POINT ( 'NONE', #12537 ) ;
#25550=CARTESIAN_POINT ( 'NONE',  ( 0.2767916011545391575, -0.1897947303541993036, -12.24854187541374628 ) ) ;
#25555=CARTESIAN_POINT ( 'NONE',  ( 0.3002738374340850891, -11.59380198135585438, 3.979745968261164446 ) ) ;
#25556=ADVANCED_FACE ( 'NONE', ( #43130 ), #17088, .F. ) ;
#25558=ORIENTED_EDGE ( 'NONE', *, *, #31745, .T. ) ;
#25562=CARTESIAN_POINT ( 'NONE',  ( 0.2648978790185602672, -6.237101853238473659, -10.53870023327869987 ) ) ;
#25564=CARTESIAN_POINT ( 'NONE',  ( 1.109979610368941882, 9.281420052101180929, 8.414317452281256493 ) ) ;
#25565=CARTESIAN_POINT ( 'NONE',  ( 1.719304012341585253, 9.242227816401774376, -8.755325027795295867 ) ) ;
#25566=CARTESIAN_POINT ( 'NONE',  ( 0.2638984909335716500, -7.718810690098997895, -9.508791614589274133 ) ) ;
#25569=VECTOR ( 'NONE', #56761, 1000.000000000000227 ) ;
#25578=CARTESIAN_POINT ( 'NONE',  ( 2.034671305878982928, -6.953089744306905295, -9.380408876026439913 ) ) ;
#25579=ORIENTED_EDGE ( 'NONE', *, *, #36913, .F. ) ;
#25599=CARTESIAN_POINT ( 'NONE',  ( 5.514970785353741078, 0.003805873180274313254, -0.002796696073589883310 ) ) ;
#25604=CARTESIAN_POINT ( 'NONE',  ( 2.290907136832897706, -2.463690939638714106, -7.243397831411124699 ) ) ;
#25608=VECTOR ( 'NONE', #52974, 1000.000000000000114 ) ;
#25611=FACE_OUTER_BOUND ( 'NONE', #37539, .T. ) ;
#25622=CARTESIAN_POINT ( 'NONE',  ( 2.368238019615120926, 3.992969450835595069, 6.556525400300555084 ) ) ;
#25625=CARTESIAN_POINT ( 'NONE',  ( 3.152665057735807075, 3.546019893115007537, -7.102135024646828221 ) ) ;
#25628=CARTESIAN_POINT ( 'NONE',  ( 3.047904605210341789, 3.577928268982092597, 7.047014837597028958 ) ) ;
#25631=CARTESIAN_POINT ( 'NONE',  ( 0.2915757698887279092, 12.25305747416128455, -0.2147157799035241121 ) ) ;
#25634=CARTESIAN_POINT ( 'NONE',  ( 2.269879328256728446, -5.949827370243832014, -4.798845682294102133 ) ) ;
#25659=CARTESIAN_POINT ( 'NONE',  ( 2.430348790457294683, -2.448665558939157272, 7.297553103283471287 ) ) ;
#25662=EDGE_CURVE ( 'NONE', #51152, #47570, #56650, .T. ) ;
#25668=ORIENTED_EDGE ( 'NONE', *, *, #921, .F. ) ;
#25673=DIRECTION ( 'NONE',  ( 0.000000000000000000, 8.881784197001252323E-16, 1.000000000000000000 ) ) ;
#25697=CARTESIAN_POINT ( 'NONE',  ( 5.514624014163232779, -0.003946330869975010931, 0.001255375129358063304 ) ) ;
#25718=CARTESIAN_POINT ( 'NONE',  ( 1.109979610371585101, -3.830786822172526307, -11.92772269523408468 ) ) ;
#25721=EDGE_CURVE ( 'NONE', #14018, #56624, #21795, .T. ) ;
#25727=CARTESIAN_POINT ( 'NONE',  ( 1.937114397841935398, 3.111612666690077855, 12.45230409340482503 ) ) ;
#25736=VERTEX_POINT ( 'NONE', #9191 ) ;
#25741=CARTESIAN_POINT ( 'NONE',  ( 2.177405672432406902, 10.01846874164783152, 5.005033771130518616 ) ) ;
#25742=CARTESIAN_POINT ( 'NONE',  ( 2.305787727787083519, -5.756228004061423320, -5.047606869483115766 ) ) ;
#25746=CARTESIAN_POINT ( 'NONE',  ( 3.152665057735501097, 6.622010822086128456, -4.377619405893580229 ) ) ;
#25751=ORIENTED_EDGE ( 'NONE', *, *, #20855, .F. ) ;
#25754=EDGE_LOOP ( 'NONE', ( #22005, #52187, #19548, #6609, #17194, #6904 ) ) ;
#25767=CARTESIAN_POINT ( 'NONE',  ( 0.3218525148189825269, 12.03385614540604109, 2.370084734146256977 ) ) ;
#25770=EDGE_CURVE ( 'NONE', #51848, #59884, #6715, .T. ) ;
#25776=CARTESIAN_POINT ( 'NONE',  ( 1.459561108993354006, -12.32692860927468459, 2.815016945600703036 ) ) ;
#25778=CARTESIAN_POINT ( 'NONE',  ( 2.268878695253354394, 7.642144312464374423, 0.1481365927653814363 ) ) ;
#25786=CARTESIAN_POINT ( 'NONE',  ( 2.256373768223411957, 7.499124080223153577, -1.457292142211135122 ) ) ;
#25787=VECTOR ( 'NONE', #48043, 1000.000000000000000 ) ;
#25797=CARTESIAN_POINT ( 'NONE',  ( 0.2650492594609224484, 10.54996119777445429, 6.218173512054799623 ) ) ;
#25801=B_SPLINE_CURVE_WITH_KNOTS ( 'NONE', 3,
 ( #4529, #49739, #35064, #44727, #50068, #14143, #10150 ),
 .UNSPECIFIED., .F., .F.,
 ( 4, 3, 4 ),
 ( 7.221291777193456067E-15, 0.002398160485434789463, 0.005002426799383989479 ),
 .UNSPECIFIED. ) ;
#25806=CARTESIAN_POINT ( 'NONE',  ( 0.9232058338315048962, -12.46548196349785798, -0.3773051331669288744 ) ) ;
#25809=CARTESIAN_POINT ( 'NONE',  ( 2.655192694323460945, -6.969384012965772257, 6.604353705985055001 ) ) ;
#25810=CARTESIAN_POINT ( 'NONE',  ( 0.3665391374699464300, -12.27992639892678106, -0.2638605131388451763 ) ) ;
#25814=VECTOR ( 'NONE', #37101, 1000.000000000000114 ) ;
#25816=ORIENTED_EDGE ( 'NONE', *, *, #59977, .F. ) ;
#25820=LINE ( 'NONE', #16160, #29756 ) ;
#25822=CARTESIAN_POINT ( 'NONE',  ( 0.2676618633000453773, 7.748413788583214945, 9.484212776852357862 ) ) ;
#25825=CARTESIAN_POINT ( 'NONE',  ( 1.549075743846619613, -1.533250336941883063, -12.58108552526800850 ) ) ;
#25829=CARTESIAN_POINT ( 'NONE',  ( 0.2958664285830449603, 11.43993536884562623, -4.398464391600207080 ) ) ;
#25839=CARTESIAN_POINT ( 'NONE',  ( 0.2676618633000434344, 11.45242956837287629, 4.339362305359467875 ) ) ;
#25860=DIRECTION ( 'NONE',  ( -1.000000000000000000, -0.000000000000000000, -0.000000000000000000 ) ) ;
#25869=CARTESIAN_POINT ( 'NONE',  ( 0.3006302518452070860, -10.72687985734938465, -5.932248915294272784 ) ) ;
#25871=FACE_OUTER_BOUND ( 'NONE', #63952, .T. ) ;
#25881=CARTESIAN_POINT ( 'NONE',  ( 1.452237505248552996, -5.807998527925814614, -11.24427360515648289 ) ) ;
#25886=CARTESIAN_POINT ( 'NONE',  ( 1.549075743845170106, -12.58108552526744184, 1.533250336942571401 ) ) ;
#25889=CARTESIAN_POINT ( 'NONE',  ( 5.516018279890452902, -0.003580555109620835435, 0.005752102158674384652 ) ) ;
#25897=CARTESIAN_POINT ( 'NONE',  ( 2.241352910868908754, 7.145045428366577411, 2.689314586382375527 ) ) ;
#25902=ORIENTED_EDGE ( 'NONE', *, *, #22345, .T. ) ;
#25905=CARTESIAN_POINT ( 'NONE',  ( 2.268878695253351285, -6.544222817598194020, -3.949362208797132734 ) ) ;
#25906=CARTESIAN_POINT ( 'NONE',  ( 2.241352910868909643, -3.744764251557037849, 6.652881166698498383 ) ) ;
#25910=CARTESIAN_POINT ( 'NONE',  ( 1.198791140420808921, 11.12379938352781927, -5.826488554585463220 ) ) ;
#25917=CARTESIAN_POINT ( 'NONE',  ( 1.375507693220405780, 4.865932489132489991, -11.64019206974694320 ) ) ;
#25922=VERTEX_POINT ( 'NONE', #19028 ) ;
#25925=CARTESIAN_POINT ( 'NONE',  ( 3.152665057734040488, 0.000000000000000000, 0.000000000000000000 ) ) ;
#25932=ORIENTED_EDGE ( 'NONE', *, *, #57218, .T. ) ;
#25937=ORIENTED_EDGE ( 'NONE', *, *, #11482, .F. ) ;
#25938=DIRECTION ( 'NONE',  ( 0.3939253465568944290, -0.7910971609033203844, -0.4679616473074870719 ) ) ;
#25941=CARTESIAN_POINT ( 'NONE',  ( 1.287602823384975226, 11.62763122279957528, 4.819820779358876983 ) ) ;
#25942=LINE ( 'NONE', #670, #4471 ) ;
#25943=CARTESIAN_POINT ( 'NONE',  ( 2.305787727787084407, 2.774453000917245671, -7.135468203929955067 ) ) ;
#25951=B_SPLINE_CURVE_WITH_KNOTS ( 'NONE', 3,
 ( #43927, #17997, #49581, #48288, #58922, #18679, #28621, #59883, #8035, #3723, #23982, #2735, #14305, #38938, #13006, #44242 ),
 .UNSPECIFIED., .F., .F.,
 ( 4, 3, 3, 3, 3, 4 ),
 ( 0.000000000000000000, 0.0002999043160758550850, 0.0005998071753053377904, 0.0008997092107378087695, 0.001204458948196017627, 0.001510329163476902947 ),
 .UNSPECIFIED. ) ;
#25954=CARTESIAN_POINT ( 'NONE',  ( 0.3160775863651059669, -10.73821170199159525, 5.922381034681560408 ) ) ;
#25979=CARTESIAN_POINT ( 'NONE',  ( 1.452237505248555660, -11.67686475128083323, 4.880303821310969958 ) ) ;
#25981=CARTESIAN_POINT ( 'NONE',  ( 2.284126774967659479, 0.1584898568958950094, -7.647017279602161821 ) ) ;
#25990=EDGE_CURVE ( 'NONE', #54859, #7383, #29640, .T. ) ;
#25993=B_SPLINE_CURVE_WITH_KNOTS ( 'NONE', 3,
 ( #52420, #63342, #27132, #22134, #17152, #37424, #57738, #7163, #12157, #3183, #24106, #18138, #23450, #8158, #18492, #28761 ),
 .UNSPECIFIED., .F., .F.,
 ( 4, 3, 3, 3, 3, 4 ),
 ( 0.000000000000000000, 0.0003017745587525266023, 0.0006035491769808768846, 0.0009053241094668210186, 0.001207275924539022655, 0.001510325902531030025 ),
 .UNSPECIFIED. ) ;
#25994=CARTESIAN_POINT ( 'NONE',  ( 3.152665057734036491, 7.923639299009025194, 0.4801242025592407647 ) ) ;
#25997=ORIENTED_EDGE ( 'NONE', *, *, #29378, .T. ) ;
#26001=CARTESIAN_POINT ( 'NONE',  ( 2.242418902652064006, 4.830735118999549549, -5.912154560271766002 ) ) ;
#26014=CARTESIAN_POINT ( 'NONE',  ( 0.3665391374699472626, 9.237363111276875927, -8.095513416941138019 ) ) ;
#26032=EDGE_CURVE ( 'NONE', #15657, #14146, #59824, .T. ) ;
#26033=CARTESIAN_POINT ( 'NONE',  ( 0.2655924914740778742, 10.58356227062117938, -6.161287456391572270 ) ) ;
#26036=( BOUNDED_SURFACE ( )  B_SPLINE_SURFACE ( 3, 1, ( 
 ( #30868, #15263 ),
 ( #20595, #25566 ),
 ( #35542, #50850 ),
 ( #41845, #5296 ) ),
 .UNSPECIFIED., .F., .F., .F. ) 
 B_SPLINE_SURFACE_WITH_KNOTS ( ( 4, 4 ),
 ( 2, 2 ),
 ( 0.000000000000000000, 1.000000000000000000 ),
 ( 0.000000000000000000, 1.000000000000000000 ),
 .UNSPECIFIED. ) 
 GEOMETRIC_REPRESENTATION_ITEM ( )  RATIONAL_B_SPLINE_SURFACE ( (
 ( 1.000000000000000000, 1.000000000000000000),
 ( 0.9942764183789327692, 0.8450855930916580938),
 ( 0.9942764183789327692, 0.8450855930916580938),
 ( 1.000000000000000000, 1.000000000000000000) ) ) 
 REPRESENTATION_ITEM ( '' )  SURFACE ( )  );
#26038=CARTESIAN_POINT ( 'NONE',  ( 2.556980015512995585, 0.2307166419793596213, 7.736177238086449748 ) ) ;
#26040=CARTESIAN_POINT ( 'NONE',  ( 5.516018279890452902, 0.005752102158673841684, -0.003580555109620817654 ) ) ;
#26042=CARTESIAN_POINT ( 'NONE',  ( 0.3474126878361827875, -4.439989671676146443, -11.44231427242454657 ) ) ;
#26050=LINE ( 'NONE', #5449, #8373 ) ;
#26051=EDGE_CURVE ( 'NONE', #39184, #31059, #5055, .T. ) ;
#26052=CARTESIAN_POINT ( 'NONE',  ( 0.2650492433740076481, 2.017984765249233092, -12.07870441534853789 ) ) ;
#26054=CARTESIAN_POINT ( 'NONE',  ( 2.941278708680199916, -4.048809123187966819, 4.615461433467243246 ) ) ;
#26057=ORIENTED_EDGE ( 'NONE', *, *, #33046, .T. ) ;
#26061=LINE ( 'NONE', #41663, #38531 ) ;
#26066=CARTESIAN_POINT ( 'NONE',  ( 2.288423627607478306, -6.543055113184245819, 3.963881558061940424 ) ) ;
#26070=ORIENTED_EDGE ( 'NONE', *, *, #38763, .T. ) ;
#26074=ADVANCED_FACE ( 'NONE', ( #50286 ), #53213, .F. ) ;
#26076=CARTESIAN_POINT ( 'NONE',  ( 0.3040950598368152291, -7.687624643091494292, 9.552450779732085451 ) ) ;
#26080=LINE ( 'NONE', #46035, #55518 ) ;
#26082=CARTESIAN_POINT ( 'NONE',  ( 3.092491956585981860, -7.905533744258676165, 0.4473002062012166880 ) ) ;
#26090=CARTESIAN_POINT ( 'NONE',  ( 0.2648978790185593790, 9.465406350830713578, -7.769924372105106336 ) ) ;
#26092=CARTESIAN_POINT ( 'NONE',  ( 2.253265082352431836, -7.637296367516837492, -0.1282654837135493442 ) ) ;
#26099=B_SPLINE_CURVE_WITH_KNOTS ( 'NONE', 3,
 ( #34826, #35159, #64766, #8940, #14871, #24221, #55132, #4624, #9911, #24888, #49519, #48860, #9560, #45164, #23588, #44828, #9243, #49828, #19891, #34525, #4277, #14241 ),
 .UNSPECIFIED., .F., .F.,
 ( 4, 3, 3, 3, 3, 3, 3, 4 ),
 ( 1.203659747349087626E-18, 4.449119708436788016E-05, 6.626296329540349705E-05, 8.803456484962513971E-05, 0.0001098060367612775466, 0.0001315774408628478463, 0.0001760698110411114653, 0.0001829697163287828600 ),
 .UNSPECIFIED. ) ;
#26101=CARTESIAN_POINT ( 'NONE',  ( 0.3160775863651096307, 12.03278055228170373, 2.365582350580104798 ) ) ;
#26102=VERTEX_POINT ( 'NONE', #50606 ) ;
#26106=CARTESIAN_POINT ( 'NONE',  ( 2.034671305879700576, -9.742055912617322733, -6.436604249851277437 ) ) ;
#26108=CARTESIAN_POINT ( 'NONE',  ( 5.514970785353741078, -0.0003039746380524631733, 0.004713149585127259823 ) ) ;
#26112=VECTOR ( 'NONE', #6834, 1000.000000000000114 ) ;
#26121=CARTESIAN_POINT ( 'NONE',  ( 1.634816307077716191, 2.910502128621766271, -12.36483956257058203 ) ) ;
#26124=ORIENTED_EDGE ( 'NONE', *, *, #18758, .T. ) ;
#26126=CARTESIAN_POINT ( 'NONE',  ( 2.491965175174699176, 1.130870800982706204, -7.634639040875287996 ) ) ;
#26128=B_SPLINE_CURVE_WITH_KNOTS ( 'NONE', 3,
 ( #58382, #39391, #29419, #8821, #28434, #64336, #49714, #33096, #59053, #7849, #29110, #48417, #3189 ),
 .UNSPECIFIED., .F., .F.,
 ( 4, 3, 3, 3, 4 ),
 ( 6.254869361644796591E-18, 6.607593386745547301E-05, 0.0001321518677373515664, 0.0001982171734706181764, 0.0002642860854759457897 ),
 .UNSPECIFIED. ) ;
#26138=CARTESIAN_POINT ( 'NONE',  ( 5.515539859299206427, 0.003740028639278347548, -0.004759416711442189703 ) ) ;
#26143=ORIENTED_EDGE ( 'NONE', *, *, #3253, .F. ) ;
#26145=EDGE_CURVE ( 'NONE', #25549, #3364, #42181, .T. ) ;
#26157=CARTESIAN_POINT ( 'NONE',  ( 2.241449424704145876, 2.553400830064077809, -7.194804211893820245 ) ) ;
#26158=CARTESIAN_POINT ( 'NONE',  ( 0.3006302518452032557, 11.43947177966008510, -4.404090606399768681 ) ) ;
#26159=ORIENTED_EDGE ( 'NONE', *, *, #48874, .T. ) ;
#26165=CARTESIAN_POINT ( 'NONE',  ( 0.3675815128205894289, 11.44679196252409348, 4.447030445008218535 ) ) ;
#26174=ORIENTED_EDGE ( 'NONE', *, *, #6326, .T. ) ;
#26177=CARTESIAN_POINT ( 'NONE',  ( 0.3040950598368144520, -8.072385578287534003, 9.229598020917661572 ) ) ;
#26185=CARTESIAN_POINT ( 'NONE',  ( 2.305787727787083519, 3.971363876084056166, -6.545285700970486786 ) ) ;
#26199=CARTESIAN_POINT ( 'NONE',  ( 0.2646305136544065406, 12.24595685781654453, 0.1321451301298271763 ) ) ;
#26201=CARTESIAN_POINT ( 'NONE',  ( 2.284126774967687457, 4.793997684221357858, 5.959830409747688407 ) ) ;
#26207=CARTESIAN_POINT ( 'NONE',  ( 2.907497136251100400, -1.009055026157924084, 7.791429554169944538 ) ) ;
#26210=CARTESIAN_POINT ( 'NONE',  ( 2.244591118396557672, 2.712243649838700144, 7.137527852925261485 ) ) ;
#26211=( BOUNDED_SURFACE ( )  B_SPLINE_SURFACE ( 3, 1, ( 
 ( #16642, #11642 ),
 ( #57213, #46568 ),
 ( #61210, #31913 ),
 ( #30603, #52235 ) ),
 .UNSPECIFIED., .F., .F., .T. ) 
 B_SPLINE_SURFACE_WITH_KNOTS ( ( 4, 4 ),
 ( 2, 2 ),
 ( 0.000000000000000000, 1.000000000000000000 ),
 ( 0.000000000000000000, 1.000000000000000000 ),
 .UNSPECIFIED. ) 
 GEOMETRIC_REPRESENTATION_ITEM ( )  RATIONAL_B_SPLINE_SURFACE ( (
 ( 1.000000000000000000, 1.000000000000000000),
 ( 0.6933888150995267674, 0.9895912004443193632),
 ( 0.6933888150995267674, 0.9895912004443193632),
 ( 1.000000000000000000, 1.000000000000000000) ) ) 
 REPRESENTATION_ITEM ( '' )  SURFACE ( )  );
#26217=CARTESIAN_POINT ( 'NONE',  ( 5.514970785353741078, -0.003929719953530088142, 0.002619824551223743064 ) ) ;
#26231=ADVANCED_FACE ( 'NONE', ( #53878 ), #26411, .F. ) ;
#26235=CARTESIAN_POINT ( 'NONE',  ( 0.4626703367445784698, -10.80124546303564337, 5.909149965570969165 ) ) ;
#26248=VERTEX_POINT ( 'NONE', #64176 ) ;
#26251=VERTEX_POINT ( 'NONE', #12306 ) ;
#26256=CARTESIAN_POINT ( 'NONE',  ( 0.2647959493198551173, 4.326188315749736724, 11.45640103018460110 ) ) ;
#26258=EDGE_CURVE ( 'NONE', #56858, #62784, #17316, .T. ) ;
#26259=CARTESIAN_POINT ( 'NONE',  ( 2.899286259009688393, -1.011320371384287986, -7.788326766693360881 ) ) ;
#26260=FACE_OUTER_BOUND ( 'NONE', #19698, .T. ) ;
#26263=CARTESIAN_POINT ( 'NONE',  ( 0.2648978790185619880, 2.256510822326142751, 12.03635331166812783 ) ) ;
#26267=B_SPLINE_CURVE_WITH_KNOTS ( 'NONE', 3,
 ( #3690, #23952, #44211, #19279, #59509, #29254, #39548, #59848, #34556, #49865, #44866, #4658, #29895, #40189, #65145, #30545 ),
 .UNSPECIFIED., .F., .F.,
 ( 4, 3, 3, 3, 3, 4 ),
 ( 3.599098170511143196E-15, 0.0002126834539179629465, 0.0004253519300366106863, 0.0006380165497223922117, 0.0007442707582427973267, 0.0009453531351419906022 ),
 .UNSPECIFIED. ) ;
#26270=CARTESIAN_POINT ( 'NONE',  ( 0.2648321136542672316, -2.265911310221893515, 12.03456865502705497 ) ) ;
#26276=ORIENTED_EDGE ( 'NONE', *, *, #5895, .F. ) ;
#26277=CARTESIAN_POINT ( 'NONE',  ( 0.2638984909335716500, -4.375449752477210907, 11.43908195192328137 ) ) ;
#26279=CARTESIAN_POINT ( 'NONE',  ( 3.100650473569739329, 6.348250400753959077, -4.737096019059198859 ) ) ;
#26281=CARTESIAN_POINT ( 'NONE',  ( 2.241526690369556096, 7.521460607153596101, 1.308664175663794227 ) ) ;
#26284=VERTEX_POINT ( 'NONE', #19926 ) ;
#26286=CARTESIAN_POINT ( 'NONE',  ( 0.3278977287071200841, 2.374069413450301536, -12.03512402322220609 ) ) ;
#26297=VERTEX_POINT ( 'NONE', #24255 ) ;
#26300=CARTESIAN_POINT ( 'NONE',  ( 3.092491956585816215, -6.622742949902576726, 4.340140213817473835 ) ) ;
#26303=CARTESIAN_POINT ( 'NONE',  ( 0.3474126878361844528, -1.876013288000134116, 12.12932967384299765 ) ) ;
#26306=ORIENTED_EDGE ( 'NONE', *, *, #42690, .F. ) ;
#26319=CARTESIAN_POINT ( 'NONE',  ( 0.3002738374340877536, 12.10874171309341918, -1.906042098268892371 ) ) ;
#26321=CARTESIAN_POINT ( 'NONE',  ( 0.3675815128205894289, 7.689697408877401941, -9.574637318041888889 ) ) ;
#26322=CARTESIAN_POINT ( 'NONE',  ( 2.241506898688418126, 4.937416071751840718, 5.822995664778275682 ) ) ;
#26324=CARTESIAN_POINT ( 'NONE',  ( 2.241352910868908754, 3.889181972941450738, 6.569501556381455387 ) ) ;
#26326=CARTESIAN_POINT ( 'NONE',  ( 2.241352910868908754, -6.652881166698538351, 3.744764251556969903 ) ) ;
#26329=CARTESIAN_POINT ( 'NONE',  ( 0.3665391374699464300, -6.368473106897203806, 10.50279796150434564 ) ) ;
#26330=CARTESIAN_POINT ( 'NONE',  ( 0.2653519890518161728, 4.188454465438684160, 11.50765826381078760 ) ) ;
#26334=EDGE_CURVE ( 'NONE', #44332, #52979, #54913, .T. ) ;
#26337=DIRECTION ( 'NONE',  ( -1.000000000000000000, -0.000000000000000000, -0.000000000000000000 ) ) ;
#26339=CARTESIAN_POINT ( 'NONE',  ( 2.491965175174414959, 7.322278065136198499, 2.439431489055664315 ) ) ;
#26342=CARTESIAN_POINT ( 'NONE',  ( 1.719304012341582588, 7.017415949614099979, -10.62216384465570762 ) ) ;
#26345=ORIENTED_EDGE ( 'NONE', *, *, #38025, .F. ) ;
#26362=CARTESIAN_POINT ( 'NONE',  ( 1.633930747250947002, 5.012862767613547987, 11.67150509329667685 ) ) ;
#26363=CARTESIAN_POINT ( 'NONE',  ( 1.375507693219673255, -3.754650692913064525, -12.04466556545244771 ) ) ;
#26370=CARTESIAN_POINT ( 'NONE',  ( 0.7446945582506641070, 10.56139717223413577, 6.508900271375134494 ) ) ;
#26374=CARTESIAN_POINT ( 'NONE',  ( 2.266490820343228130, -6.544980046121050776, 3.946561086901452686 ) ) ;
#26377=CARTESIAN_POINT ( 'NONE',  ( 0.2872850955227745917, -5.944938343726327012, 10.71476594226531986 ) ) ;
#26380=B_SPLINE_CURVE_WITH_KNOTS ( 'NONE', 3,
 ( #8944, #59813, #54507, #4943, #49524, #30201, #54827, #24225, #14246, #4281, #45167, #39516, #29528, #49832, #24553, #64145, #18922, #44833, #8608 ),
 .UNSPECIFIED., .F., .F.,
 ( 4, 3, 3, 3, 3, 3, 4 ),
 ( 0.000000000000000000, 2.831840207499405278E-05, 4.217266859840229838E-05, 5.602024318395587826E-05, 6.290810167968577719E-05, 9.120440630944289440E-05, 0.0001153103026479761575 ),
 .UNSPECIFIED. ) ;
#26393=CARTESIAN_POINT ( 'NONE',  ( 0.3040950598368152291, 8.072385578287471830, 9.229598020917713086 ) ) ;
#26400=CARTESIAN_POINT ( 'NONE',  ( 0.2648321136542691190, 9.471460387169383210, -7.762514728657997409 ) ) ;
#26406=CARTESIAN_POINT ( 'NONE',  ( 3.152665057734040488, 0.000000000000000000, 0.000000000000000000 ) ) ;
#26411=( BOUNDED_SURFACE ( )  B_SPLINE_SURFACE ( 3, 1, ( 
 ( #3691, #63496 ),
 ( #38574, #58892 ),
 ( #28929, #37595 ),
 ( #3352, #23621 ) ),
 .UNSPECIFIED., .F., .F., .F. ) 
 B_SPLINE_SURFACE_WITH_KNOTS ( ( 4, 4 ),
 ( 2, 2 ),
 ( 0.000000000000000000, 1.000000000000000000 ),
 ( 0.000000000000000000, 1.000000000000000000 ),
 .UNSPECIFIED. ) 
 GEOMETRIC_REPRESENTATION_ITEM ( )  RATIONAL_B_SPLINE_SURFACE ( (
 ( 1.000000000000000000, 1.000000000000000000),
 ( 0.6933888150995267674, 0.9895912004443193632),
 ( 0.6933888150995267674, 0.9895912004443193632),
 ( 1.000000000000000000, 1.000000000000000000) ) ) 
 REPRESENTATION_ITEM ( '' )  SURFACE ( )  );
#26427=CARTESIAN_POINT ( 'NONE',  ( 5.514970785353741078, 0.0003039746380524305930, -0.004713149585127262425 ) ) ;
#26429=CARTESIAN_POINT ( 'NONE',  ( 0.2648321136542688414, 4.321267941897666276, -11.45826514585339062 ) ) ;
#26431=B_SPLINE_CURVE_WITH_KNOTS ( 'NONE', 3,
 ( #15467, #10469, #24803, #51061, #10154, #9818, #50730, #838, #55380, #40399, #14788, #35069, #25786, #20465, #30111, #50415, #4859, #46077, #51408 ),
 .UNSPECIFIED., .F., .F.,
 ( 4, 3, 3, 3, 3, 3, 4 ),
 ( 7.298863197736074879E-18, 2.825908398831414518E-05, 4.208813692484295868E-05, 5.591713746944392975E-05, 6.279584083232444592E-05, 9.105792820297390646E-05, 0.0001153131102488855946 ),
 .UNSPECIFIED. ) ;
#26432=EDGE_CURVE ( 'NONE', #57595, #2022, #9574, .T. ) ;
#26439=CARTESIAN_POINT ( 'NONE',  ( 2.903928887687730942, -3.491800274469421428, -8.044738195290898730 ) ) ;
#26444=CARTESIAN_POINT ( 'NONE',  ( 5.536195898058073439, 0.001726268814999623981, 0.008323005098841079058 ) ) ;
#26451=CARTESIAN_POINT ( 'NONE',  ( 2.907497136250849934, 6.976431712756603787, 3.613027414876627041 ) ) ;
#26453=CARTESIAN_POINT ( 'NONE',  ( 5.516018279890452902, -0.001397286410094361001, 0.006629829924290971295 ) ) ;
#26455=CARTESIAN_POINT ( 'NONE',  ( 2.507146904658097419, 1.127530020444497572, 7.640248566386898865 ) ) ;
#26459=CARTESIAN_POINT ( 'NONE',  ( 0.2646305136544072623, 9.296005949277336811, -7.972778379581457742 ) ) ;
#26461=CARTESIAN_POINT ( 'NONE',  ( 0.2759803524722195811, 7.727919584673444753, 9.504501710971627659 ) ) ;
#26473=FACE_OUTER_BOUND ( 'NONE', #18985, .T. ) ;
#26478=CARTESIAN_POINT ( 'NONE',  ( 0.3665391374699464300, -10.50279796150432432, -6.368473106897240221 ) ) ;
#26479=CARTESIAN_POINT ( 'NONE',  ( 0.2655924914740778187, 11.52280271232876352, -4.147079829127140016 ) ) ;
#26485=EDGE_CURVE ( 'NONE', #20918, #28876, #14498, .T. ) ;
#26498=CARTESIAN_POINT ( 'NONE',  ( 0.7400311444011739015, 12.39937114182724009, -0.3548322008127505200 ) ) ;
#26501=LINE ( 'NONE', #27166, #11506 ) ;
#26505=B_SPLINE_CURVE_WITH_KNOTS ( 'NONE', 3,
 ( #17543, #12518, #21878, #32798, #7897, #38465, #7544, #2598, #38123, #28172, #48465, #6587, #43437 ),
 .UNSPECIFIED., .F., .F.,
 ( 4, 3, 3, 3, 4 ),
 ( 1.734723475976807094E-18, 6.607593386745461920E-05, 0.0001321518677373516206, 0.0001982171734706201550, 0.0002642860854759486629 ),
 .UNSPECIFIED. ) ;
#26515=EDGE_CURVE ( 'NONE', #16301, #41303, #1944, .T. ) ;
#26516=CARTESIAN_POINT ( 'NONE',  ( 2.245754705088401693, 4.822435078157734090, 5.920355780195118101 ) ) ;
#26521=CARTESIAN_POINT ( 'NONE',  ( 1.633930747250948112, -1.494486044209850428, 12.61425129500116604 ) ) ;
#26530=CARTESIAN_POINT ( 'NONE',  ( 0.2648978790185584908, 10.53870023327863770, 6.237101853238585569 ) ) ;
#26537=ADVANCED_FACE ( 'NONE', ( #58813 ), #33210, .F. ) ;
#26538=VERTEX_POINT ( 'NONE', #8239 ) ;
#26541=EDGE_LOOP ( 'NONE', ( #47503, #44418, #24958, #3836 ) ) ;
#26543=DIRECTION ( 'NONE',  ( 0.000000000000000000, 0.000000000000000000, 1.000000000000000000 ) ) ;
#26546=CARTESIAN_POINT ( 'NONE',  ( 2.969415267402681025, 7.867532449842534525, -0.3878973768010711698 ) ) ;
#26551=DIRECTION ( 'NONE',  ( 1.000000000000000000, 0.000000000000000000, 0.000000000000000000 ) ) ;
#26556=CARTESIAN_POINT ( 'NONE',  ( 0.5572780756291629833, 8.165890079445782490, -9.256402261579136592 ) ) ;
#26558=ORIENTED_EDGE ( 'NONE', *, *, #36975, .T. ) ;
#26563=CARTESIAN_POINT ( 'NONE',  ( 2.589278595513498704, 2.875840518181537409, 7.197074516942346456 ) ) ;
#26565=ORIENTED_EDGE ( 'NONE', *, *, #55697, .F. ) ;
#26574=CARTESIAN_POINT ( 'NONE',  ( 2.262775599885885391, 5.019217486250719062, -5.761998514039260222 ) ) ;
#26575=CARTESIAN_POINT ( 'NONE',  ( 0.2646305136544072623, -4.064188116014627816, 11.55263159009957441 ) ) ;
#26577=CARTESIAN_POINT ( 'NONE',  ( 1.452237505248552996, 5.807998527925892773, 11.24427360515644203 ) ) ;
#26586=CARTESIAN_POINT ( 'NONE',  ( 0.2652384770603652409, 0.06606665821615019529, -12.24598129987882444 ) ) ;
#26588=CARTESIAN_POINT ( 'NONE',  ( 0.2911222467163550598, -2.338869407810943990, 12.02952766044174382 ) ) ;
#26591=ADVANCED_FACE ( 'NONE', ( #59128 ), #12241, .T. ) ;
#26593=CARTESIAN_POINT ( 'NONE',  ( 5.514970785353741078, -0.004324946436530173639, -0.001897634820904526036 ) ) ;
#26596=ORIENTED_EDGE ( 'NONE', *, *, #41275, .F. ) ;
#26605=CARTESIAN_POINT ( 'NONE',  ( 0.2956976708475440585, 2.344604179391573062, -12.02996380804951748 ) ) ;
#26613=CARTESIAN_POINT ( 'NONE',  ( 1.109979610371588210, -5.843815872356387331, -11.08130463534545385 ) ) ;
#26629=ORIENTED_EDGE ( 'NONE', *, *, #9171, .T. ) ;
#26642=CARTESIAN_POINT ( 'NONE',  ( 2.261269890823172979, 7.131324074141454084, 2.744033622444998155 ) ) ;
#26643=ORIENTED_EDGE ( 'NONE', *, *, #24762, .F. ) ;
#26645=CARTESIAN_POINT ( 'NONE',  ( 0.2759803524722246881, 12.09509972435083291, -1.940323823244534562 ) ) ;
#26652=CARTESIAN_POINT ( 'NONE',  ( -14.47334165536099881, 5.400000000000000355, -1.000000000000000000 ) ) ;
#26662=CARTESIAN_POINT ( 'NONE',  ( 2.931247277082689173, -5.779735553870066767, -5.333206743525307658 ) ) ;
#26665=CARTESIAN_POINT ( 'NONE',  ( 2.969415267404787784, 7.525730903320808629, 2.326350273511627709 ) ) ;
#26666=CARTESIAN_POINT ( 'NONE',  ( 1.937114397841935398, 10.38782037574616801, 7.538912286488381298 ) ) ;
#26679=ORIENTED_EDGE ( 'NONE', *, *, #52132, .F. ) ;
#26685=B_SPLINE_CURVE_WITH_KNOTS ( 'NONE', 3,
 ( #14291, #44884, #25252, #50548, #56164, #24606, #19635, #9970, #10603, #39893, #4680, #45529, #65793, #24943, #40546, #45878 ),
 .UNSPECIFIED., .F., .F.,
 ( 4, 3, 3, 3, 3, 4 ),
 ( 2.328959703873127122E-15, 0.0002126834539179888047, 0.0004253519300366621859, 0.0006380165497224692985, 0.0007442707582428857976, 0.0009453531351414204203 ),
 .UNSPECIFIED. ) ;
#26688=EDGE_CURVE ( 'NONE', #56983, #14040, #30304, .T. ) ;
#26691=CARTESIAN_POINT ( 'NONE',  ( 2.903928887688508098, 0.5297564406061431308, 8.753847148605441220 ) ) ;
#26692=AXIS2_PLACEMENT_3D ( 'NONE', #63833, #12980, #48574 ) ;
#26695=CARTESIAN_POINT ( 'NONE',  ( 0.4613984246114870014, 4.475519447653987015, 11.46927345719238112 ) ) ;
#26698=EDGE_LOOP ( 'NONE', ( #54293, #35362, #34095, #50712 ) ) ;
#26699=CARTESIAN_POINT ( 'NONE',  ( -14.47334165536099881, 0.000000000000000000, 0.000000000000000000 ) ) ;
#26701=VECTOR ( 'NONE', #20927, 1000.000000000000114 ) ;
#26704=CARTESIAN_POINT ( 'NONE',  ( 5.530133899448235191, 0.01589823604557701053, -0.001661287012794096735 ) ) ;
#26705=CARTESIAN_POINT ( 'NONE',  ( 0.9296196016850856170, -9.278306863859519638, -8.327938962580805793 ) ) ;
#26707=AXIS2_PLACEMENT_3D ( 'NONE', #38986, #49333, #54304 ) ;
#26715=DIRECTION ( 'NONE',  ( -0.3865475372811021937, 0.2971585806051969536, -0.8730852074079709091 ) ) ;
#26727=CARTESIAN_POINT ( 'NONE',  ( 2.969415267405027148, -7.867532449843256614, 0.3878973768021006241 ) ) ;
#26730=B_SPLINE_CURVE_WITH_KNOTS ( 'NONE', 3,
 ( #306, #10254, #10922, #30534, #46497, #50837, #5283, #46188, #25555, #48162, #23194, #53473, #2617, #42459, #23528, #53793, #7569, #22880, #32492 ),
 .UNSPECIFIED., .F., .F.,
 ( 4, 3, 3, 3, 3, 3, 4 ),
 ( 8.523235939525396438E-18, 4.457896483014807333E-05, 6.639290541542042386E-05, 8.820687556478697556E-05, 0.0001100173248778895513, 0.0001545671401658104489, 0.0001830328308068584413 ),
 .UNSPECIFIED. ) ;
#26738=CARTESIAN_POINT ( 'NONE',  ( 2.241352910868909643, -4.970878533273721978, -5.794346703933896059 ) ) ;
#26740=CARTESIAN_POINT ( 'NONE',  ( 2.255723233588950549, -7.638048593862504454, -0.1321982600348033388 ) ) ;
#26743=CARTESIAN_POINT ( 'NONE',  ( 0.2767916011545386579, -12.02950149294535187, 2.313848297676409427 ) ) ;
#26746=CARTESIAN_POINT ( 'NONE',  ( 0.2648978790185584908, 12.03635331166812250, 2.256510822326184940 ) ) ;
#26756=ADVANCED_FACE ( 'NONE', ( #62359 ), #60381, .F. ) ;
#26767=CARTESIAN_POINT ( 'NONE',  ( 2.241526690369557873, 3.802233103835260586, -6.620271521148390903 ) ) ;
#26772=CARTESIAN_POINT ( 'NONE',  ( 0.2911222467163546712, -1.916522451062455668, -12.10399882413662276 ) ) ;
#26773=CARTESIAN_POINT ( 'NONE',  ( 2.844750968616420295, 1.031816958530457740, -7.767336242081033681 ) ) ;
#26774=CARTESIAN_POINT ( 'NONE',  ( 2.781367136452763678, -1.659348694504719335, -7.636197200465970170 ) ) ;
#26784=ORIENTED_EDGE ( 'NONE', *, *, #38652, .F. ) ;
#26785=EDGE_CURVE ( 'NONE', #28685, #7744, #18443, .T. ) ;
#26789=CARTESIAN_POINT ( 'NONE',  ( 0.2653141334712576516, -12.24612529725264665, 0.04405251235376458907 ) ) ;
#26792=EDGE_CURVE ( 'NONE', #32084, #44729, #569, .T. ) ;
#26797=CARTESIAN_POINT ( 'NONE',  ( 0.2653519991613825790, -7.888569541500585203, 9.366979519113323605 ) ) ;
#26802=CARTESIAN_POINT ( 'NONE',  ( 5.514970785353741078, -0.004713149585127531307, 0.0003039746380528782601 ) ) ;
#26803=ORIENTED_EDGE ( 'NONE', *, *, #38318, .T. ) ;
#26804=EDGE_CURVE ( 'NONE', #14742, #11008, #15221, .T. ) ;
#26805=ORIENTED_EDGE ( 'NONE', *, *, #57808, .F. ) ;
#26806=CARTESIAN_POINT ( 'NONE',  ( 2.241451721903216399, -0.06083185034801423530, 7.634225434981129155 ) ) ;
#26810=CARTESIAN_POINT ( 'NONE',  ( 0.7400311444011716810, -11.53023780418229904, 4.574267895796811700 ) ) ;
#26821=CARTESIAN_POINT ( 'NONE',  ( 2.491965175174103653, 7.560994562509278261, -1.548529392253994441 ) ) ;
#26826=CARTESIAN_POINT ( 'NONE',  ( 0.4613984246114869459, 12.17044190070617482, 1.858723191796512353 ) ) ;
#26829=CARTESIAN_POINT ( 'NONE',  ( 3.152665057734108878, -7.886634106564198277, 0.9030954876737806725 ) ) ;
#26836=CARTESIAN_POINT ( 'NONE',  ( 0.3675815128205894289, 0.2638082659428422350, 12.27743992903066328 ) ) ;
#26839=CARTESIAN_POINT ( 'NONE',  ( 2.258463476536645143, -3.937122681832530002, 6.547539277368021438 ) ) ;
#26844=VERTEX_POINT ( 'NONE', #48731 ) ;
#26849=CARTESIAN_POINT ( 'NONE',  ( 5.514624014163232779, 0.0008859786816846886709, 0.004045310349816156822 ) ) ;
#26850=CARTESIAN_POINT ( 'NONE',  ( 2.305787727787083519, 4.792270232040894307, 5.970480882365237996 ) ) ;
#26851=CARTESIAN_POINT ( 'NONE',  ( 2.268878695253352173, 1.472930498387372777, -7.500319319173564203 ) ) ;
#26855=CARTESIAN_POINT ( 'NONE',  ( 2.241534463349552198, -1.511811348926356884E-18, -7.634462073473343935 ) ) ;
#26862=CARTESIAN_POINT ( 'NONE',  ( 2.305787727787084407, -7.654065630109508689, 0.1666591538752418555 ) ) ;
#26863=ORIENTED_EDGE ( 'NONE', *, *, #39540, .T. ) ;
#26878=CARTESIAN_POINT ( 'NONE',  ( 0.3401186441510242742, 1.878666403202333246, 12.12646044229290254 ) ) ;
#26879=ORIENTED_EDGE ( 'NONE', *, *, #38104, .F. ) ;
#26884=CARTESIAN_POINT ( 'NONE',  ( 2.305787727787084407, 7.654065630109506913, -0.1666591538752953128 ) ) ;
#26887=CARTESIAN_POINT ( 'NONE',  ( 2.305787727787085295, 5.756228004061457959, 5.047606869483074910 ) ) ;
#26890=CARTESIAN_POINT ( 'NONE',  ( 0.4613984246114883891, -5.909164750631109797, 10.80075367333620662 ) ) ;
#26894=CARTESIAN_POINT ( 'NONE',  ( 0.9296196016855220456, 8.327938962581047377, -9.278306863859516085 ) ) ;
#26898=ORIENTED_EDGE ( 'NONE', *, *, #13488, .F. ) ;
#26900=CARTESIAN_POINT ( 'NONE',  ( 2.305787727787083519, 6.545285700970583598, -3.971363876083895850 ) ) ;
#26906=ORIENTED_EDGE ( 'NONE', *, *, #26985, .T. ) ;
#26912=CARTESIAN_POINT ( 'NONE',  ( 0.3057689695767474847, 4.409323295154205624, 11.43929056598607374 ) ) ;
#26921=ORIENTED_EDGE ( 'NONE', *, *, #57887, .F. ) ;
#26922=FACE_OUTER_BOUND ( 'NONE', #43189, .T. ) ;
#26925=CARTESIAN_POINT ( 'NONE',  ( 2.242418902652060453, 3.730710532462696349, -6.661183998168035636 ) ) ;
#26934=ORIENTED_EDGE ( 'NONE', *, *, #59826, .F. ) ;
#26935=LINE ( 'NONE', #1012, #49793 ) ;
#26939=CARTESIAN_POINT ( 'NONE',  ( 2.781367136451477151, 7.743208838465175603, 1.052455537429972221 ) ) ;
#26943=CARTESIAN_POINT ( 'NONE',  ( 0.3675815128205894289, 2.391755495700764289, -12.04510820461657161 ) ) ;
#26944=CARTESIAN_POINT ( 'NONE',  ( 1.948354844646954964, 2.783443994771086505, 11.63671644762409763 ) ) ;
#26946=VECTOR ( 'NONE', #49249, 999.9999999999997726 ) ;
#26958=CARTESIAN_POINT ( 'NONE',  ( 0.2648978790185619880, 2.256510822326142751, 12.03635331166812783 ) ) ;
#26985=EDGE_CURVE ( 'NONE', #64016, #11018, #17673, .T. ) ;
#26993=CARTESIAN_POINT ( 'NONE',  ( 5.516018279890452902, -0.006440244342253015342, -0.002104829434640740401 ) ) ;
#26994=DIRECTION ( 'NONE',  ( 0.000000000000000000, 0.000000000000000000, 1.000000000000000000 ) ) ;
#26996=CARTESIAN_POINT ( 'NONE',  ( 2.941278708680199916, 4.615461433467258345, 4.048809123187951720 ) ) ;
#27008=DIRECTION ( 'NONE',  ( 0.000000000000000000, 0.000000000000000000, 1.000000000000000000 ) ) ;
#27014=CARTESIAN_POINT ( 'NONE',  ( 2.903928887688490779, -8.407112942776166165, -2.496183838365682028 ) ) ;
#27029=CARTESIAN_POINT ( 'NONE',  ( 0.2646305136544072623, 4.312539723326133334, 11.46223899740601659 ) ) ;
#27030=CARTESIAN_POINT ( 'NONE',  ( 2.276905613633647629, -5.757134111949723021, 5.031956778294114585 ) ) ;
#27031=CARTESIAN_POINT ( 'NONE',  ( 2.990245332647882837, -8.465748356453849155, -0.5125330575220410356 ) ) ;
#27037=CARTESIAN_POINT ( 'NONE',  ( 1.375507693217084659, 10.61839108744976556, 6.813306181534342976 ) ) ;
#27038=CARTESIAN_POINT ( 'NONE',  ( 2.903928887688064009, -4.835706109686843668, -7.316175791236489090 ) ) ;
#27039=ORIENTED_EDGE ( 'NONE', *, *, #17299, .T. ) ;
#27042=AXIS2_PLACEMENT_3D ( 'NONE', #65617, #35692, #20090 ) ;
#27044=ORIENTED_EDGE ( 'NONE', *, *, #36104, .F. ) ;
#27047=EDGE_CURVE ( 'NONE', #49890, #12885, #5787, .T. ) ;
#27058=CARTESIAN_POINT ( 'NONE',  ( 2.844750968616406972, -7.828506085988760077, 0.3326424433134245739 ) ) ;
#27065=CARTESIAN_POINT ( 'NONE',  ( 0.2653519890518152291, 9.381125756446678565, -7.871710682401816150 ) ) ;
#27066=ORIENTED_EDGE ( 'NONE', *, *, #50713, .T. ) ;
#27068=B_SPLINE_CURVE_WITH_KNOTS ( 'NONE', 3,
 ( #7225, #2615, #43128, #57802, #22541, #63730, #18210, #42806, #37828, #12878, #48157, #58119, #13214, #53121, #13520, #63407 ),
 .UNSPECIFIED., .F., .F.,
 ( 4, 3, 3, 3, 3, 4 ),
 ( 0.000000000000000000, 0.0002999043160757327328, 0.0005998071753050931943, 0.0008997092107374458870, 0.001204458948195583296, 0.001510329163476397491 ),
 .UNSPECIFIED. ) ;
#27069=CARTESIAN_POINT ( 'NONE',  ( 2.241528039335007438, -4.895273998033963458, -5.858435878248560158 ) ) ;
#27070=CARTESIAN_POINT ( 'NONE',  ( 0.8375941296792150936, -4.612912274495883480, 11.54987202580252159 ) ) ;
#27077=CARTESIAN_POINT ( 'NONE',  ( 2.770579946183330033, 7.633739187313475227, 1.653873933978900146 ) ) ;
#27088=ADVANCED_FACE ( 'NONE', ( #60999 ), #23910, .F. ) ;
#27090=DIRECTION ( 'NONE',  ( -0.3865475372811021937, -0.8082200352954586053, -0.4442537292684469175 ) ) ;
#27091=B_SPLINE_CURVE_WITH_KNOTS ( 'NONE', 3,
 ( #11931, #52195, #1968, #48201, #32210, #1328, #6643, #52835, #6960, #27895 ),
 .UNSPECIFIED., .F., .F.,
 ( 4, 3, 3, 4 ),
 ( 1.301042606982605321E-18, 6.607638129004494304E-05, 9.911389841680519547E-05, 0.0001667630577588623654 ),
 .UNSPECIFIED. ) ;
#27095=CARTESIAN_POINT ( 'NONE',  ( 2.305787727787084407, 7.566723232958072032, 1.164987321564758371 ) ) ;
#27097=CARTESIAN_POINT ( 'NONE',  ( 1.452237505248555660, -9.303501428256085504, 8.579708443906715942 ) ) ;
#27105=CARTESIAN_POINT ( 'NONE',  ( 0.2956976708475456128, -1.911282699793644735, -12.10637007622315053 ) ) ;
#27115=CARTESIAN_POINT ( 'NONE',  ( 0.2911222467163567806, 9.248441845564686403, 8.040284153519408505 ) ) ;
#27117=VERTEX_POINT ( 'NONE', #801 ) ;
#27118=CARTESIAN_POINT ( 'NONE',  ( 0.2647959493198558945, 2.271080632828060608, 12.03358727341674950 ) ) ;
#27121=ORIENTED_EDGE ( 'NONE', *, *, #9915, .F. ) ;
#27128=CARTESIAN_POINT ( 'NONE',  ( 5.516018279890452902, 0.006771744149385265123, -0.0002248006052448750405 ) ) ;
#27131=DIRECTION ( 'NONE',  ( 0.000000000000000000, 0.000000000000000000, 1.000000000000000000 ) ) ;
#27132=CARTESIAN_POINT ( 'NONE',  ( 0.5547464869798237608, 11.69908463509556995, 3.933612953276277580 ) ) ;
#27141=CARTESIAN_POINT ( 'NONE',  ( 1.459561108993333134, -11.65083230253660140, 4.912799202119202846 ) ) ;
#27144=CARTESIAN_POINT ( 'NONE',  ( 5.514970785353741078, 0.001117786416802554229, 0.004588761610585028947 ) ) ;
#27145=EDGE_LOOP ( 'NONE', ( #46577, #21072, #62069, #32466 ) ) ;
#27148=CARTESIAN_POINT ( 'NONE',  ( 2.273267844204865273, 5.758000272829378652, -5.029122824445665607 ) ) ;
#27149=ORIENTED_EDGE ( 'NONE', *, *, #11007, .F. ) ;
#27151=CARTESIAN_POINT ( 'NONE',  ( 3.152665057736161902, 7.719888720907650992, -1.848755561854025231 ) ) ;
#27154=B_SPLINE_CURVE_WITH_KNOTS ( 'NONE', 3,
 ( #52848, #41215, #57194, #56536, #10979, #6015, #51879, #11619, #6656, #1673, #21941, #42188, #62478, #16942, #37209, #57524, #32227, #3303, #43850, #59467, #48852, #22930 ),
 .UNSPECIFIED., .F., .F.,
 ( 4, 3, 3, 3, 3, 3, 3, 4 ),
 ( 1.084202172485504434E-19, 4.449119708436884238E-05, 6.626296329540428309E-05, 8.803456484962676601E-05, 0.0001098060367612800945, 0.0001315774408628517765, 0.0001760698110411190547, 0.0001829697163287842695 ),
 .UNSPECIFIED. ) ;
#27161=EDGE_CURVE ( 'NONE', #20299, #5276, #56321, .T. ) ;
#27166=CARTESIAN_POINT ( 'NONE',  ( 2.889800649504073782, 3.882893708502047847, 4.732281052280325362 ) ) ;
#27169=ORIENTED_EDGE ( 'NONE', *, *, #27217, .F. ) ;
#27170=B_SPLINE_CURVE_WITH_KNOTS ( 'NONE', 3,
 ( #63840, #54214, #59208, #2028, #63195, #43558, #47579, #18322, #64187, #12987, #33269, #18659, #53574, #8020, #7325, #28282, #38919, #12319, #17661 ),
 .UNSPECIFIED., .F., .F.,
 ( 4, 3, 3, 3, 3, 3, 4 ),
 ( 0.000000000000000000, 2.831840207499574684E-05, 4.217266859840548322E-05, 5.602024318395963231E-05, 6.290810167969062899E-05, 9.120440630945090394E-05, 0.0001153103026479756018 ),
 .UNSPECIFIED. ) ;
#27174=( BOUNDED_SURFACE ( )  B_SPLINE_SURFACE ( 3, 1, ( 
 ( #56372, #52390 ),
 ( #21804, #42053 ),
 ( #20804, #22105 ),
 ( #31108, #62333 ) ),
 .UNSPECIFIED., .F., .F., .F. ) 
 B_SPLINE_SURFACE_WITH_KNOTS ( ( 4, 4 ),
 ( 2, 2 ),
 ( 0.000000000000000000, 1.000000000000000000 ),
 ( 0.000000000000000000, 1.000000000000000000 ),
 .UNSPECIFIED. ) 
 GEOMETRIC_REPRESENTATION_ITEM ( )  RATIONAL_B_SPLINE_SURFACE ( (
 ( 1.000000000000000000, 1.000000000000000000),
 ( 0.9942764183789327692, 0.8450855930916585379),
 ( 0.9942764183789327692, 0.8450855930916585379),
 ( 1.000000000000000000, 1.000000000000000000) ) ) 
 REPRESENTATION_ITEM ( '' )  SURFACE ( )  );
#27180=VERTEX_POINT ( 'NONE', #45362 ) ;
#27181=CARTESIAN_POINT ( 'NONE',  ( 0.3057689695767483173, 12.11137787899271956, 1.901059295890957790 ) ) ;
#27183=CARTESIAN_POINT ( 'NONE',  ( 0.2651627682582903822, -10.64925413290589695, -6.046625184671096775 ) ) ;
#27185=CIRCLE ( 'NONE', #9143, 7.938172270156617749 ) ;
#27189=( BOUNDED_SURFACE ( )  B_SPLINE_SURFACE ( 3, 1, ( 
 ( #10213, #5921 ),
 ( #30492, #55110 ),
 ( #35486, #26177 ),
 ( #20533, #41118 ) ),
 .UNSPECIFIED., .F., .F., .F. ) 
 B_SPLINE_SURFACE_WITH_KNOTS ( ( 4, 4 ),
 ( 2, 2 ),
 ( 0.000000000000000000, 1.000000000000000000 ),
 ( 0.000000000000000000, 1.000000000000000000 ),
 .UNSPECIFIED. ) 
 GEOMETRIC_REPRESENTATION_ITEM ( )  RATIONAL_B_SPLINE_SURFACE ( (
 ( 1.000000000000000000, 1.000000000000000000),
 ( 0.9942764183789327692, 0.8450855930916580938),
 ( 0.9942764183789327692, 0.8450855930916580938),
 ( 1.000000000000000000, 1.000000000000000000) ) ) 
 REPRESENTATION_ITEM ( '' )  SURFACE ( )  );
#27196=CARTESIAN_POINT ( 'NONE',  ( 1.549075743843500552, 12.65619669350982157, 0.6747257554039380878 ) ) ;
#27205=CARTESIAN_POINT ( 'NONE',  ( 2.889800649504073782, 2.030191121417214806, -5.774917447012977156 ) ) ;
#27208=CARTESIAN_POINT ( 'NONE',  ( 2.290907136834313906, 5.755317856506293239, 5.041121061900457612 ) ) ;
#27214=B_SPLINE_CURVE_WITH_KNOTS ( 'NONE', 3,
 ( #48459, #52780, #7206, #63076, #2906, #21873, #12202, #43432, #47788, #53445, #62734, #57441, #53100, #17853, #63709, #42121, #11871, #37475, #63386, #12855, #38458, #22178 ),
 .UNSPECIFIED., .F., .F.,
 ( 4, 3, 3, 3, 3, 3, 3, 4 ),
 ( 8.824766327896537836E-19, 4.449119708436589471E-05, 6.626296329540048839E-05, 8.803456484962241565E-05, 0.0001098060367612772349, 0.0001315774408628484155, 0.0001760698110411148263, 0.0001829697163287826974 ),
 .UNSPECIFIED. ) ;
#27217=EDGE_CURVE ( 'NONE', #19899, #62456, #8129, .T. ) ;
#27230=ORIENTED_EDGE ( 'NONE', *, *, #63552, .F. ) ;
#27231=CARTESIAN_POINT ( 'NONE',  ( 0.2739690278137258961, 4.360944092821455342, 11.44648082006007961 ) ) ;
#27235=CARTESIAN_POINT ( 'NONE',  ( 2.262775599886257094, 2.745802076335829067, -7.131180968652195418 ) ) ;
#27246=CARTESIAN_POINT ( 'NONE',  ( -14.47334165536100059, 7.347880794884120722E-16, 6.000000000000000888 ) ) ;
#27247=CARTESIAN_POINT ( 'NONE',  ( 0.2706063244538013945, -2.299194104693162544, 12.03021891034990887 ) ) ;
#27253=ORIENTED_EDGE ( 'NONE', *, *, #20663, .T. ) ;
#27255=CARTESIAN_POINT ( 'NONE',  ( 0.3040950598368144520, -4.428852722102808670, 11.43390362554251816 ) ) ;
#27257=CARTESIAN_POINT ( 'NONE',  ( 2.665405856346781732, 9.171500569027793759, -2.723742051529362662 ) ) ;
#27259=CARTESIAN_POINT ( 'NONE',  ( 2.261269890822073414, -6.685978463722149101, 3.699080366006672449 ) ) ;
#27264=CARTESIAN_POINT ( 'NONE',  ( 0.2652384770603652409, -2.061429379240400372, -12.07140968216696031 ) ) ;
#27268=UNCERTAINTY_MEASURE_WITH_UNIT (LENGTH_MEASURE( 1.000000000000000082E-05 ), #60094, 'distance_accuracy_value', 'NONE');
#27269=CARTESIAN_POINT ( 'NONE',  ( 2.305787727787084407, -0.1666591538752151269, -7.654065630109508689 ) ) ;
#27278=CARTESIAN_POINT ( 'NONE',  ( 0.3223008802179258558, -1.888629463821764887, 12.11889957318023114 ) ) ;
#27279=ORIENTED_EDGE ( 'NONE', *, *, #40054, .F. ) ;
#27281=ORIENTED_EDGE ( 'NONE', *, *, #39196, .T. ) ;
#27282=DIRECTION ( 'NONE',  ( -0.3939253465568944290, -0.8008152550167534356, -0.4511294145502848241 ) ) ;
#27284=B_SPLINE_CURVE_WITH_KNOTS ( 'NONE', 3,
 ( #21751, #46671, #21060, #1127, #42002, #62282, #36017, #16736, #47657, #37009, #57313, #11735, #46354, #52664, #32020, #2104 ),
 .UNSPECIFIED., .F., .F.,
 ( 4, 3, 3, 3, 3, 4 ),
 ( 0.000000000000000000, 0.0003017745587525239460, 0.0006035491769808734152, 0.0009053241094668162481, 0.001207275924540911769, 0.001510325902534833840 ),
 .UNSPECIFIED. ) ;
#27285=DIRECTION ( 'NONE',  ( -1.000000000000000000, -0.000000000000000000, -0.000000000000000000 ) ) ;
#27290=CARTESIAN_POINT ( 'NONE',  ( 0.2653141334712578736, 11.49252672845888945, -4.229817350136297449 ) ) ;
#27294=FACE_OUTER_BOUND ( 'NONE', #39153, .T. ) ;
#27300=CARTESIAN_POINT ( 'NONE',  ( 2.241506898688419014, -6.591904579673256492, 3.851253041557081591 ) ) ;
#27302=DIRECTION ( 'NONE',  ( 0.000000000000000000, 0.000000000000000000, 1.000000000000000000 ) ) ;
#27307=CARTESIAN_POINT ( 'NONE',  ( 0.2759803524722185264, -4.367180139677396156, 11.44482553421629589 ) ) ;
#27309=CARTESIAN_POINT ( 'NONE',  ( 3.152665057735933640, -5.461013642407022139, -5.761241965768077122 ) ) ;
#27313=CARTESIAN_POINT ( 'NONE',  ( 0.2767916011545383248, 12.02950149294536786, -2.313848297676325050 ) ) ;
#27323=CARTESIAN_POINT ( 'NONE',  ( 3.100650473569670940, -6.348250400753888023, 4.737096019059257479 ) ) ;
#27328=ADVANCED_FACE ( 'NONE', ( #59948 ), #14536, .F. ) ;
#27332=EDGE_CURVE ( 'NONE', #59842, #1422, #8094, .T. ) ;
#27351=ORIENTED_EDGE ( 'NONE', *, *, #24074, .F. ) ;
#27359=ORIENTED_EDGE ( 'NONE', *, *, #33573, .F. ) ;
#27366=CARTESIAN_POINT ( 'NONE',  ( 0.2958664285830415186, -7.708042451272235418, 9.529149585189916394 ) ) ;
#27377=CARTESIAN_POINT ( 'NONE',  ( 2.251139882113957658, -7.636654603229077409, -0.1241612276497447015 ) ) ;
#27382=CARTESIAN_POINT ( 'NONE',  ( 0.3675815128205894289, -6.367184624550092487, -10.50067073900658521 ) ) ;
#27384=B_SPLINE_CURVE_WITH_KNOTS ( 'NONE', 3,
 ( #11250, #51513, #12534, #58120, #31520, #1619, #62120 ),
 .UNSPECIFIED., .F., .F.,
 ( 4, 3, 4 ),
 ( 5.504479493880105401E-15, 0.002398160485434731350, 0.005002426799382268634 ),
 .UNSPECIFIED. ) ;
#27385=VERTEX_POINT ( 'NONE', #44612 ) ;
#27387=CARTESIAN_POINT ( 'NONE',  ( 2.835339799623982415, 7.649567297875990768, 1.682641786445466803 ) ) ;
#27393=DIRECTION ( 'NONE',  ( -0.3865475372811021937, -0.5778504531711091685, 0.7187975063895662986 ) ) ;
#27408=B_SPLINE_CURVE_WITH_KNOTS ( 'NONE', 3,
 ( #51258, #40599, #35273, #19685, #10020, #35913, #44932 ),
 .UNSPECIFIED., .F., .F.,
 ( 4, 3, 4 ),
 ( 4.941165900048787626E-15, 0.002398160485434632904, 0.005002426799381740410 ),
 .UNSPECIFIED. ) ;
#27442=CARTESIAN_POINT ( 'NONE',  ( 0.3675815128205894289, 5.910255304480445560, 10.76447900494942367 ) ) ;
#27447=ORIENTED_EDGE ( 'NONE', *, *, #54296, .T. ) ;
#27448=CARTESIAN_POINT ( 'NONE',  ( 2.241534463349551753, 9.451863027432619807E-16, 7.634462073473348376 ) ) ;
#27453=CARTESIAN_POINT ( 'NONE',  ( 2.665405856346791946, -5.696318245876772934, -7.686816759402922195 ) ) ;
#27460=ORIENTED_EDGE ( 'NONE', *, *, #28990, .T. ) ;
#27465=CARTESIAN_POINT ( 'NONE',  ( 2.241509619876138171, 1.363398699156149307, -7.511759925807389493 ) ) ;
#27473=CARTESIAN_POINT ( 'NONE',  ( 2.241311220309555097, 7.501736494813745715, 1.417008678104511255 ) ) ;
#27478=CARTESIAN_POINT ( 'NONE',  ( 0.2648978790185593790, -6.237101853238620208, 10.53870023327861283 ) ) ;
#27480=CARTESIAN_POINT ( 'NONE',  ( 2.305787727787083519, -2.774453000917102230, -7.135468203930011910 ) ) ;
#27494=CARTESIAN_POINT ( 'NONE',  ( 1.014383007554947813, -9.851867765302131374, -7.686901933424256761 ) ) ;
#27495=CARTESIAN_POINT ( 'NONE',  ( 3.031336079629759261, -5.388626255827020373, -5.773872239512848559 ) ) ;
#27497=CARTESIAN_POINT ( 'NONE',  ( 3.152665057734128862, 2.258875078502223133, 7.609997527621164437 ) ) ;
#27499=CARTESIAN_POINT ( 'NONE',  ( 0.2650492594609232810, -10.54996119777441344, -6.218173512054875118 ) ) ;
#27504=EDGE_LOOP ( 'NONE', ( #40861, #22581, #9579, #54000 ) ) ;
#27515=CARTESIAN_POINT ( 'NONE',  ( 5.520433897694421610, 0.002108682515300278320, 0.01491416502703811486 ) ) ;
#27521=CARTESIAN_POINT ( 'NONE',  ( 2.241534463349552198, -1.511811348926356884E-18, -7.634462073473343935 ) ) ;
#27524=B_SPLINE_CURVE_WITH_KNOTS ( 'NONE', 3,
 ( #55825, #60466, #15245, #35183, #49848, #10573, #30853, #9580, #65447, #61136, #30219, #51173, #44852 ),
 .UNSPECIFIED., .F., .F.,
 ( 4, 3, 3, 3, 4 ),
 ( 2.737610485525898696E-18, 6.607593386745464631E-05, 0.0001321518677373517562, 0.0001982171734706201821, 0.0002642860854759486629 ),
 .UNSPECIFIED. ) ;
#27525=CARTESIAN_POINT ( 'NONE',  ( 2.273267844204866606, 7.553702825375864904, 1.178226273332969365 ) ) ;
#27526=CARTESIAN_POINT ( 'NONE',  ( 0.3675815128205912052, 12.13672785388552811, -1.872154644481959895 ) ) ;
#27529=DIRECTION ( 'NONE',  ( 0.000000000000000000, 0.000000000000000000, 1.000000000000000000 ) ) ;
#27530=VERTEX_POINT ( 'NONE', #6628 ) ;
#27543=VERTEX_POINT ( 'NONE', #42162 ) ;
#27565=CARTESIAN_POINT ( 'NONE',  ( 0.3106921474978454611, -2.360654586927870557, 12.03191800497307717 ) ) ;
#27570=ORIENTED_EDGE ( 'NONE', *, *, #32455, .T. ) ;
#27572=B_SPLINE_CURVE_WITH_KNOTS ( 'NONE', 3,
 ( #25176, #60762, #8909, #29198, #35479, #60105, #14523, #29501, #9216, #55443, #50473, #49804, #4252, #65081, #29826, #19554 ),
 .UNSPECIFIED., .F., .F.,
 ( 4, 3, 3, 3, 3, 4 ),
 ( 0.000000000000000000, 0.0002176109881720242410, 0.0004352086762394595824, 0.0006528017811446875079, 0.0007615147961451692411, 0.0009453342004945818056 ),
 .UNSPECIFIED. ) ;
#27575=CARTESIAN_POINT ( 'NONE',  ( 2.253265082352431836, 5.932955906470575691, -4.810902415501073115 ) ) ;
#27578=CARTESIAN_POINT ( 'NONE',  ( 2.368238019614957501, 7.589221137922601557, 1.155661230551840113 ) ) ;
#27581=CARTESIAN_POINT ( 'NONE',  ( 1.719304012338199517, 0.000000000000000000, 0.000000000000000000 ) ) ;
#27582=FACE_OUTER_BOUND ( 'NONE', #31709, .T. ) ;
#27588=CARTESIAN_POINT ( 'NONE',  ( 0.2646305136544072623, -9.296005949277279967, 7.972778379581522579 ) ) ;
#27604=CARTESIAN_POINT ( 'NONE',  ( 2.262775599886256650, 7.227769107232081325, -2.480428346600461520 ) ) ;
#27615=CARTESIAN_POINT ( 'NONE',  ( 2.284126774969132523, 7.131638985093474048, 2.764365694978749399 ) ) ;
#27618=CARTESIAN_POINT ( 'NONE',  ( 0.3278977287071230817, 12.12129679591850540, -1.885359334311841772 ) ) ;
#27623=CARTESIAN_POINT ( 'NONE',  ( 2.259830038565000088, 3.700395974956140144, 6.684701880279339647 ) ) ;
#27629=CARTESIAN_POINT ( 'NONE',  ( 5.516018279890452902, -0.003191189039764880282, -0.005976902763919027944 ) ) ;
#27643=ORIENTED_EDGE ( 'NONE', *, *, #17818, .T. ) ;
#27652=EDGE_LOOP ( 'NONE', ( #26345, #44301, #57745, #17021 ) ) ;
#27653=CARTESIAN_POINT ( 'NONE',  ( 0.2648321136542706733, -12.03456865502704254, -2.265911310221937036 ) ) ;
#27656=CARTESIAN_POINT ( 'NONE',  ( 2.899286259009685729, -7.664525129300148620, -1.713434346771303574 ) ) ;
#27661=CARTESIAN_POINT ( 'NONE',  ( 0.5547464869798223175, 4.506704303875454620, 11.49049644196204945 ) ) ;
#27666=CARTESIAN_POINT ( 'NONE',  ( 2.259830038564998311, -0.1377140217659723054, 7.639319632525574555 ) ) ;
#27679=ORIENTED_EDGE ( 'NONE', *, *, #43605, .F. ) ;
#27680=VECTOR ( 'NONE', #2391, 999.9999999999998863 ) ;
#27684=CARTESIAN_POINT ( 'NONE',  ( 2.241317068080777020, -7.142175514530106462, 2.696905536171270601 ) ) ;
#27693=CARTESIAN_POINT ( 'NONE',  ( -14.47334165536099881, 0.000000000000000000, 4.000000000000000000 ) ) ;
#27704=CARTESIAN_POINT ( 'NONE',  ( 2.241506898688419014, 7.160521809579532437, -2.648071636522661088 ) ) ;
#27709=CARTESIAN_POINT ( 'NONE',  ( 2.406456491626409733, -10.36527681095989095, -1.188938370543056733 ) ) ;
#27711=ADVANCED_FACE ( 'NONE', ( #19202 ), #37256, .T. ) ;
#27715=CARTESIAN_POINT ( 'NONE',  ( 2.639814597422736053, 7.600559958731745169, 1.600543348184837456 ) ) ;
#27722=B_SPLINE_CURVE_WITH_KNOTS ( 'NONE', 3,
 ( #12205, #7209, #27495, #32796, #39431, #49752, #64689, #3232, #29152, #38795, #33786, #48463, #60059, #23503, #3576, #14477 ),
 .UNSPECIFIED., .F., .F.,
 ( 4, 3, 3, 3, 3, 4 ),
 ( 2.959248127215453983E-15, 0.0002126834539179688283, 0.0004253519300366227210, 0.0006380165497224124863, 0.0007442707582428192276, 0.0009453531351419241406 ),
 .UNSPECIFIED. ) ;
#27727=CARTESIAN_POINT ( 'NONE',  ( 5.516018279890452902, -0.001397286410094463784, -0.006629829924290467358 ) ) ;
#27730=B_SPLINE_CURVE_WITH_KNOTS ( 'NONE', 3,
 ( #29604, #9017, #39599, #49284, #64850, #4035, #3738, #65501, #14320, #49911, #44255, #30280, #19664, #50251, #50580, #44914 ),
 .UNSPECIFIED., .F., .F.,
 ( 4, 3, 3, 3, 3, 4 ),
 ( 5.421010862427522170E-19, 0.0003017745587525216691, 0.0006035491769808687531, 0.0009053241094668072492, 0.001207275924539389766, 0.001510325902531777474 ),
 .UNSPECIFIED. ) ;
#27742=FACE_OUTER_BOUND ( 'NONE', #45134, .T. ) ;
#27745=CARTESIAN_POINT ( 'NONE',  ( 5.516018279890452902, 0.005752102158673841684, -0.003580555109620817654 ) ) ;
#27762=CARTESIAN_POINT ( 'NONE',  ( 0.3057689695767498717, 2.355923806019203148, 12.03117299329036882 ) ) ;
#27764=ADVANCED_FACE ( 'NONE', ( #34160 ), #3132, .F. ) ;
#27770=ORIENTED_EDGE ( 'NONE', *, *, #3078, .T. ) ;
#27779=CARTESIAN_POINT ( 'NONE',  ( 1.104777566491146334, 0.4777483965053739290, 12.51694124543052311 ) ) ;
#27781=CARTESIAN_POINT ( 'NONE',  ( 1.020182472824380682, 4.691131056023482238, -11.58401323226494561 ) ) ;
#27782=EDGE_CURVE ( 'NONE', #21481, #43133, #3927, .T. ) ;
#27786=VERTEX_POINT ( 'NONE', #64732 ) ;
#27792=CARTESIAN_POINT ( 'NONE',  ( 2.491965175174554847, 1.548529392254221593, 7.560994562509386618 ) ) ;
#27808=FACE_OUTER_BOUND ( 'NONE', #2316, .T. ) ;
#27812=CARTESIAN_POINT ( 'NONE',  ( 0.3665391374699465965, 3.952034409876454824, -11.62960183138723025 ) ) ;
#27814=VECTOR ( 'NONE', #22032, 1000.000000000000227 ) ;
#27836=CARTESIAN_POINT ( 'NONE',  ( 0.3474126878361820658, 12.12932967384299410, 1.876013288000094148 ) ) ;
#27847=CARTESIAN_POINT ( 'NONE',  ( 0.2646305136544072623, 2.256625640822315759, 12.03696649559615572 ) ) ;
#27856=EDGE_CURVE ( 'NONE', #16341, #27385, #43673, .T. ) ;
#27857=CARTESIAN_POINT ( 'NONE',  ( 0.2647959493198566161, -11.45640103018461531, 4.326188315749694091 ) ) ;
#27862=CARTESIAN_POINT ( 'NONE',  ( 0.9232058338315058954, -12.46548196349786508, 0.3773051331667549579 ) ) ;
#27865=CARTESIAN_POINT ( 'NONE',  ( 2.994568964204213035, 7.537093683963823842, -2.317954327151149574 ) ) ;
#27873=CARTESIAN_POINT ( 'NONE',  ( 1.719304012338701115, -5.690355757827699534, 11.38834240361771677 ) ) ;
#27875=MECHANICAL_DESIGN_GEOMETRIC_PRESENTATION_REPRESENTATION('',(#19389),#13019);
#27877=DIRECTION ( 'NONE',  ( 0.000000000000000000, 0.000000000000000000, 1.000000000000000000 ) ) ;
#27888=ORIENTED_EDGE ( 'NONE', *, *, #3391, .F. ) ;
#27895=CARTESIAN_POINT ( 'NONE',  ( 2.241352910868909643, -7.202080440908757986, 2.532612177304417678 ) ) ;
#27901=CARTESIAN_POINT ( 'NONE',  ( 0.2915757698887260774, 11.58754481235186340, 3.989025639548677393 ) ) ;
#27905=CARTESIAN_POINT ( 'NONE',  ( 2.263328370262049916, 3.697218830763628450, -6.687792802427183325 ) ) ;
#27910=CARTESIAN_POINT ( 'NONE',  ( 2.556980015513853122, -4.067895092073517738, -6.584367695372261409 ) ) ;
#27913=CARTESIAN_POINT ( 'NONE',  ( 0.8375941296788397272, 5.882592429484509111, 10.95781044612375688 ) ) ;
#27918=ADVANCED_FACE ( 'NONE', ( #52087 ), #28545, .F. ) ;
#27920=CARTESIAN_POINT ( 'NONE',  ( 5.520433897694421610, 0.01006947824912422969, -0.01120198501134839035 ) ) ;
#27923=CARTESIAN_POINT ( 'NONE',  ( 0.2653141334712562083, 9.409392642815744168, 7.837911425448813141 ) ) ;
#27927=CARTESIAN_POINT ( 'NONE',  ( 0.9232167919969077596, 10.58277433962390113, -6.587352952801042605 ) ) ;
#27929=CARTESIAN_POINT ( 'NONE',  ( 0.2653141617321010948, -2.083144498805191258, -12.06772699408310778 ) ) ;
#27933=CIRCLE ( 'NONE', #5641, 7.938172270156617749 ) ;
#27934=CARTESIAN_POINT ( 'NONE',  ( 0.2646305136544072623, -9.465888453933013480, 7.770320294339146727 ) ) ;
#27935=CARTESIAN_POINT ( 'NONE',  ( 1.547277799339149329, -8.651049845884454470, -9.261681528764416527 ) ) ;
#27936=CARTESIAN_POINT ( 'NONE',  ( 2.251152103363646795, -3.926807817126149125, -6.550893877460189252 ) ) ;
#27947=CARTESIAN_POINT ( 'NONE',  ( 3.152665057734040488, 0.000000000000000000, 0.000000000000000000 ) ) ;
#27962=VERTEX_POINT ( 'NONE', #31473 ) ;
#27965=CARTESIAN_POINT ( 'NONE',  ( 2.247112776671467138, -2.720990995225260445, -7.135103076758478657 ) ) ;
#27968=VECTOR ( 'NONE', #19971, 1000.000000000000000 ) ;
#27970=CARTESIAN_POINT ( 'NONE',  ( 2.261269890822072970, 2.481875047312938065, 7.226741992146798133 ) ) ;
#27974=CONICAL_SURFACE ( 'NONE', #34312, 7.938172270156617749, 1.280189991382167047 ) ;
#27977=B_SPLINE_CURVE_WITH_KNOTS ( 'NONE', 3,
 ( #6284, #51188, #62132, #61794, #20593, #314, #51836 ),
 .UNSPECIFIED., .F., .F.,
 ( 4, 3, 4 ),
 ( 6.158474197255674489E-15, 0.002398160485434825892, 0.005002426799382968595 ),
 .UNSPECIFIED. ) ;
#27981=FACE_OUTER_BOUND ( 'NONE', #9966, .T. ) ;
#27993=CARTESIAN_POINT ( 'NONE',  ( 0.3654063281920725270, 6.366443614636685844, 10.50027211615249456 ) ) ;
#27994=CARTESIAN_POINT ( 'NONE',  ( 0.2834382757448005719, -2.326926314863231759, -12.02923522794684885 ) ) ;
#27998=CARTESIAN_POINT ( 'NONE',  ( 2.717984159220037110, -6.886544461123986771, -3.648459810929770786 ) ) ;
#28002=CARTESIAN_POINT ( 'NONE',  ( 5.514970785353741078, 0.001326349372336578557, 0.004532877335078321253 ) ) ;
#28009=CARTESIAN_POINT ( 'NONE',  ( 5.516018279890452902, -0.004525000489649900863, 0.005042957932159117078 ) ) ;
#28010=VECTOR ( 'NONE', #10021, 1000.000000000000227 ) ;
#28017=CARTESIAN_POINT ( 'NONE',  ( 1.937114397841932290, 10.38782037574626926, -7.538912286488240966 ) ) ;
#28020=CARTESIAN_POINT ( 'NONE',  ( 2.639814597422744047, 5.186391178752210784, -5.782006333156018307 ) ) ;
#28024=CARTESIAN_POINT ( 'NONE',  ( 2.305787727787084407, -0.1666591538753222634, 7.654065630109506024 ) ) ;
#28025=ORIENTED_EDGE ( 'NONE', *, *, #62981, .T. ) ;
#28031=CARTESIAN_POINT ( 'NONE',  ( 2.290907136834313018, 6.543263131934393684, 3.965134647956439551 ) ) ;
#28037=CARTESIAN_POINT ( 'NONE',  ( 2.257661810676418579, -7.131864446283245229, 2.739276463085656310 ) ) ;
#28038=ORIENTED_EDGE ( 'NONE', *, *, #52547, .F. ) ;
#28040=CARTESIAN_POINT ( 'NONE',  ( 2.827825597296700799, 9.007857251166790036, 0.5449445831287562658 ) ) ;
#28046=CARTESIAN_POINT ( 'NONE',  ( 2.244591118396559448, -1.431619869711802329, -7.500068934084580974 ) ) ;
#28049=CARTESIAN_POINT ( 'NONE',  ( 5.516018279890452902, -0.006771744149385265123, 0.0002248006052448276067 ) ) ;
#28051=VECTOR ( 'NONE', #31131, 1000.000000000000114 ) ;
#28056=CARTESIAN_POINT ( 'NONE',  ( 2.827825597296799831, 2.568788224597768455, 8.650999012440202307 ) ) ;
#28060=CARTESIAN_POINT ( 'NONE',  ( 0.3654063281920773565, -3.951404032559346025, 11.62642356802260757 ) ) ;
#28062=CARTESIAN_POINT ( 'NONE',  ( 0.3006302518452043104, 9.533790235540747560, 7.704827863860824522 ) ) ;
#28065=VERTEX_POINT ( 'NONE', #53065 ) ;
#28066=CARTESIAN_POINT ( 'NONE',  ( 0.9232058338315048962, -12.34162163148534930, 1.793035206307305174 ) ) ;
#28073=CARTESIAN_POINT ( 'NONE',  ( 0.3164563675027582401, -10.49799587805935097, 6.338687639235996762 ) ) ;
#28076=CARTESIAN_POINT ( 'NONE',  ( 1.937114397841935398, 12.33981801388257793, 3.531416430611335144 ) ) ;
#28083=CARTESIAN_POINT ( 'NONE',  ( 0.3040950598368144520, 2.376091969481376243, -12.02925914197702895 ) ) ;
#28089=B_SPLINE_CURVE_WITH_KNOTS ( 'NONE', 3,
 ( #21201, #45490, #20569, #65753, #35519, #20225, #40504, #55817, #10243, #30520 ),
 .UNSPECIFIED., .F., .F.,
 ( 4, 3, 3, 4 ),
 ( 1.226634733346699349E-18, 6.607638129004422475E-05, 9.911389841680472114E-05, 0.0001667630577588619047 ),
 .UNSPECIFIED. ) ;
#28093=ORIENTED_EDGE ( 'NONE', *, *, #43605, .T. ) ;
#28108=CARTESIAN_POINT ( 'NONE',  ( 0.3610902822527223832, 2.389900346488088800, 12.04327049858140519 ) ) ;
#28109=CARTESIAN_POINT ( 'NONE',  ( 0.2653519890518175051, -4.188454465438607777, -11.50765826381081602 ) ) ;
#28111=ORIENTED_EDGE ( 'NONE', *, *, #61735, .T. ) ;
#28114=CARTESIAN_POINT ( 'NONE',  ( 0.3106921474978453501, -9.542334142800513064, 7.699584408545861791 ) ) ;
#28116=CARTESIAN_POINT ( 'NONE',  ( 2.241352910868909643, 7.503490710578251566, -1.407733736974789762 ) ) ;
#28119=CARTESIAN_POINT ( 'NONE',  ( 0.3401186441510234970, 5.912862694513716377, 10.75260364139047908 ) ) ;
#28122=CARTESIAN_POINT ( 'NONE',  ( 0.3675815128205894289, 4.447030445008336663, -11.44679196252404729 ) ) ;
#28132=B_SPLINE_CURVE_WITH_KNOTS ( 'NONE', 3,
 ( #48329, #34554, #63254, #57967, #13053, #63914, #65143, #22362, #12378, #12704 ),
 .UNSPECIFIED., .F., .F.,
 ( 4, 3, 3, 4 ),
 ( 1.226634733346699349E-18, 6.607638129004543093E-05, 9.911389841680636099E-05, 0.0001667630577588615252 ),
 .UNSPECIFIED. ) ;
#28143=ORIENTED_EDGE ( 'NONE', *, *, #23754, .F. ) ;
#28146=CARTESIAN_POINT ( 'NONE',  ( 5.514970785353741078, -0.003929719953530087274, -0.002619824551223206600 ) ) ;
#28148=CARTESIAN_POINT ( 'NONE',  ( 5.520433897694421610, -0.01473594271720230636, -0.003119431460922371217 ) ) ;
#28151=CARTESIAN_POINT ( 'NONE',  ( 2.305787727787083519, 3.971363876084056166, -6.545285700970486786 ) ) ;
#28163=( BOUNDED_SURFACE ( )  B_SPLINE_SURFACE ( 3, 1, ( 
 ( #47601, #47291 ),
 ( #52282, #2392 ),
 ( #53250, #17001 ),
 ( #27629, #26329 ) ),
 .UNSPECIFIED., .F., .F., .F. ) 
 B_SPLINE_SURFACE_WITH_KNOTS ( ( 4, 4 ),
 ( 2, 2 ),
 ( 0.000000000000000000, 1.000000000000000000 ),
 ( 0.000000000000000000, 1.000000000000000000 ),
 .UNSPECIFIED. ) 
 GEOMETRIC_REPRESENTATION_ITEM ( )  RATIONAL_B_SPLINE_SURFACE ( (
 ( 1.000000000000000000, 1.000000000000000000),
 ( 0.9942764183789327692, 0.8450855930916580938),
 ( 0.9942764183789327692, 0.8450855930916580938),
 ( 1.000000000000000000, 1.000000000000000000) ) ) 
 REPRESENTATION_ITEM ( '' )  SURFACE ( )  );
#28164=ORIENTED_EDGE ( 'NONE', *, *, #57551, .F. ) ;
#28167=CARTESIAN_POINT ( 'NONE',  ( 0.000000000000000000, 7.347880794884120722E-16, 6.000000000000000888 ) ) ;
#28168=CARTESIAN_POINT ( 'NONE',  ( 1.719304012340731269, -10.22720798541492826, -7.581471372739399861 ) ) ;
#28172=CARTESIAN_POINT ( 'NONE',  ( 0.2652384529303146721, -6.180212112237588151, -10.57229402027114062 ) ) ;
#28174=CARTESIAN_POINT ( 'NONE',  ( 1.719304012340734378, -8.755325027794794934, -9.242227816401850760 ) ) ;
#28179=CARTESIAN_POINT ( 'NONE',  ( 2.653899356899829254, -3.657605971842851300, 6.857477569908428272 ) ) ;
#28183=CARTESIAN_POINT ( 'NONE',  ( 5.520433897694421610, 0.005630909886752868097, -0.01397038704729861025 ) ) ;
#28186=EDGE_LOOP ( 'NONE', ( #47204, #28527, #14209, #26306 ) ) ;
#28188=CARTESIAN_POINT ( 'NONE',  ( 2.990245332647880616, 8.248134185053359602, 1.974808303407723287 ) ) ;
#28190=CARTESIAN_POINT ( 'NONE',  ( 5.530133899448235191, 0.008946569461392248762, 0.01324661008606592763 ) ) ;
#28191=CARTESIAN_POINT ( 'NONE',  ( 0.3057689695767482618, -11.43929056598608973, 4.409323295154164768 ) ) ;
#28199=CARTESIAN_POINT ( 'NONE',  ( 2.241509619876139059, -3.850348903238759668, 6.592435552901108942 ) ) ;
#28200=CARTESIAN_POINT ( 'NONE',  ( 2.288423627607477417, 7.560204962263206596, 1.169285315515804502 ) ) ;
#28208=EDGE_CURVE ( 'NONE', #58059, #52387, #58060, .T. ) ;
#28211=CARTESIAN_POINT ( 'NONE',  ( 0.2801149460245130896, 5.954809120985864901, -10.70654700624296396 ) ) ;
#28212=CARTESIAN_POINT ( 'NONE',  ( 2.639814597422737386, 1.600543348184913617, -7.600559958731728294 ) ) ;
#28213=CARTESIAN_POINT ( 'NONE',  ( 2.931247277082686065, -1.728824746592323658, 7.672001188570254371 ) ) ;
#28218=CARTESIAN_POINT ( 'NONE',  ( 2.263328370261528999, 3.943189046766329309, 6.545781832005198808 ) ) ;
#28224=AXIS2_PLACEMENT_3D ( 'NONE', #13585, #32548, #52860 ) ;
#28226=CARTESIAN_POINT ( 'NONE',  ( 0.3278977287071239699, 8.073566434006698600, -9.235688435081650383 ) ) ;
#28229=CARTESIAN_POINT ( 'NONE',  ( 2.665405856346779956, 5.696318245876847541, 7.686816759402912425 ) ) ;
#28231=CARTESIAN_POINT ( 'NONE',  ( 2.242819959140645913, -1.426511055719359433, 7.500446639314770181 ) ) ;
#28238=CARTESIAN_POINT ( 'NONE',  ( 2.430348790457358632, -4.016278121583693128, -6.566563360302367869 ) ) ;
#28240=CARTESIAN_POINT ( 'NONE',  ( 0.7446945582507991102, 5.891988114924304298, 10.91757157182742510 ) ) ;
#28241=ORIENTED_EDGE ( 'NONE', *, *, #52551, .T. ) ;
#28242=CARTESIAN_POINT ( 'NONE',  ( 2.770579946183330478, -7.230573341413127686, -2.954332771348892273 ) ) ;
#28246=CARTESIAN_POINT ( 'NONE',  ( 0.3160775863651122397, -0.2401734240703709278, 12.26075464248082802 ) ) ;
#28249=CARTESIAN_POINT ( 'NONE',  ( 2.963017218115627571, -4.761166637500461540, -6.272673870919139638 ) ) ;
#28257=ADVANCED_FACE ( 'NONE', ( #42022 ), #21359, .F. ) ;
#28262=B_SPLINE_CURVE_WITH_KNOTS ( 'NONE', 3,
 ( #7988, #12606, #38886, #33570, #8297, #3326, #23599, #43869, #56119, #40164, #50506, #19590, #29865, #39854, #45487, #60139, #9570, #50176, #35517 ),
 .UNSPECIFIED., .F., .F.,
 ( 4, 3, 3, 3, 3, 3, 4 ),
 ( 7.866258489732282489E-18, 2.825908398831347771E-05, 4.208813692483994324E-05, 5.591713746943911183E-05, 6.279584083231893005E-05, 9.105792820296729282E-05, 0.0001153131102488839276 ),
 .UNSPECIFIED. ) ;
#28266=ORIENTED_EDGE ( 'NONE', *, *, #15464, .T. ) ;
#28270=CARTESIAN_POINT ( 'NONE',  ( 2.241451721903216399, -5.809054012306823722, -4.953785420083471003 ) ) ;
#28282=CARTESIAN_POINT ( 'NONE',  ( 2.284126774967664364, -7.558363379199190213, 1.171808575345598902 ) ) ;
#28287=CARTESIAN_POINT ( 'NONE',  ( 2.257661810676420799, -2.739276463085633662, -7.131864446283250558 ) ) ;
#28291=CARTESIAN_POINT ( 'NONE',  ( 2.241311220309554209, 2.523702734785345125, 7.205198716057793717 ) ) ;
#28293=B_SPLINE_CURVE_WITH_KNOTS ( 'NONE', 3,
 ( #2600, #27499, #17545, #33487, #37812, #53109, #17211, #22531, #58435, #48786, #27183, #57450, #58782 ),
 .UNSPECIFIED., .F., .F.,
 ( 4, 3, 3, 3, 4 ),
 ( 3.127317220692750759E-18, 6.607593386745573051E-05, 0.0001321518677373532469, 0.0001982171734706212392, 0.0002642860854759480124 ),
 .UNSPECIFIED. ) ;
#28297=CARTESIAN_POINT ( 'NONE',  ( 0.2650492594609250574, -4.291723947796392657, 11.46945808033132330 ) ) ;
#28306=CARTESIAN_POINT ( 'NONE',  ( 2.262775599886255762, -2.745802076335779329, 7.131180968652217622 ) ) ;
#28308=EDGE_CURVE ( 'NONE', #30406, #50365, #33438, .T. ) ;
#28311=CARTESIAN_POINT ( 'NONE',  ( 5.516018279890452902, 0.006771744149385740437, 0.0002248006052446895335 ) ) ;
#28312=CARTESIAN_POINT ( 'NONE',  ( 0.3341166715381284624, 6.352033667906601622, 10.49680960898228221 ) ) ;
#28313=CARTESIAN_POINT ( 'NONE',  ( 2.556980015513232285, -7.578583798307022334, 1.570584617272376082 ) ) ;
#28321=CARTESIAN_POINT ( 'NONE',  ( 2.241506898688419902, -1.364429914801466692, -7.511570207700573043 ) ) ;
#28322=CARTESIAN_POINT ( 'NONE',  ( 0.2956976708475475002, -9.245952174682493308, -8.045468685197016967 ) ) ;
#28327=EDGE_CURVE ( 'NONE', #36377, #31716, #42130, .T. ) ;
#28330=CARTESIAN_POINT ( 'NONE',  ( 3.152665057733881504, -7.719888720907738922, -1.848755561851823881 ) ) ;
#28333=CARTESIAN_POINT ( 'NONE',  ( 0.2653519789438771315, 7.888580323518872284, 9.366970421692796478 ) ) ;
#28336=B_SPLINE_CURVE_WITH_KNOTS ( 'NONE', 3,
 ( #7479, #57062, #63018, #6855, #58369, #37753, #58046, #53042, #62254, #41969, #31017, #36973, #50662, #1436, #56281, #25374, #21716, #26042, #36663, #50984, #766, #51970 ),
 .UNSPECIFIED., .F., .F.,
 ( 4, 3, 3, 3, 3, 3, 3, 4 ),
 ( 1.755771606739170543E-18, 4.449119708436968942E-05, 6.626296329540460836E-05, 8.803456484962672536E-05, 0.0001098060367612812058, 0.0001315774408628522915, 0.0001760698110411187294, 0.0001829697163287838087 ),
 .UNSPECIFIED. ) ;
#28344=ORIENTED_EDGE ( 'NONE', *, *, #21769, .T. ) ;
#28352=ORIENTED_EDGE ( 'NONE', *, *, #58799, .F. ) ;
#28353=CARTESIAN_POINT ( 'NONE',  ( 2.994568964204202821, 5.775954174106932903, 5.368337437440270143 ) ) ;
#28359=CARTESIAN_POINT ( 'NONE',  ( 0.3632410797595234664, -7.689504457927717418, 9.572936598843597267 ) ) ;
#28363=CARTESIAN_POINT ( 'NONE',  ( 5.520433897694421610, 0.01432141647227111458, 0.004666464468078371577 ) ) ;
#28365=FACE_OUTER_BOUND ( 'NONE', #62688, .T. ) ;
#28370=CARTESIAN_POINT ( 'NONE',  ( 2.241537034860907163, 7.175668896091129234, -2.606707005150471268 ) ) ;
#28373=CARTESIAN_POINT ( 'NONE',  ( 0.3632410797595285179, -3.951633449030989009, 11.62558329798850210 ) ) ;
#28384=CARTESIAN_POINT ( 'NONE',  ( 5.514970785353741078, -0.004233694591582531745, 0.002093325033904006385 ) ) ;
#28386=CARTESIAN_POINT ( 'NONE',  ( 1.719304012338199517, 0.000000000000000000, 0.000000000000000000 ) ) ;
#28387=CARTESIAN_POINT ( 'NONE',  ( 0.2801149460245113687, -10.51028947658249102, 6.294737133725765155 ) ) ;
#28391=CARTESIAN_POINT ( 'NONE',  ( 2.241352910868908754, -1.243507963608043498, -7.532448145350521429 ) ) ;
#28392=ORIENTED_EDGE ( 'NONE', *, *, #20887, .T. ) ;
#28398=CARTESIAN_POINT ( 'NONE',  ( 2.263328370261536548, -4.802372801874533081, 5.944174889971110431 ) ) ;
#28399=LINE ( 'NONE', #48699, #7830 ) ;
#28400=CARTESIAN_POINT ( 'NONE',  ( 0.3675815128205912052, -11.62724744438068569, 3.951233083390429446 ) ) ;
#28401=CARTESIAN_POINT ( 'NONE',  ( 5.516018279890452902, -0.004525000489649737799, -0.005042957932158631355 ) ) ;
#28403=CARTESIAN_POINT ( 'NONE',  ( 5.520433897694421610, 0.01473594271720288749, -0.003119431460922268435 ) ) ;
#28404=CARTESIAN_POINT ( 'NONE',  ( 5.515188684475870851, 0.004893136156457782680, 0.002166413411657369063 ) ) ;
#28412=CARTESIAN_POINT ( 'NONE',  ( 2.262775599885878730, -4.802882839669280202, -5.943524836196611538 ) ) ;
#28416=CARTESIAN_POINT ( 'NONE',  ( 0.2653141334712556532, -4.229817350136338305, -11.49252672845887879 ) ) ;
#28418=B_SPLINE_CURVE_WITH_KNOTS ( 'NONE', 3,
 ( #8530, #24478, #3589, #64382, #64069, #18552, #28822, #34119, #13513, #49131, #39114, #59406, #49459, #3898, #44415, #44755, #65036, #29780, #35438 ),
 .UNSPECIFIED., .F., .F.,
 ( 4, 3, 3, 3, 3, 3, 4 ),
 ( 0.000000000000000000, 2.831840207499612970E-05, 4.217266859840534770E-05, 5.602024318396014053E-05, 6.290810167969230950E-05, 9.120440630945263866E-05, 0.0001153103026479760220 ),
 .UNSPECIFIED. ) ;
#28421=VERTEX_POINT ( 'NONE', #14384 ) ;
#28434=CARTESIAN_POINT ( 'NONE',  ( 0.2653141617321038148, 10.62747662594938625, -6.084921229689308042 ) ) ;
#28435=VERTEX_POINT ( 'NONE', #38691 ) ;
#28442=DIRECTION ( 'NONE',  ( -0.3865475372811021937, -0.4778122177791984115, -0.7888450329201792677 ) ) ;
#28445=VERTEX_POINT ( 'NONE', #3799 ) ;
#28448=CARTESIAN_POINT ( 'NONE',  ( 1.372161826076017554, -3.755740169579909526, 12.04315837901270925 ) ) ;
#28455=CARTESIAN_POINT ( 'NONE',  ( 0.2911222467163511185, -10.50411792397754773, -6.312159098066288720 ) ) ;
#28456=CARTESIAN_POINT ( 'NONE',  ( 0.2638984909335720941, 12.24571285024409129, -0.1991813963114424380 ) ) ;
#28462=ORIENTED_EDGE ( 'NONE', *, *, #18832, .T. ) ;
#28474=CARTESIAN_POINT ( 'NONE',  ( 2.251152103363645463, 1.449454666117730106, 7.498874008626764009 ) ) ;
#28477=CARTESIAN_POINT ( 'NONE',  ( 2.844750968615173292, -6.210802026111876373, -4.777247819183616073 ) ) ;
#28484=CARTESIAN_POINT ( 'NONE',  ( 1.459561108994067880, -4.912799202119574105, -11.65083230253670799 ) ) ;
#28487=ORIENTED_EDGE ( 'NONE', *, *, #4959, .F. ) ;
#28493=CARTESIAN_POINT ( 'NONE',  ( 5.514624014163232779, -0.003830004412313258323, -0.001574979445068878025 ) ) ;
#28494=CARTESIAN_POINT ( 'NONE',  ( 2.350038591458374793, 10.33030559206027021, 2.471682575235019996 ) ) ;
#28502=CARTESIAN_POINT ( 'NONE',  ( 2.262775599886256650, -7.227769107232058232, 2.480428346600510370 ) ) ;
#28505=CARTESIAN_POINT ( 'NONE',  ( 0.3675815128205912052, -9.235491948679950269, -8.093875121226169256 ) ) ;
#28514=FACE_OUTER_BOUND ( 'NONE', #45477, .T. ) ;
#28517=CARTESIAN_POINT ( 'NONE',  ( 2.941278708680199916, -6.068329152486382938, 0.9331242451664794046 ) ) ;
#28523=CARTESIAN_POINT ( 'NONE',  ( 2.705197763288546220, 1.627208841526562422, -7.617149697727725766 ) ) ;
#28525=CARTESIAN_POINT ( 'NONE',  ( 3.047904605210430162, -1.788881754552591241, 7.698174516567103609 ) ) ;
#28527=ORIENTED_EDGE ( 'NONE', *, *, #9097, .F. ) ;
#28531=CARTESIAN_POINT ( 'NONE',  ( 1.937114397841932290, 9.228205347192453445, 8.920887662793502315 ) ) ;
#28535=CARTESIAN_POINT ( 'NONE',  ( 5.514970785353741078, -0.0003039746380524631733, 0.004713149585127259823 ) ) ;
#28538=CARTESIAN_POINT ( 'NONE',  ( 0.2717059086739037066, 10.51822005842002916, -6.276007891175617637 ) ) ;
#28545=( BOUNDED_SURFACE ( )  B_SPLINE_SURFACE ( 3, 1, ( 
 ( #16829, #56079 ),
 ( #6874, #16518 ),
 ( #56414, #41772 ),
 ( #27144, #20520 ) ),
 .UNSPECIFIED., .F., .F., .F. ) 
 B_SPLINE_SURFACE_WITH_KNOTS ( ( 4, 4 ),
 ( 2, 2 ),
 ( 0.000000000000000000, 1.000000000000000000 ),
 ( 0.000000000000000000, 1.000000000000000000 ),
 .UNSPECIFIED. ) 
 GEOMETRIC_REPRESENTATION_ITEM ( )  RATIONAL_B_SPLINE_SURFACE ( (
 ( 1.000000000000000000, 1.000000000000000000),
 ( 0.9856612449720755231, 0.9999558406602322425),
 ( 0.9856612449720755231, 0.9999558406602322425),
 ( 1.000000000000000000, 1.000000000000000000) ) ) 
 REPRESENTATION_ITEM ( '' )  SURFACE ( )  );
#28553=CARTESIAN_POINT ( 'NONE',  ( 2.368238019615270140, -3.992969450835600398, -6.556525400300609263 ) ) ;
#28560=CARTESIAN_POINT ( 'NONE',  ( 2.827825597296799387, 7.528560921609640744, 4.975864478227443932 ) ) ;
#28561=CARTESIAN_POINT ( 'NONE',  ( 0.2956976708475471116, -0.2200030809426427036, 12.25433786972505068 ) ) ;
#28566=CARTESIAN_POINT ( 'NONE',  ( 0.8320506296491552156, 10.57268643647783257, -6.546053790694065455 ) ) ;
#28572=VECTOR ( 'NONE', #30595, 1000.000000000000000 ) ;
#28577=CARTESIAN_POINT ( 'NONE',  ( 1.459561108993784773, -8.601340491611450645, -9.267924853468695545 ) ) ;
#28581=ORIENTED_EDGE ( 'NONE', *, *, #1379, .T. ) ;
#28585=ORIENTED_EDGE ( 'NONE', *, *, #11650, .F. ) ;
#28587=CARTESIAN_POINT ( 'NONE',  ( 2.994568964204206818, -3.591541975631920014, -7.020079750321929879 ) ) ;
#28594=B_SPLINE_CURVE_WITH_KNOTS ( 'NONE', 3,
 ( #15823, #50123, #50771, #4579, #10510, #30786, #45128, #21151, #65389, #5220, #36100, #5901, #19853, #40115, #45776, #572, #60407, #46432, #55429 ),
 .UNSPECIFIED., .F., .F.,
 ( 4, 3, 3, 3, 3, 3, 4 ),
 ( 0.000000000000000000, 2.831840207499706144E-05, 4.217266859840659453E-05, 5.602024318396192946E-05, 6.290810167969514198E-05, 9.120440630945896769E-05, 0.0001153103026479763472 ),
 .UNSPECIFIED. ) ;
#28596=LINE ( 'NONE', #13313, #3490 ) ;
#28601=CARTESIAN_POINT ( 'NONE',  ( 2.241352910868908754, 6.569501556381497132, -3.889181972941381460 ) ) ;
#28607=CARTESIAN_POINT ( 'NONE',  ( 2.251139882113958546, 2.495216312514881185, 7.218573619021348975 ) ) ;
#28612=ADVANCED_BREP_SHAPE_REPRESENTATION ( '', ( #29035, #24966 ), #48383 ) ;
#28613=ORIENTED_EDGE ( 'NONE', *, *, #40748, .T. ) ;
#28614=CARTESIAN_POINT ( 'NONE',  ( 0.2652384529303165039, -4.126283314267649160, 11.53005674806960279 ) ) ;
#28621=CARTESIAN_POINT ( 'NONE',  ( 1.198791140419175338, -0.5160125886328382760, 12.54673713002897628 ) ) ;
#28624=CARTESIAN_POINT ( 'NONE',  ( 0.2648978790185584908, 6.008231198268983775, 10.67083876753494032 ) ) ;
#28628=DIRECTION ( 'NONE',  ( -1.000000000000000000, 0.000000000000000000, 0.000000000000000000 ) ) ;
#28629=EDGE_CURVE ( 'NONE', #49321, #30406, #20697, .T. ) ;
#28632=CARTESIAN_POINT ( 'NONE',  ( 5.516018279890452902, 0.002527316374434305981, 0.006286471671801938804 ) ) ;
#28633=CARTESIAN_POINT ( 'NONE',  ( 0.3610902822527300993, -2.389900346488009308, -12.04327049858142296 ) ) ;
#28637=LINE ( 'NONE', #7713, #64029 ) ;
#28642=CARTESIAN_POINT ( 'NONE',  ( 2.241451721903216843, -1.265761656830151294, -7.528807736569459230 ) ) ;
#28647=CARTESIAN_POINT ( 'NONE',  ( 1.109979610370192882, 1.701361252869143748, 12.41172293674641480 ) ) ;
#28650=CARTESIAN_POINT ( 'NONE',  ( 3.100650473569524390, -7.709402782713551616, -1.818095316078554902 ) ) ;
#28657=CIRCLE ( 'NONE', #25475, 12.73084802173761787 ) ;
#28659=VERTEX_POINT ( 'NONE', #39866 ) ;
#28660=CARTESIAN_POINT ( 'NONE',  ( 2.290907136833253421, -0.1622757685885619361, 7.649199419879185946 ) ) ;
#28661=EDGE_LOOP ( 'NONE', ( #1154, #34121, #29188, #59855 ) ) ;
#28662=CARTESIAN_POINT ( 'NONE',  ( 2.305787727787084407, 7.654065630109506913, 0.1666591538752955071 ) ) ;
#28666=ORIENTED_EDGE ( 'NONE', *, *, #65797, .T. ) ;
#28670=CARTESIAN_POINT ( 'NONE',  ( 0.2676618633000442116, -7.748413788583150996, -9.484212776852418258 ) ) ;
#28674=ORIENTED_EDGE ( 'NONE', *, *, #3840, .F. ) ;
#28675=CARTESIAN_POINT ( 'NONE',  ( 3.047904605210421281, 5.772373816836818605, 5.398304302092557627 ) ) ;
#28676=CARTESIAN_POINT ( 'NONE',  ( 2.931247277082682956, -3.034789039497238772, 7.255238984871613894 ) ) ;
#28678=CARTESIAN_POINT ( 'NONE',  ( 0.3675815128205894289, -1.872154644482002528, -12.13672785388552100 ) ) ;
#28679=FACE_OUTER_BOUND ( 'NONE', #38175, .T. ) ;
#28681=LINE ( 'NONE', #64567, #41557 ) ;
#28683=CARTESIAN_POINT ( 'NONE',  ( 2.297017764050093724, -1.490897313050634665, -7.506328781223021274 ) ) ;
#28685=VERTEX_POINT ( 'NONE', #50519 ) ;
#28686=CARTESIAN_POINT ( 'NONE',  ( 0.3040950598368144520, -12.11647736519422480, 1.881452845810337227 ) ) ;
#28687=VERTEX_POINT ( 'NONE', #20235 ) ;
#28694=CARTESIAN_POINT ( 'NONE',  ( 1.452237505248552996, -8.579708443906808313, 9.303501428255998462 ) ) ;
#28699=EDGE_CURVE ( 'NONE', #5463, #64491, #57112, .T. ) ;
#28703=ORIENTED_EDGE ( 'NONE', *, *, #5304, .T. ) ;
#28707=CARTESIAN_POINT ( 'NONE',  ( 5.514970785353741078, -0.003415090918276209378, -0.003262412238248218153 ) ) ;
#28709=CARTESIAN_POINT ( 'NONE',  ( 0.2717059086739011531, -10.51822005841999363, 6.276007891175692244 ) ) ;
#28724=B_SPLINE_CURVE_WITH_KNOTS ( 'NONE', 3,
 ( #6395, #47301, #12022, #26665, #6081, #36959, #42944, #16376, #32612, #6731, #57933, #2400, #26339, #22679, #1418, #46624 ),
 .UNSPECIFIED., .F., .F.,
 ( 4, 3, 3, 3, 3, 4 ),
 ( 2.359668567760217409E-15, 0.0002126834539179711864, 0.0004253519300366280878, 0.0006380165497224201841, 0.0007442707582428287685, 0.0009453531351417518609 ),
 .UNSPECIFIED. ) ;
#28729=B_SPLINE_CURVE_WITH_KNOTS ( 'NONE', 3,
 ( #48327, #47334, #11720, #42625, #46999, #57640, #62268, #18044, #42293, #26705, #53296, #63569, #58629, #1456, #41988, #47642 ),
 .UNSPECIFIED., .F., .F.,
 ( 4, 3, 3, 3, 3, 4 ),
 ( 0.000000000000000000, 0.0002999043160758100364, 0.0005998071753052480184, 0.0008997092107376780147, 0.001204458948196762691, 0.001510329163478534020 ),
 .UNSPECIFIED. ) ;
#28730=B_SPLINE_CURVE_WITH_KNOTS ( 'NONE', 3,
 ( #51554, #26256, #21255, #32525, #27231, #52531, #43170, #57178, #33200, #36880, #62797, #47526, #26912, #11606, #22239, #16610, #47211, #63446, #31875, #58488, #41870, #57510 ),
 .UNSPECIFIED., .F., .F.,
 ( 4, 3, 3, 3, 3, 3, 3, 4 ),
 ( 1.764953265579307567E-18, 4.449119708436791404E-05, 6.626296329540252127E-05, 8.803456484962348630E-05, 0.0001098060367612760559, 0.0001315774408628449731, 0.0001760698110411088632, 0.0001829697163287805290 ),
 .UNSPECIFIED. ) ;
#28737=CARTESIAN_POINT ( 'NONE',  ( 1.719304012338517706, -0.7661785589593724799, 12.70777170744426243 ) ) ;
#28749=ORIENTED_EDGE ( 'NONE', *, *, #41138, .F. ) ;
#28761=CARTESIAN_POINT ( 'NONE',  ( 1.719304012338199517, 12.20344780065974888, 3.626341562670754914 ) ) ;
#28762=CARTESIAN_POINT ( 'NONE',  ( 0.4626703367443176229, 7.694993290995472357, 9.611037151103300147 ) ) ;
#28766=ORIENTED_EDGE ( 'NONE', *, *, #4620, .F. ) ;
#28774=CARTESIAN_POINT ( 'NONE',  ( 2.247112776669943468, 5.923998863710314922, 4.818685025483229190 ) ) ;
#28780=FACE_OUTER_BOUND ( 'NONE', #40449, .T. ) ;
#28786=CARTESIAN_POINT ( 'NONE',  ( 2.241536586108912932, -1.319514354261248190, 7.519576125149805890 ) ) ;
#28787=CARTESIAN_POINT ( 'NONE',  ( 0.3053067050349188016, 0.2307671807673981057, -12.25734436043224207 ) ) ;
#28788=CARTESIAN_POINT ( 'NONE',  ( 0.3675815128205894289, -8.093875121226139058, 9.235491948679980467 ) ) ;
#28800=CARTESIAN_POINT ( 'NONE',  ( 0.2653141334712571520, -11.52266042163704185, -4.147025708564540558 ) ) ;
#28813=CARTESIAN_POINT ( 'NONE',  ( 2.653899356899201312, -6.118160465318636554, -4.792827201941096682 ) ) ;
#28815=CARTESIAN_POINT ( 'NONE',  ( 0.9232058338315058954, 12.46548196349786153, -0.3773051331668420549 ) ) ;
#28819=EDGE_CURVE ( 'NONE', #43133, #43985, #1655, .T. ) ;
#28822=CARTESIAN_POINT ( 'NONE',  ( 2.251139882113958546, -5.929826121559315766, 4.813633939919417237 ) ) ;
#28823=ORIENTED_EDGE ( 'NONE', *, *, #1040, .F. ) ;
#28824=CARTESIAN_POINT ( 'NONE',  ( 2.305787727787083519, -2.461236246751120849, 7.249469779319902329 ) ) ;
#28825=CARTESIAN_POINT ( 'NONE',  ( 1.937114397841932290, -0.9020203649532572143, 12.80345148322678916 ) ) ;
#28830=DIRECTION ( 'NONE',  ( -0.3865475372811021382, -0.7888450329201776023, 0.4778122177792011316 ) ) ;
#28831=EDGE_CURVE ( 'NONE', #34453, #26248, #30126, .T. ) ;
#28840=DIRECTION ( 'NONE',  ( -1.000000000000000000, -0.000000000000000000, -0.000000000000000000 ) ) ;
#28841=CARTESIAN_POINT ( 'NONE',  ( 3.031336079629829872, -4.750429016921644099, 6.309383307296737797 ) ) ;
#28846=AXIS2_PLACEMENT_3D ( 'NONE', #3111, #63268, #7761 ) ;
#28847=VERTEX_POINT ( 'NONE', #15583 ) ;
#28848=ORIENTED_EDGE ( 'NONE', *, *, #34870, .T. ) ;
#28849=SURFACE_SIDE_STYLE ('',( #48494 ) ) ;
#28852=CARTESIAN_POINT ( 'NONE',  ( 2.350038591458111004, -10.18214835919901873, 3.024612895785461664 ) ) ;
#28856=ORIENTED_EDGE ( 'NONE', *, *, #23736, .F. ) ;
#28858=CARTESIAN_POINT ( 'NONE',  ( 0.9232058338315058954, -11.84276737136198321, -3.908895078357639274 ) ) ;
#28859=CARTESIAN_POINT ( 'NONE',  ( 2.269879328257228490, -5.026125315665611382, -5.759117113707886482 ) ) ;
#28876=VERTEX_POINT ( 'NONE', #36539 ) ;
#28882=CARTESIAN_POINT ( 'NONE',  ( 1.719304012340734822, -3.626341562669572305, -12.20344780066098345 ) ) ;
#28887=DIRECTION ( 'NONE',  ( 0.000000000000000000, 0.000000000000000000, 1.000000000000000000 ) ) ;
#28888=ADVANCED_FACE ( 'NONE', ( #55513 ), #62146, .F. ) ;
#28893=EDGE_CURVE ( 'NONE', #60970, #13659, #39490, .T. ) ;
#28899=CARTESIAN_POINT ( 'NONE',  ( 2.491965175174687186, 5.121563073453788029, 5.773748672882028643 ) ) ;
#28915=CARTESIAN_POINT ( 'NONE',  ( 2.259025283528085293, -3.937899517809441807, -6.547290863799084981 ) ) ;
#28916=CARTESIAN_POINT ( 'NONE',  ( 1.719304012341629884, 8.755325027796281745, -9.242227816402079910 ) ) ;
#28920=ORIENTED_EDGE ( 'NONE', *, *, #41275, .T. ) ;
#28924=CARTESIAN_POINT ( 'NONE',  ( 2.247112776671282841, 4.997244136394094483, 5.774169979602185698 ) ) ;
#28925=CARTESIAN_POINT ( 'NONE',  ( 2.899286259009683508, -3.614094927251888301, -6.972741252562093983 ) ) ;
#28927=CARTESIAN_POINT ( 'NONE',  ( 0.3632410797595257423, 9.235006602299463907, -8.092233745354546315 ) ) ;
#28929=CARTESIAN_POINT ( 'NONE',  ( 5.520433897694421610, -0.007971295965052502958, 0.01278034823631960838 ) ) ;
#28940=CARTESIAN_POINT ( 'NONE',  ( 2.241449424704146320, 6.580749518451852076, -3.870245369721753814 ) ) ;
#28941=( BOUNDED_SURFACE ( )  B_SPLINE_SURFACE ( 3, 1, ( 
 ( #30796, #20182 ),
 ( #51116, #46132 ),
 ( #20841, #16183 ),
 ( #36791, #26478 ) ),
 .UNSPECIFIED., .F., .F., .T. ) 
 B_SPLINE_SURFACE_WITH_KNOTS ( ( 4, 4 ),
 ( 2, 2 ),
 ( 0.000000000000000000, 1.000000000000000000 ),
 ( 0.000000000000000000, 1.000000000000000000 ),
 .UNSPECIFIED. ) 
 GEOMETRIC_REPRESENTATION_ITEM ( )  RATIONAL_B_SPLINE_SURFACE ( (
 ( 1.000000000000000000, 1.000000000000000000),
 ( 0.9942764183789327692, 0.8450855930916580938),
 ( 0.9942764183789327692, 0.8450855930916580938),
 ( 1.000000000000000000, 1.000000000000000000) ) ) 
 REPRESENTATION_ITEM ( '' )  SURFACE ( )  );
#28967=EDGE_CURVE ( 'NONE', #39587, #34853, #3174, .T. ) ;
#28968=CARTESIAN_POINT ( 'NONE',  ( 0.2638984909335716500, -5.950360275954980516, -10.70468911391670375 ) ) ;
#28970=CARTESIAN_POINT ( 'NONE',  ( 0.3675815128205912052, 3.951233083390468526, 11.62724744438066971 ) ) ;
#28971=CARTESIAN_POINT ( 'NONE',  ( 3.092491956585171398, -7.707758057368747195, 1.813286239165102121 ) ) ;
#28985=CARTESIAN_POINT ( 'NONE',  ( 1.719304012339833099, -9.242227816401946683, 8.755325027794301107 ) ) ;
#28989=CARTESIAN_POINT ( 'NONE',  ( 0.3675815128205912052, -12.13672785388549080, -1.872154644482208585 ) ) ;
#28990=EDGE_CURVE ( 'NONE', #21572, #646, #18249, .T. ) ;
#28991=CARTESIAN_POINT ( 'NONE',  ( 1.937114397841932290, 12.80345148322679272, 0.9020203649532124723 ) ) ;
#29009=CARTESIAN_POINT ( 'NONE',  ( 2.305787727787085295, -7.249469779319927198, 2.461236246751046242 ) ) ;
#29010=ADVANCED_FACE ( 'NONE', ( #28514 ), #41741, .F. ) ;
#29012=VERTEX_POINT ( 'NONE', #49788 ) ;
#29021=CARTESIAN_POINT ( 'NONE',  ( 0.3109076770649022436, -9.239379580302159667, 8.060731492642771556 ) ) ;
#29027=CARTESIAN_POINT ( 'NONE',  ( 2.241352910868908754, 6.569501556381497132, -3.889181972941381460 ) ) ;
#29029=ORIENTED_EDGE ( 'NONE', *, *, #11650, .T. ) ;
#29035=MANIFOLD_SOLID_BREP ( 'Keyway', #1534 ) ;
#29036=CARTESIAN_POINT ( 'NONE',  ( 0.3632410797595244101, 3.951633449031067169, -11.62558329798846479 ) ) ;
#29038=CARTESIAN_POINT ( 'NONE',  ( 0.3164563675027666778, -3.967501530099160956, 11.60369811966061704 ) ) ;
#29041=CARTESIAN_POINT ( 'NONE',  ( 0.3341166715381361230, 9.559079491641874426, 7.691251065848372370 ) ) ;
#29044=ORIENTED_EDGE ( 'NONE', *, *, #18360, .F. ) ;
#29046=CARTESIAN_POINT ( 'NONE',  ( 1.937114397841932290, -12.76557247858999311, 1.334979369128383331 ) ) ;
#29051=CARTESIAN_POINT ( 'NONE',  ( 0.2646305136544072623, 6.008537389229567260, -10.67138229758223389 ) ) ;
#29056=CARTESIAN_POINT ( 'NONE',  ( 0.2646305136544072623, -7.770320294339112976, -9.465888453933038349 ) ) ;
#29059=CARTESIAN_POINT ( 'NONE',  ( 0.2759803524722194701, 10.70204612651785325, -5.960075719898730640 ) ) ;
#29062=ORIENTED_EDGE ( 'NONE', *, *, #13044, .T. ) ;
#29065=CARTESIAN_POINT ( 'NONE',  ( 2.305787727787083519, -5.756228004061423320, -5.047606869483115766 ) ) ;
#29072=B_SPLINE_CURVE_WITH_KNOTS ( 'NONE', 3,
 ( #56141, #24584, #36177, #14579, #60476, #45856, #9593 ),
 .UNSPECIFIED., .F., .F.,
 ( 4, 3, 4 ),
 ( 3.688038945365320759E-15, 0.002398160485434608184, 0.005002426799381520968 ),
 .UNSPECIFIED. ) ;
#29078=CARTESIAN_POINT ( 'NONE',  ( 0.2648978790185619880, -12.08224454301447182, -1.996248716311752824 ) ) ;
#29083=DIRECTION ( 'NONE',  ( 1.000000000000000000, 0.000000000000000000, 0.000000000000000000 ) ) ;
#29085=DIRECTION ( 'NONE',  ( -1.000000000000000000, -0.000000000000000000, -0.000000000000000000 ) ) ;
#29086=CARTESIAN_POINT ( 'NONE',  ( 0.2956976708475477222, -12.10637007622313632, 1.911282699793684925 ) ) ;
#29095=VERTEX_POINT ( 'NONE', #10853 ) ;
#29102=CARTESIAN_POINT ( 'NONE',  ( 2.305787727787084851, -7.566723232958062262, -1.164987321564809886 ) ) ;
#29106=CARTESIAN_POINT ( 'NONE',  ( 0.8375941296788365076, 7.696026447556312711, 9.769835228043566744 ) ) ;
#29110=CARTESIAN_POINT ( 'NONE',  ( 0.2651627682582915480, 10.56115808354091712, -6.199212018117330913 ) ) ;
#29128=EDGE_CURVE ( 'NONE', #37857, #19254, #28594, .T. ) ;
#29130=CARTESIAN_POINT ( 'NONE',  ( 0.3278977287071226376, 0.2481246099269766026, -12.26453627383316025 ) ) ;
#29133=CARTESIAN_POINT ( 'NONE',  ( 2.655192694324043590, 6.604353705983746714, 6.969384012964340513 ) ) ;
#29135=CARTESIAN_POINT ( 'NONE',  ( 2.261269890822072526, 3.940687015735738097, -6.546486799463070660 ) ) ;
#29137=( BOUNDED_SURFACE ( )  B_SPLINE_SURFACE ( 3, 1, ( 
 ( #3014, #33587 ),
 ( #18306, #39212 ),
 ( #9271, #4310 ),
 ( #64480, #54197 ) ),
 .UNSPECIFIED., .F., .F., .F. ) 
 B_SPLINE_SURFACE_WITH_KNOTS ( ( 4, 4 ),
 ( 2, 2 ),
 ( 0.000000000000000000, 1.000000000000000000 ),
 ( 0.000000000000000000, 1.000000000000000000 ),
 .UNSPECIFIED. ) 
 GEOMETRIC_REPRESENTATION_ITEM ( )  RATIONAL_B_SPLINE_SURFACE ( (
 ( 1.000000000000000000, 1.000000000000000000),
 ( 0.9942764183789327692, 0.8450855930916580938),
 ( 0.9942764183789327692, 0.8450855930916580938),
 ( 1.000000000000000000, 1.000000000000000000) ) ) 
 REPRESENTATION_ITEM ( '' )  SURFACE ( )  );
#29138=ORIENTED_EDGE ( 'NONE', *, *, #20938, .F. ) ;
#29140=CARTESIAN_POINT ( 'NONE',  ( 1.549075743844144037, 3.694639393664535199, 12.12370443967527400 ) ) ;
#29151=CARTESIAN_POINT ( 'NONE',  ( 2.263328370261528555, 1.466596409249160127, 7.499672967744983154 ) ) ;
#29152=CARTESIAN_POINT ( 'NONE',  ( 2.653899356900406570, -5.192946150929565796, -5.782420802795875225 ) ) ;
#29155=CARTESIAN_POINT ( 'NONE',  ( 3.031336079628672575, -6.309383307296084986, -4.750429016921874137 ) ) ;
#29162=CARTESIAN_POINT ( 'NONE',  ( 2.556980015513593774, -3.668282146013208678, 6.815084337351732913 ) ) ;
#29163=CARTESIAN_POINT ( 'NONE',  ( 1.014383007554953142, -4.688516792764541918, -11.58298623339619660 ) ) ;
#29164=ORIENTED_EDGE ( 'NONE', *, *, #13250, .F. ) ;
#29166=FACE_OUTER_BOUND ( 'NONE', #5086, .T. ) ;
#29173=CARTESIAN_POINT ( 'NONE',  ( 2.177405672430728245, 10.27382588316567436, -4.457418613957222497 ) ) ;
#29177=CARTESIAN_POINT ( 'NONE',  ( 2.276198483117256810, -7.236140649716383599, 2.469789406312209668 ) ) ;
#29178=CARTESIAN_POINT ( 'NONE',  ( 5.515539859299206427, -0.0008592514567753351158, 0.005991790098944297510 ) ) ;
#29181=LINE ( 'NONE', #59124, #40711 ) ;
#29183=CARTESIAN_POINT ( 'NONE',  ( 2.241317068080784125, 7.533758201955892631, 1.235499051333795784 ) ) ;
#29188=ORIENTED_EDGE ( 'NONE', *, *, #5895, .T. ) ;
#29189=LINE ( 'NONE', #28517, #57681 ) ;
#29195=CARTESIAN_POINT ( 'NONE',  ( 2.247112776671933876, -4.997244136395391223, -5.774169979601344593 ) ) ;
#29196=ORIENTED_EDGE ( 'NONE', *, *, #40087, .F. ) ;
#29197=ORIENTED_EDGE ( 'NONE', *, *, #64353, .T. ) ;
#29198=CARTESIAN_POINT ( 'NONE',  ( 2.507146904658098752, 0.2163149345877656282, -7.719969556433173175 ) ) ;
#29205=VECTOR ( 'NONE', #47022, 1000.000000000000114 ) ;
#29212=CARTESIAN_POINT ( 'NONE',  ( 2.269879328256728890, 7.642470739868882035, -0.1483462450597493598 ) ) ;
#29213=CARTESIAN_POINT ( 'NONE',  ( 0.2652384529303125626, 7.820949643217270264, -9.423437232855587098 ) ) ;
#29214=CARTESIAN_POINT ( 'NONE',  ( 0.2653519789438753551, -9.366970421692828452, 7.888580323518841197 ) ) ;
#29215=EDGE_CURVE ( 'NONE', #7317, #22476, #47561, .T. ) ;
#29217=CARTESIAN_POINT ( 'NONE',  ( 2.241536586108911155, -7.517390684805879353, 1.331908602351616011 ) ) ;
#29221=CARTESIAN_POINT ( 'NONE',  ( 2.406456491626380423, -10.41426194695414686, 0.6290357040719805060 ) ) ;
#29224=FACE_OUTER_BOUND ( 'NONE', #60049, .T. ) ;
#29226=CARTESIAN_POINT ( 'NONE',  ( 0.3675815128205894289, -4.447030445008257615, 11.44679196252407927 ) ) ;
#29228=CARTESIAN_POINT ( 'NONE',  ( 2.241506898688418570, -4.877157973187019380, 5.873558213059462574 ) ) ;
#29229=DIRECTION ( 'NONE',  ( 0.000000000000000000, 0.000000000000000000, 1.000000000000000000 ) ) ;
#29233=CARTESIAN_POINT ( 'NONE',  ( 3.152665057734023613, 0.4801242025591827001, -7.923639299008664594 ) ) ;
#29243=LINE ( 'NONE', #40176, #62844 ) ;
#29251=CARTESIAN_POINT ( 'NONE',  ( 2.241317068080784569, 4.977030124433354352, 5.789053609344733786 ) ) ;
#29252=CARTESIAN_POINT ( 'NONE',  ( 2.931247277082680291, -3.607110715259699951, -6.988361004535472709 ) ) ;
#29254=CARTESIAN_POINT ( 'NONE',  ( 2.844750968616391429, 6.613363922490658631, -4.202329849280680207 ) ) ;
#29260=CARTESIAN_POINT ( 'NONE',  ( 2.655192694323718960, -7.714239566600834763, -5.716669423975402786 ) ) ;
#29261=CIRCLE ( 'NONE', #28224, 12.73084802173761787 ) ;
#29262=CARTESIAN_POINT ( 'NONE',  ( 2.177405672433373685, 11.17876532284936530, -0.6747479782256756708 ) ) ;
#29267=CARTESIAN_POINT ( 'NONE',  ( 2.241526690369555652, 6.602966219605691300, -3.832206765347519362 ) ) ;
#29272=ORIENTED_EDGE ( 'NONE', *, *, #8704, .F. ) ;
#29273=ORIENTED_EDGE ( 'NONE', *, *, #14702, .F. ) ;
#29280=ORIENTED_EDGE ( 'NONE', *, *, #14777, .F. ) ;
#29286=VERTEX_POINT ( 'NONE', #17157 ) ;
#29287=CARTESIAN_POINT ( 'NONE',  ( 1.283627346226322130, 11.16434663959558904, 5.810034161408879072 ) ) ;
#29296=VECTOR ( 'NONE', #2810, 1000.000000000000227 ) ;
#29301=ORIENTED_EDGE ( 'NONE', *, *, #40597, .F. ) ;
#29305=CARTESIAN_POINT ( 'NONE',  ( 0.3106921474978470155, -9.239619355094093933, -8.060345844326381126 ) ) ;
#29308=CARTESIAN_POINT ( 'NONE',  ( 3.152665057736164123, 5.461013642407259283, 5.761241965767907480 ) ) ;
#29309=CARTESIAN_POINT ( 'NONE',  ( 1.462291587749436683, 1.569662666436903997, 12.54737685278351655 ) ) ;
#29311=CARTESIAN_POINT ( 'NONE',  ( 2.507146904658098308, -5.128007631637100161, 5.774795220010169317 ) ) ;
#29312=CARTESIAN_POINT ( 'NONE',  ( 1.719304012341412724, 2.961219984259706450, -12.38166659046466300 ) ) ;
#29315=B_SPLINE_CURVE_WITH_KNOTS ( 'NONE', 3,
 ( #64522, #4029, #54891, #34904, #18993, #60524, #4707, #45241, #50248, #25278, #5015, #65192, #60201, #39595, #29939, #65498, #55212, #19659, #39259 ),
 .UNSPECIFIED., .F., .F.,
 ( 4, 3, 3, 3, 3, 3, 4 ),
 ( 8.641030098560686409E-18, 2.825908398831582569E-05, 4.208813692484607576E-05, 5.591713746944476323E-05, 6.279584083232501513E-05, 9.105792820297718617E-05, 0.0001153131102488831687 ),
 .UNSPECIFIED. ) ;
#29318=VERTEX_POINT ( 'NONE', #24424 ) ;
#29323=( BOUNDED_SURFACE ( )  B_SPLINE_SURFACE ( 3, 1, ( 
 ( #17766, #44322 ),
 ( #33378, #39335 ),
 ( #49362, #43020 ),
 ( #43338, #53677 ) ),
 .UNSPECIFIED., .F., .F., .F. ) 
 B_SPLINE_SURFACE_WITH_KNOTS ( ( 4, 4 ),
 ( 2, 2 ),
 ( 0.000000000000000000, 1.000000000000000000 ),
 ( 0.000000000000000000, 1.000000000000000000 ),
 .UNSPECIFIED. ) 
 GEOMETRIC_REPRESENTATION_ITEM ( )  RATIONAL_B_SPLINE_SURFACE ( (
 ( 1.000000000000000000, 1.000000000000000000),
 ( 0.6933888150995267674, 0.9895912004443193632),
 ( 0.6933888150995267674, 0.9895912004443193632),
 ( 1.000000000000000000, 1.000000000000000000) ) ) 
 REPRESENTATION_ITEM ( '' )  SURFACE ( )  );
#29335=CARTESIAN_POINT ( 'NONE',  ( 0.2646305136544065406, 9.465888453933068547, -7.770320294339078337 ) ) ;
#29337=ORIENTED_EDGE ( 'NONE', *, *, #40744, .T. ) ;
#29342=DIRECTION ( 'NONE',  ( -0.3865475372811021937, -0.9220659470476462172, 0.01937500237528096830 ) ) ;
#29347=CARTESIAN_POINT ( 'NONE',  ( 1.375507693218919636, -10.03411718356142046, 7.647735792765052665 ) ) ;
#29353=DIRECTION ( 'NONE',  ( -1.000000000000000000, -0.000000000000000000, -0.000000000000000000 ) ) ;
#29358=EDGE_LOOP ( 'NONE', ( #10025, #52897, #38064, #10684 ) ) ;
#29359=B_SPLINE_CURVE_WITH_KNOTS ( 'NONE', 3,
 ( #58898, #22972, #7672, #23958, #53883, #2369, #59203, #18957, #22643, #53568, #44217, #8321, #27604, #3695, #3356, #37918, #43226, #8015, #3024 ),
 .UNSPECIFIED., .F., .F.,
 ( 4, 3, 3, 3, 3, 3, 4 ),
 ( 4.336808689942017736E-19, 2.831840207499692930E-05, 4.217266859840731959E-05, 5.602024318396171940E-05, 6.290810167969236371E-05, 9.120440630945234051E-05, 0.0001153103026479759542 ),
 .UNSPECIFIED. ) ;
#29360=ORIENTED_EDGE ( 'NONE', *, *, #33515, .T. ) ;
#29365=CARTESIAN_POINT ( 'NONE',  ( 0.9232167919969098691, 1.756271097262231073, -12.34114433434356251 ) ) ;
#29378=EDGE_CURVE ( 'NONE', #35137, #47422, #26128, .T. ) ;
#29385=CARTESIAN_POINT ( 'NONE',  ( 1.937114397841932290, -3.531416430611214796, -12.33981801388261346 ) ) ;
#29411=CARTESIAN_POINT ( 'NONE',  ( 0.2657645697724702605, -6.253766234003993674, 10.52916014490829077 ) ) ;
#29414=CARTESIAN_POINT ( 'NONE',  ( 1.462291587748365540, 7.633056170898332660, 10.08151577214832173 ) ) ;
#29419=CARTESIAN_POINT ( 'NONE',  ( 0.2651627923886338278, 10.64925183219501470, -6.046629261473224659 ) ) ;
#29426=CARTESIAN_POINT ( 'NONE',  ( 5.530133899448235191, 0.001661287012794350655, -0.01589823604557753789 ) ) ;
#29427=CARTESIAN_POINT ( 'NONE',  ( 2.260457164925428586, 5.941202713842286265, 4.804526096744350383 ) ) ;
#29431=ORIENTED_EDGE ( 'NONE', *, *, #57033, .F. ) ;
#29440=VERTEX_POINT ( 'NONE', #30717 ) ;
#29446=CARTESIAN_POINT ( 'NONE',  ( 3.152665057734131526, -0.9030954876737319337, -7.886634106564212487 ) ) ;
#29456=CARTESIAN_POINT ( 'NONE',  ( 1.719304012338201737, 9.242227816402087015, 8.755325027793320558 ) ) ;
#29458=CARTESIAN_POINT ( 'NONE',  ( 3.152665057734125309, -6.622010822086626725, -4.377619405892440696 ) ) ;
#29498=CARTESIAN_POINT ( 'NONE',  ( 2.251152103364165935, -5.004701566806020629, -5.769488058190294311 ) ) ;
#29501=CARTESIAN_POINT ( 'NONE',  ( 2.770579946183334030, 0.3031629740256825967, -7.804957730865686116 ) ) ;
#29507=EDGE_CURVE ( 'NONE', #36274, #13985, #19789, .T. ) ;
#29510=ADVANCED_FACE ( 'NONE', ( #20762 ), #5247, .F. ) ;
#29528=CARTESIAN_POINT ( 'NONE',  ( 2.262775599886255762, -7.499645832851588700, -1.465770593192964544 ) ) ;
#29531=CARTESIAN_POINT ( 'NONE',  ( 2.907497136251153691, 5.319973245618665025, 5.781215374755499958 ) ) ;
#29536=CONICAL_SURFACE ( 'NONE', #42243, 7.938172270156617749, 1.280189991382167047 ) ;
#29543=VERTEX_POINT ( 'NONE', #21762 ) ;
#29548=CONICAL_SURFACE ( 'NONE', #43512, 7.938172270156617749, 1.280189991382167047 ) ;
#29550=ORIENTED_EDGE ( 'NONE', *, *, #45767, .F. ) ;
#29553=CARTESIAN_POINT ( 'NONE',  ( 2.259025283527870798, 5.014999102875606241, 5.764013728792329871 ) ) ;
#29556=CARTESIAN_POINT ( 'NONE',  ( 0.3537226245948385528, 12.27287980220284780, 0.2609894354289943874 ) ) ;
#29558=CARTESIAN_POINT ( 'NONE',  ( 0.3341166715381307384, 9.234320413907912695, -8.078283863465406611 ) ) ;
#29565=CARTESIAN_POINT ( 'NONE',  ( 2.903928887688380645, -7.046356840275715072, -5.221047506680895900 ) ) ;
#29575=CARTESIAN_POINT ( 'NONE',  ( 0.2655924914740778742, 2.083162675473772207, -12.06787830249863092 ) ) ;
#29588=EDGE_CURVE ( 'NONE', #36493, #23316, #51471, .T. ) ;
#29591=CARTESIAN_POINT ( 'NONE',  ( 1.719304012338199517, 0.000000000000000000, 0.000000000000000000 ) ) ;
#29594=ORIENTED_EDGE ( 'NONE', *, *, #4786, .F. ) ;
#29598=CARTESIAN_POINT ( 'NONE',  ( 1.549075743846936026, 10.12891450359603773, -7.618376504786640524 ) ) ;
#29599=CARTESIAN_POINT ( 'NONE',  ( 0.3106921474978474040, 3.971572160646753336, 11.60027394202199780 ) ) ;
#29604=CARTESIAN_POINT ( 'NONE',  ( 0.3675815128205894289, 6.367184624550164429, 10.50067073900654080 ) ) ;
#29608=CARTESIAN_POINT ( 'NONE',  ( 1.283627346226359878, 9.985833283678269723, 7.660435136228929132 ) ) ;
#29614=CARTESIAN_POINT ( 'NONE',  ( 0.7446945582514985507, 1.802628359587814311, 12.27434006248804721 ) ) ;
#29618=CARTESIAN_POINT ( 'NONE',  ( 0.2915757698887312954, -12.10419100255477787, -1.916267336493298501 ) ) ;
#29622=CARTESIAN_POINT ( 'NONE',  ( 1.937114397841935398, 12.76557247858998423, 1.334979369128467042 ) ) ;
#29626=ADVANCED_FACE ( 'NONE', ( #56686 ), #52453, .F. ) ;
#29630=CARTESIAN_POINT ( 'NONE',  ( 0.2646305136544065406, -2.256625640822397472, 12.03696649559613796 ) ) ;
#29633=B_SPLINE_CURVE_WITH_KNOTS ( 'NONE', 3,
 ( #23556, #33191, #6952, #48832, #48504, #37529, #42835, #53152, #2645, #43829, #28213, #12563, #17906, #28525, #18242, #1958 ),
 .UNSPECIFIED., .F., .F.,
 ( 4, 3, 3, 3, 3, 4 ),
 ( 0.000000000000000000, 0.0002176109881720254336, 0.0004352086762394624013, 0.0006528017811446896763, 0.0007615147961451724937, 0.0009453342004947376054 ),
 .UNSPECIFIED. ) ;
#29634=CARTESIAN_POINT ( 'NONE',  ( 2.251139882114756130, -1.203816215708022552, -7.542197031255136963 ) ) ;
#29638=ORIENTED_EDGE ( 'NONE', *, *, #29507, .T. ) ;
#29640=B_SPLINE_CURVE_WITH_KNOTS ( 'NONE', 3,
 ( #6513, #38657, #17138, #3435, #64245, #18720, #37412, #54289, #26789, #47088, #1544, #12144, #32417 ),
 .UNSPECIFIED., .F., .F.,
 ( 4, 3, 3, 3, 4 ),
 ( 2.737610485525898696E-18, 6.607593386745463275E-05, 0.0001321518677373517020, 0.0001982171734706200737, 0.0002642860854759484460 ),
 .UNSPECIFIED. ) ;
#29643=ORIENTED_EDGE ( 'NONE', *, *, #8356, .T. ) ;
#29645=CARTESIAN_POINT ( 'NONE',  ( 0.2739690278137243973, -9.264642836915884416, 8.012873994335658168 ) ) ;
#29649=VECTOR ( 'NONE', #52617, 1000.000000000000114 ) ;
#29657=ORIENTED_EDGE ( 'NONE', *, *, #51435, .T. ) ;
#29662=CARTESIAN_POINT ( 'NONE',  ( 1.014383007554954474, -6.628652139012841005, -10.59286224865788206 ) ) ;
#29664=CARTESIAN_POINT ( 'NONE',  ( 0.000000000000000000, 0.000000000000000000, -12.15774668701806149 ) ) ;
#29665=CARTESIAN_POINT ( 'NONE',  ( 0.3675815128205912052, 11.62724744438071056, -3.951233083390353062 ) ) ;
#29671=ORIENTED_EDGE ( 'NONE', *, *, #31825, .T. ) ;
#29672=B_SPLINE_CURVE_WITH_KNOTS ( 'NONE', 3,
 ( #54658, #44625, #64918, #60935, #19397, #10371, #39323, #15372, #39662, #50638, #14054, #3798, #75, #30007, #59962, #14383, #4433, #44313, #15034 ),
 .UNSPECIFIED., .F., .F.,
 ( 4, 3, 3, 3, 3, 3, 4 ),
 ( 1.182973382901717356E-17, 4.457896483014837149E-05, 6.639290541542138609E-05, 8.820687556478841213E-05, 0.0001100173248778912589, 0.0001545671401658127800, 0.0001830328308068567065 ),
 .UNSPECIFIED. ) ;
#29681=CARTESIAN_POINT ( 'NONE',  ( 2.266490820341528600, 7.230273269341637388, 2.476945027125681431 ) ) ;
#29687=CARTESIAN_POINT ( 'NONE',  ( 0.2653519991613814688, -7.854838327448906199, -9.395283368383257283 ) ) ;
#29690=EDGE_CURVE ( 'NONE', #47363, #39116, #2351, .T. ) ;
#29700=CARTESIAN_POINT ( 'NONE',  ( 2.276198483117261251, 6.697332984100312636, -3.688810392808482330 ) ) ;
#29709=CARTESIAN_POINT ( 'NONE',  ( 2.259025283528087957, 0.1366755880739711493, 7.639069972920475848 ) ) ;
#29711=CARTESIAN_POINT ( 'NONE',  ( 0.3401186441510257730, -12.12646044229290254, 1.878666403202292834 ) ) ;
#29718=VERTEX_POINT ( 'NONE', #48665 ) ;
#29723=LINE ( 'NONE', #55991, #42068 ) ;
#29728=CARTESIAN_POINT ( 'NONE',  ( 5.520433897694421610, 0.01278034823632016002, -0.007971295965052641735 ) ) ;
#29729=CARTESIAN_POINT ( 'NONE',  ( 0.5572780756279074321, 7.697784780878702549, 9.649189244958369827 ) ) ;
#29749=CARTESIAN_POINT ( 'NONE',  ( 2.288423627607478306, -7.504187945869063014, 1.486973602181125287 ) ) ;
#29752=CARTESIAN_POINT ( 'NONE',  ( 2.242819959140645913, 7.634209046698939183, 0.1024002568249643141 ) ) ;
#29756=VECTOR ( 'NONE', #10500, 1000.000000000000114 ) ;
#29766=CARTESIAN_POINT ( 'NONE',  ( 0.9232058338315048962, 11.58467545991553926, 4.617996777200612080 ) ) ;
#29773=CARTESIAN_POINT ( 'NONE',  ( 2.781367136451494471, -6.179587792204012331, -4.783057651000591548 ) ) ;
#29780=CARTESIAN_POINT ( 'NONE',  ( 2.298277635560276089, -5.967558917212167025, 4.791911337974153362 ) ) ;
#29782=CARTESIAN_POINT ( 'NONE',  ( 5.514624014163232779, 0.001921576324372091180, -0.003668383633201698427 ) ) ;
#29783=CARTESIAN_POINT ( 'NONE',  ( 2.440552418640468346, 6.568204543009822594, 4.020120046181057560 ) ) ;
#29787=CARTESIAN_POINT ( 'NONE',  ( 1.549075743844149367, -6.912427991522798187, 10.62322497417012634 ) ) ;
#29790=DIRECTION ( 'NONE',  ( 0.3865475372811020272, -0.8730852074079779035, 0.2971585806051764145 ) ) ;
#29794=EDGE_CURVE ( 'NONE', #20687, #23822, #43536, .T. ) ;
#29803=CONICAL_SURFACE ( 'NONE', #44657, 7.938172270156617749, 1.280189991382167047 ) ;
#29815=CONICAL_SURFACE ( 'NONE', #50011, 7.938172270156617749, 1.280189991382167047 ) ;
#29817=CARTESIAN_POINT ( 'NONE',  ( 0.2911222467163511740, 11.44063169461055374, 4.392242282524896346 ) ) ;
#29825=ORIENTED_EDGE ( 'NONE', *, *, #34661, .T. ) ;
#29826=CARTESIAN_POINT ( 'NONE',  ( 3.100650473569752208, 0.4517506188709136117, -7.907988569972083326 ) ) ;
#29834=CARTESIAN_POINT ( 'NONE',  ( 2.770579946183326925, -4.165025702425888099, 6.607710183380618219 ) ) ;
#29838=ORIENTED_EDGE ( 'NONE', *, *, #22089, .T. ) ;
#29839=CARTESIAN_POINT ( 'NONE',  ( 2.284126774967663032, -1.483972655035265653, 7.503320429541877168 ) ) ;
#29843=CARTESIAN_POINT ( 'NONE',  ( 2.241506898688418570, 5.873558213059478561, 4.877157973186999840 ) ) ;
#29865=CARTESIAN_POINT ( 'NONE',  ( 2.256373768223412846, -3.703993494727557234, 6.681391662621571470 ) ) ;
#29868=CARTESIAN_POINT ( 'NONE',  ( 1.547277799337862803, 2.861188171558548543, 12.34637640861301300 ) ) ;
#29869=EDGE_CURVE ( 'NONE', #18739, #5409, #64166, .T. ) ;
#29870=VECTOR ( 'NONE', #25938, 999.9999999999997726 ) ;
#29875=ORIENTED_EDGE ( 'NONE', *, *, #46482, .T. ) ;
#29877=CARTESIAN_POINT ( 'NONE',  ( 0.2958664285830431839, -0.2205161970873538990, -12.25438626999990355 ) ) ;
#29881=EDGE_CURVE ( 'NONE', #22893, #47422, #60255, .T. ) ;
#29890=CARTESIAN_POINT ( 'NONE',  ( 2.305787727787083519, -6.545285700970500109, -3.971363876084033961 ) ) ;
#29895=CARTESIAN_POINT ( 'NONE',  ( 2.491965175174665426, 6.575382551509702189, -4.041154086925421218 ) ) ;
#29899=ORIENTED_EDGE ( 'NONE', *, *, #49428, .T. ) ;
#29900=CARTESIAN_POINT ( 'NONE',  ( 0.3106921474978485143, -12.03191800497307007, -2.360654586927916743 ) ) ;
#29906=CARTESIAN_POINT ( 'NONE',  ( 2.034671305879535375, 10.44529075078724922, -5.218565780489550221 ) ) ;
#29912=CARTESIAN_POINT ( 'NONE',  ( 2.903928887688958849, 8.712847781147546655, 0.9983813550129092551 ) ) ;
#29916=ORIENTED_EDGE ( 'NONE', *, *, #59472, .F. ) ;
#29919=CARTESIAN_POINT ( 'NONE',  ( 2.639814597422734721, -6.851176153958504322, 3.659458430304324494 ) ) ;
#29925=VERTEX_POINT ( 'NONE', #56935 ) ;
#29938=CARTESIAN_POINT ( 'NONE',  ( 2.941278708680199916, 5.721889327162151595, 2.226055275041809889 ) ) ;
#29939=CARTESIAN_POINT ( 'NONE',  ( 2.247112776671464029, -6.670755883245737650, -3.716786765232512835 ) ) ;
#29940=EDGE_CURVE ( 'NONE', #49481, #18779, #16672, .T. ) ;
#29944=CARTESIAN_POINT ( 'NONE',  ( 0.3675815128205912052, -10.50067073900647330, -6.367184624550275451 ) ) ;
#29946=CARTESIAN_POINT ( 'NONE',  ( 0.2958664285830431839, 10.72286791615088752, 5.936220506376270301 ) ) ;
#29954=CARTESIAN_POINT ( 'NONE',  ( 1.459561108994217316, 5.767168887068948813, -11.25243317554941136 ) ) ;
#29964=CARTESIAN_POINT ( 'NONE',  ( 2.247112776671464918, -5.923998863713016760, -4.818685025480720974 ) ) ;
#29971=ORIENTED_EDGE ( 'NONE', *, *, #58640, .T. ) ;
#29973=FACE_OUTER_BOUND ( 'NONE', #59452, .T. ) ;
#29974=CARTESIAN_POINT ( 'NONE',  ( 3.047904605210390638, -7.561255571389383867, 2.299870214474525110 ) ) ;
#29982=CARTESIAN_POINT ( 'NONE',  ( 2.717984159219838158, 3.648459810929824521, -6.886544461123881966 ) ) ;
#29991=CARTESIAN_POINT ( 'NONE',  ( 2.305787727787084407, -6.711944854845797614, -3.682701754025583085 ) ) ;
#30004=CARTESIAN_POINT ( 'NONE',  ( 0.2767916011545408228, -12.24854187541374095, 0.1897947303542399933 ) ) ;
#30005=CARTESIAN_POINT ( 'NONE',  ( 5.514970785353741078, -0.001117786416802142449, 0.004588761610584822515 ) ) ;
#30007=CARTESIAN_POINT ( 'NONE',  ( 0.2759803524722196366, -4.011137970318874757, -11.57441428600636968 ) ) ;
#30010=CARTESIAN_POINT ( 'NONE',  ( 3.152665057734040488, 0.000000000000000000, 0.000000000000000000 ) ) ;
#30011=EDGE_CURVE ( 'NONE', #6270, #49268, #21287, .T. ) ;
#30027=CARTESIAN_POINT ( 'NONE',  ( 2.305787727787084407, 0.1666591538752685842, 7.654065630109507801 ) ) ;
#30029=CARTESIAN_POINT ( 'NONE',  ( 0.2653519890518152291, -7.871710682401847237, -9.381125756446651920 ) ) ;
#30039=ORIENTED_EDGE ( 'NONE', *, *, #37079, .T. ) ;
#30047=ORIENTED_EDGE ( 'NONE', *, *, #54064, .T. ) ;
#30051=LINE ( 'NONE', #21046, #32889 ) ;
#30055=EDGE_LOOP ( 'NONE', ( #59689, #37426, #44525, #16450 ) ) ;
#30057=ORIENTED_EDGE ( 'NONE', *, *, #53131, .T. ) ;
#30064=CARTESIAN_POINT ( 'NONE',  ( 1.719304012338199517, 0.000000000000000000, 0.000000000000000000 ) ) ;
#30072=CARTESIAN_POINT ( 'NONE',  ( 0.2638984909335720941, -11.57533005135176474, -4.001111175853858448 ) ) ;
#30082=DIRECTION ( 'NONE',  ( 0.000000000000000000, 0.000000000000000000, 1.000000000000000000 ) ) ;
#30083=CARTESIAN_POINT ( 'NONE',  ( 2.256373768221667131, 5.936694589809198064, 4.807932997209342751 ) ) ;
#30085=( BOUNDED_SURFACE ( )  B_SPLINE_SURFACE ( 3, 1, ( 
 ( #36474, #56786 ),
 ( #15838, #10211 ),
 ( #60764, #46447 ),
 ( #50475, #50786 ) ),
 .UNSPECIFIED., .F., .F., .F. ) 
 B_SPLINE_SURFACE_WITH_KNOTS ( ( 4, 4 ),
 ( 2, 2 ),
 ( 0.000000000000000000, 1.000000000000000000 ),
 ( 0.000000000000000000, 1.000000000000000000 ),
 .UNSPECIFIED. ) 
 GEOMETRIC_REPRESENTATION_ITEM ( )  RATIONAL_B_SPLINE_SURFACE ( (
 ( 1.000000000000000000, 1.000000000000000000),
 ( 0.9942764183789327692, 0.8450855930916585379),
 ( 0.9942764183789327692, 0.8450855930916585379),
 ( 1.000000000000000000, 1.000000000000000000) ) ) 
 REPRESENTATION_ITEM ( '' )  SURFACE ( )  );
#30089=CARTESIAN_POINT ( 'NONE',  ( 0.2648978790185584908, 11.46165506714228322, 4.312320170909275774 ) ) ;
#30099=CARTESIAN_POINT ( 'NONE',  ( 2.298277635560279197, 7.651596582281724679, 0.1650558796844366904 ) ) ;
#30111=CARTESIAN_POINT ( 'NONE',  ( 2.247112776671464918, 7.499199956302008196, -1.440655381229385190 ) ) ;
#30119=CARTESIAN_POINT ( 'NONE',  ( 2.241352910868910531, 5.794346703933913822, -4.970878533273699773 ) ) ;
#30123=CARTESIAN_POINT ( 'NONE',  ( 1.948354844644523132, -4.761851831285707881, -10.97658859990240998 ) ) ;
#30124=CARTESIAN_POINT ( 'NONE',  ( 0.3665391374699464300, -12.04754782681755998, -2.392238720110583472 ) ) ;
#30125=CARTESIAN_POINT ( 'NONE',  ( 0.3665391374699465965, 12.27992639892678284, -0.2638605131387583569 ) ) ;
#30126=B_SPLINE_CURVE_WITH_KNOTS ( 'NONE', 3,
 ( #56492, #15268, #10939, #5979, #50853, #30550, #35206, #5300, #24931, #45864, #11271, #20598, #61799, #19928, #26235, #40193 ),
 .UNSPECIFIED., .F., .F.,
 ( 4, 3, 3, 3, 3, 4 ),
 ( 0.000000000000000000, 0.0002999043160757333833, 0.0005998071753050970975, 0.0008997092107374508744, 0.001204458948195599125, 0.001510329163476425464 ),
 .UNSPECIFIED. ) ;
#30129=CARTESIAN_POINT ( 'NONE',  ( 1.937114397841932290, 12.45230409340481437, 3.111612666690119156 ) ) ;
#30133=CARTESIAN_POINT ( 'NONE',  ( 0.3665391374699467075, -12.27992639892678284, -0.2638605131388441216 ) ) ;
#30140=LINE ( 'NONE', #9504, #11067 ) ;
#30148=CARTESIAN_POINT ( 'NONE',  ( 0.3401186441510221092, 7.690203051556021130, 9.562489599411557961 ) ) ;
#30151=CARTESIAN_POINT ( 'NONE',  ( 0.3675815128205894289, -1.872154644482002528, -12.13672785388552100 ) ) ;
#30152=CARTESIAN_POINT ( 'NONE',  ( 0.3675815128205912052, -11.44679196252406506, -4.447030445008294919 ) ) ;
#30155=CARTESIAN_POINT ( 'NONE',  ( 2.269879328255106188, 1.181008584587388999, -7.552124491909401272 ) ) ;
#30184=CARTESIAN_POINT ( 'NONE',  ( 2.835339799623988188, 4.197472173747801349, -6.612744557053391148 ) ) ;
#30188=VECTOR ( 'NONE', #34025, 1000.000000000000114 ) ;
#30195=B_SPLINE_CURVE_WITH_KNOTS ( 'NONE', 3,
 ( #58805, #53797, #19185, #13223, #33508, #54110, #44771, #64715, #8232, #33810, #4227, #44130, #28502, #24495, #29177, #49472, #3912, #39456, #59759 ),
 .UNSPECIFIED., .F., .F.,
 ( 4, 3, 3, 3, 3, 3, 4 ),
 ( 0.000000000000000000, 2.831840207499378850E-05, 4.217266859840141746E-05, 5.602024318395757232E-05, 6.290810167968961255E-05, 9.120440630944950803E-05, 0.0001153103026479763337 ),
 .UNSPECIFIED. ) ;
#30199=ORIENTED_EDGE ( 'NONE', *, *, #14214, .T. ) ;
#30201=CARTESIAN_POINT ( 'NONE',  ( 2.249013661412228693, -7.499157010299424719, -1.444210756221623759 ) ) ;
#30206=CARTESIAN_POINT ( 'NONE',  ( 2.242418902651891255, 2.517330194228720064, -7.207816731001243760 ) ) ;
#30212=B_SPLINE_CURVE_WITH_KNOTS ( 'NONE', 3,
 ( #55566, #48950, #64857, #19671, #14000, #19339, #3408, #64225, #8702, #18699, #39930, #38957, #59248, #39605, #13669, #28985 ),
 .UNSPECIFIED., .F., .F.,
 ( 4, 3, 3, 3, 3, 4 ),
 ( 0.000000000000000000, 0.0003017745587525273612, 0.0006035491769808764510, 0.0009053241094668200428, 0.001207275924539990414, 0.001510325902532977686 ),
 .UNSPECIFIED. ) ;
#30214=CARTESIAN_POINT ( 'NONE',  ( 0.3665391374699467075, 12.27992639892678461, 0.2638605131387583569 ) ) ;
#30216=ORIENTED_EDGE ( 'NONE', *, *, #1015, .T. ) ;
#30219=CARTESIAN_POINT ( 'NONE',  ( 0.2651627682582924916, 12.24583720278846677, -0.08809604936510406770 ) ) ;
#30240=CARTESIAN_POINT ( 'NONE',  ( 5.514970785353741078, 0.004713149585127261558, 0.0003039746380524470729 ) ) ;
#30254=VERTEX_POINT ( 'NONE', #14606 ) ;
#30255=CARTESIAN_POINT ( 'NONE',  ( 2.770579946183328257, -6.910873157406261846, 3.639932028439796241 ) ) ;
#30256=EDGE_CURVE ( 'NONE', #11727, #61427, #47449, .T. ) ;
#30258=CARTESIAN_POINT ( 'NONE',  ( 0.2911222467163572802, 11.58731125337565437, -3.989243506922225624 ) ) ;
#30261=EDGE_LOOP ( 'NONE', ( #18041, #10143, #414, #18805 ) ) ;
#30268=ORIENTED_EDGE ( 'NONE', *, *, #17938, .F. ) ;
#30269=CARTESIAN_POINT ( 'NONE',  ( 2.298277635560095788, -2.461898367585350300, -7.246601281227178504 ) ) ;
#30279=ORIENTED_EDGE ( 'NONE', *, *, #6886, .F. ) ;
#30280=CARTESIAN_POINT ( 'NONE',  ( 1.372161826076010005, 6.811451307636476216, 10.61825687422740927 ) ) ;
#30281=EDGE_CURVE ( 'NONE', #38082, #58835, #14894, .T. ) ;
#30288=CARTESIAN_POINT ( 'NONE',  ( 2.524535260912121437, 4.054303386867375458, 6.580044328001015685 ) ) ;
#30291=CARTESIAN_POINT ( 'NONE',  ( 2.256373768223419063, -4.807932997207736037, 5.936694589811255973 ) ) ;
#30292=CARTESIAN_POINT ( 'NONE',  ( 0.4613984246114870569, 5.909164750631185292, -10.80075367333616221 ) ) ;
#30293=CARTESIAN_POINT ( 'NONE',  ( 2.241352910868908754, 3.889181972941541776, -6.569501556381402096 ) ) ;
#30294=CARTESIAN_POINT ( 'NONE',  ( 2.835339799623979751, 3.628068688271675502, 6.941489812670536885 ) ) ;
#30296=CARTESIAN_POINT ( 'NONE',  ( 0.3654063281920768569, -12.13594617907220297, -1.872466061177207708 ) ) ;
#30297=( BOUNDED_SURFACE ( )  B_SPLINE_SURFACE ( 3, 1, ( 
 ( #65239, #29335 ),
 ( #18730, #41182 ),
 ( #8401, #19707 ),
 ( #54300, #15587 ) ),
 .UNSPECIFIED., .F., .F., .F. ) 
 B_SPLINE_SURFACE_WITH_KNOTS ( ( 4, 4 ),
 ( 2, 2 ),
 ( 0.000000000000000000, 1.000000000000000000 ),
 ( 0.000000000000000000, 1.000000000000000000 ),
 .UNSPECIFIED. ) 
 GEOMETRIC_REPRESENTATION_ITEM ( )  RATIONAL_B_SPLINE_SURFACE ( (
 ( 1.000000000000000000, 1.000000000000000000),
 ( 0.9942764183789327692, 0.8450855930916580938),
 ( 0.9942764183789327692, 0.8450855930916580938),
 ( 1.000000000000000000, 1.000000000000000000) ) ) 
 REPRESENTATION_ITEM ( '' )  SURFACE ( )  );
#30300=FACE_OUTER_BOUND ( 'NONE', #54390, .T. ) ;
#30301=CARTESIAN_POINT ( 'NONE',  ( 2.249013661412227805, 0.1200550008340211805, -7.636012530783590435 ) ) ;
#30304=B_SPLINE_CURVE_WITH_KNOTS ( 'NONE', 3,
 ( #35115, #64404, #24504, #14508, #39137, #34785, #30155, #45436, #9519, #44779, #24846, #50455, #64723, #59430, #19194, #59767, #14196, #34483, #54786 ),
 .UNSPECIFIED., .F., .F.,
 ( 4, 3, 3, 3, 3, 3, 4 ),
 ( 6.952433221959954168E-18, 2.825908398991504083E-05, 4.208813692702534923E-05, 5.591713747220676827E-05, 6.279584083537379164E-05, 9.105792820726774008E-05, 0.0001153131102486950596 ),
 .UNSPECIFIED. ) ;
#30307=B_SPLINE_CURVE_WITH_KNOTS ( 'NONE', 3,
 ( #53168, #7614, #48206, #28226, #32529, #23906, #2658, #53515, #58842, #17919, #22919, #43173, #23232, #38858, #63449, #38179, #62802, #3640, #52839 ),
 .UNSPECIFIED., .F., .F.,
 ( 4, 3, 3, 3, 3, 3, 4 ),
 ( 1.158841720744533638E-17, 4.457896483014629118E-05, 6.639290541541733389E-05, 8.820687556478164942E-05, 0.0001100173248778832900, 0.0001545671401657995527, 0.0001830328308068548092 ),
 .UNSPECIFIED. ) ;
#30313=CARTESIAN_POINT ( 'NONE',  ( 0.2646305136544065406, -0.1321451301298699199, 12.24595685781654453 ) ) ;
#30318=CARTESIAN_POINT ( 'NONE',  ( 5.516018279890452902, 0.002104829434641014487, 0.006440244342253419532 ) ) ;
#30320=ORIENTED_EDGE ( 'NONE', *, *, #35237, .F. ) ;
#30340=CARTESIAN_POINT ( 'NONE',  ( 5.514624014163232779, 0.004104370840204389984, 0.0005510299962881913495 ) ) ;
#30344=CARTESIAN_POINT ( 'NONE',  ( 0.2646305136544072623, -4.064188116014475938, -11.55263159009962592 ) ) ;
#30348=ORIENTED_EDGE ( 'NONE', *, *, #11193, .F. ) ;
#30350=EDGE_LOOP ( 'NONE', ( #10343, #49561, #10827, #35445 ) ) ;
#30354=CARTESIAN_POINT ( 'NONE',  ( 0.2717059086739013196, 8.007130974640039867, 9.268607328094562448 ) ) ;
#30357=CARTESIAN_POINT ( 'NONE',  ( -14.47334165536100059, 0.000000000000000000, 0.000000000000000000 ) ) ;
#30359=FACE_OUTER_BOUND ( 'NONE', #11484, .T. ) ;
#30360=AXIS2_PLACEMENT_3D ( 'NONE', #61760, #5944, #16556 ) ;
#30366=CARTESIAN_POINT ( 'NONE',  ( 0.4626703367443509851, 12.07256244737112816, 2.416235258139790343 ) ) ;
#30382=CARTESIAN_POINT ( 'NONE',  ( 2.305787727787084407, -0.1666591538752151269, -7.654065630109508689 ) ) ;
#30385=ORIENTED_EDGE ( 'NONE', *, *, #18863, .T. ) ;
#30402=CARTESIAN_POINT ( 'NONE',  ( 2.241449424704146764, -2.553400830064028071, 7.194804211893837120 ) ) ;
#30406=VERTEX_POINT ( 'NONE', #54728 ) ;
#30407=ORIENTED_EDGE ( 'NONE', *, *, #4625, .F. ) ;
#30408=CARTESIAN_POINT ( 'NONE',  ( 0.3218525148189898544, 9.550803867331183028, -7.695007528464921087 ) ) ;
#30410=ADVANCED_FACE ( 'NONE', ( #38769 ), #830, .T. ) ;
#30426=CARTESIAN_POINT ( 'NONE',  ( 2.261269890822072970, 7.639767381742371022, 0.1394916642590125211 ) ) ;
#30434=CARTESIAN_POINT ( 'NONE',  ( 2.941278708680199916, 2.226055275041868509, -5.721889327162129391 ) ) ;
#30435=ADVANCED_FACE ( 'NONE', ( #14454 ), #40976, .F. ) ;
#30442=CARTESIAN_POINT ( 'NONE',  ( 2.835339799623985080, -0.3287452556171230889, 7.825540862019409794 ) ) ;
#30443=CARTESIAN_POINT ( 'NONE',  ( 0.2638984909335716500, -12.02508546958695490, -2.322601104020790341 ) ) ;
#30447=CARTESIAN_POINT ( 'NONE',  ( 5.514970785353741078, 0.003415090918276187260, 0.003262412238248241138 ) ) ;
#30448=CARTESIAN_POINT ( 'NONE',  ( 5.520433897694421610, -0.004666464468078229330, 0.01432141647227116142 ) ) ;
#30452=CARTESIAN_POINT ( 'NONE',  ( 2.994568964204073591, 6.620406464816390724, 4.283796412555422428 ) ) ;
#30456=CARTESIAN_POINT ( 'NONE',  ( 1.198791140417959200, -6.720248575442489880, 10.60778679489404652 ) ) ;
#30465=CARTESIAN_POINT ( 'NONE',  ( 0.2657645697724695943, 7.755260067564157644, 9.477802844074060928 ) ) ;
#30466=CARTESIAN_POINT ( 'NONE',  ( 2.305787727787084407, -2.461236246751023593, -7.249469779319933416 ) ) ;
#30472=CARTESIAN_POINT ( 'NONE',  ( 0.3474126878361853965, 11.44231427242455723, -4.439989671676105587 ) ) ;
#30479=CARTESIAN_POINT ( 'NONE',  ( 0.3665391374699467075, 3.952034409876297172, 11.62960183138728532 ) ) ;
#30492=CARTESIAN_POINT ( 'NONE',  ( 5.515188684475870851, -0.0003622115669627103194, -0.005339000964282158458 ) ) ;
#30501=CARTESIAN_POINT ( 'NONE',  ( 2.241509619876138171, 5.823675573301077435, 4.936617871859525053 ) ) ;
#30512=CARTESIAN_POINT ( 'NONE',  ( 0.2651627682582886614, 0.08809604936506143513, 12.24583720278848631 ) ) ;
#30513=CARTESIAN_POINT ( 'NONE',  ( 5.516018279890452902, -0.006286471671801945743, 0.002527316374434286465 ) ) ;
#30514=CARTESIAN_POINT ( 'NONE',  ( 2.524535260912230683, -7.646662375930282529, -1.123794384999050378 ) ) ;
#30515=CARTESIAN_POINT ( 'NONE',  ( 2.269879328256533491, 2.474479066008462347, -7.232310762824027073 ) ) ;
#30519=CARTESIAN_POINT ( 'NONE',  ( 1.287602823386676532, -12.47973441446164955, 1.639728374786187715 ) ) ;
#30520=CARTESIAN_POINT ( 'NONE',  ( 2.241352910868909643, -6.569501556381414531, -3.889181972941518683 ) ) ;
#30521=VECTOR ( 'NONE', #30976, 1000.000000000000114 ) ;
#30534=CARTESIAN_POINT ( 'NONE',  ( 0.3278977287071272451, -11.60975784853194348, 3.961557589215566999 ) ) ;
#30538=VERTEX_POINT ( 'NONE', #30089 ) ;
#30544=CARTESIAN_POINT ( 'NONE',  ( 0.9296196016816602459, 9.278306863859487663, 8.327938962579152005 ) ) ;
#30545=CARTESIAN_POINT ( 'NONE',  ( 2.305787727787083519, 6.545285700970583598, -3.971363876083895850 ) ) ;
#30547=FACE_OUTER_BOUND ( 'NONE', #14398, .T. ) ;
#30548=CARTESIAN_POINT ( 'NONE',  ( 1.198791140419050105, -12.54673713002894075, -0.5160125886328322808 ) ) ;
#30550=CARTESIAN_POINT ( 'NONE',  ( 1.287602823386676310, -11.16629420487802449, 5.809161206980312464 ) ) ;
#30552=CARTESIAN_POINT ( 'NONE',  ( 0.6473888112830232799, -2.472751636945289100, -12.12394591856681103 ) ) ;
#30557=ORIENTED_EDGE ( 'NONE', *, *, #44950, .T. ) ;
#30565=CARTESIAN_POINT ( 'NONE',  ( 2.994568964204205930, -7.020079750321915668, 3.591541975631944883 ) ) ;
#30576=ORIENTED_EDGE ( 'NONE', *, *, #35237, .T. ) ;
#30578=EDGE_LOOP ( 'NONE', ( #12665, #53886, #25321, #65594 ) ) ;
#30582=ORIENTED_EDGE ( 'NONE', *, *, #29378, .F. ) ;
#30595=DIRECTION ( 'NONE',  ( -0.3939253465568943180, -0.1500280335741535909, 0.9068155327749427563 ) ) ;
#30603=CARTESIAN_POINT ( 'NONE',  ( 5.536195898058073439, -0.006672323185952951791, -0.005266167600748141754 ) ) ;
#30604=CARTESIAN_POINT ( 'NONE',  ( 2.241352910868908754, 2.532612177304442991, 7.202080440908749992 ) ) ;
#30606=CARTESIAN_POINT ( 'NONE',  ( 2.305787727787084407, -5.047606869483094449, 5.756228004061441084 ) ) ;
#30607=CARTESIAN_POINT ( 'NONE',  ( 0.9232058338315058954, 9.306586124266710058, -8.301689855530073103 ) ) ;
#30608=CARTESIAN_POINT ( 'NONE',  ( 2.255723233588950993, 0.1321982600348293457, -7.638048593862501789 ) ) ;
#30615=CARTESIAN_POINT ( 'NONE',  ( 0.3675815128205894289, -12.13672785388551389, 1.872154644482044938 ) ) ;
#30617=CARTESIAN_POINT ( 'NONE',  ( 2.241526690369557429, 3.832206765347585975, 6.602966219605648668 ) ) ;
#30621=VECTOR ( 'NONE', #59466, 999.9999999999998863 ) ;
#30623=CARTESIAN_POINT ( 'NONE',  ( 5.515539859299206427, 0.001241880655086934895, 0.005924322247675113152 ) ) ;
#30629=CARTESIAN_POINT ( 'NONE',  ( 2.556980015513758087, -2.429125721802469329, 7.348538402679460013 ) ) ;
#30635=EDGE_CURVE ( 'NONE', #40530, #33180, #58525, .T. ) ;
#30643=CIRCLE ( 'NONE', #51901, 12.73084802173761787 ) ;
#30645=CARTESIAN_POINT ( 'NONE',  ( 2.241352910868910531, 5.794346703933913822, -4.970878533273699773 ) ) ;
#30651=ORIENTED_EDGE ( 'NONE', *, *, #58503, .F. ) ;
#30653=CARTESIAN_POINT ( 'NONE',  ( 0.3218525148189809726, -4.423735011438902909, 11.43947393562874915 ) ) ;
#30658=CARTESIAN_POINT ( 'NONE',  ( 0.3474126878361804005, 8.085727498271769065, 9.233692382639393514 ) ) ;
#30679=CARTESIAN_POINT ( 'NONE',  ( 0.3278977287071248026, -5.917385921415723615, -10.74546228373873191 ) ) ;
#30694=CARTESIAN_POINT ( 'NONE',  ( 2.242418902651940105, -6.561482094363274342, 3.903399295463823915 ) ) ;
#30696=EDGE_LOOP ( 'NONE', ( #43815, #13638, #32107, #32788 ) ) ;
#30700=EDGE_CURVE ( 'NONE', #58005, #24593, #23526, .T. ) ;
#30708=CARTESIAN_POINT ( 'NONE',  ( 0.2652384529303124516, 4.126283314267730873, -11.53005674806958503 ) ) ;
#30709=CARTESIAN_POINT ( 'NONE',  ( 0.3040950598368144520, 3.956873563689532247, 11.60568999039896454 ) ) ;
#30710=CARTESIAN_POINT ( 'NONE',  ( 0.3675815128205894289, -10.76447900494936327, -5.910255304480558358 ) ) ;
#30712=CARTESIAN_POINT ( 'NONE',  ( 5.516018279890452902, 0.002104829434640673614, -0.006440244342253036158 ) ) ;
#30715=CARTESIAN_POINT ( 'NONE',  ( 2.305787727787083519, 1.164987321564732392, 7.566723232958076473 ) ) ;
#30717=CARTESIAN_POINT ( 'NONE',  ( 2.241352910868909643, 7.503490710578251566, -1.407733736974789762 ) ) ;
#30720=ORIENTED_EDGE ( 'NONE', *, *, #20426, .F. ) ;
#30726=CARTESIAN_POINT ( 'NONE',  ( 0.6511581176957887962, -2.473966499148019693, 12.12498040206527072 ) ) ;
#30736=CARTESIAN_POINT ( 'NONE',  ( 2.241451721903216399, 1.265761656830201920, 7.528807736569452125 ) ) ;
#30737=CARTESIAN_POINT ( 'NONE',  ( 0.9232167919969109793, -12.19756235544080170, 2.570564963838106731 ) ) ;
#30746=CARTESIAN_POINT ( 'NONE',  ( 2.665405856346787949, 9.505137710817303187, -1.089747929268594095 ) ) ;
#30753=CARTESIAN_POINT ( 'NONE',  ( 2.969415267404188707, 6.276215141898544125, 4.760005747566447454 ) ) ;
#30755=ORIENTED_EDGE ( 'NONE', *, *, #15796, .F. ) ;
#30756=CARTESIAN_POINT ( 'NONE',  ( 0.2651627923886300531, 10.56116046379974271, 6.199207987242133733 ) ) ;
#30757=CARTESIAN_POINT ( 'NONE',  ( 3.092491956585992519, 0.9322768171840450924, -7.863103788722456855 ) ) ;
#30764=CARTESIAN_POINT ( 'NONE',  ( 2.241528039335008327, -3.803597072146486457, -6.619488482362972270 ) ) ;
#30766=CARTESIAN_POINT ( 'NONE',  ( 2.251139882113959878, 1.203816215709547111, 7.542197031254625372 ) ) ;
#30771=CARTESIAN_POINT ( 'NONE',  ( 3.047904605210409734, 0.9519317672906866257, 7.845751380824976806 ) ) ;
#30781=CARTESIAN_POINT ( 'NONE',  ( 0.6511581176971025231, -1.822219471613997221, -12.23990098761649570 ) ) ;
#30783=CARTESIAN_POINT ( 'NONE',  ( 2.241537034860906275, 2.615577641485621996, -7.172440248506130267 ) ) ;
#30786=CARTESIAN_POINT ( 'NONE',  ( 2.249013661412228249, -5.000301708456363237, 5.772355099776667053 ) ) ;
#30792=CARTESIAN_POINT ( 'NONE',  ( 2.653899356900376816, 1.606012885791718192, 7.604196386057602730 ) ) ;
#30796=CARTESIAN_POINT ( 'NONE',  ( 5.514970785353741078, 0.004713149585127535644, -0.0003039746380528477398 ) ) ;
#30801=CARTESIAN_POINT ( 'NONE',  ( 2.589278595513308190, 7.587119248534321514, -1.582391164331529598 ) ) ;
#30802=ORIENTED_EDGE ( 'NONE', *, *, #40593, .T. ) ;
#30805=DIRECTION ( 'NONE',  ( 0.000000000000000000, 0.000000000000000000, 1.000000000000000000 ) ) ;
#30810=CARTESIAN_POINT ( 'NONE',  ( 0.3654063281920720829, 11.62642356802261823, 3.951404032559308277 ) ) ;
#30821=CARTESIAN_POINT ( 'NONE',  ( 0.2915757698887283533, -10.71881693660618140, -5.940579417090889436 ) ) ;
#30834=CARTESIAN_POINT ( 'NONE',  ( 0.2646305136544072623, 0.1321451301299527148, -12.24595685781654453 ) ) ;
#30835=CARTESIAN_POINT ( 'NONE',  ( 0.2650492594609232255, -12.07870403910582624, 2.017987075343919745 ) ) ;
#30840=CARTESIAN_POINT ( 'NONE',  ( 2.368238019615081402, 2.455958560214755781, -7.273245349264682247 ) ) ;
#30845=CARTESIAN_POINT ( 'NONE',  ( 5.536195898058073439, 0.008496323383586771791, -0.0002547682446684141071 ) ) ;
#30847=CARTESIAN_POINT ( 'NONE',  ( 2.247112776671468026, 2.720990995225304410, 7.135103076758457341 ) ) ;
#30848=( BOUNDED_SURFACE ( )  B_SPLINE_SURFACE ( 3, 1, ( 
 ( #58834, #18895 ),
 ( #59451, #13254 ),
 ( #33534, #49175 ),
 ( #8259, #28531 ) ),
 .UNSPECIFIED., .F., .F., .F. ) 
 B_SPLINE_SURFACE_WITH_KNOTS ( ( 4, 4 ),
 ( 2, 2 ),
 ( 0.000000000000000000, 1.000000000000000000 ),
 ( 0.000000000000000000, 1.000000000000000000 ),
 .UNSPECIFIED. ) 
 GEOMETRIC_REPRESENTATION_ITEM ( )  RATIONAL_B_SPLINE_SURFACE ( (
 ( 1.000000000000000000, 1.000000000000000000),
 ( 0.6933888150995267674, 0.9895912004443193632),
 ( 0.6933888150995267674, 0.9895912004443193632),
 ( 1.000000000000000000, 1.000000000000000000) ) ) 
 REPRESENTATION_ITEM ( '' )  SURFACE ( )  );
#30853=CARTESIAN_POINT ( 'NONE',  ( 0.2653519890518151181, 12.24619734961135542, -8.824939166405896469E-06 ) ) ;
#30856=CARTESIAN_POINT ( 'NONE',  ( 5.515188684475870851, 0.005339000964281803707, 0.0003622115669623466238 ) ) ;
#30857=CARTESIAN_POINT ( 'NONE',  ( 2.305787727787083519, -7.135468203929965725, -2.774453000917220802 ) ) ;
#30861=ORIENTED_EDGE ( 'NONE', *, *, #32247, .T. ) ;
#30863=CARTESIAN_POINT ( 'NONE',  ( 2.253265082352432724, -6.549959928643412255, -3.929729351083060873 ) ) ;
#30867=CARTESIAN_POINT ( 'NONE',  ( 1.194176325881332934, 9.279760592562206867, -8.457794872459018620 ) ) ;
#30868=CARTESIAN_POINT ( 'NONE',  ( 5.514970785353741078, 0.004532877335078713300, 0.001326349372336309675 ) ) ;
#30876=CARTESIAN_POINT ( 'NONE',  ( 0.3537226245948376091, 10.49813096858609640, 6.362463382302304460 ) ) ;
#30882=ORIENTED_EDGE ( 'NONE', *, *, #53754, .T. ) ;
#30885=CARTESIAN_POINT ( 'NONE',  ( 2.406456491627780636, 10.36527681095535769, 1.188938370542462097 ) ) ;
#30888=CARTESIAN_POINT ( 'NONE',  ( 2.717984159219746232, 2.930214355830766948, 7.221467817271564726 ) ) ;
#30896=EDGE_LOOP ( 'NONE', ( #42462, #29550, #50372, #51262 ) ) ;
#30901=DIRECTION ( 'NONE',  ( 0.000000000000000000, 0.000000000000000000, -1.000000000000000000 ) ) ;
#30908=ADVANCED_FACE ( 'NONE', ( #39328 ), #597, .F. ) ;
#30915=CARTESIAN_POINT ( 'NONE',  ( 0.3040950598368152291, -8.072385578287409658, -9.229598020917764600 ) ) ;
#30916=CARTESIAN_POINT ( 'NONE',  ( 1.375507693220546113, 10.03411718356233706, -7.647735792764737361 ) ) ;
#30919=CARTESIAN_POINT ( 'NONE',  ( 1.109979610372547443, -10.60154531817216572, -6.674783385105683919 ) ) ;
#30924=EDGE_LOOP ( 'NONE', ( #48753, #5159, #49898, #31558 ) ) ;
#30929=CARTESIAN_POINT ( 'NONE',  ( 2.253265082352139625, -3.707567016434152318, -6.678225412356649571 ) ) ;
#30931=CARTESIAN_POINT ( 'NONE',  ( 2.241506898688418126, 7.525229609709738199, 1.286963596520017461 ) ) ;
#30934=CARTESIAN_POINT ( 'NONE',  ( 1.719304012341582588, 5.690355757825640737, -11.38834240361563488 ) ) ;
#30944=CARTESIAN_POINT ( 'NONE',  ( 0.2653519789438783527, -2.104833950422661193, 12.06397564829375746 ) ) ;
#30948=AXIS2_PLACEMENT_3D ( 'NONE', #41104, #57083, #16181 ) ;
#30957=ORIENTED_EDGE ( 'NONE', *, *, #18021, .F. ) ;
#30959=CARTESIAN_POINT ( 'NONE',  ( 3.100650473569641186, 3.129198107108005278, -7.276570693048371119 ) ) ;
#30967=DIRECTION ( 'NONE',  ( 0.3939253465568944290, -0.3052156353794323596, -0.8669868725995567571 ) ) ;
#30975=ORIENTED_EDGE ( 'NONE', *, *, #1205, .F. ) ;
#30976=DIRECTION ( 'NONE',  ( -0.3939253465568944290, -0.8669868725995537595, -0.3052156353794409638 ) ) ;
#30990=CARTESIAN_POINT ( 'NONE',  ( 5.515188684475870851, -0.004322737127823994552, -0.003154373509839847670 ) ) ;
#30994=ORIENTED_EDGE ( 'NONE', *, *, #4130, .T. ) ;
#31001=CARTESIAN_POINT ( 'NONE',  ( 0.2646305136544065406, 10.67138229758229429, 6.008537389229452685 ) ) ;
#31007=VERTEX_POINT ( 'NONE', #81 ) ;
#31014=CARTESIAN_POINT ( 'NONE',  ( 0.3665391374699465965, 0.2638605131387155023, 12.27992639892678461 ) ) ;
#31017=CARTESIAN_POINT ( 'NONE',  ( 0.2958664285830442386, -4.398464391600247048, -11.43993536884560669 ) ) ;
#31019=EDGE_CURVE ( 'NONE', #57990, #5000, #48160, .T. ) ;
#31023=ADVANCED_FACE ( 'NONE', ( #21345 ), #43098, .F. ) ;
#31026=CARTESIAN_POINT ( 'NONE',  ( 2.258463476536646919, 6.683417898966930615, -3.701774005560789504 ) ) ;
#31028=CARTESIAN_POINT ( 'NONE',  ( 0.5572780756287527559, -3.933334466452446332, -11.70006938410077346 ) ) ;
#31059=VERTEX_POINT ( 'NONE', #61572 ) ;
#31068=CARTESIAN_POINT ( 'NONE',  ( 2.262775599886255762, -7.640237753423681610, -0.1412024122916668845 ) ) ;
#31069=ORIENTED_EDGE ( 'NONE', *, *, #44532, .T. ) ;
#31072=CARTESIAN_POINT ( 'NONE',  ( 0.3474126878361803450, -12.03947592323248372, 2.385599230262000159 ) ) ;
#31077=CARTESIAN_POINT ( 'NONE',  ( 0.3053067050349164147, 12.03105545708856283, 2.355726819985464182 ) ) ;
#31084=CARTESIAN_POINT ( 'NONE',  ( 0.6473888112830256114, -10.54705164520783178, 6.470260187014684305 ) ) ;
#31086=CARTESIAN_POINT ( 'NONE',  ( 1.633930747251837845, -12.36466318969074685, 2.909970528251258681 ) ) ;
#31108=CARTESIAN_POINT ( 'NONE',  ( 5.514970785353741078, 0.003929719953530069060, 0.002619824551223233922 ) ) ;
#31116=ORIENTED_EDGE ( 'NONE', *, *, #60346, .F. ) ;
#31122=CARTESIAN_POINT ( 'NONE',  ( 2.770579946183328257, 1.056759439485575491, 7.739026583264747572 ) ) ;
#31123=VERTEX_POINT ( 'NONE', #62887 ) ;
#31131=DIRECTION ( 'NONE',  ( 0.3939253465568943180, -0.6978179301705759174, -0.5982248387291217995 ) ) ;
#31134=CARTESIAN_POINT ( 'NONE',  ( 0.2651627923886330507, -7.938954356958149994, 9.324231535593082043 ) ) ;
#31139=CARTESIAN_POINT ( 'NONE',  ( 0.5547464869798244269, 0.3049355384529007784, 12.33891836761636362 ) ) ;
#31151=ORIENTED_EDGE ( 'NONE', *, *, #33952, .F. ) ;
#31173=CARTESIAN_POINT ( 'NONE',  ( 1.104777566491146557, 12.51694124543052133, -0.4777483965054175608 ) ) ;
#31178=CARTESIAN_POINT ( 'NONE',  ( 0.2834382757447998502, -10.71064820518738969, -5.949714385480752377 ) ) ;
#31180=CIRCLE ( 'NONE', #52405, 4.000000000000000000 ) ;
#31185=B_SPLINE_CURVE_WITH_KNOTS ( 'NONE', 3,
 ( #50939, #50297, #45286, #5062, #49953, #20336, #19708, #4752, #65544, #19376, #30629, #25326, #5387, #25659, #25013, #19039 ),
 .UNSPECIFIED., .F., .F.,
 ( 4, 3, 3, 3, 3, 4 ),
 ( 2.813154621161213038E-15, 0.0002126834539179820556, 0.0004253519300366505849, 0.0006380165497224521681, 0.0007442707582428671493, 0.0009453531351415104091 ),
 .UNSPECIFIED. ) ;
#31186=ORIENTED_EDGE ( 'NONE', *, *, #35927, .F. ) ;
#31187=CARTESIAN_POINT ( 'NONE',  ( 5.516018279890452902, 0.005976902763918716562, 0.003191189039764460479 ) ) ;
#31193=DIRECTION ( 'NONE',  ( 1.000000000000000000, -0.000000000000000000, -0.000000000000000000 ) ) ;
#31194=CARTESIAN_POINT ( 'NONE',  ( 2.288423627607358846, 2.464337058688887971, -7.242304196986070863 ) ) ;
#31198=CARTESIAN_POINT ( 'NONE',  ( 0.7446945582518242901, -12.27434006248818577, 1.802628359587700846 ) ) ;
#31199=CARTESIAN_POINT ( 'NONE',  ( 3.152665057734040488, 0.000000000000000000, 0.000000000000000000 ) ) ;
#31202=CARTESIAN_POINT ( 'NONE',  ( 2.273267844204864385, 2.756477528575298042, 7.130811676080282879 ) ) ;
#31222=CARTESIAN_POINT ( 'NONE',  ( 1.719304012341585253, 11.38834240361577521, -5.690355757825364513 ) ) ;
#31224=ORIENTED_EDGE ( 'NONE', *, *, #9097, .T. ) ;
#31234=ORIENTED_EDGE ( 'NONE', *, *, #11842, .F. ) ;
#31237=CARTESIAN_POINT ( 'NONE',  ( 0.9232058338315058954, 10.60677148422253424, -6.559496812049550485 ) ) ;
#31238=CARTESIAN_POINT ( 'NONE',  ( 2.305787727787084407, 3.971363876083963351, 6.545285700970541853 ) ) ;
#31251=CARTESIAN_POINT ( 'NONE',  ( 1.020182472820975184, 11.58401323226438606, 4.691131056021832002 ) ) ;
#31252=CARTESIAN_POINT ( 'NONE',  ( 2.639814597422739162, -1.095525832903433416, -7.689608172406203757 ) ) ;
#31262=CARTESIAN_POINT ( 'NONE',  ( 0.3002738374340832572, -2.350339881555025379, 12.03040002643110640 ) ) ;
#31263=CARTESIAN_POINT ( 'NONE',  ( 2.350038591457284554, -4.746773736940665955, -9.502240128961169319 ) ) ;
#31264=CARTESIAN_POINT ( 'NONE',  ( 2.373367633546870525, -7.676289145832773109, -0.1808255748566272858 ) ) ;
#31265=EDGE_CURVE ( 'NONE', #47037, #57528, #12429, .T. ) ;
#31273=CARTESIAN_POINT ( 'NONE',  ( 2.835339799623981971, 6.206025468804425849, -4.778327228934518445 ) ) ;
#31284=CARTESIAN_POINT ( 'NONE',  ( 0.3109076770648991350, 12.25911371383828907, -0.2359198520041591307 ) ) ;
#31286=CARTESIAN_POINT ( 'NONE',  ( 0.3675815128205894289, -5.910255304480370953, -10.76447900494946452 ) ) ;
#31292=ORIENTED_EDGE ( 'NONE', *, *, #12435, .F. ) ;
#31293=CARTESIAN_POINT ( 'NONE',  ( 0.2653519789438759657, 2.148225749114993199, 12.05632450344283768 ) ) ;
#31311=CARTESIAN_POINT ( 'NONE',  ( 2.251139882114757018, 7.133642337268560674, 2.728563091336710933 ) ) ;
#31313=CARTESIAN_POINT ( 'NONE',  ( 0.3675815128205912052, 12.13672785388552811, -1.872154644481959895 ) ) ;
#31314=VERTEX_POINT ( 'NONE', #61188 ) ;
#31334=CARTESIAN_POINT ( 'NONE',  ( 2.241352910868908754, 7.532448145350508995, 1.243507963608119438 ) ) ;
#31337=CARTESIAN_POINT ( 'NONE',  ( 1.634816307077841424, 12.16351623921594260, -3.661851000130128320 ) ) ;
#31338=FACE_OUTER_BOUND ( 'NONE', #46794, .T. ) ;
#31358=CARTESIAN_POINT ( 'NONE',  ( 2.665405856346786617, -9.549966053095406693, -0.5773576323838727209 ) ) ;
#31365=CARTESIAN_POINT ( 'NONE',  ( 0.8375941296786741930, 10.57337970710546493, 6.548446001455325849 ) ) ;
#31373=CARTESIAN_POINT ( 'NONE',  ( 0.2739690278137261736, -5.965352196073669511, 10.69833303470763575 ) ) ;
#31391=CARTESIAN_POINT ( 'NONE',  ( 0.9232058338315048962, -11.84276737136203828, 3.908895078357480291 ) ) ;
#31393=CARTESIAN_POINT ( 'NONE',  ( 0.2655924914740778187, 6.084990060696511271, 10.62761259256418889 ) ) ;
#31403=CARTESIAN_POINT ( 'NONE',  ( 1.198791140417946988, -2.686891236232506586, 12.26651935498910184 ) ) ;
#31404=CARTESIAN_POINT ( 'NONE',  ( 0.2717059086739030405, -12.03041489115253349, 2.300075171420195019 ) ) ;
#31421=CARTESIAN_POINT ( 'NONE',  ( 0.2646305136544065406, 6.237419468587079407, 10.53923716745248917 ) ) ;
#31425=CARTESIAN_POINT ( 'NONE',  ( 0.2833330754217412428, 4.379886056891059809, -11.44258640049857512 ) ) ;
#31429=CARTESIAN_POINT ( 'NONE',  ( 0.6511581176971786844, 2.473966499148548603, -12.12498040206563665 ) ) ;
#31433=CARTESIAN_POINT ( 'NONE',  ( 0.2653141617320998735, 10.58343467791296533, 6.161204121352730212 ) ) ;
#31443=CARTESIAN_POINT ( 'NONE',  ( 2.261269890822073414, 1.189259211195942800, 7.547924622047982091 ) ) ;
#31445=CARTESIAN_POINT ( 'NONE',  ( 3.031336079629544322, 7.038432939676056321, 3.582646412484421727 ) ) ;
#31447=CARTESIAN_POINT ( 'NONE',  ( 5.520433897694421610, 0.003119431460922217261, 0.01473594271720289964 ) ) ;
#31457=CARTESIAN_POINT ( 'NONE',  ( 0.2653519890518161728, -7.871697161810750742, 9.381137101569645864 ) ) ;
#31459=( BOUNDED_SURFACE ( )  B_SPLINE_SURFACE ( 3, 1, ( 
 ( #26593, #46886 ),
 ( #16629, #36898 ),
 ( #48535, #8283 ),
 ( #6978, #42194 ) ),
 .UNSPECIFIED., .F., .F., .F. ) 
 B_SPLINE_SURFACE_WITH_KNOTS ( ( 4, 4 ),
 ( 2, 2 ),
 ( 0.000000000000000000, 1.000000000000000000 ),
 ( 0.000000000000000000, 1.000000000000000000 ),
 .UNSPECIFIED. ) 
 GEOMETRIC_REPRESENTATION_ITEM ( )  RATIONAL_B_SPLINE_SURFACE ( (
 ( 1.000000000000000000, 1.000000000000000000),
 ( 0.9856612449720755231, 0.9999558406602322425),
 ( 0.9856612449720755231, 0.9999558406602322425),
 ( 1.000000000000000000, 1.000000000000000000) ) ) 
 REPRESENTATION_ITEM ( '' )  SURFACE ( )  );
#31463=CARTESIAN_POINT ( 'NONE',  ( 0.2834382757448035139, 11.44241760114840467, -4.380429851625208926 ) ) ;
#31471=CARTESIAN_POINT ( 'NONE',  ( 2.430348790457563357, 1.528169972228492712, 7.544199152379105655 ) ) ;
#31473=CARTESIAN_POINT ( 'NONE',  ( 1.719304012341460908, 3.626341562669523011, -12.20344780066162649 ) ) ;
#31475=DIRECTION ( 'NONE',  ( -1.000000000000000000, -0.000000000000000000, -0.000000000000000000 ) ) ;
#31479=ORIENTED_EDGE ( 'NONE', *, *, #25384, .F. ) ;
#31489=CARTESIAN_POINT ( 'NONE',  ( 1.719304012339844867, -11.67935079956417610, 5.066286238786176455 ) ) ;
#31492=CARTESIAN_POINT ( 'NONE',  ( 2.770579946183338915, 4.165025702425937837, -6.607710183380588020 ) ) ;
#31495=CARTESIAN_POINT ( 'NONE',  ( 3.152665057735194232, -3.161213418914472051, -7.281573230474045921 ) ) ;
#31503=ORIENTED_EDGE ( 'NONE', *, *, #38104, .T. ) ;
#31506=CARTESIAN_POINT ( 'NONE',  ( 20.00005080000000035, 3.872983346207417021, 1.000000000000000000 ) ) ;
#31508=ORIENTED_EDGE ( 'NONE', *, *, #16502, .F. ) ;
#31509=DIRECTION ( 'NONE',  ( -1.000000000000000000, -0.000000000000000000, -0.000000000000000000 ) ) ;
#31511=CARTESIAN_POINT ( 'NONE',  ( 1.198791140418998813, -12.44572864632790932, 1.670544840358051841 ) ) ;
#31513=CARTESIAN_POINT ( 'NONE',  ( 0.2833330754217385228, 6.300330022379362127, -10.50818856955511471 ) ) ;
#31514=CARTESIAN_POINT ( 'NONE',  ( 2.280717697723836146, 2.762096098144338985, 7.131299706077038003 ) ) ;
#31520=CARTESIAN_POINT ( 'NONE',  ( 2.655192694323875280, -9.337840456948674372, 2.234846078477743969 ) ) ;
#31526=ORIENTED_EDGE ( 'NONE', *, *, #54926, .F. ) ;
#31533=CARTESIAN_POINT ( 'NONE',  ( 1.198791140419928070, -7.669598593074918647, -9.943044756149140184 ) ) ;
#31545=ADVANCED_FACE ( 'NONE', ( #26922, #47222 ), #18263, .T. ) ;
#31550=CARTESIAN_POINT ( 'NONE',  ( 2.653899356900128126, 2.902068786425453073, 7.209790345489556884 ) ) ;
#31553=ADVANCED_FACE ( 'NONE', ( #48522 ), #7314, .T. ) ;
#31556=CARTESIAN_POINT ( 'NONE',  ( 0.2869720083484362805, 11.58405933820307077, -3.994435966589948706 ) ) ;
#31558=ORIENTED_EDGE ( 'NONE', *, *, #39165, .F. ) ;
#31559=EDGE_LOOP ( 'NONE', ( #15082, #50556, #24309, #58877 ) ) ;
#31562=CARTESIAN_POINT ( 'NONE',  ( 3.100650473569749987, -0.9283202922944330249, -7.866294126167268530 ) ) ;
#31573=CARTESIAN_POINT ( 'NONE',  ( 0.4626703367449018223, -10.51809671647426292, -6.399577980714925118 ) ) ;
#31576=CARTESIAN_POINT ( 'NONE',  ( -14.47334165536100059, 7.347880794884120722E-16, 6.000000000000000888 ) ) ;
#31579=CARTESIAN_POINT ( 'NONE',  ( 5.530133899448235191, 0.01293763278443408986, -0.009387834778845371292 ) ) ;
#31581=CARTESIAN_POINT ( 'NONE',  ( 2.573738926104375047, 6.081632213771451134, -4.796056562246111987 ) ) ;
#31584=ORIENTED_EDGE ( 'NONE', *, *, #17864, .T. ) ;
#31585=CARTESIAN_POINT ( 'NONE',  ( 2.903928887688294491, 3.918141038919765062, -7.845932231841970861 ) ) ;
#31586=CARTESIAN_POINT ( 'NONE',  ( 0.2657645697724696499, 2.275433120353249627, -12.03308811492266805 ) ) ;
#31589=DIRECTION ( 'NONE',  ( -1.000000000000000000, -0.000000000000000000, -0.000000000000000000 ) ) ;
#31593=CARTESIAN_POINT ( 'NONE',  ( 0.2652384529303141170, -2.061422456317107077, 12.07141085622971666 ) ) ;
#31596=CARTESIAN_POINT ( 'NONE',  ( 0.3665391374699465965, 7.691255657244421506, -9.576575648338943481 ) ) ;
#31597=B_SPLINE_CURVE_WITH_KNOTS ( 'NONE', 3,
 ( #14170, #9496, #19830, #48791, #13206, #39440, #4553, #29163, #19169, #55065, #49760, #18850, #28484, #33793, #23855, #44116 ),
 .UNSPECIFIED., .F., .F.,
 ( 4, 3, 3, 3, 3, 4 ),
 ( 2.710505431213761567E-19, 0.0003017745587525280659, 0.0006035491769808807878, 0.0009053241094668280659, 0.001207275924540836525, 0.001510325902534664921 ),
 .UNSPECIFIED. ) ;
#31617=CARTESIAN_POINT ( 'NONE',  ( 2.297017764050236277, 4.791851130936026770, -5.967068736727147993 ) ) ;
#31624=CARTESIAN_POINT ( 'NONE',  ( 0.7400311444011693496, 7.698344902199217188, -9.726551103566730916 ) ) ;
#31626=B_SPLINE_CURVE_WITH_KNOTS ( 'NONE', 3,
 ( #35853, #30876, #48990, #51196, #5648, #49330, #3448, #24340, #59279, #14033, #44293, #23716, #33987, #44606, #54638, #8739, #64564, #19038, #34324 ),
 .UNSPECIFIED., .F., .F.,
 ( 4, 3, 3, 3, 3, 3, 4 ),
 ( 7.903714856861513238E-18, 4.457896483014812754E-05, 6.639290541542165714E-05, 8.820687556479086513E-05, 0.0001100173248778937932, 0.0001545671401658124818, 0.0001830328308068605555 ),
 .UNSPECIFIED. ) ;
#31627=CARTESIAN_POINT ( 'NONE',  ( 2.241352910868908310, 4.970878533273761946, 5.794346703933863196 ) ) ;
#31631=CARTESIAN_POINT ( 'NONE',  ( 2.241528039335007882, -6.619488482362960724, 3.803597072146510438 ) ) ;
#31636=( BOUNDED_SURFACE ( )  B_SPLINE_SURFACE ( 3, 1, ( 
 ( #37105, #37442 ),
 ( #12172, #22485 ),
 ( #31782, #11200 ),
 ( #56777, #6218 ) ),
 .UNSPECIFIED., .F., .F., .F. ) 
 B_SPLINE_SURFACE_WITH_KNOTS ( ( 4, 4 ),
 ( 2, 2 ),
 ( 0.000000000000000000, 1.000000000000000000 ),
 ( 0.000000000000000000, 1.000000000000000000 ),
 .UNSPECIFIED. ) 
 GEOMETRIC_REPRESENTATION_ITEM ( )  RATIONAL_B_SPLINE_SURFACE ( (
 ( 1.000000000000000000, 1.000000000000000000),
 ( 0.9942764183789327692, 0.8450855930916585379),
 ( 0.9942764183789327692, 0.8450855930916585379),
 ( 1.000000000000000000, 1.000000000000000000) ) ) 
 REPRESENTATION_ITEM ( '' )  SURFACE ( )  );
#31639=CARTESIAN_POINT ( 'NONE',  ( 2.373367633546871858, -5.764146204907428128, -5.072743978105297202 ) ) ;
#31646=CARTESIAN_POINT ( 'NONE',  ( 0.9232058338315058954, -7.723624854284779850, 9.791640253608122180 ) ) ;
#31651=EDGE_CURVE ( 'NONE', #63267, #32172, #33852, .T. ) ;
#31659=VECTOR ( 'NONE', #15437, 1000.000000000000114 ) ;
#31667=CARTESIAN_POINT ( 'NONE',  ( 1.194176325881332268, 4.773862381874729444, 11.61285876598807754 ) ) ;
#31672=CARTESIAN_POINT ( 'NONE',  ( 0.2648978790185584908, -12.24533305150758089, -0.1321385342563691223 ) ) ;
#31674=CARTESIAN_POINT ( 'NONE',  ( 3.152665057736233845, -4.725420687649230622, 6.378477742801980988 ) ) ;
#31679=CARTESIAN_POINT ( 'NONE',  ( 0.3057689695767527027, -5.928746590069652989, 10.73077184758789393 ) ) ;
#31681=ORIENTED_EDGE ( 'NONE', *, *, #41184, .F. ) ;
#31693=CARTESIAN_POINT ( 'NONE',  ( 2.717984159220113494, -7.788152353089298430, 0.2836133496102792861 ) ) ;
#31703=CARTESIAN_POINT ( 'NONE',  ( 2.284126774967659035, -7.647017279602160933, -0.1584898568958676424 ) ) ;
#31705=ORIENTED_EDGE ( 'NONE', *, *, #10396, .T. ) ;
#31706=CARTESIAN_POINT ( 'NONE',  ( 1.459561108992593281, 8.601340491610839578, 9.267924853468722191 ) ) ;
#31707=FACE_OUTER_BOUND ( 'NONE', #48888, .T. ) ;
#31708=CARTESIAN_POINT ( 'NONE',  ( 0.2801149460245139777, -12.02936836014264621, 2.320387321174126605 ) ) ;
#31709=EDGE_LOOP ( 'NONE', ( #63849, #13323, #40320, #9317 ) ) ;
#31716=VERTEX_POINT ( 'NONE', #48848 ) ;
#31720=CARTESIAN_POINT ( 'NONE',  ( 1.452237505248555660, 6.833827325205318992, 10.65201107290469906 ) ) ;
#31728=CARTESIAN_POINT ( 'NONE',  ( 0.3665391374699472626, 6.368473106897130087, 10.50279796150439005 ) ) ;
#31729=CARTESIAN_POINT ( 'NONE',  ( 0.3002738374340850891, 4.403689978763226875, -11.43949898053766390 ) ) ;
#31732=EDGE_CURVE ( 'NONE', #41303, #18751, #36084, .T. ) ;
#31738=EDGE_LOOP ( 'NONE', ( #50770, #34072, #46968, #54048 ) ) ;
#31745=EDGE_CURVE ( 'NONE', #47135, #16200, #2818, .T. ) ;
#31747=CARTESIAN_POINT ( 'NONE',  ( 5.520433897694421610, -0.01186170453199831935, 0.009283255140285138346 ) ) ;
#31750=CARTESIAN_POINT ( 'NONE',  ( 2.241352910868908754, -3.889181972941404553, -6.569501556381482921 ) ) ;
#31754=VERTEX_POINT ( 'NONE', #39499 ) ;
#31759=ORIENTED_EDGE ( 'NONE', *, *, #8704, .T. ) ;
#31767=CARTESIAN_POINT ( 'NONE',  ( 0.2759803524722221346, -11.44482553421628346, -4.367180139677437900 ) ) ;
#31768=CARTESIAN_POINT ( 'NONE',  ( 0.3278977287071219160, 5.917385921415800887, 10.74546228373869283 ) ) ;
#31769=CARTESIAN_POINT ( 'NONE',  ( 0.2646305136544072623, 10.67138229758229606, 6.008537389229454462 ) ) ;
#31771=ORIENTED_EDGE ( 'NONE', *, *, #60575, .T. ) ;
#31777=EDGE_CURVE ( 'NONE', #12414, #11179, #44824, .T. ) ;
#31782=CARTESIAN_POINT ( 'NONE',  ( 5.515188684475870851, -0.004322737127823499288, 0.003154373509839884532 ) ) ;
#31786=ORIENTED_EDGE ( 'NONE', *, *, #9571, .T. ) ;
#31787=CARTESIAN_POINT ( 'NONE',  ( 2.556980015513709237, 7.578583798307162667, -1.570584617272491768 ) ) ;
#31790=CARTESIAN_POINT ( 'NONE',  ( 2.241537034860906275, 1.330359961362386878, -7.517665055735998081 ) ) ;
#31800=EDGE_LOOP ( 'NONE', ( #30957, #5790, #41742, #39705 ) ) ;
#31804=EDGE_CURVE ( 'NONE', #30254, #8001, #36926, .T. ) ;
#31812=B_SPLINE_CURVE_WITH_KNOTS ( 'NONE', 3,
 ( #44640, #14396, #34669, #39998, #54967, #65275, #9395, #29681, #55290, #60281, #14705, #50975, #35328, #755, #56270, #51958, #51641, #6401, #45319 ),
 .UNSPECIFIED., .F., .F.,
 ( 4, 3, 3, 3, 3, 3, 4 ),
 ( 7.217888169571747161E-18, 2.825908398991472574E-05, 4.208813692702314017E-05, 5.591713747220622617E-05, 6.279584083537281586E-05, 9.105792820726668299E-05, 0.0001153131102486956423 ),
 .UNSPECIFIED. ) ;
#31814=CARTESIAN_POINT ( 'NONE',  ( 0.3665391374699464300, 12.27992639892678284, 0.2638605131387594671 ) ) ;
#31817=CARTESIAN_POINT ( 'NONE',  ( 2.262775599886276634, 4.802882839669051940, 5.943524836196961481 ) ) ;
#31819=ADVANCED_FACE ( 'NONE', ( #32134 ), #10492, .T. ) ;
#31821=CARTESIAN_POINT ( 'NONE',  ( 2.305787727787083519, 2.461236246751071555, 7.249469779319919205 ) ) ;
#31822=CARTESIAN_POINT ( 'NONE',  ( 2.241506898688419902, -0.03933068055385580131, -7.634383346098562839 ) ) ;
#31823=CARTESIAN_POINT ( 'NONE',  ( 0.5547464869798254261, -1.842327806480229757, 12.20441397277155815 ) ) ;
#31825=EDGE_CURVE ( 'NONE', #58095, #44356, #41645, .T. ) ;
#31831=( BOUNDED_SURFACE ( )  B_SPLINE_SURFACE ( 3, 1, ( 
 ( #35811, #26199 ),
 ( #36145, #51153 ),
 ( #5263, #65745 ),
 ( #41464, #31814 ) ),
 .UNSPECIFIED., .F., .F., .F. ) 
 B_SPLINE_SURFACE_WITH_KNOTS ( ( 4, 4 ),
 ( 2, 2 ),
 ( 0.000000000000000000, 1.000000000000000000 ),
 ( 0.000000000000000000, 1.000000000000000000 ),
 .UNSPECIFIED. ) 
 GEOMETRIC_REPRESENTATION_ITEM ( )  RATIONAL_B_SPLINE_SURFACE ( (
 ( 1.000000000000000000, 1.000000000000000000),
 ( 0.9942764183789327692, 0.8450855930916580938),
 ( 0.9942764183789327692, 0.8450855930916580938),
 ( 1.000000000000000000, 1.000000000000000000) ) ) 
 REPRESENTATION_ITEM ( '' )  SURFACE ( )  );
#31835=ORIENTED_EDGE ( 'NONE', *, *, #20855, .T. ) ;
#31839=B_SPLINE_CURVE_WITH_KNOTS ( 'NONE', 3,
 ( #38202, #54506, #28560, #13904, #24224, #43192, #44490 ),
 .UNSPECIFIED., .F., .F.,
 ( 4, 3, 4 ),
 ( 0.000000000000000000, 0.001700533616330591980, 0.005002426799371264415 ),
 .UNSPECIFIED. ) ;
#31840=CARTESIAN_POINT ( 'NONE',  ( 5.515539859299206427, 0.005924322247674738452, 0.001241880655086611586 ) ) ;
#31850=CARTESIAN_POINT ( 'NONE',  ( 2.524535260910446777, 7.725637239509726584, -0.2211075636754606388 ) ) ;
#31851=CARTESIAN_POINT ( 'NONE',  ( 5.514970785353741078, 0.002619824551223220045, -0.003929719953530077733 ) ) ;
#31854=CARTESIAN_POINT ( 'NONE',  ( 1.104777566491147889, -5.844728374724341258, 11.07886329447274676 ) ) ;
#31857=FACE_OUTER_BOUND ( 'NONE', #12995, .T. ) ;
#31859=CARTESIAN_POINT ( 'NONE',  ( 0.9232058338315048962, 0.3773051331669723951, -12.46548196349785798 ) ) ;
#31866=ORIENTED_EDGE ( 'NONE', *, *, #18832, .F. ) ;
#31874=ORIENTED_EDGE ( 'NONE', *, *, #5754, .F. ) ;
#31875=CARTESIAN_POINT ( 'NONE',  ( 0.3610902822527172207, 4.444884365376601032, 11.44530431865294418 ) ) ;
#31884=CARTESIAN_POINT ( 'NONE',  ( 0.2648978790185619880, -9.465406350830555482, -7.769924372105300847 ) ) ;
#31887=CARTESIAN_POINT ( 'NONE',  ( 2.899286259009557387, 4.769992516330251675, 6.239228647238516778 ) ) ;
#31902=CARTESIAN_POINT ( 'NONE',  ( 2.247206125382827935, -6.670391186503669800, 3.717496781928072203 ) ) ;
#31905=CARTESIAN_POINT ( 'NONE',  ( 0.3053067050349139722, 2.355726819985581422, -12.03105545708854685 ) ) ;
#31913=CARTESIAN_POINT ( 'NONE',  ( 1.452237505248552996, -11.24427360515646512, 5.807998527925852805 ) ) ;
#31918=CARTESIAN_POINT ( 'NONE',  ( 0.3675815128205894289, 11.62724744438065727, 3.951233083390508050 ) ) ;
#31928=ORIENTED_EDGE ( 'NONE', *, *, #65095, .F. ) ;
#31934=DIRECTION ( 'NONE',  ( -1.000000000000000000, -0.000000000000000000, -0.000000000000000000 ) ) ;
#31952=CARTESIAN_POINT ( 'NONE',  ( 2.241449424704146764, 4.954182807723340076, 5.808712090826627872 ) ) ;
#31957=CARTESIAN_POINT ( 'NONE',  ( 1.287602823388475759, 6.765713844066192806, -10.61402828236309759 ) ) ;
#31958=DIRECTION ( 'NONE',  ( 0.3865475372811020272, -0.6938894834606043061, -0.6075346789811185699 ) ) ;
#31970=CARTESIAN_POINT ( 'NONE',  ( 0.2648978790185584908, -7.972372351883092456, 9.295532325666423290 ) ) ;
#31971=CARTESIAN_POINT ( 'NONE',  ( 5.516018279890452902, 0.0009545156522404378389, -0.006707902355168868236 ) ) ;
#31974=ORIENTED_EDGE ( 'NONE', *, *, #52910, .T. ) ;
#31978=EDGE_LOOP ( 'NONE', ( #38006, #37702, #57293, #48981 ) ) ;
#31981=CARTESIAN_POINT ( 'NONE',  ( 2.241352910868908754, 4.843133558968205854, -5.901537464758406237 ) ) ;
#31982=ORIENTED_EDGE ( 'NONE', *, *, #14802, .T. ) ;
#31992=CARTESIAN_POINT ( 'NONE',  ( 0.2911222467163592231, -5.940753417478847886, -10.71854909364325614 ) ) ;
#31999=CARTESIAN_POINT ( 'NONE',  ( 0.3278977287071236368, -12.26453627383315848, -0.2481246099269338867 ) ) ;
#32001=ORIENTED_EDGE ( 'NONE', *, *, #36041, .T. ) ;
#32007=CARTESIAN_POINT ( 'NONE',  ( 2.247206125383337749, 6.554642244887925351, 3.917979829729163921 ) ) ;
#32008=ORIENTED_EDGE ( 'NONE', *, *, #56631, .T. ) ;
#32013=CARTESIAN_POINT ( 'NONE',  ( 2.280717697723837034, -7.131299706077048661, 2.762096098144314560 ) ) ;
#32018=CARTESIAN_POINT ( 'NONE',  ( 0.8375941296809037429, -11.54987202580284489, -4.612912274496607345 ) ) ;
#32020=CARTESIAN_POINT ( 'NONE',  ( 1.633930747253118376, -0.7186603069043160374, -12.68212725188779544 ) ) ;
#32031=CARTESIAN_POINT ( 'NONE',  ( 0.2651627923886347715, 9.437479615842747194, -7.803990550466204823 ) ) ;
#32036=CARTESIAN_POINT ( 'NONE',  ( 1.109979610369590253, -4.732439402373736392, 11.59954799439085349 ) ) ;
#32044=ORIENTED_EDGE ( 'NONE', *, *, #60346, .T. ) ;
#32057=LINE ( 'NONE', #47696, #30188 ) ;
#32062=CARTESIAN_POINT ( 'NONE',  ( 0.3401186441510233305, 4.436257390736984441, -11.44115600261386767 ) ) ;
#32065=CARTESIAN_POINT ( 'NONE',  ( 0.2653519789438776311, 12.05632450344285544, -2.148225749114869743 ) ) ;
#32074=EDGE_CURVE ( 'NONE', #8430, #64491, #40106, .T. ) ;
#32083=CARTESIAN_POINT ( 'NONE',  ( 2.298277635560280086, 1.166137492762227224, 7.564013289873174450 ) ) ;
#32084=VERTEX_POINT ( 'NONE', #22506 ) ;
#32085=CARTESIAN_POINT ( 'NONE',  ( 2.430348790457427910, 6.761480562106370940, 3.678671624790056605 ) ) ;
#32099=DIRECTION ( 'NONE',  ( -1.000000000000000000, -0.000000000000000000, -0.000000000000000000 ) ) ;
#32101=B_SPLINE_CURVE_WITH_KNOTS ( 'NONE', 3,
 ( #13771, #23116, #59043, #34063, #54379, #19451, #40355, #55006, #10427, #5476, #19778, #65618, #55338 ),
 .UNSPECIFIED., .F., .F.,
 ( 4, 3, 3, 3, 4 ),
 ( 8.673617379884035472E-19, 6.607593386745623195E-05, 0.0001321518677373556051, 0.0001982171734706223505, 0.0002642860854759480666 ),
 .UNSPECIFIED. ) ;
#32103=CARTESIAN_POINT ( 'NONE',  ( 1.459561108992816880, 0.6317018236571978473, 12.62847742794662409 ) ) ;
#32107=ORIENTED_EDGE ( 'NONE', *, *, #10910, .T. ) ;
#32111=CARTESIAN_POINT ( 'NONE',  ( 0.8320506296491606557, -11.54877388447407860, 4.610676791972301736 ) ) ;
#32117=ORIENTED_EDGE ( 'NONE', *, *, #46390, .F. ) ;
#32123=CARTESIAN_POINT ( 'NONE',  ( 2.257661810676417691, -7.224098098130513179, -2.485866587321456933 ) ) ;
#32134=FACE_OUTER_BOUND ( 'NONE', #18243, .T. ) ;
#32141=CARTESIAN_POINT ( 'NONE',  ( 5.516018279890452902, 0.004180585980734530596, -0.005331956019561480582 ) ) ;
#32143=ORIENTED_EDGE ( 'NONE', *, *, #14242, .T. ) ;
#32145=EDGE_LOOP ( 'NONE', ( #18485, #25333 ) ) ;
#32147=FACE_OUTER_BOUND ( 'NONE', #227, .T. ) ;
#32152=CARTESIAN_POINT ( 'NONE',  ( 0.3006302518452025341, 12.10891847026072199, 1.905681544119282034 ) ) ;
#32159=CARTESIAN_POINT ( 'NONE',  ( 0.3218525148189821383, 6.342972338926943010, -10.49750909897045936 ) ) ;
#32163=ORIENTED_EDGE ( 'NONE', *, *, #56789, .F. ) ;
#32164=CARTESIAN_POINT ( 'NONE',  ( 2.241352910868908754, -6.652881166698485949, -3.744764251557062718 ) ) ;
#32172=VERTEX_POINT ( 'NONE', #61620 ) ;
#32182=CARTESIAN_POINT ( 'NONE',  ( 2.259025283528083072, -1.191911401085066435, 7.546748801935439843 ) ) ;
#32191=CARTESIAN_POINT ( 'NONE',  ( 1.452237505248552996, 0.5922625322518776381, -12.64182585313125351 ) ) ;
#32193=EDGE_CURVE ( 'NONE', #16970, #25922, #56987, .T. ) ;
#32198=CARTESIAN_POINT ( 'NONE',  ( 2.941278708680199916, -4.615461433467229924, -4.048809123187982806 ) ) ;
#32199=EDGE_CURVE ( 'NONE', #23561, #20597, #12309, .T. ) ;
#32210=CARTESIAN_POINT ( 'NONE',  ( 2.241536586108914708, -7.171901127201312676, 2.617055111126424638 ) ) ;
#32211=CARTESIAN_POINT ( 'NONE',  ( 2.242819959140601060, 4.985618132689532800, -5.782321801516662418 ) ) ;
#32214=VECTOR ( 'NONE', #23203, 1000.000000000000114 ) ;
#32224=CARTESIAN_POINT ( 'NONE',  ( 3.152665057736135701, -1.848755561854027452, -7.719888720907647439 ) ) ;
#32226=CARTESIAN_POINT ( 'NONE',  ( 2.259025283528611538, 3.701170455110545987, -6.683966451873481596 ) ) ;
#32227=CARTESIAN_POINT ( 'NONE',  ( 0.3341166715381306829, -8.078283863465435033, -9.234320413907880720 ) ) ;
#32231=VECTOR ( 'NONE', #61972, 1000.000000000000114 ) ;
#32233=CARTESIAN_POINT ( 'NONE',  ( 2.994568964204208594, -7.263701055179705435, -3.069094401380853210 ) ) ;
#32236=CARTESIAN_POINT ( 'NONE',  ( 5.515188684475870851, -0.002166413411657830065, -0.004893136156457991714 ) ) ;
#32237=CARTESIAN_POINT ( 'NONE',  ( 0.2869720083484346151, -0.2084396331387487200, 12.25163264065381874 ) ) ;
#32239=CARTESIAN_POINT ( 'NONE',  ( 3.152665057734120868, 6.378477742800529704, -4.725420687650643714 ) ) ;
#32247=EDGE_CURVE ( 'NONE', #54467, #19899, #16339, .T. ) ;
#32251=CARTESIAN_POINT ( 'NONE',  ( 5.514970785353741078, 0.004694330894494369230, -0.0005190732562558711188 ) ) ;
#32252=CARTESIAN_POINT ( 'NONE',  ( 0.2651627682582919920, -2.039709641845663057, 12.07509313786331795 ) ) ;
#32259=CARTESIAN_POINT ( 'NONE',  ( 3.031336079629648683, -6.621879275826741740, 4.304138522350468676 ) ) ;
#32282=CARTESIAN_POINT ( 'NONE',  ( 0.2911222467163586680, 12.10399882413662631, -1.916522451062410592 ) ) ;
#32285=CARTESIAN_POINT ( 'NONE',  ( 2.241509619876139503, 4.877966158328305823, 5.872890204493035782 ) ) ;
#32292=CARTESIAN_POINT ( 'NONE',  ( 1.634816307077887831, 6.964001572436961496, -10.62369813896834359 ) ) ;
#32298=CARTESIAN_POINT ( 'NONE',  ( 0.2648321136542688414, -4.321267941897585452, 11.45826514585342082 ) ) ;
#32302=VERTEX_POINT ( 'NONE', #12683 ) ;
#32303=CARTESIAN_POINT ( 'NONE',  ( 2.941278708680199916, -6.021511413163968207, 1.198640839021288818 ) ) ;
#32305=CARTESIAN_POINT ( 'NONE',  ( 0.2647959493198550618, 12.03358727341677614, -2.271080632827937595 ) ) ;
#32311=CARTESIAN_POINT ( 'NONE',  ( 2.827825597296802496, 3.592949031604531385, -8.278234963587674855 ) ) ;
#32317=CARTESIAN_POINT ( 'NONE',  ( 0.2646305136544065406, 12.03696649559614507, 2.256625640822357060 ) ) ;
#32324=CARTESIAN_POINT ( 'NONE',  ( 2.177405672432021877, -3.189307221897416333, 10.73538068360473829 ) ) ;
#32329=B_SPLINE_CURVE_WITH_KNOTS ( 'NONE', 3,
 ( #32820, #16893, #26878, #21898, #47493, #37506, #7921, #2621, #42143, #37163, #32495, #57473, #1934, #62762, #17232, #57811, #22884, #43135, #63414 ),
 .UNSPECIFIED., .F., .F.,
 ( 4, 3, 3, 3, 3, 3, 4 ),
 ( 7.962060684260449495E-18, 4.457896483014778873E-05, 6.639290541542104728E-05, 8.820687556478873739E-05, 0.0001100173248778919230, 0.0001545671401658130781, 0.0001830328308068591189 ),
 .UNSPECIFIED. ) ;
#32330=ADVANCED_FACE ( 'NONE', ( #17705 ), #60294, .T. ) ;
#32334=CARTESIAN_POINT ( 'NONE',  ( 0.3218525148189843588, -12.26259572563018629, -0.2444206315274449481 ) ) ;
#32344=ORIENTED_EDGE ( 'NONE', *, *, #50713, .F. ) ;
#32345=ADVANCED_FACE ( 'NONE', ( #12040 ), #15895, .F. ) ;
#32356=CARTESIAN_POINT ( 'NONE',  ( 2.556980015514282556, -7.736177238086868968, 0.2307166419797217205 ) ) ;
#32361=CIRCLE ( 'NONE', #52573, 12.73084802173761787 ) ;
#32368=CARTESIAN_POINT ( 'NONE',  ( 0.3675815128205894289, -4.447030445008257615, 11.44679196252407927 ) ) ;
#32376=CARTESIAN_POINT ( 'NONE',  ( 3.152665057734126197, 7.719888720907812640, 1.848755561852068130 ) ) ;
#32381=CARTESIAN_POINT ( 'NONE',  ( 2.941278708680199916, -3.842273877444594365, 4.788765081995617123 ) ) ;
#32382=CARTESIAN_POINT ( 'NONE',  ( 2.305787727787085295, 7.249469779319941409, -2.461236246750998724 ) ) ;
#32388=ORIENTED_EDGE ( 'NONE', *, *, #43354, .T. ) ;
#32390=CARTESIAN_POINT ( 'NONE',  ( 5.515539859299206427, 0.002251761459665530159, -0.005618668168217195655 ) ) ;
#32394=EDGE_CURVE ( 'NONE', #35774, #37322, #47625, .T. ) ;
#32399=CARTESIAN_POINT ( 'NONE',  ( 2.241352910868910531, 5.794346703933913822, -4.970878533273699773 ) ) ;
#32416=EDGE_CURVE ( 'NONE', #14585, #59854, #16180, .T. ) ;
#32417=CARTESIAN_POINT ( 'NONE',  ( 0.2648978790185602672, -12.24533305150758267, 0.1321385342561976484 ) ) ;
#32424=CARTESIAN_POINT ( 'NONE',  ( 0.2956976708475445581, -9.528782683728138636, 7.708404409946622238 ) ) ;
#32432=VERTEX_POINT ( 'NONE', #13356 ) ;
#32455=EDGE_CURVE ( 'NONE', #41431, #34740, #36788, .T. ) ;
#32461=ORIENTED_EDGE ( 'NONE', *, *, #33394, .T. ) ;
#32466=ORIENTED_EDGE ( 'NONE', *, *, #3500, .T. ) ;
#32470=ORIENTED_EDGE ( 'NONE', *, *, #3739, .T. ) ;
#32473=CARTESIAN_POINT ( 'NONE',  ( 0.5547464869798250930, -9.648168635481788158, -7.697709668896167479 ) ) ;
#32478=LINE ( 'NONE', #57126, #15169 ) ;
#32483=CARTESIAN_POINT ( 'NONE',  ( 2.297017764050093280, -0.1647869190091210967, -7.651182381906875385 ) ) ;
#32489=LINE ( 'NONE', #58796, #33080 ) ;
#32490=FACE_OUTER_BOUND ( 'NONE', #61798, .T. ) ;
#32491=CARTESIAN_POINT ( 'NONE',  ( 0.9232058338315048962, 10.98407661738936980, -5.905985151448033932 ) ) ;
#32492=CARTESIAN_POINT ( 'NONE',  ( 0.2648978790185593790, -11.55204314799266818, 4.063980959785006952 ) ) ;
#32495=CARTESIAN_POINT ( 'NONE',  ( 0.2911222467163546712, 1.916522451062537380, 12.10399882413661210 ) ) ;
#32499=CARTESIAN_POINT ( 'NONE',  ( 0.2671309869109486645, -9.484919892054763935, -7.747281147400640222 ) ) ;
#32503=CARTESIAN_POINT ( 'NONE',  ( 2.247206125383339081, 5.774712443418709817, 4.996658593546202454 ) ) ;
#32504=CARTESIAN_POINT ( 'NONE',  ( 20.00005080000000035, 5.400000000000000355, -1.000000000000000000 ) ) ;
#32505=ORIENTED_EDGE ( 'NONE', *, *, #49826, .F. ) ;
#32507=CARTESIAN_POINT ( 'NONE',  ( 0.6473888112830256114, -5.898884566269086527, 10.87693551365369693 ) ) ;
#32508=ORIENTED_EDGE ( 'NONE', *, *, #8356, .F. ) ;
#32511=B_SPLINE_CURVE_WITH_KNOTS ( 'NONE', 3,
 ( #16546, #37129, #10543, #47141, #1593, #21866, #56102, #31178, #57431, #30821, #5599, #25869, #46156, #603, #20864, #19454, #46037, #44691, #45360, #64981, #35029, #30710 ),
 .UNSPECIFIED., .F., .F.,
 ( 4, 3, 3, 3, 3, 3, 3, 4 ),
 ( 3.157244383156457514E-18, 4.449119708436502735E-05, 6.626296329540230443E-05, 8.803456484962803995E-05, 0.0001098060367612831709, 0.0001315774408628536197, 0.0001760698110411167507, 0.0001829697163287809627 ),
 .UNSPECIFIED. ) ;
#32516=CARTESIAN_POINT ( 'NONE',  ( 2.276905613634094383, -5.031956778294427224, -5.757134111949650190 ) ) ;
#32521=ORIENTED_EDGE ( 'NONE', *, *, #9571, .F. ) ;
#32525=CARTESIAN_POINT ( 'NONE',  ( 0.2717059086739034846, 4.354191483751273850, 11.44824199474644644 ) ) ;
#32526=CARTESIAN_POINT ( 'NONE',  ( 2.245754705088265801, 4.993005209687336077, -5.777230445738716469 ) ) ;
#32529=CARTESIAN_POINT ( 'NONE',  ( 0.3218525148189849694, 8.069481661595467870, -9.236582760335897646 ) ) ;
#32536=CARTESIAN_POINT ( 'NONE',  ( 5.514624014163232779, -0.0008859786816847168602, -0.004045310349816150751 ) ) ;
#32537=CARTESIAN_POINT ( 'NONE',  ( 0.3278977287071214719, -2.374069413450224708, 12.03512402322222385 ) ) ;
#32539=CARTESIAN_POINT ( 'NONE',  ( 0.2872850955227752023, -11.58431228138436886, -3.994021792079210709 ) ) ;
#32540=B_SPLINE_CURVE_WITH_KNOTS ( 'NONE', 3,
 ( #59818, #53853, #3323, #64456, #29531, #14556, #24895, #54172, #49835, #39188, #43865, #4284, #28899, #49209, #34834, #3665 ),
 .UNSPECIFIED., .F., .F.,
 ( 4, 3, 3, 3, 3, 4 ),
 ( 2.740913356018627282E-15, 0.0002126834539179616455, 0.0004253519300366086805, 0.0006380165497223901517, 0.0007442707582427936404, 0.0009453531351420096842 ),
 .UNSPECIFIED. ) ;
#32545=EDGE_CURVE ( 'NONE', #17057, #36493, #2675, .T. ) ;
#32548=DIRECTION ( 'NONE',  ( -1.000000000000000000, -0.000000000000000000, -0.000000000000000000 ) ) ;
#32557=EDGE_CURVE ( 'NONE', #18517, #27530, #21085, .T. ) ;
#32562=CARTESIAN_POINT ( 'NONE',  ( 1.948354844646613238, -5.347695345043367965, 10.70340528295498927 ) ) ;
#32570=VERTEX_POINT ( 'NONE', #40929 ) ;
#32572=CARTESIAN_POINT ( 'NONE',  ( 2.373367633546870969, -3.681545031436607385, -6.738274194514252358 ) ) ;
#32580=CARTESIAN_POINT ( 'NONE',  ( 2.241352910868908754, -4.843133558968167662, 5.901537464758438212 ) ) ;
#32586=( BOUNDED_SURFACE ( )  B_SPLINE_SURFACE ( 3, 1, ( 
 ( #45411, #36427 ),
 ( #30448, #55738 ),
 ( #61354, #9838 ),
 ( #26444, #30129 ) ),
 .UNSPECIFIED., .F., .F., .F. ) 
 B_SPLINE_SURFACE_WITH_KNOTS ( ( 4, 4 ),
 ( 2, 2 ),
 ( 0.000000000000000000, 1.000000000000000000 ),
 ( 0.000000000000000000, 1.000000000000000000 ),
 .UNSPECIFIED. ) 
 GEOMETRIC_REPRESENTATION_ITEM ( )  RATIONAL_B_SPLINE_SURFACE ( (
 ( 1.000000000000000000, 1.000000000000000000),
 ( 0.6933888150995267674, 0.9895912004443193632),
 ( 0.6933888150995267674, 0.9895912004443193632),
 ( 1.000000000000000000, 1.000000000000000000) ) ) 
 REPRESENTATION_ITEM ( '' )  SURFACE ( )  );
#32589=CARTESIAN_POINT ( 'NONE',  ( 2.259830038566063681, 7.131511317046705045, 2.742210045660591788 ) ) ;
#32597=CARTESIAN_POINT ( 'NONE',  ( 0.2651627682582944345, -4.105539787731786738, 11.53745347823613443 ) ) ;
#32598=CARTESIAN_POINT ( 'NONE',  ( 2.990245332647833099, -2.413832934171117550, -8.130497889782899890 ) ) ;
#32608=CARTESIAN_POINT ( 'NONE',  ( 0.2956976708475410054, -4.397965666276502539, 11.44006538352184954 ) ) ;
#32609=CARTESIAN_POINT ( 'NONE',  ( 2.256373768221665355, 6.681391662619836858, 3.703993494729489910 ) ) ;
#32612=CARTESIAN_POINT ( 'NONE',  ( 2.653899356900242701, 7.388433688587512371, 2.411250235128028940 ) ) ;
#32613=CARTESIAN_POINT ( 'NONE',  ( 0.3223008802179240240, 12.03398982086836710, -2.370176598416207092 ) ) ;
#32624=EDGE_CURVE ( 'NONE', #26538, #44286, #22550, .T. ) ;
#32636=CARTESIAN_POINT ( 'NONE',  ( 3.047904605210412399, 5.398304302092612694, -5.772373816836767091 ) ) ;
#32646=ORIENTED_EDGE ( 'NONE', *, *, #264, .T. ) ;
#32653=ORIENTED_EDGE ( 'NONE', *, *, #50916, .T. ) ;
#32656=ORIENTED_EDGE ( 'NONE', *, *, #14540, .T. ) ;
#32664=CARTESIAN_POINT ( 'NONE',  ( 2.524535260912988743, -7.725637239510562360, 0.2211075636761446472 ) ) ;
#32667=CARTESIAN_POINT ( 'NONE',  ( 1.937114397841932290, -12.33981801388260457, 3.531416430611253876 ) ) ;
#32669=CARTESIAN_POINT ( 'NONE',  ( 5.514970785353741078, 0.0003039746380524305930, -0.004713149585127262425 ) ) ;
#32674=ORIENTED_EDGE ( 'NONE', *, *, #39320, .T. ) ;
#32681=CARTESIAN_POINT ( 'NONE',  ( 0.2869720083484339490, 12.02930764912520978, 2.332746648244237608 ) ) ;
#32682=ORIENTED_EDGE ( 'NONE', *, *, #41142, .T. ) ;
#32683=B_SPLINE_CURVE_WITH_KNOTS ( 'NONE', 3,
 ( #18590, #59139, #62787, #57834, #32516, #9213, #28859, #64736, #33834, #40458, #54135, #59446, #13867, #29498, #29195, #14208, #14520, #49170, #34495 ),
 .UNSPECIFIED., .F., .F.,
 ( 4, 3, 3, 3, 3, 3, 4 ),
 ( 6.209365080825174961E-18, 2.825908398782148371E-05, 4.208813692417141740E-05, 5.591713746859297335E-05, 6.279584083138583855E-05, 9.105792820165378189E-05, 0.0001153131102489443041 ),
 .UNSPECIFIED. ) ;
#32688=B_SPLINE_CURVE_WITH_KNOTS ( 'NONE', 3,
 ( #44507, #64787, #39533, #63757, #3929, #64418, #33528, #59444, #7944, #23555, #44456, #58477, #63436, #23890, #58827, #8252, #59138, #53816, #13551 ),
 .UNSPECIFIED., .F., .F.,
 ( 4, 3, 3, 3, 3, 3, 4 ),
 ( 6.209365080825174961E-18, 2.825908398831632713E-05, 4.208813692484372439E-05, 5.591713746944466836E-05, 6.279584083232523197E-05, 9.105792820297400132E-05, 0.0001153131102488854861 ),
 .UNSPECIFIED. ) ;
#32689=CARTESIAN_POINT ( 'NONE',  ( 2.241451721903215066, -7.153019588493058301, -2.668222118333522186 ) ) ;
#32707=CARTESIAN_POINT ( 'NONE',  ( 2.241352910868909643, 7.532448145350525870, -1.243507963608017075 ) ) ;
#32710=DIRECTION ( 'NONE',  ( 0.3865475372811021382, 0.8082200352954648226, -0.4442537292684356487 ) ) ;
#32712=CARTESIAN_POINT ( 'NONE',  ( 2.589278595513889059, -1.582391164331770295, -7.587119248534476057 ) ) ;
#32713=EDGE_CURVE ( 'NONE', #8677, #24896, #12168, .T. ) ;
#32723=CARTESIAN_POINT ( 'NONE',  ( 0.5547464869798239828, -12.20441397277156170, -1.842327806480273500 ) ) ;
#32732=EDGE_CURVE ( 'NONE', #60151, #46959, #1104, .T. ) ;
#32743=VERTEX_POINT ( 'NONE', #60800 ) ;
#32754=CARTESIAN_POINT ( 'NONE',  ( 5.530133899448235191, -0.01111090067015115673, -0.01149180883054598014 ) ) ;
#32767=CARTESIAN_POINT ( 'NONE',  ( 0.2638984909335716500, 5.950360275955056011, 10.70468911391666644 ) ) ;
#32770=CARTESIAN_POINT ( 'NONE',  ( 5.530133899448235191, -0.01459891979722814301, -0.006510401266731771081 ) ) ;
#32773=CARTESIAN_POINT ( 'NONE',  ( 2.290907136833251645, 3.965134647955987024, -6.543263131934253352 ) ) ;
#32777=EDGE_LOOP ( 'NONE', ( #63434, #56846, #15118, #40090 ) ) ;
#32778=CARTESIAN_POINT ( 'NONE',  ( 2.931247277082688285, 4.248542803114433219, -6.618030015945689293 ) ) ;
#32779=EDGE_CURVE ( 'NONE', #25087, #14103, #25309, .T. ) ;
#32783=CARTESIAN_POINT ( 'NONE',  ( 3.152665057735396736, -5.761241965768377327, 5.461013642406604696 ) ) ;
#32788=ORIENTED_EDGE ( 'NONE', *, *, #32803, .F. ) ;
#32796=CARTESIAN_POINT ( 'NONE',  ( 2.969415267404944103, -5.354299007565654911, -5.777543886622379610 ) ) ;
#32798=CARTESIAN_POINT ( 'NONE',  ( 0.2652384770603674613, -6.065775245581090047, -10.63836422907230350 ) ) ;
#32801=AXIS2_PLACEMENT_3D ( 'NONE', #63969, #63624, #12757 ) ;
#32803=EDGE_CURVE ( 'NONE', #19720, #64984, #28089, .T. ) ;
#32813=CARTESIAN_POINT ( 'NONE',  ( 0.3675815128205894289, -5.910255304480370953, -10.76447900494946452 ) ) ;
#32815=DIRECTION ( 'NONE',  ( 0.000000000000000000, 0.000000000000000000, 1.000000000000000000 ) ) ;
#32820=CARTESIAN_POINT ( 'NONE',  ( 0.3675815128205894289, 1.872154644482084684, 12.13672785388550679 ) ) ;
#32821=VERTEX_POINT ( 'NONE', #5952 ) ;
#32824=CARTESIAN_POINT ( 'NONE',  ( 2.655192694322970670, 9.337840456951635559, -2.234846078478380793 ) ) ;
#32825=CARTESIAN_POINT ( 'NONE',  ( 1.547277799339728643, 3.695326562728670883, -12.12286970032385014 ) ) ;
#32828=CARTESIAN_POINT ( 'NONE',  ( 2.268878695254630706, 5.759001817705426518, 5.025754889200215736 ) ) ;
#32852=B_SPLINE_CURVE_WITH_KNOTS ( 'NONE', 3,
 ( #31821, #18195, #48140, #1913, #17208, #53451, #52785, #58433, #22184, #62407, #37810, #22864, #2911, #16871, #1607, #27497 ),
 .UNSPECIFIED., .F., .F.,
 ( 4, 3, 3, 3, 3, 4 ),
 ( 0.000000000000000000, 0.0002176109881720192808, 0.0004352086762394508004, 0.0006528017811446763406, 0.0007615147961451593749, 0.0009453342004947440022 ),
 .UNSPECIFIED. ) ;
#32859=CARTESIAN_POINT ( 'NONE',  ( 0.2655924914740778187, -2.083162675473532399, -12.06787830249867355 ) ) ;
#32860=CARTESIAN_POINT ( 'NONE',  ( 0.2717059086738999318, 11.56868249951481786, 4.023283916512469638 ) ) ;
#32864=FACE_OUTER_BOUND ( 'NONE', #25754, .T. ) ;
#32875=CARTESIAN_POINT ( 'NONE',  ( 2.705197763288545332, -7.218866228162265308, -2.925192046931980094 ) ) ;
#32879=CARTESIAN_POINT ( 'NONE',  ( 2.242819959140645913, 5.913965034148218614, -4.828731837260174409 ) ) ;
#32889=VECTOR ( 'NONE', #782, 1000.000000000000114 ) ;
#32892=CARTESIAN_POINT ( 'NONE',  ( 2.903928887687982741, -3.918141038920174513, 7.845932231842924764 ) ) ;
#32893=CARTESIAN_POINT ( 'NONE',  ( 1.719304012340734378, -8.755325027794794934, -9.242227816401850760 ) ) ;
#32901=CARTESIAN_POINT ( 'NONE',  ( 2.259025283528087957, -6.547290863799063665, 3.937899517809461791 ) ) ;
#32911=CARTESIAN_POINT ( 'NONE',  ( 5.514624014163232779, -0.0001700579043838964816, -0.004137701579365772077 ) ) ;
#32922=CARTESIAN_POINT ( 'NONE',  ( 2.297017764050093280, -2.771707546665545419, -7.133399178907342097 ) ) ;
#32925=ORIENTED_EDGE ( 'NONE', *, *, #55911, .T. ) ;
#32926=CARTESIAN_POINT ( 'NONE',  ( 2.284126774967659479, 2.466502196988966666, 7.240052432235658308 ) ) ;
#32927=EDGE_CURVE ( 'NONE', #20597, #23499, #20069, .T. ) ;
#32931=CARTESIAN_POINT ( 'NONE',  ( 2.253265082352433613, 3.707567016433813922, 6.678225412356958657 ) ) ;
#32949=CARTESIAN_POINT ( 'NONE',  ( 0.2915757698887249671, 6.312478057070456394, 10.50410115670271516 ) ) ;
#32951=CARTESIAN_POINT ( 'NONE',  ( 2.653899356899475759, -7.604196386057373580, 1.606012885791342271 ) ) ;
#32952=ORIENTED_EDGE ( 'NONE', *, *, #13044, .F. ) ;
#32969=CARTESIAN_POINT ( 'NONE',  ( 5.516018279890452902, 0.006286471671801929263, -0.002527316374434327665 ) ) ;
#32971=B_SPLINE_CURVE_WITH_KNOTS ( 'NONE', 3,
 ( #52288, #31639, #41951, #51951, #6079, #56263, #46957, #5758, #16018, #6391, #26662, #40980, #10706, #84, #15686, #1416 ),
 .UNSPECIFIED., .F., .F.,
 ( 4, 3, 3, 3, 3, 4 ),
 ( 4.336808689942017255E-19, 0.0002176109881720263281, 0.0004352086762394657081, 0.0006528017811446956394, 0.0007615147961451794326, 0.0009453342004944464971 ),
 .UNSPECIFIED. ) ;
#32977=EDGE_LOOP ( 'NONE', ( #31508, #52898, #7003, #50030 ) ) ;
#32983=CARTESIAN_POINT ( 'NONE',  ( 0.3341166715381286290, 1.881279064088004827, -12.12403120948087931 ) ) ;
#32985=CARTESIAN_POINT ( 'NONE',  ( 1.948354844645469264, -6.595573209516436997, -9.982942661983956967 ) ) ;
#32995=CARTESIAN_POINT ( 'NONE',  ( 0.3160775863651110185, -12.03278055228169485, -2.365582350580189619 ) ) ;
#33013=ORIENTED_EDGE ( 'NONE', *, *, #532, .T. ) ;
#33019=CARTESIAN_POINT ( 'NONE',  ( 0.2872850955227732594, -3.994021792079174293, 11.58431228138438307 ) ) ;
#33022=CARTESIAN_POINT ( 'NONE',  ( 0.2648978790185593790, -11.55204314799266818, 4.063980959785006952 ) ) ;
#33028=ORIENTED_EDGE ( 'NONE', *, *, #32732, .T. ) ;
#33035=CARTESIAN_POINT ( 'NONE',  ( 0.3223008802179194165, -10.49760329338524301, 6.343104382804274799 ) ) ;
#33046=EDGE_CURVE ( 'NONE', #5538, #59522, #64952, .T. ) ;
#33056=ORIENTED_EDGE ( 'NONE', *, *, #19271, .F. ) ;
#33058=CARTESIAN_POINT ( 'NONE',  ( 0.2676618633000489855, -1.968216791520412734, -12.08777609394270947 ) ) ;
#33059=CARTESIAN_POINT ( 'NONE',  ( 5.516018279890452902, -0.002104829434640716982, 0.006440244342253021413 ) ) ;
#33071=CARTESIAN_POINT ( 'NONE',  ( 1.372161826076676139, -12.51237317864394072, -1.607409531431686744 ) ) ;
#33073=CARTESIAN_POINT ( 'NONE',  ( 0.3675815128205894289, 2.391755495700603973, 12.04510820461660003 ) ) ;
#33075=ORIENTED_EDGE ( 'NONE', *, *, #61455, .T. ) ;
#33076=EDGE_CURVE ( 'NONE', #47363, #36221, #26050, .T. ) ;
#33080=VECTOR ( 'NONE', #48476, 999.9999999999998863 ) ;
#33084=CARTESIAN_POINT ( 'NONE',  ( 0.3218525148189810836, -9.550803867331117303, 7.695007528464986812 ) ) ;
#33085=CARTESIAN_POINT ( 'NONE',  ( 0.3665391374699464300, -9.576575648339069602, 7.691255657244259858 ) ) ;
#33090=CARTESIAN_POINT ( 'NONE',  ( 0.2869720083484369466, 5.945302302873249900, 10.71444492121018754 ) ) ;
#33096=CARTESIAN_POINT ( 'NONE',  ( 0.2653519789438759657, 10.59450269107742137, -6.142177718873826464 ) ) ;
#33098=VERTEX_POINT ( 'NONE', #6102 ) ;
#33109=CARTESIAN_POINT ( 'NONE',  ( 0.2759803524722215795, 11.57441428600638744, -4.011137970318830348 ) ) ;
#33121=CARTESIAN_POINT ( 'NONE',  ( 1.452237505248555660, 3.767214359061289652, -12.08199618361509131 ) ) ;
#33136=CARTESIAN_POINT ( 'NONE',  ( 2.241352910868910531, -3.889181972941495147, 6.569501556381427854 ) ) ;
#33141=CARTESIAN_POINT ( 'NONE',  ( 2.245754705088393255, 1.435454129948307456, -7.499730934370265167 ) ) ;
#33142=VERTEX_POINT ( 'NONE', #7063 ) ;
#33143=CARTESIAN_POINT ( 'NONE',  ( 0.2648978790185593790, 12.08224454301448958, 1.996248716311670446 ) ) ;
#33148=CARTESIAN_POINT ( 'NONE',  ( 2.717984159219453133, -3.648459810929832070, 6.886544461123724759 ) ) ;
#33153=CARTESIAN_POINT ( 'NONE',  ( 0.2646305136544072623, 1.996350543472996675, 12.08286001766536089 ) ) ;
#33163=CARTESIAN_POINT ( 'NONE',  ( 0.3006302518452027006, -11.43947177966005135, 4.404090606399839736 ) ) ;
#33167=EDGE_LOOP ( 'NONE', ( #36040, #9297, #55651, #30720 ) ) ;
#33170=CARTESIAN_POINT ( 'NONE',  ( 2.305787727787084407, -4.792270232040933386, 5.970480882365206909 ) ) ;
#33173=CARTESIAN_POINT ( 'NONE',  ( 2.242819959140784025, 5.782321801516017601, 4.985618132690376569 ) ) ;
#33180=VERTEX_POINT ( 'NONE', #47630 ) ;
#33188=CARTESIAN_POINT ( 'NONE',  ( 0.3341166715381294616, 5.914486946114060117, -10.74942732659225975 ) ) ;
#33190=CARTESIAN_POINT ( 'NONE',  ( 2.963017218115622242, 1.744728040077008879, -7.679262289252030804 ) ) ;
#33191=CARTESIAN_POINT ( 'NONE',  ( 2.373367633546872302, -1.511052049479969295, 7.528269033630150098 ) ) ;
#33197=CARTESIAN_POINT ( 'NONE',  ( 2.247112776671468470, 3.918650674719098337, 6.554209700763984792 ) ) ;
#33200=CARTESIAN_POINT ( 'NONE',  ( 0.2872850955227733150, 4.386654201695149524, 11.44140577127595115 ) ) ;
#33205=CARTESIAN_POINT ( 'NONE',  ( 3.152665057734126197, 7.719888720907812640, 1.848755561852068130 ) ) ;
#33209=ORIENTED_EDGE ( 'NONE', *, *, #40319, .T. ) ;
#33210=( BOUNDED_SURFACE ( )  B_SPLINE_SURFACE ( 3, 1, ( 
 ( #37515, #13230 ),
 ( #43466, #2941 ),
 ( #48490, #33517 ),
 ( #13537, #18225 ) ),
 .UNSPECIFIED., .F., .F., .F. ) 
 B_SPLINE_SURFACE_WITH_KNOTS ( ( 4, 4 ),
 ( 2, 2 ),
 ( 0.000000000000000000, 1.000000000000000000 ),
 ( 0.000000000000000000, 1.000000000000000000 ),
 .UNSPECIFIED. ) 
 GEOMETRIC_REPRESENTATION_ITEM ( )  RATIONAL_B_SPLINE_SURFACE ( (
 ( 1.000000000000000000, 1.000000000000000000),
 ( 0.9942764183789327692, 0.8450855930916580938),
 ( 0.9942764183789327692, 0.8450855930916580938),
 ( 1.000000000000000000, 1.000000000000000000) ) ) 
 REPRESENTATION_ITEM ( '' )  SURFACE ( )  );
#33212=CARTESIAN_POINT ( 'NONE',  ( 2.963017218115482354, 4.761166637500529042, 6.272673870919030392 ) ) ;
#33213=CARTESIAN_POINT ( 'NONE',  ( 2.276905613634085057, 3.688905863353115322, -6.697548486791003342 ) ) ;
#33214=CARTESIAN_POINT ( 'NONE',  ( -14.47334165536100059, 0.000000000000000000, 1.000000000000000000 ) ) ;
#33221=CARTESIAN_POINT ( 'NONE',  ( 3.152665057736217413, -7.923639299008909731, 0.4801242025612903475 ) ) ;
#33223=AXIS2_PLACEMENT_3D ( 'NONE', #60557, #5372, #45274 ) ;
#33228=CARTESIAN_POINT ( 'NONE',  ( 2.241534463349551753, 9.451863027432619807E-16, 7.634462073473348376 ) ) ;
#33230=CARTESIAN_POINT ( 'NONE',  ( 0.2652384529303126182, 9.423437232855667034, 7.820949643217174341 ) ) ;
#33231=CARTESIAN_POINT ( 'NONE',  ( 2.705197763288547996, -4.789125516644078040, -6.142723737672437068 ) ) ;
#33237=CARTESIAN_POINT ( 'NONE',  ( 0.2651627682582914369, -2.213224986694501517, -12.04449770099953554 ) ) ;
#33243=CARTESIAN_POINT ( 'NONE',  ( 2.717984159219154261, -0.2836133496099048079, -7.788152353088992896 ) ) ;
#33245=CARTESIAN_POINT ( 'NONE',  ( 2.266490820343227242, -3.946561086901428261, -6.544980046121064099 ) ) ;
#33246=ADVANCED_FACE ( 'NONE', ( #3418 ), #48190, .F. ) ;
#33251=CARTESIAN_POINT ( 'NONE',  ( 2.263328370261315836, 5.019946231381084978, 5.761609105518099128 ) ) ;
#33252=CARTESIAN_POINT ( 'NONE',  ( 2.705197763288545776, -3.649695155981463657, -6.881024880055383264 ) ) ;
#33254=CARTESIAN_POINT ( 'NONE',  ( 5.520433897694421610, 0.007082458259338569526, -0.01329351892498007413 ) ) ;
#33259=CIRCLE ( 'NONE', #4618, 12.73084802173761787 ) ;
#33262=CARTESIAN_POINT ( 'NONE',  ( 5.515188684475870851, -0.004893136156457767935, -0.002166413411657401155 ) ) ;
#33268=DIRECTION ( 'NONE',  ( 0.000000000000000000, 0.000000000000000000, 1.000000000000000000 ) ) ;
#33269=CARTESIAN_POINT ( 'NONE',  ( 2.259830038565000976, -7.547174990768408698, 1.190932096469625279 ) ) ;
#33281=VECTOR ( 'NONE', #56463, 1000.000000000000114 ) ;
#33282=CARTESIAN_POINT ( 'NONE',  ( 2.990245332647870402, 6.814589384235040015, -5.049055049623153657 ) ) ;
#33288=CARTESIAN_POINT ( 'NONE',  ( 1.459561108994998246, 11.65083230253685009, -4.912799202120054609 ) ) ;
#33289=CARTESIAN_POINT ( 'NONE',  ( 3.152665057734040488, 0.000000000000000000, 0.000000000000000000 ) ) ;
#33291=ORIENTED_EDGE ( 'NONE', *, *, #56996, .F. ) ;
#33295=CARTESIAN_POINT ( 'NONE',  ( 2.258463476536644698, -2.740340677911279776, 7.131741622455330720 ) ) ;
#33297=CARTESIAN_POINT ( 'NONE',  ( 0.3665391374699465965, -12.04754782681758662, 2.392238720110418715 ) ) ;
#33299=CARTESIAN_POINT ( 'NONE',  ( 3.152665057736161902, 7.719888720907650992, -1.848755561854025231 ) ) ;
#33300=CARTESIAN_POINT ( 'NONE',  ( 0.3006302518452026451, 12.03044280705497648, -2.350739146140467195 ) ) ;
#33301=CARTESIAN_POINT ( 'NONE',  ( 2.368238019615056533, -7.526794520527601229, 1.509700170844538558 ) ) ;
#33311=CARTESIAN_POINT ( 'NONE',  ( 0.3401186441510238856, -9.233880480307249172, -8.081824149807792068 ) ) ;
#33315=CARTESIAN_POINT ( 'NONE',  ( 3.152665057734040488, 0.000000000000000000, 0.000000000000000000 ) ) ;
#33320=CARTESIAN_POINT ( 'NONE',  ( 5.516018279890452902, 0.004180585980734981624, 0.005331956019561726046 ) ) ;
#33321=CARTESIAN_POINT ( 'NONE',  ( 0.3665391374699472626, -1.872534962004881454, 12.13918562134718115 ) ) ;
#33324=CARTESIAN_POINT ( 'NONE',  ( 0.2652384770603670727, 7.820955051613327491, 9.423432754625759245 ) ) ;
#33338=CARTESIAN_POINT ( 'NONE',  ( 2.255723233589907117, 6.548644987607097789, 3.933511348458858858 ) ) ;
#33354=CARTESIAN_POINT ( 'NONE',  ( 0.2739690278137230095, -7.732471127692660318, 9.499928778897087867 ) ) ;
#33364=ORIENTED_EDGE ( 'NONE', *, *, #56850, .T. ) ;
#33378=CARTESIAN_POINT ( 'NONE',  ( 5.530133899448235191, -0.01589823604557702441, 0.001661287012793988965 ) ) ;
#33382=AXIS2_PLACEMENT_3D ( 'NONE', #42189, #16943, #2322 ) ;
#33383=EDGE_CURVE ( 'NONE', #19254, #21572, #15020, .T. ) ;
#33390=LINE ( 'NONE', #59319, #21131 ) ;
#33394=EDGE_CURVE ( 'NONE', #58530, #12917, #60257, .T. ) ;
#33395=( BOUNDED_SURFACE ( )  B_SPLINE_SURFACE ( 3, 1, ( 
 ( #30005, #25033 ),
 ( #4431, #25344 ),
 ( #24701, #39982 ),
 ( #61248, #30344 ) ),
 .UNSPECIFIED., .F., .F., .F. ) 
 B_SPLINE_SURFACE_WITH_KNOTS ( ( 4, 4 ),
 ( 2, 2 ),
 ( 0.000000000000000000, 1.000000000000000000 ),
 ( 0.000000000000000000, 1.000000000000000000 ),
 .UNSPECIFIED. ) 
 GEOMETRIC_REPRESENTATION_ITEM ( )  RATIONAL_B_SPLINE_SURFACE ( (
 ( 1.000000000000000000, 1.000000000000000000),
 ( 0.9856612449720755231, 0.9999558406602322425),
 ( 0.9856612449720755231, 0.9999558406602322425),
 ( 1.000000000000000000, 1.000000000000000000) ) ) 
 REPRESENTATION_ITEM ( '' )  SURFACE ( )  );
#33410=CARTESIAN_POINT ( 'NONE',  ( 5.520433897694421610, 0.01505375422439122861, -0.0005131706886598833180 ) ) ;
#33412=CARTESIAN_POINT ( 'NONE',  ( 2.258463476536300973, -4.806099079317786682, -5.939075453322352871 ) ) ;
#33414=ORIENTED_EDGE ( 'NONE', *, *, #13930, .F. ) ;
#33421=B_SPLINE_CURVE_WITH_KNOTS ( 'NONE', 3,
 ( #12302, #32572, #52576, #38571, #59195, #42898, #33252, #43543, #44209, #28925, #29252, #8312, #28587, #63183, #53560, #63825 ),
 .UNSPECIFIED., .F., .F.,
 ( 4, 3, 3, 3, 3, 4 ),
 ( 0.000000000000000000, 0.0002176109881720231839, 0.0004352086762394577393, 0.0006528017811446839300, 0.0007615147961451657717, 0.0009453342004947017183 ),
 .UNSPECIFIED. ) ;
#33427=CARTESIAN_POINT ( 'NONE',  ( 2.241506898688417682, 7.511570207700577484, -1.364429914801440491 ) ) ;
#33428=CARTESIAN_POINT ( 'NONE',  ( 2.266490820343225909, -7.550546162186916099, -1.183790889241807420 ) ) ;
#33432=CARTESIAN_POINT ( 'NONE',  ( 1.372161826076019109, 0.5897614319402071370, 12.60140585080791631 ) ) ;
#33433=ORIENTED_EDGE ( 'NONE', *, *, #48878, .T. ) ;
#33438=B_SPLINE_CURVE_WITH_KNOTS ( 'NONE', 3,
 ( #47036, #56340, #6465, #31404, #10786, #26743, #31708, #61994, #56011, #46055, #5836, #506, #20444, #21772, #25425, #45707, #41702, #31072, #51384, #52018, #1495, #51705 ),
 .UNSPECIFIED., .F., .F.,
 ( 4, 3, 3, 3, 3, 3, 3, 4 ),
 ( 1.311167604876506724E-18, 4.449119708436815798E-05, 6.626296329540360547E-05, 8.803456484962558695E-05, 0.0001098060367612788341, 0.0001315774408628489034, 0.0001760698110411144739, 0.0001829697163287813692 ),
 .UNSPECIFIED. ) ;
#33439=ORIENTED_EDGE ( 'NONE', *, *, #38652, .T. ) ;
#33447=VERTEX_POINT ( 'NONE', #378 ) ;
#33449=CARTESIAN_POINT ( 'NONE',  ( 0.9232167919969134218, -3.872606616958349957, 11.84868134597555489 ) ) ;
#33450=CARTESIAN_POINT ( 'NONE',  ( 3.152665057734040488, 0.000000000000000000, 0.000000000000000000 ) ) ;
#33451=B_SPLINE_CURVE_WITH_KNOTS ( 'NONE', 3,
 ( #24403, #50363, #29711, #40023, #4810, #8463, #25076, #34049, #59336, #29086, #18782, #19766, #44351, #49393, #14097, #38730, #4137, #45025, #9764 ),
 .UNSPECIFIED., .F., .F.,
 ( 4, 3, 3, 3, 3, 3, 4 ),
 ( 9.120196284301400213E-18, 4.457896483014723308E-05, 6.639290541541900085E-05, 8.820687556478805976E-05, 0.0001100173248778910014, 0.0001545671401658117229, 0.0001830328308068583328 ),
 .UNSPECIFIED. ) ;
#33453=LINE ( 'NONE', #13173, #42769 ) ;
#33458=CARTESIAN_POINT ( 'NONE',  ( 3.152665057736074417, -6.622010822085853121, 4.377619405894153992 ) ) ;
#33459=B_SPLINE_CURVE_WITH_KNOTS ( 'NONE', 3,
 ( #57700, #47396, #11460, #52384, #47707, #53360, #52046, #32065, #58023, #42354, #57037, #47065, #6491 ),
 .UNSPECIFIED., .F., .F.,
 ( 4, 3, 3, 3, 4 ),
 ( 2.602085213965210642E-18, 6.607593386745516130E-05, 0.0001321518677373524609, 0.0001982171734706215916, 0.0002642860854759484460 ),
 .UNSPECIFIED. ) ;
#33462=ADVANCED_FACE ( 'NONE', ( #20657 ), #54593, .F. ) ;
#33469=EDGE_LOOP ( 'NONE', ( #27230, #58814, #57740, #996 ) ) ;
#33471=CARTESIAN_POINT ( 'NONE',  ( 2.524535260912817769, 4.796565674004647839, -6.060306679219011450 ) ) ;
#33473=CARTESIAN_POINT ( 'NONE',  ( 0.2653519890518140634, -11.50766430042467370, -4.188437879978375022 ) ) ;
#33477=CARTESIAN_POINT ( 'NONE',  ( 5.536195898058073439, 0.0002547682446685005180, 0.008496323383586770056 ) ) ;
#33480=CARTESIAN_POINT ( 'NONE',  ( 0.3040950598368144520, 11.60568999039900362, -3.956873563689416784 ) ) ;
#33484=ORIENTED_EDGE ( 'NONE', *, *, #29588, .F. ) ;
#33485=CARTESIAN_POINT ( 'NONE',  ( 2.305787727787084407, -5.970480882365190034, -4.792270232040956479 ) ) ;
#33487=CARTESIAN_POINT ( 'NONE',  ( 0.2652384770603652409, -10.57229757085618260, -6.180206054297716634 ) ) ;
#33493=CARTESIAN_POINT ( 'NONE',  ( 5.516018279890452902, -0.002527316374434348482, -0.006286471671801920590 ) ) ;
#33495=ADVANCED_FACE ( 'NONE', ( #2348 ), #34163, .F. ) ;
#33501=EDGE_CURVE ( 'NONE', #4057, #63452, #53917, .T. ) ;
#33502=CARTESIAN_POINT ( 'NONE',  ( 1.719304012338199517, 12.70777170743846796, 0.7661785589580254463 ) ) ;
#33503=EDGE_CURVE ( 'NONE', #16245, #39958, #42887, .T. ) ;
#33506=ADVANCED_FACE ( 'NONE', ( #38216 ), #61343, .F. ) ;
#33508=CARTESIAN_POINT ( 'NONE',  ( 2.247206125382827491, -7.214589497757600611, 2.502718378778785002 ) ) ;
#33513=CARTESIAN_POINT ( 'NONE',  ( 2.247206125382827935, 7.539576157880618190, -1.211896144126850094 ) ) ;
#33515=EDGE_CURVE ( 'NONE', #7543, #22716, #57883, .T. ) ;
#33517=CARTESIAN_POINT ( 'NONE',  ( 0.3040950598368144520, 7.687624643091433008, 9.552450779732136965 ) ) ;
#33524=CARTESIAN_POINT ( 'NONE',  ( 2.941278708680199916, 6.068329152486375833, 0.9331242451665199278 ) ) ;
#33528=CARTESIAN_POINT ( 'NONE',  ( 2.269879328256727113, 6.544400685875880086, -3.949706986712128387 ) ) ;
#33534=CARTESIAN_POINT ( 'NONE',  ( 5.530133899448235191, -0.009387834778845766809, 0.01293763278443448191 ) ) ;
#33540=EDGE_CURVE ( 'NONE', #34853, #25053, #38832, .T. ) ;
#33542=FACE_OUTER_BOUND ( 'NONE', #7889, .T. ) ;
#33544=DIRECTION ( 'NONE',  ( -1.000000000000000000, -0.000000000000000000, -0.000000000000000000 ) ) ;
#33548=CARTESIAN_POINT ( 'NONE',  ( 2.350038591457884962, 2.471682575235502277, -10.33030559206184051 ) ) ;
#33549=CARTESIAN_POINT ( 'NONE',  ( 0.2653141516239115316, -0.04404488958242430696, 12.24612533180317797 ) ) ;
#33570=CARTESIAN_POINT ( 'NONE',  ( 2.280717697723835258, -3.687451363405612970, 6.699799459371652333 ) ) ;
#33573=EDGE_CURVE ( 'NONE', #11101, #11073, #37068, .T. ) ;
#33575=B_SPLINE_CURVE_WITH_KNOTS ( 'NONE', 3,
 ( #40652, #51312, #25045, #750, #15042, #65271, #19735, #39994, #60945, #15384, #60277, #47942, #41628, #2054, #42258, #17357 ),
 .UNSPECIFIED., .F., .F.,
 ( 4, 3, 3, 3, 3, 4 ),
 ( 0.000000000000000000, 0.0003017745587525249760, 0.0006035491769808738489, 0.0009053241094668170071, 0.001207275924540017736, 0.001510325902533033848 ),
 .UNSPECIFIED. ) ;
#33579=CARTESIAN_POINT ( 'NONE',  ( 2.556980015513105720, 5.777953785406880982, -5.149458076504359383 ) ) ;
#33581=ADVANCED_FACE ( 'NONE', ( #34214 ), #64280, .F. ) ;
#33586=ORIENTED_EDGE ( 'NONE', *, *, #1062, .F. ) ;
#33587=CARTESIAN_POINT ( 'NONE',  ( 0.2646305136544065406, 4.312539723326288765, -11.46223899740595620 ) ) ;
#33596=CARTESIAN_POINT ( 'NONE',  ( 0.2638984909335720941, 11.43908195192335953, -4.375449752477019949 ) ) ;
#33605=( BOUNDED_SURFACE ( )  B_SPLINE_SURFACE ( 3, 1, ( 
 ( #25599, #26575 ),
 ( #346, #46534 ),
 ( #46869, #20624 ),
 ( #5672, #35876 ) ),
 .UNSPECIFIED., .F., .F., .F. ) 
 B_SPLINE_SURFACE_WITH_KNOTS ( ( 4, 4 ),
 ( 2, 2 ),
 ( 0.000000000000000000, 1.000000000000000000 ),
 ( 0.000000000000000000, 1.000000000000000000 ),
 .UNSPECIFIED. ) 
 GEOMETRIC_REPRESENTATION_ITEM ( )  RATIONAL_B_SPLINE_SURFACE ( (
 ( 1.000000000000000000, 1.000000000000000000),
 ( 0.9856612449720755231, 0.9999558406602322425),
 ( 0.9856612449720755231, 0.9999558406602322425),
 ( 1.000000000000000000, 1.000000000000000000) ) ) 
 REPRESENTATION_ITEM ( '' )  SURFACE ( )  );
#33610=CARTESIAN_POINT ( 'NONE',  ( 2.245754705088395475, 2.506725724682664413, 7.212684575686784783 ) ) ;
#33614=CARTESIAN_POINT ( 'NONE',  ( 2.255723233588952326, 3.704537245405040924, 6.680843247642330951 ) ) ;
#33615=CARTESIAN_POINT ( 'NONE',  ( 2.889800649504073782, -6.016320774579801522, -1.129261637821672215 ) ) ;
#33618=CARTESIAN_POINT ( 'NONE',  ( 1.719304012341202004, 11.67935079956989775, -5.066286238790292273 ) ) ;
#33628=CARTESIAN_POINT ( 'NONE',  ( 5.515539859299206427, 0.005991790098944300112, 0.0008592514567753142991 ) ) ;
#33629=CARTESIAN_POINT ( 'NONE',  ( 0.2717059086739013751, 6.276007891175726883, 10.51822005841996877 ) ) ;
#33630=CARTESIAN_POINT ( 'NONE',  ( 0.3164563675027689538, -2.365891945210734981, -12.03284811452139991 ) ) ;
#33632=ORIENTED_EDGE ( 'NONE', *, *, #61195, .F. ) ;
#33634=ORIENTED_EDGE ( 'NONE', *, *, #2264, .T. ) ;
#33637=CARTESIAN_POINT ( 'NONE',  ( 5.514624014163232779, 0.003668383633201691488, 0.001921576324372104407 ) ) ;
#33643=CARTESIAN_POINT ( 'NONE',  ( 1.719304012338820131, 1.452142814150020556, 12.64775761152757561 ) ) ;
#33668=CARTESIAN_POINT ( 'NONE',  ( 2.931247277082674074, 5.779735553870104958, 5.333206743525262361 ) ) ;
#33669=CARTESIAN_POINT ( 'NONE',  ( 2.899286259009686173, -3.018334250363132298, 7.250549018622930220 ) ) ;
#33670=FACE_OUTER_BOUND ( 'NONE', #45503, .T. ) ;
#33678=DIRECTION ( 'NONE',  ( 0.000000000000000000, 0.000000000000000000, 1.000000000000000000 ) ) ;
#33686=CARTESIAN_POINT ( 'NONE',  ( 0.3057689695767522586, -3.975296631252044133, 11.59726335252432783 ) ) ;
#33687=CARTESIAN_POINT ( 'NONE',  ( 0.2653141334712577071, -11.49252672845885925, 4.229817350136370280 ) ) ;
#33706=CARTESIAN_POINT ( 'NONE',  ( 1.719304012340653998, -9.242227816403676854, -8.755325027797448811 ) ) ;
#33709=ADVANCED_FACE ( 'NONE', ( #46816 ), #2346, .F. ) ;
#33712=DIRECTION ( 'NONE',  ( -0.3939253465568943180, 0.6978179301705840221, -0.5982248387291124736 ) ) ;
#33716=CARTESIAN_POINT ( 'NONE',  ( 5.530133899448235191, 0.01459891979722878833, -0.006510401266731667864 ) ) ;
#33725=DIRECTION ( 'NONE',  ( 0.3865475372811020827, 0.4778122177792094027, -0.7888450329201726063 ) ) ;
#33736=CARTESIAN_POINT ( 'NONE',  ( 5.515188684475870851, 0.0005703990286340047521, -0.005320786921497682072 ) ) ;
#33752=CARTESIAN_POINT ( 'NONE',  ( 1.452237505248552996, -12.34692280296790479, -2.778494755359182111 ) ) ;
#33754=EDGE_LOOP ( 'NONE', ( #2049, #3004, #53744, #36207 ) ) ;
#33759=LINE ( 'NONE', #12176, #38560 ) ;
#33761=ORIENTED_EDGE ( 'NONE', *, *, #16204, .F. ) ;
#33762=CARTESIAN_POINT ( 'NONE',  ( 2.256373768223415066, -7.499124080223147359, 1.457292142211195074 ) ) ;
#33764=CARTESIAN_POINT ( 'NONE',  ( 0.3106921474978491804, 0.2354703039889815830, -12.25904950202576771 ) ) ;
#33770=CARTESIAN_POINT ( 'NONE',  ( 2.242819959140647690, 3.905785747114015383, -6.560218843829733970 ) ) ;
#33771=ORIENTED_EDGE ( 'NONE', *, *, #31804, .F. ) ;
#33775=CARTESIAN_POINT ( 'NONE',  ( 1.375507693217718153, 3.754650692913772847, 12.04466556545155065 ) ) ;
#33776=CARTESIAN_POINT ( 'NONE',  ( 2.907497136250996927, 4.769582063554166140, -6.243048412628978916 ) ) ;
#33786=CARTESIAN_POINT ( 'NONE',  ( 2.556980015514183524, -5.149458076504853210, -5.777953785406920950 ) ) ;
#33788=CARTESIAN_POINT ( 'NONE',  ( 0.2651627923886311078, 12.04449855907068390, 2.213220384814313935 ) ) ;
#33793=CARTESIAN_POINT ( 'NONE',  ( 1.547277799339520366, -4.961646058324188147, -11.66196709685601363 ) ) ;
#33797=CARTESIAN_POINT ( 'NONE',  ( 2.257661810676419023, -2.485866587321432952, 7.224098098130517620 ) ) ;
#33798=CARTESIAN_POINT ( 'NONE',  ( 0.9232058338315048962, -0.3773051331668853536, 12.46548196349785975 ) ) ;
#33801=CARTESIAN_POINT ( 'NONE',  ( 0.2646305136544072623, 12.03696649559614862, 2.256625640822354839 ) ) ;
#33802=CARTESIAN_POINT ( 'NONE',  ( 2.827825597296802940, 8.776379025186180627, 2.100863646776085503 ) ) ;
#33805=CARTESIAN_POINT ( 'NONE',  ( 0.3218525148189792517, -8.069481661595405697, 9.236582760335950937 ) ) ;
#33806=CARTESIAN_POINT ( 'NONE',  ( 0.2648978790185584908, 12.24533305150758089, 0.1321385342562836074 ) ) ;
#33810=CARTESIAN_POINT ( 'NONE',  ( 2.258463476536643810, -7.224688073723619652, 2.484972401833223543 ) ) ;
#33812=CARTESIAN_POINT ( 'NONE',  ( 0.3109076770649036314, -9.542672295796769788, -7.699281309344426560 ) ) ;
#33815=CARTESIAN_POINT ( 'NONE',  ( 2.251139882113960322, 7.542197031254634254, -1.203816215709469839 ) ) ;
#33816=CARTESIAN_POINT ( 'NONE',  ( 2.241352910868910531, -3.889181972941495147, 6.569501556381427854 ) ) ;
#33818=CARTESIAN_POINT ( 'NONE',  ( 2.889800649504073782, -1.129261637821651121, 6.016320774579804187 ) ) ;
#33827=CIRCLE ( 'NONE', #63539, 12.73084802173761787 ) ;
#33832=CARTESIAN_POINT ( 'NONE',  ( 1.452237505248555660, -12.08199618361510552, -3.767214359061247464 ) ) ;
#33834=CARTESIAN_POINT ( 'NONE',  ( 2.263328370262063238, -5.019946231381820390, -5.761609105517779383 ) ) ;
#33836=ORIENTED_EDGE ( 'NONE', *, *, #11700, .F. ) ;
#33845=CARTESIAN_POINT ( 'NONE',  ( 2.889800649504073782, -4.732281052280285394, -3.882893708502096697 ) ) ;
#33847=CARTESIAN_POINT ( 'NONE',  ( 1.452237505248555660, -5.807998527925970933, 11.24427360515640295 ) ) ;
#33852=LINE ( 'NONE', #2317, #64515 ) ;
#33854=CARTESIAN_POINT ( 'NONE',  ( 0.2651627923886306637, 7.938954356958216607, -9.324231535593035858 ) ) ;
#33863=CARTESIAN_POINT ( 'NONE',  ( 0.2767916011545382138, -11.57477803659170768, -4.010899340181539152 ) ) ;
#33866=ADVANCED_FACE ( 'NONE', ( #37824 ), #61743, .F. ) ;
#33870=EDGE_CURVE ( 'NONE', #62784, #51848, #19642, .T. ) ;
#33884=DIRECTION ( 'NONE',  ( 0.000000000000000000, 0.000000000000000000, 1.000000000000000000 ) ) ;
#33888=EDGE_LOOP ( 'NONE', ( #22970, #32505, #8014, #49844 ) ) ;
#33895=VERTEX_POINT ( 'NONE', #48064 ) ;
#33902=CARTESIAN_POINT ( 'NONE',  ( 1.719304012339819332, -7.581471372739574832, 10.22720798541442555 ) ) ;
#33914=CARTESIAN_POINT ( 'NONE',  ( 2.373367633546870969, 7.151506276328627898, 2.795365972209097549 ) ) ;
#33915=CARTESIAN_POINT ( 'NONE',  ( 2.241317068080781905, -2.696905536171245732, -7.142175514530103797 ) ) ;
#33919=LINE ( 'NONE', #13635, #43779 ) ;
#33929=CARTESIAN_POINT ( 'NONE',  ( 2.941278708680199916, 3.842273877444625896, -4.788765081995591366 ) ) ;
#33940=CARTESIAN_POINT ( 'NONE',  ( 2.080613030138688480, 5.400000000000000355, 1.000000000000000000 ) ) ;
#33941=CARTESIAN_POINT ( 'NONE',  ( 2.717984159219104079, -7.620583877640514814, 1.631703089059925338 ) ) ;
#33943=EDGE_LOOP ( 'NONE', ( #17264, #9568, #24869, #48655 ) ) ;
#33952=EDGE_CURVE ( 'NONE', #14132, #37036, #24441, .T. ) ;
#33953=CARTESIAN_POINT ( 'NONE',  ( 0.2911222467163562255, -9.248441845564627783, -8.040284153519465349 ) ) ;
#33962=CARTESIAN_POINT ( 'NONE',  ( 0.2653141334712595389, 7.905403790036969802, 9.352759824582522086 ) ) ;
#33971=ORIENTED_EDGE ( 'NONE', *, *, #43413, .F. ) ;
#33973=( BOUNDED_SURFACE ( )  B_SPLINE_SURFACE ( 3, 1, ( 
 ( #44488, #65108 ),
 ( #19579, #1262 ),
 ( #4938, #21191 ),
 ( #31187, #10549 ) ),
 .UNSPECIFIED., .F., .F., .F. ) 
 B_SPLINE_SURFACE_WITH_KNOTS ( ( 4, 4 ),
 ( 2, 2 ),
 ( 0.000000000000000000, 1.000000000000000000 ),
 ( 0.000000000000000000, 1.000000000000000000 ),
 .UNSPECIFIED. ) 
 GEOMETRIC_REPRESENTATION_ITEM ( )  RATIONAL_B_SPLINE_SURFACE ( (
 ( 1.000000000000000000, 1.000000000000000000),
 ( 0.6933888150995267674, 0.9895912004443193632),
 ( 0.6933888150995267674, 0.9895912004443193632),
 ( 1.000000000000000000, 1.000000000000000000) ) ) 
 REPRESENTATION_ITEM ( '' )  SURFACE ( )  );
#33975=CARTESIAN_POINT ( 'NONE',  ( 0.2650492594609231700, 6.027447650185369099, 10.66007682546619506 ) ) ;
#33979=VERTEX_POINT ( 'NONE', #2847 ) ;
#33981=CARTESIAN_POINT ( 'NONE',  ( 0.3537226245948354442, -7.688925565304952414, -9.569332148897542467 ) ) ;
#33985=CARTESIAN_POINT ( 'NONE',  ( 2.573738926104374602, -2.868819712476760042, 7.194322927777948351 ) ) ;
#33987=CARTESIAN_POINT ( 'NONE',  ( 0.2833330754217400771, 10.50818856955517866, 6.300330022379253769 ) ) ;
#33989=ORIENTED_EDGE ( 'NONE', *, *, #5245, .F. ) ;
#33996=ADVANCED_FACE ( 'NONE', ( #8142 ), #43476, .T. ) ;
#33998=CARTESIAN_POINT ( 'NONE',  ( 0.2717059086739033180, -6.276007891175655828, -10.51822005842000785 ) ) ;
#34002=DIRECTION ( 'NONE',  ( 0.000000000000000000, 0.000000000000000000, 1.000000000000000000 ) ) ;
#34004=CARTESIAN_POINT ( 'NONE',  ( 0.9232058338315048962, -8.301689855530229423, 9.306586124266566173 ) ) ;
#34012=ORIENTED_EDGE ( 'NONE', *, *, #44714, .F. ) ;
#34015=DIRECTION ( 'NONE',  ( 0.000000000000000000, 0.000000000000000000, 1.000000000000000000 ) ) ;
#34020=CARTESIAN_POINT ( 'NONE',  ( 0.3401186441510234415, 10.75260364139053415, -5.912862694513600026 ) ) ;
#34025=DIRECTION ( 'NONE',  ( 0.3865475372811021382, -0.7187975063895761796, 0.5778504531710970671 ) ) ;
#34039=CARTESIAN_POINT ( 'NONE',  ( 5.536195898058073439, 0.006344799443924024202, -0.005656495196971017721 ) ) ;
#34040=CARTESIAN_POINT ( 'NONE',  ( 0.3040950598368152291, -11.43390362554256257, 4.428852722102693207 ) ) ;
#34048=CARTESIAN_POINT ( 'NONE',  ( 3.152665057734040488, 0.000000000000000000, 0.000000000000000000 ) ) ;
#34049=CARTESIAN_POINT ( 'NONE',  ( 0.3053067050349171918, -12.11120005789972609, 1.901204202464632287 ) ) ;
#34059=VECTOR ( 'NONE', #50674, 1000.000000000000114 ) ;
#34061=ORIENTED_EDGE ( 'NONE', *, *, #21484, .F. ) ;
#34063=CARTESIAN_POINT ( 'NONE',  ( 0.2652384770603681829, 6.180206054297750384, -10.57229757085615596 ) ) ;
#34064=CARTESIAN_POINT ( 'NONE',  ( 0.2759803524722186374, -6.288205958087853098, 10.51260004517010671 ) ) ;
#34067=CARTESIAN_POINT ( 'NONE',  ( 0.7446945582507944472, 7.698291984229363116, 9.728576129009507412 ) ) ;
#34072=ORIENTED_EDGE ( 'NONE', *, *, #26785, .F. ) ;
#34073=EDGE_LOOP ( 'NONE', ( #29360, #14843, #22830, #36271 ) ) ;
#34077=CARTESIAN_POINT ( 'NONE',  ( 0.2646305136544072623, -12.08286001766536799, 1.996350543472957151 ) ) ;
#34079=CARTESIAN_POINT ( 'NONE',  ( 2.276905613632195902, 5.955225895209577125, 4.795880183930062657 ) ) ;
#34087=CARTESIAN_POINT ( 'NONE',  ( 0.3675815128205894289, 0.2638082659430137644, -12.27743992903065973 ) ) ;
#34095=ORIENTED_EDGE ( 'NONE', *, *, #13428, .T. ) ;
#34096=CARTESIAN_POINT ( 'NONE',  ( 0.7446945582511054207, 3.906659168237073487, 11.77484212699327415 ) ) ;
#34102=CARTESIAN_POINT ( 'NONE',  ( 2.990245332647884613, -0.9653152459622390547, -8.426135047918871024 ) ) ;
#34107=CARTESIAN_POINT ( 'NONE',  ( 2.244591118396557228, 1.431619869711851400, 7.500068934084574757 ) ) ;
#34110=CARTESIAN_POINT ( 'NONE',  ( 3.092491956584956014, -6.343509225034599908, -4.738927301402582337 ) ) ;
#34119=CARTESIAN_POINT ( 'NONE',  ( 2.253265082352432724, -5.932955906470540164, 4.810902415501113083 ) ) ;
#34121=ORIENTED_EDGE ( 'NONE', *, *, #2414, .T. ) ;
#34123=CARTESIAN_POINT ( 'NONE',  ( 2.276905613633648962, -2.469846004795358763, 7.236369456722870908 ) ) ;
#34127=ADVANCED_FACE ( 'NONE', ( #54994 ), #18839, .F. ) ;
#34130=B_SPLINE_CURVE_WITH_KNOTS ( 'NONE', 3,
 ( #22927, #11943, #18266, #48525, #33213, #52543, #21938, #2977, #27905, #63455, #32226, #11618, #23239, #53524, #6971, #42187, #26925, #7966, #47225 ),
 .UNSPECIFIED., .F., .F.,
 ( 4, 3, 3, 3, 3, 3, 4 ),
 ( 8.251341272764500075E-18, 2.825908398783091627E-05, 4.208813692418309291E-05, 5.591713746860777948E-05, 6.279584083140069212E-05, 9.105792820167411068E-05, 0.0001153131102489391135 ),
 .UNSPECIFIED. ) ;
#34133=CARTESIAN_POINT ( 'NONE',  ( 0.2759803524722221346, -8.018167820447549943, 9.260954523383706061 ) ) ;
#34141=CARTESIAN_POINT ( 'NONE',  ( 5.514970785353741078, -0.002093325033903841153, 0.004233694591582948079 ) ) ;
#34144=CARTESIAN_POINT ( 'NONE',  ( 2.298277635560286303, 7.564013289873170898, -1.166137492762147287 ) ) ;
#34149=ORIENTED_EDGE ( 'NONE', *, *, #8619, .F. ) ;
#34157=CONICAL_SURFACE ( 'NONE', #11849, 12.73084802173761787, 0.3217505529694027477 ) ;
#34159=EDGE_CURVE ( 'NONE', #56656, #63445, #30051, .T. ) ;
#34160=FACE_OUTER_BOUND ( 'NONE', #5543, .T. ) ;
#34163=( BOUNDED_SURFACE ( )  B_SPLINE_SURFACE ( 3, 1, ( 
 ( #32251, #27588 ),
 ( #48554, #22273 ),
 ( #43532, #2006 ),
 ( #7651, #27934 ) ),
 .UNSPECIFIED., .F., .F., .F. ) 
 B_SPLINE_SURFACE_WITH_KNOTS ( ( 4, 4 ),
 ( 2, 2 ),
 ( 0.000000000000000000, 1.000000000000000000 ),
 ( 0.000000000000000000, 1.000000000000000000 ),
 .UNSPECIFIED. ) 
 GEOMETRIC_REPRESENTATION_ITEM ( )  RATIONAL_B_SPLINE_SURFACE ( (
 ( 1.000000000000000000, 1.000000000000000000),
 ( 0.9856612449720755231, 0.9999558406602322425),
 ( 0.9856612449720755231, 0.9999558406602322425),
 ( 1.000000000000000000, 1.000000000000000000) ) ) 
 REPRESENTATION_ITEM ( '' )  SURFACE ( )  );
#34175=CARTESIAN_POINT ( 'NONE',  ( 0.2915757698887279648, 10.50410115670278444, -6.312478057070352477 ) ) ;
#34179=CARTESIAN_POINT ( 'NONE',  ( 0.2739690278137220658, 11.57167385487633560, 4.016979056590812114 ) ) ;
#34182=CARTESIAN_POINT ( 'NONE',  ( 0.2653141617321004841, 7.905395731875621834, -9.352766656399982281 ) ) ;
#34187=CARTESIAN_POINT ( 'NONE',  ( 0.8375941296813829151, 0.3844307390191658569, -12.43103843094074357 ) ) ;
#34188=CIRCLE ( 'NONE', #39507, 7.938172270156617749 ) ;
#34191=CARTESIAN_POINT ( 'NONE',  ( 1.634816307074680841, 5.718391684266664221, 11.34285134320760946 ) ) ;
#34199=CARTESIAN_POINT ( 'NONE',  ( 0.2638984909335716500, 11.43908195192329735, 4.375449752477170939 ) ) ;
#34200=CARTESIAN_POINT ( 'NONE',  ( 0.2653519789438766874, 9.395292406847929101, 7.854827495960845063 ) ) ;
#34201=CARTESIAN_POINT ( 'NONE',  ( 5.515188684475870851, -0.002166413411657383374, 0.004893136156457774874 ) ) ;
#34214=FACE_OUTER_BOUND ( 'NONE', #23909, .T. ) ;
#34230=CARTESIAN_POINT ( 'NONE',  ( 0.2956976708475453353, 12.25433786972505601, 0.2200030809426018197 ) ) ;
#34233=CARTESIAN_POINT ( 'NONE',  ( 0.7446945582518608164, -12.40088838629985624, -0.3561743995936417218 ) ) ;
#34246=CARTESIAN_POINT ( 'NONE',  ( 2.639814597422738274, 7.207158938903946321, 2.896050884406557557 ) ) ;
#34252=DIRECTION ( 'NONE',  ( 0.3865475372811021937, -0.9046932595863048654, -0.1791957239473693231 ) ) ;
#34268=CARTESIAN_POINT ( 'NONE',  ( 1.194176325881339151, 11.12159247766672898, 5.827386336992917748 ) ) ;
#34272=EDGE_LOOP ( 'NONE', ( #34149, #24614, #35928, #55442 ) ) ;
#34274=LINE ( 'NONE', #29938, #4205 ) ;
#34275=CARTESIAN_POINT ( 'NONE',  ( 1.719304012338199517, 0.000000000000000000, 0.000000000000000000 ) ) ;
#34281=ORIENTED_EDGE ( 'NONE', *, *, #61, .F. ) ;
#34286=CARTESIAN_POINT ( 'NONE',  ( 2.907497136250361880, 4.235253383576015551, 6.617189382231051908 ) ) ;
#34290=CARTESIAN_POINT ( 'NONE',  ( 2.177405672433136541, -2.605669267165103165, -10.89176600224354274 ) ) ;
#34308=CARTESIAN_POINT ( 'NONE',  ( 2.835339799623982415, -7.466040501142048313, 2.367573116406950895 ) ) ;
#34310=CARTESIAN_POINT ( 'NONE',  ( 2.241506898688419458, 3.851253041557103796, 6.591904579673240505 ) ) ;
#34312=AXIS2_PLACEMENT_3D ( 'NONE', #2998, #38888, #42531 ) ;
#34318=B_SPLINE_CURVE_WITH_KNOTS ( 'NONE', 3,
 ( #39702, #5122, #50362, #24088, #59998, #40341, #9420, #60980, #60638, #34693, #29709, #45670, #4477, #44349, #24747, #35682, #65298, #40022, #60309 ),
 .UNSPECIFIED., .F., .F.,
 ( 4, 3, 3, 3, 3, 3, 4 ),
 ( 6.759600587344756714E-18, 2.825908398831169217E-05, 4.208813692483723273E-05, 5.591713746943635389E-05, 6.279584083231494560E-05, 9.105792820296123484E-05, 0.0001153131102488860418 ),
 .UNSPECIFIED. ) ;
#34319=B_SPLINE_CURVE_WITH_KNOTS ( 'NONE', 3,
 ( #56188, #10627, #15939, #11305, #31263, #1003, #46883 ),
 .UNSPECIFIED., .F., .F.,
 ( 4, 3, 4 ),
 ( 0.000000000000000000, 0.001700533616330528446, 0.005002426799371318192 ),
 .UNSPECIFIED. ) ;
#34324=CARTESIAN_POINT ( 'NONE',  ( 0.2648978790185584908, 10.53870023327863770, 6.237101853238585569 ) ) ;
#34335=CARTESIAN_POINT ( 'NONE',  ( 0.2915757698887319060, -6.312478057070384452, -10.50410115670275069 ) ) ;
#34337=CARTESIAN_POINT ( 'NONE',  ( 0.3675815128205894289, -8.093875121226016489, -9.235491948680088825 ) ) ;
#34338=CARTESIAN_POINT ( 'NONE',  ( 0.2739690278137253410, 4.016979056590924912, -11.57167385487629474 ) ) ;
#34339=CARTESIAN_POINT ( 'NONE',  ( 5.530133899448235191, -0.01293763278443444721, -0.009387834778845806707 ) ) ;
#34346=VERTEX_POINT ( 'NONE', #65453 ) ;
#34355=CARTESIAN_POINT ( 'NONE',  ( 0.2648978790185619880, 6.008231198269132989, -10.67083876753485328 ) ) ;
#34356=CARTESIAN_POINT ( 'NONE',  ( 0.2958664285830389651, -10.50235171906344789, 6.318165763623585285 ) ) ;
#34359=CARTESIAN_POINT ( 'NONE',  ( 0.3278977287071212499, 10.74546228373874790, -5.917385921415685424 ) ) ;
#34361=CARTESIAN_POINT ( 'NONE',  ( 2.305787727787083519, 7.135468203930020792, -2.774453000917077805 ) ) ;
#34363=VERTEX_POINT ( 'NONE', #35195 ) ;
#34368=ORIENTED_EDGE ( 'NONE', *, *, #20663, .F. ) ;
#34404=CARTESIAN_POINT ( 'NONE',  ( 0.2648978790185593790, -6.237101853238620208, 10.53870023327861283 ) ) ;
#34405=CARTESIAN_POINT ( 'NONE',  ( 2.260457164927185847, -7.547495527593552467, -1.190240296002748277 ) ) ;
#34421=CARTESIAN_POINT ( 'NONE',  ( 0.2655924914740778187, -12.06787830249866467, 2.083162675473574588 ) ) ;
#34424=ORIENTED_EDGE ( 'NONE', *, *, #532, .F. ) ;
#34427=VECTOR ( 'NONE', #27282, 1000.000000000000114 ) ;
#34433=CARTESIAN_POINT ( 'NONE',  ( 2.177405672432084938, 7.702458780349609846, 8.129711416438519578 ) ) ;
#34453=VERTEX_POINT ( 'NONE', #21219 ) ;
#34454=CARTESIAN_POINT ( 'NONE',  ( 2.589278595512557235, -6.089088204448533936, -4.794929105510985501 ) ) ;
#34455=CARTESIAN_POINT ( 'NONE',  ( 5.515539859299206427, 0.004509673239148487972, -0.004037661319611322332 ) ) ;
#34456=CARTESIAN_POINT ( 'NONE',  ( 2.350038591458129655, 7.710465783963716291, 7.305692696275574605 ) ) ;
#34470=CARTESIAN_POINT ( 'NONE',  ( 0.3401186441510204994, -8.081824149807760094, 9.233880480307277594 ) ) ;
#34474=CARTESIAN_POINT ( 'NONE',  ( 0.3675815128205912052, 12.04510820461662668, -2.391755495700480516 ) ) ;
#34475=ORIENTED_EDGE ( 'NONE', *, *, #41731, .T. ) ;
#34479=CARTESIAN_POINT ( 'NONE',  ( 2.524535260912981194, -4.796565674004606983, 6.060306679219116255 ) ) ;
#34481=CARTESIAN_POINT ( 'NONE',  ( 2.941278708680199916, 2.226055275041790349, 5.721889327162159589 ) ) ;
#34483=CARTESIAN_POINT ( 'NONE',  ( 2.241317068080784125, 1.235499051335310794, -7.533758201955659040 ) ) ;
#34485=EDGE_LOOP ( 'NONE', ( #16016, #26558, #18037, #22591 ) ) ;
#34486=CARTESIAN_POINT ( 'NONE',  ( 5.515539859299206427, -0.002856745161749578953, 0.005336559634876932544 ) ) ;
#34490=CARTESIAN_POINT ( 'NONE',  ( 2.941278708680199916, -1.972702289975964973, -5.814102272488608669 ) ) ;
#34492=CARTESIAN_POINT ( 'NONE',  ( 0.3675815128205894289, 5.910255304480596550, -10.76447900494934196 ) ) ;
#34495=CARTESIAN_POINT ( 'NONE',  ( 2.241352910868909643, -4.970878533273721978, -5.794346703933896059 ) ) ;
#34496=ORIENTED_EDGE ( 'NONE', *, *, #11482, .T. ) ;
#34497=ORIENTED_EDGE ( 'NONE', *, *, #49342, .T. ) ;
#34498=CARTESIAN_POINT ( 'NONE',  ( 2.259025283528085737, -7.225123487442752790, -2.484282765458421860 ) ) ;
#34508=CARTESIAN_POINT ( 'NONE',  ( 0.2653519890518156732, -10.60551359205155109, 6.123106317427121859 ) ) ;
#34510=CARTESIAN_POINT ( 'NONE',  ( 0.3223008802179184173, 11.60682919296352011, 3.964361764750220285 ) ) ;
#34514=CARTESIAN_POINT ( 'NONE',  ( 3.152665057734119536, 1.848755561852129858, -7.719888720907784219 ) ) ;
#34518=CARTESIAN_POINT ( 'NONE',  ( 2.241537034860907607, -7.519304283075084250, 1.321063441155965190 ) ) ;
#34523=ORIENTED_EDGE ( 'NONE', *, *, #7127, .F. ) ;
#34525=CARTESIAN_POINT ( 'NONE',  ( 0.3632410797595240770, 0.2628628737173456797, 12.27601307605976899 ) ) ;
#34529=CARTESIAN_POINT ( 'NONE',  ( 1.937114397841935398, 1.334979369128593163, -12.76557247858997002 ) ) ;
#34530=CARTESIAN_POINT ( 'NONE',  ( 0.2648978790185602672, -12.03635331166813494, 2.256510822326103671 ) ) ;
#34534=CARTESIAN_POINT ( 'NONE',  ( 2.350038591457884074, 0.6402934222730660707, -10.60256821300862029 ) ) ;
#34543=CARTESIAN_POINT ( 'NONE',  ( 0.3610902822527192191, -0.2623004149193758350, -12.27530799859939314 ) ) ;
#34553=CARTESIAN_POINT ( 'NONE',  ( 2.889800649504073782, 6.016320774579807740, 1.129261637821630693 ) ) ;
#34554=CARTESIAN_POINT ( 'NONE',  ( 2.241449424704146320, 4.860179885671878530, -5.887589908049596588 ) ) ;
#34556=CARTESIAN_POINT ( 'NONE',  ( 2.653899356900482509, 6.596318473603900223, -4.109946795501497441 ) ) ;
#34562=ADVANCED_FACE ( 'NONE', ( #36846 ), #56726, .F. ) ;
#34565=EDGE_LOOP ( 'NONE', ( #17043, #26805, #33291, #49871 ) ) ;
#34581=ADVANCED_FACE ( 'NONE', ( #10258 ), #22730, .F. ) ;
#34585=CARTESIAN_POINT ( 'NONE',  ( 2.284126774967659923, -7.131638985093294636, -2.764365694977863441 ) ) ;
#34587=ORIENTED_EDGE ( 'NONE', *, *, #3253, .T. ) ;
#34593=CARTESIAN_POINT ( 'NONE',  ( 0.2648978790185584908, -10.67083876753496341, 6.008231198268946471 ) ) ;
#34597=B_SPLINE_CURVE_WITH_KNOTS ( 'NONE', 3,
 ( #31750, #56046, #51084, #45749, #50748, #21124, #30764, #45413, #61356, #6185 ),
 .UNSPECIFIED., .F., .F.,
 ( 4, 3, 3, 4 ),
 ( 1.226634733346699349E-18, 6.607638129004513277E-05, 9.911389841680585955E-05, 0.0001667630577588622028 ),
 .UNSPECIFIED. ) ;
#34600=CARTESIAN_POINT ( 'NONE',  ( 2.297017764050093280, -7.651182381906875385, 0.1647869190091477420 ) ) ;
#34608=ORIENTED_EDGE ( 'NONE', *, *, #43540, .T. ) ;
#34611=ADVANCED_FACE ( 'NONE', ( #22551 ), #2754, .F. ) ;
#34621=ORIENTED_EDGE ( 'NONE', *, *, #9099, .T. ) ;
#34622=FACE_OUTER_BOUND ( 'NONE', #7488, .T. ) ;
#34625=CARTESIAN_POINT ( 'NONE',  ( 2.241509619876136838, 3.784042210004710416, 6.630717740088868162 ) ) ;
#34627=B_SPLINE_CURVE_WITH_KNOTS ( 'NONE', 3,
 ( #21552, #41820, #31823, #47160, #35518, #61124, #15558, #619, #1274, #1609, #20879, #934, #52138, #25538, #26521, #16226 ),
 .UNSPECIFIED., .F., .F.,
 ( 4, 3, 3, 3, 3, 4 ),
 ( 0.000000000000000000, 0.0003017745587525247591, 0.0006035491769808746078, 0.0009053241094668185249, 0.001207275924539397789, 0.001510325902531782461 ),
 .UNSPECIFIED. ) ;
#34631=ADVANCED_FACE ( 'NONE', ( #38145 ), #2150, .T. ) ;
#34661=EDGE_CURVE ( 'NONE', #34740, #56858, #32329, .T. ) ;
#34665=CARTESIAN_POINT ( 'NONE',  ( 2.305787727787084407, 4.792270232040973355, -5.970480882365174047 ) ) ;
#34667=CARTESIAN_POINT ( 'NONE',  ( 5.515539859299206427, -0.001241880655086631752, 0.005924322247674733248 ) ) ;
#34668=CARTESIAN_POINT ( 'NONE',  ( 0.2648978790185593790, 10.67083876753491900, 6.008231198269021078 ) ) ;
#34669=CARTESIAN_POINT ( 'NONE',  ( 2.288423627606498201, 7.242304196985708487, 2.464337058689050064 ) ) ;
#34686=CARTESIAN_POINT ( 'NONE',  ( 2.253265082352434945, 6.678225412356993296, -3.707567016433741980 ) ) ;
#34691=EDGE_LOOP ( 'NONE', ( #30975, #25816, #53556, #53324 ) ) ;
#34692=AXIS2_PLACEMENT_3D ( 'NONE', #34983, #19406, #34015 ) ;
#34693=CARTESIAN_POINT ( 'NONE',  ( 2.260457164927188511, 0.1384509728649064020, 7.639515169785717319 ) ) ;
#34705=ORIENTED_EDGE ( 'NONE', *, *, #22444, .F. ) ;
#34706=CARTESIAN_POINT ( 'NONE',  ( 1.549075743845218955, -12.34675572956545153, -2.862200647102061346 ) ) ;
#34708=CARTESIAN_POINT ( 'NONE',  ( 0.2676618633000455993, -6.262131165853799253, 10.52491907319759967 ) ) ;
#34712=CARTESIAN_POINT ( 'NONE',  ( 1.287602823385180839, 7.659913635102068241, 9.987902848012801371 ) ) ;
#34727=( BOUNDED_SURFACE ( )  B_SPLINE_SURFACE ( 3, 1, ( 
 ( #60199, #56187 ),
 ( #46239, #35244 ),
 ( #50245, #65496 ),
 ( #9996, #4359 ) ),
 .UNSPECIFIED., .F., .F., .F. ) 
 B_SPLINE_SURFACE_WITH_KNOTS ( ( 4, 4 ),
 ( 2, 2 ),
 ( 0.000000000000000000, 1.000000000000000000 ),
 ( 0.000000000000000000, 1.000000000000000000 ),
 .UNSPECIFIED. ) 
 GEOMETRIC_REPRESENTATION_ITEM ( )  RATIONAL_B_SPLINE_SURFACE ( (
 ( 1.000000000000000000, 1.000000000000000000),
 ( 0.6933888150995267674, 0.9895912004443193632),
 ( 0.6933888150995267674, 0.9895912004443193632),
 ( 1.000000000000000000, 1.000000000000000000) ) ) 
 REPRESENTATION_ITEM ( '' )  SURFACE ( )  );
#34729=CARTESIAN_POINT ( 'NONE',  ( 5.520433897694421610, -0.01505375422439122687, 0.0005131706886599850161 ) ) ;
#34735=CARTESIAN_POINT ( 'NONE',  ( 1.283627346226613009, -12.28700367512546343, 2.725559306498961831 ) ) ;
#34740=VERTEX_POINT ( 'NONE', #14499 ) ;
#34741=ORIENTED_EDGE ( 'NONE', *, *, #49428, .F. ) ;
#34742=DIRECTION ( 'NONE',  ( 0.000000000000000000, 0.000000000000000000, 1.000000000000000000 ) ) ;
#34754=CARTESIAN_POINT ( 'NONE',  ( 2.305787727787083519, 5.970480882365222897, 4.792270232040915623 ) ) ;
#34758=CARTESIAN_POINT ( 'NONE',  ( 5.514970785353741078, 0.004324946436530306346, -0.001897634820904968824 ) ) ;
#34760=EDGE_CURVE ( 'NONE', #10376, #15607, #11602, .T. ) ;
#34764=CARTESIAN_POINT ( 'NONE',  ( 2.259025283528085737, -2.484282765458397435, 7.225123487442759895 ) ) ;
#34771=CARTESIAN_POINT ( 'NONE',  ( 0.7446945582506544481, 12.40088838629945300, 0.3561743995932071249 ) ) ;
#34783=CARTESIAN_POINT ( 'NONE',  ( 0.000000000000000000, 1.523986892267801462E-15, 12.15774668701806149 ) ) ;
#34785=CARTESIAN_POINT ( 'NONE',  ( 2.273267844203311849, 1.178226273334160412, -7.553702825375153473 ) ) ;
#34789=ORIENTED_EDGE ( 'NONE', *, *, #49065, .T. ) ;
#34803=ADVANCED_FACE ( 'NONE', ( #40434 ), #9483, .F. ) ;
#34806=EDGE_LOOP ( 'NONE', ( #57757, #63497, #41044, #2620 ) ) ;
#34809=LINE ( 'NONE', #45800, #63428 ) ;
#34810=CARTESIAN_POINT ( 'NONE',  ( 2.440552418640494992, -4.020120046181088647, 6.568204543009814600 ) ) ;
#34812=CARTESIAN_POINT ( 'NONE',  ( 0.3341166715381236330, 11.61315925169694729, 3.958014133396652312 ) ) ;
#34814=CARTESIAN_POINT ( 'NONE',  ( 1.719304012339881282, -12.20344780066076318, 3.626341562669963992 ) ) ;
#34819=CARTESIAN_POINT ( 'NONE',  ( 0.9296196016848956578, 0.4155906739605440547, -12.46069139398492176 ) ) ;
#34823=EDGE_CURVE ( 'NONE', #58530, #51219, #25820, .T. ) ;
#34826=CARTESIAN_POINT ( 'NONE',  ( 0.2648978790185602672, 0.1321385342562404197, 12.24533305150758089 ) ) ;
#34828=ORIENTED_EDGE ( 'NONE', *, *, #39476, .T. ) ;
#34831=CARTESIAN_POINT ( 'NONE',  ( 2.241509619876138171, -4.936617871859544593, 5.823675573301060560 ) ) ;
#34833=CARTESIAN_POINT ( 'NONE',  ( 0.2652384529303136174, -12.04846370803830524, 2.191562200667146687 ) ) ;
#34834=CARTESIAN_POINT ( 'NONE',  ( 2.368238019615418466, 5.070835960313035962, 5.763545178420164561 ) ) ;
#34835=VERTEX_POINT ( 'NONE', #20823 ) ;
#34836=CARTESIAN_POINT ( 'NONE',  ( 5.515539859299206427, -0.006049968793488395835, -0.0001942659352248416859 ) ) ;
#34837=CARTESIAN_POINT ( 'NONE',  ( 2.305787727787084407, 0.1666591538752685842, 7.654065630109507801 ) ) ;
#34839=CARTESIAN_POINT ( 'NONE',  ( 1.372161826076019109, 2.769012792636492026, 12.30755118281438243 ) ) ;
#34850=ORIENTED_EDGE ( 'NONE', *, *, #11035, .T. ) ;
#34853=VERTEX_POINT ( 'NONE', #56755 ) ;
#34870=EDGE_CURVE ( 'NONE', #37505, #5308, #16456, .T. ) ;
#34873=VECTOR ( 'NONE', #7900, 1000.000000000000114 ) ;
#34881=EDGE_LOOP ( 'NONE', ( #13813, #40643, #15859, #27149 ) ) ;
#34887=CARTESIAN_POINT ( 'NONE',  ( 0.3537226245948384418, 11.62199823003439292, -3.952322262392271579 ) ) ;
#34889=ORIENTED_EDGE ( 'NONE', *, *, #57375, .F. ) ;
#34897=CARTESIAN_POINT ( 'NONE',  ( 2.261269890821707484, -2.481875047313262250, -7.226741992146552995 ) ) ;
#34904=CARTESIAN_POINT ( 'NONE',  ( 2.280717697723833037, -6.699799459371637234, -3.687451363405637839 ) ) ;
#34907=CARTESIAN_POINT ( 'NONE',  ( 2.273267844204866606, -7.643541951623946673, 0.1513603614830237865 ) ) ;
#34910=CARTESIAN_POINT ( 'NONE',  ( 0.2767916011545367705, 10.70244578860295981, 5.959903879715624520 ) ) ;
#34912=CARTESIAN_POINT ( 'NONE',  ( 2.963017218115624907, 7.004145770368821466, -3.599595431209413388 ) ) ;
#34916=EDGE_CURVE ( 'NONE', #44487, #36493, #64781, .T. ) ;
#34926=CARTESIAN_POINT ( 'NONE',  ( 2.241352910868908310, 2.689314586382351546, 7.145045428366586293 ) ) ;
#34927=CARTESIAN_POINT ( 'NONE',  ( 2.280717697723835258, -5.957695241725366131, -4.794838658391083364 ) ) ;
#34939=CARTESIAN_POINT ( 'NONE',  ( 2.241352910868908754, -1.243507963608043498, -7.532448145350521429 ) ) ;
#34944=DIRECTION ( 'NONE',  ( -0.3939253465568944290, 0.1500280335741595583, -0.9068155327749417571 ) ) ;
#34952=EDGE_LOOP ( 'NONE', ( #49464, #19636, #23544, #16337 ) ) ;
#34954=VECTOR ( 'NONE', #48936, 1000.000000000000000 ) ;
#34963=ORIENTED_EDGE ( 'NONE', *, *, #46482, .F. ) ;
#34966=VECTOR ( 'NONE', #17650, 1000.000000000000114 ) ;
#34971=CARTESIAN_POINT ( 'NONE',  ( 2.251152103363648571, 5.769488058190800572, -5.004701566805173307 ) ) ;
#34983=CARTESIAN_POINT ( 'NONE',  ( 3.152665057734040488, 0.000000000000000000, 0.000000000000000000 ) ) ;
#34985=CARTESIAN_POINT ( 'NONE',  ( 5.516018279890452902, 0.005331956019561711300, -0.004180585980734999839 ) ) ;
#34987=CARTESIAN_POINT ( 'NONE',  ( 0.2657645697724699274, 10.68050050043099297, -5.991637049003132098 ) ) ;
#34990=CARTESIAN_POINT ( 'NONE',  ( 2.639814597422732056, -6.111633106000453175, 4.793557287999607119 ) ) ;
#35001=ORIENTED_EDGE ( 'NONE', *, *, #60502, .F. ) ;
#35011=EDGE_CURVE ( 'NONE', #63287, #32302, #28336, .T. ) ;
#35015=EDGE_LOOP ( 'NONE', ( #18581, #44871, #58986, #53058 ) ) ;
#35019=VERTEX_POINT ( 'NONE', #61934 ) ;
#35023=ORIENTED_EDGE ( 'NONE', *, *, #28819, .T. ) ;
#35026=CARTESIAN_POINT ( 'NONE',  ( 0.3002738374340813143, -6.323236184341188171, 10.50101454678642021 ) ) ;
#35029=CARTESIAN_POINT ( 'NONE',  ( 0.3654063281920716388, -10.76363796011281337, -5.910280591919169879 ) ) ;
#35031=B_SPLINE_CURVE_WITH_KNOTS ( 'NONE', 3,
 ( #58072, #22149, #22486, #48751, #13168, #2210, #33449, #42090, #53742, #37444, #63045, #28448, #3203, #57755, #62372, #47759 ),
 .UNSPECIFIED., .F., .F.,
 ( 4, 3, 3, 3, 3, 4 ),
 ( 0.000000000000000000, 0.0003017745587525256807, 0.0006035491769808747162, 0.0009053241094668175492, 0.001207275924539396488, 0.001510325902531783112 ),
 .UNSPECIFIED. ) ;
#35037=CARTESIAN_POINT ( 'NONE',  ( 5.516018279890452902, 0.001397286410094419331, 0.006629829924290476899 ) ) ;
#35050=CARTESIAN_POINT ( 'NONE',  ( 2.251152103361937939, 5.930529991875680196, 4.812779263777095196 ) ) ;
#35053=ORIENTED_EDGE ( 'NONE', *, *, #25662, .F. ) ;
#35055=ORIENTED_EDGE ( 'NONE', *, *, #16528, .T. ) ;
#35063=CARTESIAN_POINT ( 'NONE',  ( 3.152665057736164123, 5.461013642407259283, 5.761241965767907480 ) ) ;
#35064=CARTESIAN_POINT ( 'NONE',  ( 2.177405672431368622, 1.276675186593990263, -11.12610351585605173 ) ) ;
#35069=CARTESIAN_POINT ( 'NONE',  ( 2.257661810676416803, 7.499185766072606008, -1.459225434025898327 ) ) ;
#35078=CARTESIAN_POINT ( 'NONE',  ( 1.452237505248555660, -12.55261342181974626, -1.611965288198859314 ) ) ;
#35080=ORIENTED_EDGE ( 'NONE', *, *, #5860, .T. ) ;
#35081=CARTESIAN_POINT ( 'NONE',  ( 2.655192694322446201, -3.822392723569365991, -8.807900729504780202 ) ) ;
#35084=CARTESIAN_POINT ( 'NONE',  ( 2.903928887688265625, -6.032681461746786766, -6.365315087929473314 ) ) ;
#35092=CARTESIAN_POINT ( 'NONE',  ( 2.247112776671467582, -2.501955819907531353, 7.214825360831409462 ) ) ;
#35095=ORIENTED_EDGE ( 'NONE', *, *, #19539, .F. ) ;
#35096=CARTESIAN_POINT ( 'NONE',  ( 1.375507693217726590, -6.813306181534734662, 10.61839108744977445 ) ) ;
#35107=CARTESIAN_POINT ( 'NONE',  ( 0.3278977287071211388, 7.693417476735527671, 9.554671284920326357 ) ) ;
#35110=( BOUNDED_SURFACE ( )  B_SPLINE_SURFACE ( 3, 1, ( 
 ( #41368, #11137 ),
 ( #56709, #10144 ),
 ( #36046, #14774 ),
 ( #5506, #9805 ) ),
 .UNSPECIFIED., .F., .F., .F. ) 
 B_SPLINE_SURFACE_WITH_KNOTS ( ( 4, 4 ),
 ( 2, 2 ),
 ( 0.000000000000000000, 1.000000000000000000 ),
 ( 0.000000000000000000, 1.000000000000000000 ),
 .UNSPECIFIED. ) 
 GEOMETRIC_REPRESENTATION_ITEM ( )  RATIONAL_B_SPLINE_SURFACE ( (
 ( 1.000000000000000000, 1.000000000000000000),
 ( 0.6933888150995267674, 0.9895912004443193632),
 ( 0.6933888150995267674, 0.9895912004443193632),
 ( 1.000000000000000000, 1.000000000000000000) ) ) 
 REPRESENTATION_ITEM ( '' )  SURFACE ( )  );
#35111=CARTESIAN_POINT ( 'NONE',  ( 0.3675815128205894289, -9.574637318041910206, -7.689697408877373519 ) ) ;
#35112=CARTESIAN_POINT ( 'NONE',  ( 1.462291587751302302, -1.569662666436036469, -12.54737685278425197 ) ) ;
#35115=CARTESIAN_POINT ( 'NONE',  ( 2.305787727787084407, 1.164987321564833422, -7.566723232958059597 ) ) ;
#35116=ORIENTED_EDGE ( 'NONE', *, *, #21422, .F. ) ;
#35122=CARTESIAN_POINT ( 'NONE',  ( 0.2759803524722169721, 11.44482553421631010, 4.367180139677351747 ) ) ;
#35137=VERTEX_POINT ( 'NONE', #22171 ) ;
#35142=CARTESIAN_POINT ( 'NONE',  ( 3.047904605210424389, -4.313929735713912805, 6.622084192655478319 ) ) ;
#35143=CARTESIAN_POINT ( 'NONE',  ( 0.2648978790185584908, -10.67083876753496341, 6.008231198268946471 ) ) ;
#35146=ORIENTED_EDGE ( 'NONE', *, *, #46062, .T. ) ;
#35147=CARTESIAN_POINT ( 'NONE',  ( 2.288423627607476529, 7.648392725410192661, -0.1612945702822020377 ) ) ;
#35159=CARTESIAN_POINT ( 'NONE',  ( 0.2647959493198550618, 0.1469673141001566208, 12.24513905663510549 ) ) ;
#35164=CARTESIAN_POINT ( 'NONE',  ( 0.2648978790185602672, -12.24533305150758267, 0.1321385342561976484 ) ) ;
#35166=AXIS2_PLACEMENT_3D ( 'NONE', #24349, #13394, #33678 ) ;
#35168=CARTESIAN_POINT ( 'NONE',  ( 2.276905613633474434, 2.469846004795502648, -7.236369456722756333 ) ) ;
#35170=CARTESIAN_POINT ( 'NONE',  ( 5.515188684475870851, -0.005320786921497274412, 0.0005703990286342659364 ) ) ;
#35171=CARTESIAN_POINT ( 'NONE',  ( 2.524535260912004198, 2.434550409953288863, -7.335347545455379148 ) ) ;
#35173=ADVANCED_FACE ( 'NONE', ( #25871 ), #12030, .F. ) ;
#35176=FACE_OUTER_BOUND ( 'NONE', #19031, .T. ) ;
#35179=VERTEX_POINT ( 'NONE', #61416 ) ;
#35180=CARTESIAN_POINT ( 'NONE',  ( 5.530133899448235191, 0.003876417824003331770, 0.01550764871776277344 ) ) ;
#35183=CARTESIAN_POINT ( 'NONE',  ( 0.2652384770603652409, 12.24598129987882444, 0.06606665821602195066 ) ) ;
#35194=B_SPLINE_CURVE_WITH_KNOTS ( 'NONE', 3,
 ( #59071, #39081, #29749, #24791, #13479, #45070, #23823, #48756, #55035, #44084, #64356, #13175, #33762, #44721, #65005, #4176, #43753, #64034, #49430 ),
 .UNSPECIFIED., .F., .F.,
 ( 4, 3, 3, 3, 3, 3, 4 ),
 ( 6.447129612864634281E-18, 2.825908398831150243E-05, 4.208813692483755799E-05, 5.591713746943746520E-05, 6.279584083231628730E-05, 9.105792820296214286E-05, 0.0001153131102488863264 ),
 .UNSPECIFIED. ) ;
#35195=CARTESIAN_POINT ( 'NONE',  ( 2.241352910868908310, 4.843133558968128582, 5.901537464758471074 ) ) ;
#35196=EDGE_LOOP ( 'NONE', ( #29062, #3839, #47494, #15506 ) ) ;
#35199=DIRECTION ( 'NONE',  ( 0.000000000000000000, 0.000000000000000000, -1.000000000000000000 ) ) ;
#35200=CARTESIAN_POINT ( 'NONE',  ( 0.2833330754217401881, 12.25052326018167470, 0.2021515668286114065 ) ) ;
#35206=CARTESIAN_POINT ( 'NONE',  ( 1.198791140418999035, -11.12379938352691156, 5.826488554585893986 ) ) ;
#35222=ORIENTED_EDGE ( 'NONE', *, *, #32199, .T. ) ;
#35227=CARTESIAN_POINT ( 'NONE',  ( 0.3053067050349176359, 11.59706307017088811, -3.975408458060398331 ) ) ;
#35232=CARTESIAN_POINT ( 'NONE',  ( 2.889800649504073782, 5.267262008933668582, 3.118861721612583793 ) ) ;
#35237=EDGE_CURVE ( 'NONE', #32084, #18779, #37037, .T. ) ;
#35243=VERTEX_POINT ( 'NONE', #32783 ) ;
#35244=CARTESIAN_POINT ( 'NONE',  ( 0.9232058338315048962, 6.559496812049809833, -10.60677148422237259 ) ) ;
#35255=CARTESIAN_POINT ( 'NONE',  ( 0.6473888112830261665, 9.687359867659798951, 7.698027285532502262 ) ) ;
#35263=CARTESIAN_POINT ( 'NONE',  ( 2.406456491627547933, -2.427896847125293078, -10.14681500355714228 ) ) ;
#35264=CARTESIAN_POINT ( 'NONE',  ( 2.931247277082678071, 3.607110715259749689, 6.988361004535447840 ) ) ;
#35268=DIRECTION ( 'NONE',  ( -1.000000000000000000, -0.000000000000000000, -0.000000000000000000 ) ) ;
#35273=CARTESIAN_POINT ( 'NONE',  ( 2.177405672432016104, -1.276675186593669187, 11.12610351585390411 ) ) ;
#35278=VECTOR ( 'NONE', #1672, 1000.000000000000000 ) ;
#35282=CARTESIAN_POINT ( 'NONE',  ( 0.3665391374699464300, -0.2638605131388023217, 12.27992639892678106 ) ) ;
#35302=VERTEX_POINT ( 'NONE', #12846 ) ;
#35308=CARTESIAN_POINT ( 'NONE',  ( 1.719304012340734378, -7.017415949613340587, -10.62216384465587282 ) ) ;
#35312=CARTESIAN_POINT ( 'NONE',  ( 0.2801149460245160872, -12.24954625471155722, 0.1962575296604981423 ) ) ;
#35328=CARTESIAN_POINT ( 'NONE',  ( 2.256373768221671128, 7.223078030709081609, 2.487510024223419158 ) ) ;
#35336=CARTESIAN_POINT ( 'NONE',  ( 0.5572780756279746006, 12.09922454589784380, 2.443667122521326007 ) ) ;
#35348=CARTESIAN_POINT ( 'NONE',  ( 0.2648978790185602672, 1.996248716311790128, -12.08224454301446826 ) ) ;
#35362=ORIENTED_EDGE ( 'NONE', *, *, #1281, .F. ) ;
#35374=DIRECTION ( 'NONE',  ( 0.3939253465568943735, 0.3234796780324362686, -0.8603393047164948904 ) ) ;
#35386=CARTESIAN_POINT ( 'NONE',  ( 0.2956976708475548277, 9.528782683728200809, -7.708404409946551183 ) ) ;
#35394=ORIENTED_EDGE ( 'NONE', *, *, #57442, .T. ) ;
#35427=CARTESIAN_POINT ( 'NONE',  ( 2.589278595512946701, 6.089088204448742658, 4.794929105510930434 ) ) ;
#35430=CARTESIAN_POINT ( 'NONE',  ( 2.406456491624145766, -4.152987573058577908, -9.571062220827512235 ) ) ;
#35431=CARTESIAN_POINT ( 'NONE',  ( 5.515188684475870851, 0.004442604682416617309, -0.002983184900675344906 ) ) ;
#35438=CARTESIAN_POINT ( 'NONE',  ( 2.305787727787084407, -5.970480882365253983, 4.792270232040873879 ) ) ;
#35441=CARTESIAN_POINT ( 'NONE',  ( 1.452237505248552996, -12.64182585313125706, -0.5922625322518334512 ) ) ;
#35444=EDGE_CURVE ( 'NONE', #36108, #37474, #39422, .T. ) ;
#35445=ORIENTED_EDGE ( 'NONE', *, *, #40300, .T. ) ;
#35450=CARTESIAN_POINT ( 'NONE',  ( 2.639814597422733833, 1.095525832903487817, 7.689608172406200204 ) ) ;
#35455=CARTESIAN_POINT ( 'NONE',  ( 0.2869720083484343376, 7.715523637151767922, 9.519277517057126659 ) ) ;
#35465=ORIENTED_EDGE ( 'NONE', *, *, #20103, .T. ) ;
#35466=FILL_AREA_STYLE ('',( #41768 ) ) ;
#35470=EDGE_CURVE ( 'NONE', #45493, #23985, #59722, .T. ) ;
#35478=EDGE_LOOP ( 'NONE', ( #6018, #35080, #55026, #16186, #23558, #6047, #27570, #29825, #9744, #56671, #11414, #9292, #51731, #47950, #57913, #42196, #65541, #54701, #31503, #24638, #26070, #8789, #11434, #30199, #26906, #39784, #56831, #62370, #56859, #43980, #248, #15857, #17591, #49623, #52022, #38873, #54576, #28344, #10852, #1634, #30882, #8041, #64556, #28613, #38969, #64675, #13340, #24294, #42182, #50794, #59080, #58307, #40844, #44858, #9604, #22041, #34475, #12501, #29671, #10572, #56219, #57447, #19637, #37137, #5631, #21240, #2036, #37983, #4144, #53415, #12269, #34587, #10669, #5806, #25997, #44924, #48513, #63918, #33364, #31069, #65042, #63837, #7589, #49344, #40367, #49801, #20186, #48084, #62907, #51843, #40865, #30039, #32388, #9146, #58667, #47523, #15185, #32646, #63953, #5268, #7414, #45268, #29029, #20238, #28462, #35465, #49836, #38417, #63019, #34621, #49415, #1924 ) ) ;
#35479=CARTESIAN_POINT ( 'NONE',  ( 2.573738926104375047, 0.2352053552898537014, -7.741646296020610052 ) ) ;
#35486=CARTESIAN_POINT ( 'NONE',  ( 5.515539859299206427, -0.001241880655086973709, -0.005924322247675104479 ) ) ;
#35489=CARTESIAN_POINT ( 'NONE',  ( 0.2648978790185619880, -10.53870023327867855, 6.237101853238509186 ) ) ;
#35491=CARTESIAN_POINT ( 'NONE',  ( 3.152665057734040488, 0.000000000000000000, 0.000000000000000000 ) ) ;
#35493=CARTESIAN_POINT ( 'NONE',  ( 2.244591118396557672, 7.634724215899723276, -0.1074970442784372593 ) ) ;
#35496=CARTESIAN_POINT ( 'NONE',  ( 2.241526690369556540, 5.859443871527043157, 4.894066724724273953 ) ) ;
#35497=CARTESIAN_POINT ( 'NONE',  ( 2.241506898688417682, -7.511570207700569490, 1.364429914801493338 ) ) ;
#35504=EDGE_LOOP ( 'NONE', ( #4023, #2715, #47724, #24705 ) ) ;
#35509=CONICAL_SURFACE ( 'NONE', #21720, 7.938172270156617749, 1.280189991382167047 ) ;
#35511=CARTESIAN_POINT ( 'NONE',  ( 0.2646305136544065406, 11.46223899740599883, 4.312539723326170638 ) ) ;
#35512=CARTESIAN_POINT ( 'NONE',  ( 2.653899356899763973, -7.694895988366324602, -1.091629880170596811 ) ) ;
#35513=CARTESIAN_POINT ( 'NONE',  ( 2.273267844204675647, 2.472013099045248463, -7.234348261136679170 ) ) ;
#35515=ORIENTED_EDGE ( 'NONE', *, *, #52818, .T. ) ;
#35517=CARTESIAN_POINT ( 'NONE',  ( 2.241352910868909643, -3.744764251557037849, 6.652881166698498383 ) ) ;
#35518=CARTESIAN_POINT ( 'NONE',  ( 0.7400311444011727913, -1.803686700615490635, 12.27261279799597560 ) ) ;
#35519=CARTESIAN_POINT ( 'NONE',  ( 2.241536586108912488, -6.614789707676438368, -3.811784405792419950 ) ) ;
#35534=VERTEX_POINT ( 'NONE', #22018 ) ;
#35535=CARTESIAN_POINT ( 'NONE',  ( 5.515188684475870851, 0.004322737127823972868, 0.003154373509839877594 ) ) ;
#35537=CARTESIAN_POINT ( 'NONE',  ( 2.276198483117255922, -6.543270001966377869, -3.955655305430039625 ) ) ;
#35538=DIRECTION ( 'NONE',  ( 0.3865475372811021937, 0.5778504531710993986, 0.7187975063895742922 ) ) ;
#35540=CARTESIAN_POINT ( 'NONE',  ( 0.5572780756278378211, 9.256402261579090407, 8.165890079445167871 ) ) ;
#35541=CARTESIAN_POINT ( 'NONE',  ( 0.8320506296491578802, 9.275353261146646489, -8.282532257448718127 ) ) ;
#35542=CARTESIAN_POINT ( 'NONE',  ( 5.515539859299206427, 0.006049968793488819975, -0.0001942659352250742744 ) ) ;
#35544=VERTEX_POINT ( 'NONE', #15779 ) ;
#35546=CARTESIAN_POINT ( 'NONE',  ( 2.639814597422741826, -2.414168779979533941, -7.382549681340934811 ) ) ;
#35548=CARTESIAN_POINT ( 'NONE',  ( 0.5547464869798235387, -2.442933571354888755, -12.09851097165511646 ) ) ;
#35558=CARTESIAN_POINT ( 'NONE',  ( 0.2646305136544072623, 2.256625640822473411, -12.03696649559612553 ) ) ;
#35561=ORIENTED_EDGE ( 'NONE', *, *, #58765, .T. ) ;
#35562=CARTESIAN_POINT ( 'NONE',  ( 2.440552418640496324, -6.765628357760804512, 3.678171968408304959 ) ) ;
#35565=ORIENTED_EDGE ( 'NONE', *, *, #63145, .F. ) ;
#35566=EDGE_CURVE ( 'NONE', #22574, #20918, #36916, .T. ) ;
#35569=CARTESIAN_POINT ( 'NONE',  ( 2.589278595512759740, -5.779442428606794913, 5.163950571302105885 ) ) ;
#35575=CARTESIAN_POINT ( 'NONE',  ( 2.305787727787084407, -2.461236246751023593, -7.249469779319933416 ) ) ;
#35576=ORIENTED_EDGE ( 'NONE', *, *, #54686, .F. ) ;
#35582=CARTESIAN_POINT ( 'NONE',  ( 0.2869720083484343376, -10.71444492121020708, 5.945302302873217926 ) ) ;
#35583=CARTESIAN_POINT ( 'NONE',  ( 0.9232058338315048962, -9.306586124266539528, -8.301689855530263173 ) ) ;
#35593=CARTESIAN_POINT ( 'NONE',  ( 2.305787727787084407, -3.682701754025465846, -6.711944854845862451 ) ) ;
#35603=CARTESIAN_POINT ( 'NONE',  ( 0.3474126878361798454, 12.27082419038178429, -0.2587235634078462465 ) ) ;
#35608=CARTESIAN_POINT ( 'NONE',  ( 2.247206125382827935, 0.1157489416152577000, -7.635476611656031309 ) ) ;
#35612=VERTEX_POINT ( 'NONE', #38283 ) ;
#35616=CARTESIAN_POINT ( 'NONE',  ( 2.242819959140783137, -1.224821922055089773, -7.536009875295528460 ) ) ;
#35620=CARTESIAN_POINT ( 'NONE',  ( 0.2648978790185584908, -12.24533305150758089, -0.1321385342563691223 ) ) ;
#35626=EDGE_CURVE ( 'NONE', #3473, #38228, #64693, .T. ) ;
#35642=CARTESIAN_POINT ( 'NONE',  ( 0.3223008802179250232, -12.26274332232494046, 0.2444878876722800243 ) ) ;
#35645=CARTESIAN_POINT ( 'NONE',  ( 2.665405856346777291, -3.808819464940497390, 8.776564688671616210 ) ) ;
#35649=ORIENTED_EDGE ( 'NONE', *, *, #19810, .F. ) ;
#35650=CARTESIAN_POINT ( 'NONE',  ( 0.3537226245948354997, -4.442821955543875490, 11.44347094181050473 ) ) ;
#35656=CARTESIAN_POINT ( 'NONE',  ( 1.719304012341537957, 12.20344780066137602, -3.626341562669237906 ) ) ;
#35662=DIRECTION ( 'NONE',  ( 0.000000000000000000, 0.000000000000000000, 1.000000000000000000 ) ) ;
#35664=CARTESIAN_POINT ( 'NONE',  ( 2.717984159218876261, 0.2836133496098577345, 7.788152353088898749 ) ) ;
#35666=CARTESIAN_POINT ( 'NONE',  ( 0.2651627923886305527, -7.803990550466243015, -9.437479615842727654 ) ) ;
#35677=CARTESIAN_POINT ( 'NONE',  ( 2.350038591458104342, -10.60256821300789909, -0.6402934222729869118 ) ) ;
#35682=CARTESIAN_POINT ( 'NONE',  ( 2.244591118396559004, 0.1074970442784154295, 7.634724215899725941 ) ) ;
#35685=VERTEX_POINT ( 'NONE', #54259 ) ;
#35687=CARTESIAN_POINT ( 'NONE',  ( 2.241352910868908310, 6.569501556381442953, 3.889181972941473386 ) ) ;
#35691=VERTEX_POINT ( 'NONE', #9023 ) ;
#35692=DIRECTION ( 'NONE',  ( -1.000000000000000000, -0.000000000000000000, -0.000000000000000000 ) ) ;
#35702=EDGE_CURVE ( 'NONE', #55428, #48647, #2068, .T. ) ;
#35705=CARTESIAN_POINT ( 'NONE',  ( 5.515539859299206427, 0.001886660928063890567, 0.005751553894234958178 ) ) ;
#35707=ORIENTED_EDGE ( 'NONE', *, *, #13428, .F. ) ;
#35716=( BOUNDED_SURFACE ( )  B_SPLINE_SURFACE ( 3, 1, ( 
 ( #58990, #12734 ),
 ( #6543, #63945 ),
 ( #13401, #11198 ),
 ( #63282, #41774 ) ),
 .UNSPECIFIED., .F., .F., .F. ) 
 B_SPLINE_SURFACE_WITH_KNOTS ( ( 4, 4 ),
 ( 2, 2 ),
 ( 0.000000000000000000, 1.000000000000000000 ),
 ( 0.000000000000000000, 1.000000000000000000 ),
 .UNSPECIFIED. ) 
 GEOMETRIC_REPRESENTATION_ITEM ( )  RATIONAL_B_SPLINE_SURFACE ( (
 ( 1.000000000000000000, 1.000000000000000000),
 ( 0.6933888150995267674, 0.9895912004443193632),
 ( 0.6933888150995267674, 0.9895912004443193632),
 ( 1.000000000000000000, 1.000000000000000000) ) ) 
 REPRESENTATION_ITEM ( '' )  SURFACE ( )  );
#35717=ORIENTED_EDGE ( 'NONE', *, *, #22772, .T. ) ;
#35724=CARTESIAN_POINT ( 'NONE',  ( 0.2648321136542701182, 0.1417061099916467892, -12.24520788540325711 ) ) ;
#35725=B_SPLINE_CURVE_WITH_KNOTS ( 'NONE', 3,
 ( #62183, #10319, #58184, #6669, #63472, #23254, #26939, #57870, #48544, #12602, #17944, #38206, #58520, #37891, #27578, #12949 ),
 .UNSPECIFIED., .F., .F.,
 ( 4, 3, 3, 3, 3, 4 ),
 ( 1.955623278354240332E-15, 0.0002126834539180125759, 0.0004253519300367125471, 0.0006380165497225470357, 0.0007442707582429773042, 0.0009453531351407216520 ),
 .UNSPECIFIED. ) ;
#35726=CARTESIAN_POINT ( 'NONE',  ( 0.4613984246114871679, -12.07219521825821751, 2.415907815801364489 ) ) ;
#35747=CARTESIAN_POINT ( 'NONE',  ( 2.844750968616169828, -7.242618984642912316, 2.990088422897453579 ) ) ;
#35750=CARTESIAN_POINT ( 'NONE',  ( 0.3665391374699472626, -12.04754782681758662, 2.392238720110420047 ) ) ;
#35751=CARTESIAN_POINT ( 'NONE',  ( 2.245754705088394587, 1.216173395688240566, 7.538396044169875410 ) ) ;
#35753=CARTESIAN_POINT ( 'NONE',  ( 0.7446945582511163009, -6.508900271375360091, 10.56139717223417840 ) ) ;
#35756=CARTESIAN_POINT ( 'NONE',  ( 2.373367633546869637, 1.154895193356632488, 7.591069096728999099 ) ) ;
#35760=CARTESIAN_POINT ( 'NONE',  ( 2.524535260912516677, -7.335347545455598528, -2.434550409953180949 ) ) ;
#35770=CARTESIAN_POINT ( 'NONE',  ( 0.3654063281920754136, 11.44627072062585071, -4.446369912832391691 ) ) ;
#35774=VERTEX_POINT ( 'NONE', #14634 ) ;
#35775=PRESENTATION_STYLE_ASSIGNMENT (( #45780 ) ) ;
#35777=CARTESIAN_POINT ( 'NONE',  ( 0.3106921474978435183, 11.43920276778357348, 4.414111574791866666 ) ) ;
#35784=EDGE_CURVE ( 'NONE', #44220, #59359, #19504, .T. ) ;
#35786=ORIENTED_EDGE ( 'NONE', *, *, #24455, .T. ) ;
#35787=DIRECTION ( 'NONE',  ( 0.000000000000000000, 0.000000000000000000, 1.000000000000000000 ) ) ;
#35791=CARTESIAN_POINT ( 'NONE',  ( 1.452237505248555660, 4.880303821311009926, 11.67686475128081369 ) ) ;
#35802=CARTESIAN_POINT ( 'NONE',  ( 5.516018279890452902, 0.005976902763919037485, -0.003191189039764858598 ) ) ;
#35805=CARTESIAN_POINT ( 'NONE',  ( 0.3675815128205912052, -11.44679196252412368, 4.447030445008141264 ) ) ;
#35806=CARTESIAN_POINT ( 'NONE',  ( 3.152665057734119536, 7.281573230474295499, 3.161213418913482620 ) ) ;
#35811=CARTESIAN_POINT ( 'NONE',  ( 5.514970785353741078, -0.003929719953530088142, 0.002619824551223746099 ) ) ;
#35812=CARTESIAN_POINT ( 'NONE',  ( 5.514624014163232779, -0.0008859786816842371007, 0.004045310349816136873 ) ) ;
#35813=CARTESIAN_POINT ( 'NONE',  ( 0.2653519991613830786, -12.06397323649777320, 2.104847849998821907 ) ) ;
#35814=CARTESIAN_POINT ( 'NONE',  ( 0.3665391374699467075, -5.911453292029529294, -10.76665847464319015 ) ) ;
#35828=CARTESIAN_POINT ( 'NONE',  ( 0.2801149460245144773, -0.1962575296604573138, -12.24954625471156255 ) ) ;
#35829=CARTESIAN_POINT ( 'NONE',  ( 2.241352910868908310, 7.202080440908741998, 2.532612177304466972 ) ) ;
#35838=CARTESIAN_POINT ( 'NONE',  ( 5.514624014163232779, -0.003278974416024624076, 0.002529391395135295768 ) ) ;
#35841=CARTESIAN_POINT ( 'NONE',  ( 2.941278708680199916, -3.842273877444530417, -4.788765081995669526 ) ) ;
#35842=CARTESIAN_POINT ( 'NONE',  ( 0.3665391374699467075, 10.50279796150436873, 6.368473106897165614 ) ) ;
#35853=CARTESIAN_POINT ( 'NONE',  ( 0.3675815128205894289, 10.50067073900651771, 6.367184624550202621 ) ) ;
#35866=EDGE_CURVE ( 'NONE', #49268, #46786, #16326, .T. ) ;
#35868=CARTESIAN_POINT ( 'NONE',  ( 0.7400311444011690165, -11.77295732453931976, -3.907401494355040139 ) ) ;
#35874=CARTESIAN_POINT ( 'NONE',  ( 1.634816307074477892, 11.67158647524040660, 5.013416918607531692 ) ) ;
#35876=CARTESIAN_POINT ( 'NONE',  ( 0.2646305136544072623, -4.312539723326208829, 11.46223899740598817 ) ) ;
#35877=CARTESIAN_POINT ( 'NONE',  ( 2.261269890822072526, 2.744033622443712961, -7.131324074141551783 ) ) ;
#35889=CARTESIAN_POINT ( 'NONE',  ( 0.2646305136544065406, -7.972778379581487940, -9.296005949277303060 ) ) ;
#35892=CARTESIAN_POINT ( 'NONE',  ( 2.770579946183332698, -7.804957730865690557, -0.3031629740256557293 ) ) ;
#35896=( BOUNDED_SURFACE ( )  B_SPLINE_SURFACE ( 3, 1, ( 
 ( #43672, #7790 ),
 ( #8771, #38702 ),
 ( #44019, #3811 ),
 ( #38357, #29056 ) ),
 .UNSPECIFIED., .F., .F., .F. ) 
 B_SPLINE_SURFACE_WITH_KNOTS ( ( 4, 4 ),
 ( 2, 2 ),
 ( 0.000000000000000000, 1.000000000000000000 ),
 ( 0.000000000000000000, 1.000000000000000000 ),
 .UNSPECIFIED. ) 
 GEOMETRIC_REPRESENTATION_ITEM ( )  RATIONAL_B_SPLINE_SURFACE ( (
 ( 1.000000000000000000, 1.000000000000000000),
 ( 0.9856612449720755231, 0.9999558406602322425),
 ( 0.9856612449720755231, 0.9999558406602322425),
 ( 1.000000000000000000, 1.000000000000000000) ) ) 
 REPRESENTATION_ITEM ( '' )  SURFACE ( )  );
#35901=CARTESIAN_POINT ( 'NONE',  ( 2.262775599885880062, -3.697834000591908143, -6.687241191563379594 ) ) ;
#35902=CARTESIAN_POINT ( 'NONE',  ( 2.241352910868908754, 7.503490710578232914, 1.407733736974891681 ) ) ;
#35907=CARTESIAN_POINT ( 'NONE',  ( 2.963017218115618245, 3.599595431209491991, 7.004145770368786827 ) ) ;
#35913=CARTESIAN_POINT ( 'NONE',  ( 2.903928887688530303, -0.9983813550131019898, 8.712847781148955306 ) ) ;
#35915=EDGE_CURVE ( 'NONE', #34835, #59884, #61755, .T. ) ;
#35922=CARTESIAN_POINT ( 'NONE',  ( 0.2638984909335720941, -9.508791614589142682, -7.718810690099158656 ) ) ;
#35925=CARTESIAN_POINT ( 'NONE',  ( 0.2739690278137235091, -1.946552041162990410, 12.09341522051409612 ) ) ;
#35927=EDGE_CURVE ( 'NONE', #8838, #5064, #1255, .T. ) ;
#35928=ORIENTED_EDGE ( 'NONE', *, *, #18085, .F. ) ;
#35930=ORIENTED_EDGE ( 'NONE', *, *, #20655, .F. ) ;
#35939=CARTESIAN_POINT ( 'NONE',  ( 5.515188684475870851, 0.005194992164431481291, 0.001283816547384742691 ) ) ;
#35952=B_SPLINE_CURVE_WITH_KNOTS ( 'NONE', 3,
 ( #29233, #64151, #39521, #50175, #34534, #49529, #18627 ),
 .UNSPECIFIED., .F., .F.,
 ( 4, 3, 4 ),
 ( 0.000000000000000000, 0.001700533616330558153, 0.005002426799371352019 ),
 .UNSPECIFIED. ) ;
#35959=CARTESIAN_POINT ( 'NONE',  ( 2.177405672432779049, 10.73538068360231534, 3.189307221896654720 ) ) ;
#35967=CARTESIAN_POINT ( 'NONE',  ( 0.2767916011545372701, 8.018602152763861568, 9.260929738915262277 ) ) ;
#35976=ORIENTED_EDGE ( 'NONE', *, *, #1218, .T. ) ;
#36014=CARTESIAN_POINT ( 'NONE',  ( 1.549075743846070496, -11.66216484053767921, -4.962709020480940758 ) ) ;
#36017=CARTESIAN_POINT ( 'NONE',  ( 0.9232167919969108683, -0.4134278310082157293, -12.45862789703290829 ) ) ;
#36019=CARTESIAN_POINT ( 'NONE',  ( 0.3665391374699464300, 3.952034409876296284, 11.62960183138728354 ) ) ;
#36022=CARTESIAN_POINT ( 'NONE',  ( 0.2648978790185602672, -4.063980959785125080, 11.55204314799262555 ) ) ;
#36023=CARTESIAN_POINT ( 'NONE',  ( 0.2638984909335720941, 8.023974293733179053, 9.252728947331103626 ) ) ;
#36026=B_SPLINE_CURVE_WITH_KNOTS ( 'NONE', 3,
 ( #23888, #9211, #4246, #64417, #3624, #44152, #28211, #8904, #18239, #18889, #63435, #17903, #53815, #23217, #48830, #43478, #33188, #43825, #13244, #14206, #44455, #34492 ),
 .UNSPECIFIED., .F., .F.,
 ( 4, 3, 3, 3, 3, 3, 3, 4 ),
 ( 8.940560153363745023E-19, 4.449119708436590826E-05, 6.626296329540418823E-05, 8.803456484962658983E-05, 0.0001098060367612806366, 0.0001315774408628531860, 0.0001760698110411187023, 0.0001829697163287827787 ),
 .UNSPECIFIED. ) ;
#36031=EDGE_LOOP ( 'NONE', ( #29899, #50852, #18955, #6648 ) ) ;
#36040=ORIENTED_EDGE ( 'NONE', *, *, #9151, .F. ) ;
#36041=EDGE_CURVE ( 'NONE', #28445, #30406, #60714, .T. ) ;
#36043=CARTESIAN_POINT ( 'NONE',  ( 0.3278977287071221380, 12.03512402322223274, 2.374069413450185184 ) ) ;
#36046=CARTESIAN_POINT ( 'NONE',  ( 5.520433897694421610, 0.01473594271720232718, 0.003119431460922271037 ) ) ;
#36055=VECTOR ( 'NONE', #44025, 1000.000000000000114 ) ;
#36068=CARTESIAN_POINT ( 'NONE',  ( 0.2653519789438754661, 10.61653328464227641, 6.104019611498609166 ) ) ;
#36069=FACE_OUTER_BOUND ( 'NONE', #45546, .T. ) ;
#36072=ADVANCED_FACE ( 'NONE', ( #24894 ), #4451, .T. ) ;
#36078=CARTESIAN_POINT ( 'NONE',  ( 2.258463476536646475, 1.192666169132632570, 7.546439757228810663 ) ) ;
#36084=B_SPLINE_CURVE_WITH_KNOTS ( 'NONE', 3,
 ( #3298, #7964, #28231, #23237, #18608, #38862, #59156, #13567, #60774, #50795, #9232, #8925, #65411, #3948, #15209, #29839, #59794, #49817, #24536 ),
 .UNSPECIFIED., .F., .F.,
 ( 4, 3, 3, 3, 3, 3, 4 ),
 ( 2.168404344971008868E-19, 2.831840207499545546E-05, 4.217266859840393823E-05, 5.602024318395990336E-05, 6.290810167969312265E-05, 9.120440630944972487E-05, 0.0001153103026479762659 ),
 .UNSPECIFIED. ) ;
#36092=LINE ( 'NONE', #56396, #28051 ) ;
#36095=CARTESIAN_POINT ( 'NONE',  ( 1.109979610372146652, -1.701361252868426988, -12.41172293674716443 ) ) ;
#36100=CARTESIAN_POINT ( 'NONE',  ( 2.259830038564999644, -5.015955067335966966, 5.763537486834654722 ) ) ;
#36104=EDGE_CURVE ( 'NONE', #11407, #33979, #2314, .T. ) ;
#36105=DIRECTION ( 'NONE',  ( 0.9486832985018464059, 0.000000000000000000, -0.3162277646628405270 ) ) ;
#36108=VERTEX_POINT ( 'NONE', #20874 ) ;
#36113=ORIENTED_EDGE ( 'NONE', *, *, #21769, .F. ) ;
#36118=CARTESIAN_POINT ( 'NONE',  ( 0.9232058338315058954, 4.617996777200573888, 11.58467545991555525 ) ) ;
#36126=CARTESIAN_POINT ( 'NONE',  ( 0.5572780756284647641, -11.70006938410064912, 3.933334466452514722 ) ) ;
#36142=B_SPLINE_CURVE_WITH_KNOTS ( 'NONE', 3,
 ( #39166, #48520, #59459, #28229, #53518, #43496, #63776 ),
 .UNSPECIFIED., .F., .F.,
 ( 4, 3, 4 ),
 ( 0.000000000000000000, 0.001700533616330569429, 0.005002426799371238395 ),
 .UNSPECIFIED. ) ;
#36143=EDGE_CURVE ( 'NONE', #35685, #3821, #42427, .T. ) ;
#36145=CARTESIAN_POINT ( 'NONE',  ( 5.515188684475870851, -0.003857086913166418371, 0.003709313826050277332 ) ) ;
#36147=CARTESIAN_POINT ( 'NONE',  ( 0.2638984909335716500, -4.001111175853667490, -11.57533005135182869 ) ) ;
#36148=EDGE_CURVE ( 'NONE', #62968, #44872, #15865, .T. ) ;
#36150=B_SPLINE_CURVE_WITH_KNOTS ( 'NONE', 3,
 ( #50990, #14723, #50354, #59991, #55313, #9753, #4801, #34686, #15068, #31026, #54982, #55658, #9410, #45337, #29700, #50008, #4467, #19757, #40013 ),
 .UNSPECIFIED., .F., .F.,
 ( 4, 3, 3, 3, 3, 3, 4 ),
 ( 0.000000000000000000, 2.831840207499875211E-05, 4.217266859840889846E-05, 5.602024318396385392E-05, 6.290810167969526395E-05, 9.120440630945454957E-05, 0.0001153103026479750733 ),
 .UNSPECIFIED. ) ;
#36154=CARTESIAN_POINT ( 'NONE',  ( 0.3675815128205894289, -12.13672785388551389, 1.872154644482044938 ) ) ;
#36158=CARTESIAN_POINT ( 'NONE',  ( 1.719304012339826659, -12.64775761152879596, -1.452142814149639305 ) ) ;
#36165=CARTESIAN_POINT ( 'NONE',  ( 1.719304012341273280, -2.961219984259375160, -12.38166659046469675 ) ) ;
#36167=ADVANCED_FACE ( 'NONE', ( #42123 ), #57104, .F. ) ;
#36174=EDGE_CURVE ( 'NONE', #34363, #14439, #48706, .T. ) ;
#36177=CARTESIAN_POINT ( 'NONE',  ( 2.177405672432031203, 6.173731551722755562, 9.343720763423021936 ) ) ;
#36186=CARTESIAN_POINT ( 'NONE',  ( 3.047904605210435935, -2.299870214474486030, -7.561255571389412289 ) ) ;
#36187=ORIENTED_EDGE ( 'NONE', *, *, #44968, .F. ) ;
#36206=EDGE_LOOP ( 'NONE', ( #54475, #42544, #18228, #4201 ) ) ;
#36207=ORIENTED_EDGE ( 'NONE', *, *, #15390, .F. ) ;
#36214=CARTESIAN_POINT ( 'NONE',  ( 2.305787727787084407, -1.164987321564681100, -7.566723232958083578 ) ) ;
#36215=CARTESIAN_POINT ( 'NONE',  ( 2.268878695253353950, 2.752970156154584291, -7.130600918714350200 ) ) ;
#36221=VERTEX_POINT ( 'NONE', #46473 ) ;
#36225=CARTESIAN_POINT ( 'NONE',  ( 0.2653519890538383330, 0.02202236966339091162, -12.24619734961521544 ) ) ;
#36229=CARTESIAN_POINT ( 'NONE',  ( 1.020182472824579412, -10.59341968305535175, -6.631405022220755008 ) ) ;
#36238=CARTESIAN_POINT ( 'NONE',  ( 2.705197763288545776, 6.142723737672452167, -4.789125516644054947 ) ) ;
#36241=EDGE_CURVE ( 'NONE', #49252, #23349, #17009, .T. ) ;
#36252=CARTESIAN_POINT ( 'NONE',  ( 0.2767916011545383248, 12.24854187541374628, -0.1897947303543257302 ) ) ;
#36255=CARTESIAN_POINT ( 'NONE',  ( 0.9296196016843304433, -5.870433615766820878, -10.99907063288908304 ) ) ;
#36257=CARTESIAN_POINT ( 'NONE',  ( 2.251139882113957214, 0.1241612276497709028, -7.636654603229075633 ) ) ;
#36261=EDGE_LOOP ( 'NONE', ( #50361, #41897, #17258, #25932 ) ) ;
#36270=CARTESIAN_POINT ( 'NONE',  ( 0.2834382757447995727, -1.927645269570966269, 12.09963924911735411 ) ) ;
#36271=ORIENTED_EDGE ( 'NONE', *, *, #51870, .F. ) ;
#36274=VERTEX_POINT ( 'NONE', #2593 ) ;
#36279=CIRCLE ( 'NONE', #20390, 12.73084802173761787 ) ;
#36285=EDGE_LOOP ( 'NONE', ( #45553, #21251, #26159, #61182 ) ) ;
#36286=CARTESIAN_POINT ( 'NONE',  ( 0.3218525148189835816, 12.11874253990393413, -1.888670068297527260 ) ) ;
#36292=CARTESIAN_POINT ( 'NONE',  ( 2.241352910868909643, -4.970878533273721978, -5.794346703933896059 ) ) ;
#36293=CARTESIAN_POINT ( 'NONE',  ( 2.257661810676418579, 3.936095962955294958, 6.547845034191107416 ) ) ;
#36302=CARTESIAN_POINT ( 'NONE',  ( 0.2652384770603670172, 4.126289928142402808, 11.53005438969045393 ) ) ;
#36311=EDGE_CURVE ( 'NONE', #59870, #56327, #61397, .T. ) ;
#36315=DIRECTION ( 'NONE',  ( 0.000000000000000000, -1.000000000000000000, 0.000000000000000000 ) ) ;
#36316=AXIS2_PLACEMENT_3D ( 'NONE', #6943, #26551, #27529 ) ;
#36320=ORIENTED_EDGE ( 'NONE', *, *, #53780, .T. ) ;
#36321=CARTESIAN_POINT ( 'NONE',  ( 5.536195898058073439, 0.004027525919832433861, 0.007485416011287818715 ) ) ;
#36328=EDGE_CURVE ( 'NONE', #18651, #58059, #47191, .T. ) ;
#36341=B_SPLINE_CURVE_WITH_KNOTS ( 'NONE', 3,
 ( #51367, #26082, #61630, #26727, #6784, #27058, #57660, #31693, #12076, #2109, #32356, #32664, #2457, #62604, #57317, #42644 ),
 .UNSPECIFIED., .F., .F.,
 ( 4, 3, 3, 3, 3, 4 ),
 ( 2.668793006540488735E-15, 0.0002126834539179618081, 0.0004253519300366075421, 0.0006380165497223889591, 0.0007442707582427920141, 0.0009453531351420071905 ),
 .UNSPECIFIED. ) ;
#36350=CARTESIAN_POINT ( 'NONE',  ( 1.198791140417307499, 10.60778679489402165, 6.720248575442116845 ) ) ;
#36357=ORIENTED_EDGE ( 'NONE', *, *, #11145, .F. ) ;
#36358=CARTESIAN_POINT ( 'NONE',  ( 3.152665057736013132, 7.281573230473836311, -3.161213418915250095 ) ) ;
#36365=CARTESIAN_POINT ( 'NONE',  ( 0.2646305136544065406, -7.770320294339235545, 9.465888453932937097 ) ) ;
#36374=CARTESIAN_POINT ( 'NONE',  ( 5.514970785353741078, -0.0005190732562558867313, -0.004694330894494369230 ) ) ;
#36376=CARTESIAN_POINT ( 'NONE',  ( 2.241352910868908310, -2.532612177304491397, 7.202080440908734005 ) ) ;
#36377=VERTEX_POINT ( 'NONE', #4198 ) ;
#36380=B_SPLINE_CURVE_WITH_KNOTS ( 'NONE', 3,
 ( #18366, #63546, #28321, #58256, #53613, #58605, #48307, #18019, #28642, #43270 ),
 .UNSPECIFIED., .F., .F.,
 ( 4, 3, 3, 4 ),
 ( 8.673617379884035472E-19, 6.607638129004487527E-05, 9.911389841680542587E-05, 0.0001667630577588620944 ),
 .UNSPECIFIED. ) ;
#36383=CARTESIAN_POINT ( 'NONE',  ( 2.241352910868908754, -4.843133558968088614, -5.901537464758503937 ) ) ;
#36392=ADVANCED_FACE ( 'NONE', ( #14476 ), #39213, .F. ) ;
#36402=CARTESIAN_POINT ( 'NONE',  ( 1.719304012338199517, 0.000000000000000000, 0.000000000000000000 ) ) ;
#36403=LINE ( 'NONE', #16767, #7185 ) ;
#36411=VECTOR ( 'NONE', #60540, 1000.000000000000114 ) ;
#36421=CARTESIAN_POINT ( 'NONE',  ( 2.177405672429650885, -4.457418613958688880, -10.27382588316896950 ) ) ;
#36427=CARTESIAN_POINT ( 'NONE',  ( 0.3665391374699467075, 12.04754782681757419, 2.392238720110499983 ) ) ;
#36431=CARTESIAN_POINT ( 'NONE',  ( 2.259830038565000532, 1.190932096469649260, 7.547174990768408698 ) ) ;
#36436=CARTESIAN_POINT ( 'NONE',  ( 0.3665391374699467075, 11.62960183138732617, -3.952034409876181709 ) ) ;
#36439=CARTESIAN_POINT ( 'NONE',  ( 2.573738926104373714, 1.112690714006538073, 7.664876274722913330 ) ) ;
#36453=CARTESIAN_POINT ( 'NONE',  ( 5.514970785353741078, -0.002093325033904051488, -0.004233694591582509194 ) ) ;
#36457=VECTOR ( 'NONE', #48238, 999.9999999999998863 ) ;
#36459=CARTESIAN_POINT ( 'NONE',  ( 1.283627346226609234, -11.62704807385636130, 4.817767733507167804 ) ) ;
#36469=ORIENTED_EDGE ( 'NONE', *, *, #2172, .T. ) ;
#36472=CARTESIAN_POINT ( 'NONE',  ( 3.031336079629336044, 7.694633165537301700, -1.779751109289334110 ) ) ;
#36474=CARTESIAN_POINT ( 'NONE',  ( 5.516018279890452902, 0.005042957932158584518, -0.004525000489649788973 ) ) ;
#36480=CARTESIAN_POINT ( 'NONE',  ( 2.249013661412230469, 7.499157010299435377, 1.444210756221575576 ) ) ;
#36482=CARTESIAN_POINT ( 'NONE',  ( 0.6511581176963838757, -11.73752429815123932, 3.919972364658685926 ) ) ;
#36483=CARTESIAN_POINT ( 'NONE',  ( 2.639814597422743159, 4.103563379978107051, -6.594772041715895483 ) ) ;
#36485=CARTESIAN_POINT ( 'NONE',  ( 2.241352910868910531, 5.901537464758454199, 4.843133558968147234 ) ) ;
#36489=CARTESIAN_POINT ( 'NONE',  ( 1.937114397841932290, 7.538912286488345771, 10.38782037574618933 ) ) ;
#36493=VERTEX_POINT ( 'NONE', #15787 ) ;
#36497=( BOUNDED_SURFACE ( )  B_SPLINE_SURFACE ( 3, 1, ( 
 ( #2156, #22433 ),
 ( #48393, #58349 ),
 ( #3160, #12771 ),
 ( #33059, #53365 ) ),
 .UNSPECIFIED., .F., .F., .F. ) 
 B_SPLINE_SURFACE_WITH_KNOTS ( ( 4, 4 ),
 ( 2, 2 ),
 ( 0.000000000000000000, 1.000000000000000000 ),
 ( 0.000000000000000000, 1.000000000000000000 ),
 .UNSPECIFIED. ) 
 GEOMETRIC_REPRESENTATION_ITEM ( )  RATIONAL_B_SPLINE_SURFACE ( (
 ( 1.000000000000000000, 1.000000000000000000),
 ( 0.6933888150995267674, 0.9895912004443193632),
 ( 0.6933888150995267674, 0.9895912004443193632),
 ( 1.000000000000000000, 1.000000000000000000) ) ) 
 REPRESENTATION_ITEM ( '' )  SURFACE ( )  );
#36502=CARTESIAN_POINT ( 'NONE',  ( 2.290907136833271185, 4.792500160339683291, 5.963935563308448096 ) ) ;
#36504=ORIENTED_EDGE ( 'NONE', *, *, #1205, .T. ) ;
#36506=CARTESIAN_POINT ( 'NONE',  ( 5.514970785353741078, -0.001326349372336609999, -0.004532877335078314314 ) ) ;
#36508=CARTESIAN_POINT ( 'NONE',  ( 1.719304012339844867, -12.64775761152577971, 1.452142814149586902 ) ) ;
#36509=CARTESIAN_POINT ( 'NONE',  ( 3.152665057733776699, 4.377619405892044568, -6.622010822086680015 ) ) ;
#36512=DIRECTION ( 'NONE',  ( 0.3939253465568944290, 0.1500280335741414617, 0.9068155327749447547 ) ) ;
#36513=CARTESIAN_POINT ( 'NONE',  ( 2.276905613633648962, 2.759436818562492011, 7.130967020394704647 ) ) ;
#36514=( BOUNDED_SURFACE ( )  B_SPLINE_SURFACE ( 3, 1, ( 
 ( #46613, #56606 ),
 ( #30990, #45971 ),
 ( #21689, #57594 ),
 ( #47292, #61908 ) ),
 .UNSPECIFIED., .F., .F., .F. ) 
 B_SPLINE_SURFACE_WITH_KNOTS ( ( 4, 4 ),
 ( 2, 2 ),
 ( 0.000000000000000000, 1.000000000000000000 ),
 ( 0.000000000000000000, 1.000000000000000000 ),
 .UNSPECIFIED. ) 
 GEOMETRIC_REPRESENTATION_ITEM ( )  RATIONAL_B_SPLINE_SURFACE ( (
 ( 1.000000000000000000, 1.000000000000000000),
 ( 0.9942764183789327692, 0.8450855930916580938),
 ( 0.9942764183789327692, 0.8450855930916580938),
 ( 1.000000000000000000, 1.000000000000000000) ) ) 
 REPRESENTATION_ITEM ( '' )  SURFACE ( )  );
#36539=CARTESIAN_POINT ( 'NONE',  ( 0.3675815128205912052, 12.13672785388552811, -1.872154644481959895 ) ) ;
#36542=CARTESIAN_POINT ( 'NONE',  ( 2.827825597296803828, 8.073505504738418992, -4.031992772938910008 ) ) ;
#36548=ADVANCED_FACE ( 'NONE', ( #51415, #5865 ), #62329, .F. ) ;
#36560=VERTEX_POINT ( 'NONE', #7452 ) ;
#36564=CARTESIAN_POINT ( 'NONE',  ( 2.373367633546871414, -1.154895193356581196, -7.591069096729007093 ) ) ;
#36565=CARTESIAN_POINT ( 'NONE',  ( 2.276198483117258586, 2.759333101207245953, -7.130755363255136814 ) ) ;
#36574=CARTESIAN_POINT ( 'NONE',  ( 0.2650492594609233921, 0.1101156276918464766, -12.24562116224018382 ) ) ;
#36576=CARTESIAN_POINT ( 'NONE',  ( 0.2648978790185593790, 1.996248716311628479, 12.08224454301449313 ) ) ;
#36581=ORIENTED_EDGE ( 'NONE', *, *, #57506, .F. ) ;
#36584=CARTESIAN_POINT ( 'NONE',  ( 3.152665057736177445, 3.161213418915486795, 7.281573230473766145 ) ) ;
#36589=VERTEX_POINT ( 'NONE', #32707 ) ;
#36593=CARTESIAN_POINT ( 'NONE',  ( 0.2706063244538028378, 2.299194104693242036, -12.03021891034989110 ) ) ;
#36601=CARTESIAN_POINT ( 'NONE',  ( 3.152665057734108878, -7.886634106564198277, 0.9030954876737806725 ) ) ;
#36602=CARTESIAN_POINT ( 'NONE',  ( 2.242819959140646358, 0.1024002568250429734, -7.634209046698936518 ) ) ;
#36604=VERTEX_POINT ( 'NONE', #2508 ) ;
#36606=CARTESIAN_POINT ( 'NONE',  ( 2.524535260912772472, -6.580044328001124043, 4.054303386867624148 ) ) ;
#36608=CARTESIAN_POINT ( 'NONE',  ( 0.8320506296491662068, -7.696193170530679417, 9.767350172724400537 ) ) ;
#36616=ADVANCED_FACE ( 'NONE', ( #27742 ), #4475, .F. ) ;
#36647=ORIENTED_EDGE ( 'NONE', *, *, #32545, .T. ) ;
#36653=DIRECTION ( 'NONE',  ( 0.000000000000000000, 0.000000000000000000, 1.000000000000000000 ) ) ;
#36655=CARTESIAN_POINT ( 'NONE',  ( 1.937114397841935398, -7.538912286488415049, 10.38782037574614137 ) ) ;
#36658=CARTESIAN_POINT ( 'NONE',  ( 2.963017218115608031, -6.272673870919120986, 4.761166637500490850 ) ) ;
#36661=CARTESIAN_POINT ( 'NONE',  ( 5.520433897694421610, 0.01491416502703810966, -0.002108682515300329928 ) ) ;
#36663=CARTESIAN_POINT ( 'NONE',  ( 0.3610902822527234379, -4.444884365376528201, -11.44530431865297793 ) ) ;
#36670=CARTESIAN_POINT ( 'NONE',  ( 2.256373768223412846, -5.765785888499252998, 5.011614056001910456 ) ) ;
#36675=CARTESIAN_POINT ( 'NONE',  ( 0.2869720083484376127, -12.25163264065381341, -0.2084396331387939061 ) ) ;
#36687=ORIENTED_EDGE ( 'NONE', *, *, #62506, .F. ) ;
#36706=CARTESIAN_POINT ( 'NONE',  ( 3.152665057734095555, 3.546019893116337141, 7.102135024645864547 ) ) ;
#36708=CARTESIAN_POINT ( 'NONE',  ( 2.241352910868908310, 4.970878533273761946, 5.794346703933863196 ) ) ;
#36710=CARTESIAN_POINT ( 'NONE',  ( 2.259830038564998311, -7.639319632525574555, -0.1377140217659982568 ) ) ;
#36715=CARTESIAN_POINT ( 'NONE',  ( 5.516018279890452902, -0.004525000489649737799, -0.005042957932158631355 ) ) ;
#36741=CARTESIAN_POINT ( 'NONE',  ( 0.2956976708475473892, 4.397965666276587804, -11.44006538352181757 ) ) ;
#36748=CARTESIAN_POINT ( 'NONE',  ( 0.3401186441510232750, -1.878666403202251534, -12.12646044229291853 ) ) ;
#36758=CARTESIAN_POINT ( 'NONE',  ( 2.284126774967666140, 1.171808575345623327, 7.558363379199187548 ) ) ;
#36760=CARTESIAN_POINT ( 'NONE',  ( 2.491965175174354119, 6.787433375639490230, 3.673871285745579307 ) ) ;
#36766=DIRECTION ( 'NONE',  ( 1.000000000000000000, -0.000000000000000000, -0.000000000000000000 ) ) ;
#36767=B_SPLINE_CURVE_WITH_KNOTS ( 'NONE', 3,
 ( #34337, #40632, #23609, #43533, #53866, #58533, #59185, #53551, #8304, #48245, #8960, #7652, #28577, #27935, #63815, #32893 ),
 .UNSPECIFIED., .F., .F.,
 ( 4, 3, 3, 3, 3, 4 ),
 ( 5.963111948670274387E-19, 0.0003017745587525257891, 0.0006035491769808736320, 0.0009053241094668170071, 0.001207275924540513433, 0.001510325902534028712 ),
 .UNSPECIFIED. ) ;
#36778=CARTESIAN_POINT ( 'NONE',  ( 0.2717059086739053719, 11.44824199474648552, -4.354191483751156611 ) ) ;
#36782=CARTESIAN_POINT ( 'NONE',  ( 2.241532322987418890, -0.01048837931141704399, 7.634455956583345859 ) ) ;
#36787=CARTESIAN_POINT ( 'NONE',  ( 2.990245332647718079, 0.9653152459624684267, 8.426135047918773324 ) ) ;
#36788=B_SPLINE_CURVE_WITH_KNOTS ( 'NONE', 3,
 ( #33643, #38961, #13673, #29309, #49296, #59571, #9329, #28647, #14003, #19342, #49604, #29614, #24003, #4044, #50263, #48953 ),
 .UNSPECIFIED., .F., .F.,
 ( 4, 3, 3, 3, 3, 4 ),
 ( 0.000000000000000000, 0.0002999043160757735530, 0.0005998071753051757021, 0.0008997092107375666671, 0.001204458948195450806, 0.001510329163476011082 ),
 .UNSPECIFIED. ) ;
#36790=VERTEX_POINT ( 'NONE', #46003 ) ;
#36791=CARTESIAN_POINT ( 'NONE',  ( 5.516018279890452902, 0.005976902763919037485, -0.003191189039764858598 ) ) ;
#36799=CARTESIAN_POINT ( 'NONE',  ( 0.3665391374699472626, -3.952034409876374443, 11.62960183138725689 ) ) ;
#36804=CARTESIAN_POINT ( 'NONE',  ( 1.719304012338834786, 2.961219984257995819, 12.38166659046419227 ) ) ;
#36811=CARTESIAN_POINT ( 'NONE',  ( 3.047904605210438156, 4.313929735713965208, -6.622084192655445456 ) ) ;
#36813=CARTESIAN_POINT ( 'NONE',  ( 3.152665057734040488, 0.000000000000000000, 0.000000000000000000 ) ) ;
#36825=CARTESIAN_POINT ( 'NONE',  ( 2.255723233588966536, 4.808373255828867876, 5.936060085173582301 ) ) ;
#36826=CARTESIAN_POINT ( 'NONE',  ( 2.261269890822072082, 1.464004156081748942, -7.499479675451353522 ) ) ;
#36833=CARTESIAN_POINT ( 'NONE',  ( 0.3002738374340819805, 6.323236184341269883, -10.50101454678637936 ) ) ;
#36834=EDGE_CURVE ( 'NONE', #2995, #41256, #1311, .T. ) ;
#36846=FACE_OUTER_BOUND ( 'NONE', #45495, .T. ) ;
#36853=CARTESIAN_POINT ( 'NONE',  ( 2.589278595511360415, 7.746633201026548399, -0.2408616556815215415 ) ) ;
#36855=CARTESIAN_POINT ( 'NONE',  ( 0.6511581176980835162, 12.23990098761684919, -1.822219471613748087 ) ) ;
#36859=CARTESIAN_POINT ( 'NONE',  ( 1.283627346226608346, -5.810034161408860420, 11.16434663959570273 ) ) ;
#36871=DIRECTION ( 'NONE',  ( 0.3939253465568944290, 0.6978179301705716986, 0.5982248387291266845 ) ) ;
#36880=CARTESIAN_POINT ( 'NONE',  ( 0.2915757698887274096, 4.392559307431903370, 11.44067056871811161 ) ) ;
#36895=CARTESIAN_POINT ( 'NONE',  ( 0.3040950598368152291, 11.60568999039894678, 3.956873563689569551 ) ) ;
#36898=CARTESIAN_POINT ( 'NONE',  ( 0.2655924914740778742, 12.05257978623656889, -2.169924872617939648 ) ) ;
#36901=CARTESIAN_POINT ( 'NONE',  ( 0.3610902822527233269, 10.76187877352513134, 5.910495176556216812 ) ) ;
#36913=EDGE_CURVE ( 'NONE', #18433, #57362, #58949, .T. ) ;
#36915=CARTESIAN_POINT ( 'NONE',  ( 2.241352910868909643, -6.569501556381469598, 3.889181972941426313 ) ) ;
#36916=B_SPLINE_CURVE_WITH_KNOTS ( 'NONE', 3,
 ( #17025, #5857, #10470, #30746, #2415, #17701, #46078 ),
 .UNSPECIFIED., .F., .F.,
 ( 4, 3, 4 ),
 ( 0.000000000000000000, 0.001700533616330544709, 0.005002426799371397989 ),
 .UNSPECIFIED. ) ;
#36919=B_SPLINE_CURVE_WITH_KNOTS ( 'NONE', 3,
 ( #57916, #33282, #53587, #18673, #48923, #23307, #12333 ),
 .UNSPECIFIED., .F., .F.,
 ( 4, 3, 4 ),
 ( 0.000000000000000000, 0.001700533616330576585, 0.005002426799371340743 ),
 .UNSPECIFIED. ) ;
#36926=B_SPLINE_CURVE_WITH_KNOTS ( 'NONE', 3,
 ( #34814, #14537, #9546, #4607, #40139, #14858, #25190, #55456, #9896, #45463, #65730, #40476, #36482, #36126, #21180, #21528 ),
 .UNSPECIFIED., .F., .F.,
 ( 4, 3, 3, 3, 3, 4 ),
 ( 0.000000000000000000, 0.0002999043160757356601, 0.0005998071753051037111, 0.0008997092107374638848, 0.001204458948195666346, 0.001510329163476545160 ),
 .UNSPECIFIED. ) ;
#36935=VECTOR ( 'NONE', #26715, 1000.000000000000114 ) ;
#36938=B_SPLINE_CURVE_WITH_KNOTS ( 'NONE', 3,
 ( #46104, #12141, #51745, #51088, #25809, #62665, #11802 ),
 .UNSPECIFIED., .F., .F.,
 ( 4, 3, 4 ),
 ( 8.157409164538106469E-15, 0.002398160485435165898, 0.005002426799384885464 ),
 .UNSPECIFIED. ) ;
#36944=CARTESIAN_POINT ( 'NONE',  ( 0.5547464869798228726, 7.697709668896196789, -9.648168635481763289 ) ) ;
#36948=CARTESIAN_POINT ( 'NONE',  ( 5.514970785353741078, -0.004694330894494374434, 0.0005190732562558384843 ) ) ;
#36949=DIRECTION ( 'NONE',  ( -1.000000000000000000, -0.000000000000000000, -0.000000000000000000 ) ) ;
#36959=CARTESIAN_POINT ( 'NONE',  ( 2.844750968616162723, 7.470159816919374585, 2.364925124213946628 ) ) ;
#36960=CARTESIAN_POINT ( 'NONE',  ( 1.549075743846873632, 12.12370443967657252, -3.694639393663405436 ) ) ;
#36973=CARTESIAN_POINT ( 'NONE',  ( 0.3006302518452046990, -4.404090606399806873, -11.43947177966006556 ) ) ;
#36975=EDGE_CURVE ( 'NONE', #21980, #47209, #54328, .T. ) ;
#36981=CARTESIAN_POINT ( 'NONE',  ( 0.2657645697724700939, -5.991637049003168514, -10.68050050043097166 ) ) ;
#36985=CARTESIAN_POINT ( 'NONE',  ( 2.288423627607475197, -5.755330594805005084, 5.039850887180246986 ) ) ;
#36991=CARTESIAN_POINT ( 'NONE',  ( 0.2759803524722223567, -12.24828167798667167, -0.1894460813477297501 ) ) ;
#36994=ADVANCED_FACE ( 'NONE', ( #38293 ), #59631, .F. ) ;
#36996=VERTEX_POINT ( 'NONE', #8712 ) ;
#36997=CARTESIAN_POINT ( 'NONE',  ( 2.245754705088791159, 6.556487589644730996, 3.913944702467391679 ) ) ;
#37007=CARTESIAN_POINT ( 'NONE',  ( 1.375507693219669481, -11.64019206974686327, -4.865932489132057448 ) ) ;
#37009=CARTESIAN_POINT ( 'NONE',  ( 1.194176325881337819, -0.5141316333310350650, -12.54527478469375623 ) ) ;
#37024=CARTESIAN_POINT ( 'NONE',  ( 1.462291587748804300, -4.914320681885039122, 11.65117843858572755 ) ) ;
#37026=CARTESIAN_POINT ( 'NONE',  ( 1.719304012338398469, 8.755325027793414705, 9.242227816402090568 ) ) ;
#37028=CARTESIAN_POINT ( 'NONE',  ( 5.515539859299206427, 0.001886660928063779545, -0.005751553894235449972 ) ) ;
#37029=ORIENTED_EDGE ( 'NONE', *, *, #12002, .F. ) ;
#37033=CARTESIAN_POINT ( 'NONE',  ( 2.573738926104372826, 7.583190312075771544, 1.575954828885281822 ) ) ;
#37036=VERTEX_POINT ( 'NONE', #36158 ) ;
#37037=B_SPLINE_CURVE_WITH_KNOTS ( 'NONE', 3,
 ( #1594, #21867, #42112, #1903, #38111, #8512, #33473, #63379, #28800, #59085, #64046, #37799, #58093 ),
 .UNSPECIFIED., .F., .F.,
 ( 4, 3, 3, 3, 4 ),
 ( 3.878959614448864246E-18, 6.607593386745498512E-05, 0.0001321518677373520001, 0.0001982171734706217813, 0.0002642860854759490966 ),
 .UNSPECIFIED. ) ;
#37041=CARTESIAN_POINT ( 'NONE',  ( 1.937114397841935398, 7.182898292393766759, 10.63710405811936255 ) ) ;
#37042=CARTESIAN_POINT ( 'NONE',  ( 1.719304012339833099, -9.242227816401946683, 8.755325027794301107 ) ) ;
#37049=CARTESIAN_POINT ( 'NONE',  ( 0.3053067050349195233, 4.409108891833811938, -11.43920902168902032 ) ) ;
#37059=CARTESIAN_POINT ( 'NONE',  ( 2.889800649504073782, 5.728825117897707209, 2.156828754871487064 ) ) ;
#37060=CARTESIAN_POINT ( 'NONE',  ( 0.2706063244538067791, -1.954041462022338971, -12.09107863371558444 ) ) ;
#37063=B_SPLINE_CURVE_WITH_KNOTS ( 'NONE', 3,
 ( #35806, #55798, #61107, #10227, #15539, #46157, #7124 ),
 .UNSPECIFIED., .F., .F.,
 ( 4, 3, 4 ),
 ( 0.000000000000000000, 0.001700533616330553600, 0.005002426799371221047 ),
 .UNSPECIFIED. ) ;
#37065=ADVANCED_FACE ( 'NONE', ( #35176 ), #63881, .F. ) ;
#37068=CIRCLE ( 'NONE', #17963, 7.938172270156617749 ) ;
#37070=EDGE_LOOP ( 'NONE', ( #61804, #60357, #50040, #30348 ) ) ;
#37074=CARTESIAN_POINT ( 'NONE',  ( 2.253265082352138737, -4.810902415501418616, -5.932955906470167129 ) ) ;
#37077=CARTESIAN_POINT ( 'NONE',  ( 0.2671309869109485535, 2.286013846430026142, 12.03155065772886090 ) ) ;
#37079=EDGE_CURVE ( 'NONE', #5369, #13777, #57500, .T. ) ;
#37096=ORIENTED_EDGE ( 'NONE', *, *, #49370, .F. ) ;
#37097=CARTESIAN_POINT ( 'NONE',  ( 2.241352910868909643, -0.08337961031709527349, 7.633946224498472155 ) ) ;
#37098=VERTEX_POINT ( 'NONE', #51815 ) ;
#37099=PRODUCT_CONTEXT ( 'NONE', #65029, 'mechanical' ) ;
#37101=DIRECTION ( 'NONE',  ( -0.3939253465568944290, 0.5833358547425184781, -0.7103112711423392733 ) ) ;
#37105=CARTESIAN_POINT ( 'NONE',  ( 5.516018279890452902, -0.006286471671801945743, 0.002527316374434286465 ) ) ;
#37110=CARTESIAN_POINT ( 'NONE',  ( 2.969415267404512448, 7.680649281077198687, -1.748187016698217411 ) ) ;
#37121=AXIS2_PLACEMENT_3D ( 'NONE', #24090, #59031, #19440 ) ;
#37129=CARTESIAN_POINT ( 'NONE',  ( 0.2647959493198558945, -10.67808515296906791, -5.995292100780899247 ) ) ;
#37132=CARTESIAN_POINT ( 'NONE',  ( 0.3665391374699472626, 4.447929964102847578, 11.44911061034387956 ) ) ;
#37134=ORIENTED_EDGE ( 'NONE', *, *, #33383, .T. ) ;
#37137=ORIENTED_EDGE ( 'NONE', *, *, #6162, .T. ) ;
#37139=CARTESIAN_POINT ( 'NONE',  ( 0.2655924914740778742, -0.04405032194294832004, -12.24627751708824341 ) ) ;
#37141=CARTESIAN_POINT ( 'NONE',  ( 2.241311220309555985, 1.417008678104584307, -7.501736494813729728 ) ) ;
#37142=EDGE_CURVE ( 'NONE', #26538, #15657, #52481, .T. ) ;
#37144=CARTESIAN_POINT ( 'NONE',  ( 0.2671309869109474988, 12.08782215308012020, 1.966882337881730392 ) ) ;
#37162=ORIENTED_EDGE ( 'NONE', *, *, #8355, .F. ) ;
#37163=CARTESIAN_POINT ( 'NONE',  ( 0.2956976708475454463, 1.911282699793726669, 12.10637007622313988 ) ) ;
#37169=CARTESIAN_POINT ( 'NONE',  ( 2.177405672430401395, 10.89176600225243341, -2.605669267167184167 ) ) ;
#37173=CARTESIAN_POINT ( 'NONE',  ( 0.2646305136544065406, 0.1321451301297855152, 12.24595685781654453 ) ) ;
#37179=CARTESIAN_POINT ( 'NONE',  ( 1.719304012341585475, 10.62216384465587993, -7.017415949613843296 ) ) ;
#37185=CARTESIAN_POINT ( 'NONE',  ( 2.430348790457391051, 2.814990071338047350, 7.164221884688230624 ) ) ;
#37192=B_SPLINE_CURVE_WITH_KNOTS ( 'NONE', 3,
 ( #51638, #62551, #6083, #7044, #5764, #61579, #42946, #37637, #12669, #13343, #3735, #49279, #17693 ),
 .UNSPECIFIED., .F., .F.,
 ( 4, 3, 3, 3, 4 ),
 ( 2.453269466693398698E-18, 6.607593386745292514E-05, 0.0001321518677373508346, 0.0001982171734706214832, 0.0002642860854759498013 ),
 .UNSPECIFIED. ) ;
#37196=EDGE_CURVE ( 'NONE', #63452, #2298, #9897, .T. ) ;
#37197=CARTESIAN_POINT ( 'NONE',  ( 1.719304012341585253, 9.242227816401774376, -8.755325027795295867 ) ) ;
#37201=CONICAL_SURFACE ( 'NONE', #55241, 7.938172270156617749, 1.280189991382167047 ) ;
#37209=CARTESIAN_POINT ( 'NONE',  ( 0.3164563675027631806, -8.065346584422186993, -9.237806174449842089 ) ) ;
#37218=CARTESIAN_POINT ( 'NONE',  ( 2.290907136833250757, 5.963935563308487176, -4.792500160339624671 ) ) ;
#37221=CARTESIAN_POINT ( 'NONE',  ( 2.259830038564997867, -6.684701880279348529, 3.700395974956117051 ) ) ;
#37223=ORIENTED_EDGE ( 'NONE', *, *, #15390, .T. ) ;
#37229=EDGE_CURVE ( 'NONE', #25053, #36560, #54246, .T. ) ;
#37230=B_SPLINE_CURVE_WITH_KNOTS ( 'NONE', 3,
 ( #36376, #30402, #51692, #61001, #46361, #41349, #55999, #6134, #5823, #65320 ),
 .UNSPECIFIED., .F., .F.,
 ( 4, 3, 3, 4 ),
 ( 8.673617379884035472E-19, 6.607638129004461778E-05, 9.911389841680439588E-05, 0.0001667630577588628533 ),
 .UNSPECIFIED. ) ;
#37234=PRODUCT_DEFINITION_CONTEXT ( 'detailed design', #64631, 'design' ) ;
#37235=CARTESIAN_POINT ( 'NONE',  ( 5.514624014163232779, -0.003278974416025000511, -0.002529391395134995228 ) ) ;
#37237=CARTESIAN_POINT ( 'NONE',  ( 1.020182472823639053, -5.858468047365780862, -11.03967505355413081 ) ) ;
#37246=CARTESIAN_POINT ( 'NONE',  ( 0.2650492433740052056, 2.234874822562896490, 12.04046084639674241 ) ) ;
#37249=CARTESIAN_POINT ( 'NONE',  ( 0.3675815128205894289, -7.689697408877338880, 9.574637318041938627 ) ) ;
#37255=CARTESIAN_POINT ( 'NONE',  ( 2.373367633546871414, 7.676289145832773109, 0.1808255748565736620 ) ) ;
#37256=CONICAL_SURFACE ( 'NONE', #61699, 7.938172270156617749, 1.280189991382167047 ) ;
#37265=( BOUNDED_SURFACE ( )  B_SPLINE_SURFACE ( 3, 1, ( 
 ( #64844, #18008 ),
 ( #53602, #28968 ),
 ( #33628, #38269 ),
 ( #28311, #48604 ) ),
 .UNSPECIFIED., .F., .F., .F. ) 
 B_SPLINE_SURFACE_WITH_KNOTS ( ( 4, 4 ),
 ( 2, 2 ),
 ( 0.000000000000000000, 1.000000000000000000 ),
 ( 0.000000000000000000, 1.000000000000000000 ),
 .UNSPECIFIED. ) 
 GEOMETRIC_REPRESENTATION_ITEM ( )  RATIONAL_B_SPLINE_SURFACE ( (
 ( 1.000000000000000000, 1.000000000000000000),
 ( 0.9942764183789327692, 0.8450855930916580938),
 ( 0.9942764183789327692, 0.8450855930916580938),
 ( 1.000000000000000000, 1.000000000000000000) ) ) 
 REPRESENTATION_ITEM ( '' )  SURFACE ( )  );
#37271=CARTESIAN_POINT ( 'NONE',  ( 0.3106921474978520115, 12.11369598333779507, -1.896868624982938289 ) ) ;
#37278=CARTESIAN_POINT ( 'NONE',  ( 2.241449424704146320, -6.580749518451827207, 3.870245369721799555 ) ) ;
#37280=CARTESIAN_POINT ( 'NONE',  ( 1.375507693220547223, 6.813306181536364470, -10.61839108744984550 ) ) ;
#37282=ORIENTED_EDGE ( 'NONE', *, *, #32803, .T. ) ;
#37285=EDGE_CURVE ( 'NONE', #39958, #23378, #303, .T. ) ;
#37287=( BOUNDED_SURFACE ( )  B_SPLINE_SURFACE ( 3, 1, ( 
 ( #26453, #36436 ),
 ( #31447, #6192 ),
 ( #21478, #17795 ),
 ( #59034, #48401 ) ),
 .UNSPECIFIED., .F., .F., .F. ) 
 B_SPLINE_SURFACE_WITH_KNOTS ( ( 4, 4 ),
 ( 2, 2 ),
 ( 0.000000000000000000, 1.000000000000000000 ),
 ( 0.000000000000000000, 1.000000000000000000 ),
 .UNSPECIFIED. ) 
 GEOMETRIC_REPRESENTATION_ITEM ( )  RATIONAL_B_SPLINE_SURFACE ( (
 ( 1.000000000000000000, 1.000000000000000000),
 ( 0.6933888150995267674, 0.9895912004443193632),
 ( 0.6933888150995267674, 0.9895912004443193632),
 ( 1.000000000000000000, 1.000000000000000000) ) ) 
 REPRESENTATION_ITEM ( '' )  SURFACE ( )  );
#37293=CARTESIAN_POINT ( 'NONE',  ( 0.2834382757448009604, 6.300836243950157289, 10.50792790568170432 ) ) ;
#37301=ORIENTED_EDGE ( 'NONE', *, *, #31804, .T. ) ;
#37302=CARTESIAN_POINT ( 'NONE',  ( 2.990245332647882393, 3.377079998295721808, -7.779904630197268744 ) ) ;
#37308=ORIENTED_EDGE ( 'NONE', *, *, #22672, .F. ) ;
#37313=CARTESIAN_POINT ( 'NONE',  ( 3.152665057735546839, 0.4801242025606423658, 7.923639299008859105 ) ) ;
#37314=B_SPLINE_CURVE_WITH_KNOTS ( 'NONE', 3,
 ( #50849, #45860, #20246, #24925, #56145, #55168, #40527 ),
 .UNSPECIFIED., .F., .F.,
 ( 4, 3, 4 ),
 ( 0.000000000000000000, 0.001700533616330518905, 0.005002426799371241864 ),
 .UNSPECIFIED. ) ;
#37322=VERTEX_POINT ( 'NONE', #65676 ) ;
#37326=ORIENTED_EDGE ( 'NONE', *, *, #6886, .T. ) ;
#37330=VECTOR ( 'NONE', #47497, 1000.000000000000114 ) ;
#37334=ORIENTED_EDGE ( 'NONE', *, *, #49696, .F. ) ;
#37342=CARTESIAN_POINT ( 'NONE',  ( 5.515539859299206427, 0.006049968793488397570, 0.0001942659352248016788 ) ) ;
#37346=CARTESIAN_POINT ( 'NONE',  ( 0.2671309869109471657, -7.747281147400610912, 9.484919892054794133 ) ) ;
#37351=ORIENTED_EDGE ( 'NONE', *, *, #57993, .F. ) ;
#37352=CARTESIAN_POINT ( 'NONE',  ( 0.2650492433740071485, 9.309907554970086707, -7.955688793815992810 ) ) ;
#37357=CARTESIAN_POINT ( 'NONE',  ( 0.6511581176957849104, -4.541862140119324209, 11.51117493088887045 ) ) ;
#37360=CARTESIAN_POINT ( 'NONE',  ( 0.6473888112830245012, 8.203438694127655140, 9.263269341114806821 ) ) ;
#37365=ADVANCED_FACE ( 'NONE', ( #10168 ), #4865, .F. ) ;
#37373=CARTESIAN_POINT ( 'NONE',  ( 0.4613984246114880561, -10.51786362586218893, 6.399144685811677391 ) ) ;
#37376=CARTESIAN_POINT ( 'NONE',  ( 5.530133899448235191, 0.006510401266731621894, -0.01459891979722821240 ) ) ;
#37397=CARTESIAN_POINT ( 'NONE',  ( 2.717984159220127260, -1.631703089060319911, -7.620583877640776826 ) ) ;
#37403=ORIENTED_EDGE ( 'NONE', *, *, #26485, .F. ) ;
#37406=CARTESIAN_POINT ( 'NONE',  ( 0.2676618633000477643, 9.277614237849274303, 7.994628339664862082 ) ) ;
#37408=CARTESIAN_POINT ( 'NONE',  ( 1.719304012339826659, -12.64775761152879596, -1.452142814149639305 ) ) ;
#37412=CARTESIAN_POINT ( 'NONE',  ( 0.2653519890518162283, -12.24619734961135187, 8.824939080896778643E-06 ) ) ;
#37418=CARTESIAN_POINT ( 'NONE',  ( 0.3002738374340819250, -9.533456882268691146, 7.705051734330245594 ) ) ;
#37420=CARTESIAN_POINT ( 'NONE',  ( 0.3040950598368152291, -5.912066680610686298, 10.74226959800789594 ) ) ;
#37421=CARTESIAN_POINT ( 'NONE',  ( 2.241509619876139059, 7.525055189891922680, -1.287997509666494400 ) ) ;
#37423=FACE_OUTER_BOUND ( 'NONE', #3805, .T. ) ;
#37424=CARTESIAN_POINT ( 'NONE',  ( 0.8320506296491609888, 11.81055997318803996, 3.891425424503343944 ) ) ;
#37426=ORIENTED_EDGE ( 'NONE', *, *, #36241, .F. ) ;
#37435=CARTESIAN_POINT ( 'NONE',  ( 1.719304012338199295, 12.70777170743846796, -0.7661785589580241140 ) ) ;
#37441=ORIENTED_EDGE ( 'NONE', *, *, #51371, .F. ) ;
#37442=CARTESIAN_POINT ( 'NONE',  ( 0.3665391374699472626, 1.872534962004960724, -12.13918562134716694 ) ) ;
#37444=CARTESIAN_POINT ( 'NONE',  ( 1.194176325881339595, -3.807610977967000654, 11.96454551582841219 ) ) ;
#37467=CARTESIAN_POINT ( 'NONE',  ( 2.430348790457107278, -2.814990071337903910, -7.164221884688188879 ) ) ;
#37474=VERTEX_POINT ( 'NONE', #8796 ) ;
#37475=CARTESIAN_POINT ( 'NONE',  ( 0.3474126878361824544, 7.689340002166858312, -9.566300984424323417 ) ) ;
#37478=CARTESIAN_POINT ( 'NONE',  ( 0.8320506296491597675, -9.767350172724373891, -7.696193170530718497 ) ) ;
#37479=CARTESIAN_POINT ( 'NONE',  ( 2.242819959140644581, 1.426511055719408283, -7.500446639314762187 ) ) ;
#37482=CARTESIAN_POINT ( 'NONE',  ( 0.2872850955227749803, 12.10187515377843326, 1.921748909352199775 ) ) ;
#37483=CARTESIAN_POINT ( 'NONE',  ( 2.241352910868908310, -0.08337961031698915004, -7.633946224498474820 ) ) ;
#37489=CARTESIAN_POINT ( 'NONE',  ( 2.305787727787084407, -0.1666591538752151269, -7.654065630109508689 ) ) ;
#37497=CARTESIAN_POINT ( 'NONE',  ( 5.514624014163232779, -0.004045310349816146414, 0.0008859786816847309548 ) ) ;
#37504=ORIENTED_EDGE ( 'NONE', *, *, #39789, .F. ) ;
#37505=VERTEX_POINT ( 'NONE', #44346 ) ;
#37506=CARTESIAN_POINT ( 'NONE',  ( 0.3160775863651129614, 1.892533050396167260, 12.11619190710938732 ) ) ;
#37512=CARTESIAN_POINT ( 'NONE',  ( 1.719304012340734378, -7.581471372739226666, -10.22720798541506682 ) ) ;
#37514=CARTESIAN_POINT ( 'NONE',  ( 2.256373768223411069, -1.195444820369733430, 7.545294827890043798 ) ) ;
#37515=CARTESIAN_POINT ( 'NONE',  ( 5.514970785353741078, -0.004532877335078721974, -0.001326349372336278450 ) ) ;
#37517=ORIENTED_EDGE ( 'NONE', *, *, #3391, .T. ) ;
#37529=CARTESIAN_POINT ( 'NONE',  ( 2.639814597422740050, -1.600543348184864545, 7.600559958731741617 ) ) ;
#37531=ORIENTED_EDGE ( 'NONE', *, *, #41500, .T. ) ;
#37535=ORIENTED_EDGE ( 'NONE', *, *, #13468, .F. ) ;
#37537=CARTESIAN_POINT ( 'NONE',  ( 2.297017764050091948, 3.968300849026757948, 6.543724852214691801 ) ) ;
#37539=EDGE_LOOP ( 'NONE', ( #12508, #27351, #43357, #29273 ) ) ;
#37553=CARTESIAN_POINT ( 'NONE',  ( 2.373367633546855426, 4.795703124519890892, 5.996611082971977424 ) ) ;
#37556=CARTESIAN_POINT ( 'NONE',  ( 0.2956976708475454463, -2.344604179391494458, 12.02996380804952814 ) ) ;
#37567=ORIENTED_EDGE ( 'NONE', *, *, #21930, .T. ) ;
#37568=CARTESIAN_POINT ( 'NONE',  ( 2.655192694324000069, 3.822392723567352490, 8.807900729499975157 ) ) ;
#37574=CARTESIAN_POINT ( 'NONE',  ( 2.290907136833251645, -6.705538900522852508, 3.684064771923238002 ) ) ;
#37576=CARTESIAN_POINT ( 'NONE',  ( 0.5547464869798224285, 10.53334899235179734, -6.433541106624982575 ) ) ;
#37583=CARTESIAN_POINT ( 'NONE',  ( 5.516018279890452902, 0.005331956019561467572, 0.004180585980734550546 ) ) ;
#37588=ORIENTED_EDGE ( 'NONE', *, *, #42555, .T. ) ;
#37590=CARTESIAN_POINT ( 'NONE',  ( 2.269879328256733775, -6.544400685875852552, 3.949706986712179013 ) ) ;
#37591=CARTESIAN_POINT ( 'NONE',  ( 2.781367136452546962, -6.608147481822088665, 4.171010984503177532 ) ) ;
#37595=CARTESIAN_POINT ( 'NONE',  ( 0.9232058338315058954, -9.791640253608095534, -7.723624854284817154 ) ) ;
#37604=ORIENTED_EDGE ( 'NONE', *, *, #54266, .F. ) ;
#37606=CARTESIAN_POINT ( 'NONE',  ( 1.719304012339844867, -11.38834240361479644, 5.690355757826019989 ) ) ;
#37611=CARTESIAN_POINT ( 'NONE',  ( 2.255723233589907117, 7.132203433012072935, 2.736592204238131210 ) ) ;
#37620=CARTESIAN_POINT ( 'NONE',  ( 2.350038591456828474, -3.024612895786653599, -10.18214835920313455 ) ) ;
#37622=AXIS2_PLACEMENT_3D ( 'NONE', #34275, #19324, #39917 ) ;
#37631=CARTESIAN_POINT ( 'NONE',  ( 5.536195898058073439, 0.007230647766619090894, 0.004468797463753810574 ) ) ;
#37636=CARTESIAN_POINT ( 'NONE',  ( 0.3109076770648994126, 6.333869442011780926, 10.49874397806408410 ) ) ;
#37637=CARTESIAN_POINT ( 'NONE',  ( 0.2653519789438769649, -9.395292406847872257, -7.854827495960904571 ) ) ;
#37650=CARTESIAN_POINT ( 'NONE',  ( 0.3665391374699464300, 12.04754782681757241, 2.392238720110500427 ) ) ;
#37662=CARTESIAN_POINT ( 'NONE',  ( 2.247206125382828379, -0.1157489416152055195, 7.635476611656038415 ) ) ;
#37663=CARTESIAN_POINT ( 'NONE',  ( 0.3401186441510248848, -12.26845925752607158, -0.2556125181571129446 ) ) ;
#37665=( BOUNDED_SURFACE ( )  B_SPLINE_SURFACE ( 3, 1, ( 
 ( #54867, #9289 ),
 ( #44227, #29575 ),
 ( #49882, #4333 ),
 ( #25251, #35558 ) ),
 .UNSPECIFIED., .F., .F., .F. ) 
 B_SPLINE_SURFACE_WITH_KNOTS ( ( 4, 4 ),
 ( 2, 2 ),
 ( 0.000000000000000000, 1.000000000000000000 ),
 ( 0.000000000000000000, 1.000000000000000000 ),
 .UNSPECIFIED. ) 
 GEOMETRIC_REPRESENTATION_ITEM ( )  RATIONAL_B_SPLINE_SURFACE ( (
 ( 1.000000000000000000, 1.000000000000000000),
 ( 0.9856612449720755231, 0.9999558406602322425),
 ( 0.9856612449720755231, 0.9999558406602322425),
 ( 1.000000000000000000, 1.000000000000000000) ) ) 
 REPRESENTATION_ITEM ( '' )  SURFACE ( )  );
#37666=ORIENTED_EDGE ( 'NONE', *, *, #63620, .F. ) ;
#37671=UNCERTAINTY_MEASURE_WITH_UNIT (LENGTH_MEASURE( 1.000000000000000082E-05 ), #18881, 'distance_accuracy_value', 'NONE');
#37672=CARTESIAN_POINT ( 'NONE',  ( 2.305787727787084407, 6.545285700970527643, 3.971363876083986888 ) ) ;
#37675=CARTESIAN_POINT ( 'NONE',  ( 0.2647959493198558945, -5.995292100780861944, 10.67808515296908922 ) ) ;
#37678=CARTESIAN_POINT ( 'NONE',  ( 0.2956976708475479443, -12.02996380804952459, -2.344604179391541088 ) ) ;
#37681=DIRECTION ( 'NONE',  ( 0.3939253465568944290, 0.9190910618577644575, 0.009718094113442748289 ) ) ;
#37692=EDGE_CURVE ( 'NONE', #59870, #8677, #24744, .T. ) ;
#37695=CARTESIAN_POINT ( 'NONE',  ( 0.2655924914740778742, 6.161287456391684181, 10.58356227062111543 ) ) ;
#37696=ORIENTED_EDGE ( 'NONE', *, *, #38318, .F. ) ;
#37701=CARTESIAN_POINT ( 'NONE',  ( 2.241352910868908310, -7.633946224498473043, -0.08337961031712197435 ) ) ;
#37702=ORIENTED_EDGE ( 'NONE', *, *, #7609, .F. ) ;
#37707=ORIENTED_EDGE ( 'NONE', *, *, #39255, .F. ) ;
#37725=CARTESIAN_POINT ( 'NONE',  ( 2.288423627607481414, -4.792733268640415822, 5.962686897379188444 ) ) ;
#37732=CARTESIAN_POINT ( 'NONE',  ( 0.3675815128205894289, -1.872154644482002528, -12.13672785388552100 ) ) ;
#37752=ADVANCED_FACE ( 'NONE', ( #46012 ), #20959, .F. ) ;
#37753=CARTESIAN_POINT ( 'NONE',  ( 0.2767916011545379917, -4.367596755337373793, -11.44495079483528777 ) ) ;
#37755=CARTESIAN_POINT ( 'NONE',  ( 0.3160775863651076878, -9.546663463486092738, 7.697077652699416461 ) ) ;
#37757=CARTESIAN_POINT ( 'NONE',  ( 2.241449424704145876, 7.507583637787367259, -1.386092121067129757 ) ) ;
#37760=CARTESIAN_POINT ( 'NONE',  ( 0.2648321136542699517, 5.999882851577475584, 10.67551415837652051 ) ) ;
#37763=CARTESIAN_POINT ( 'NONE',  ( 1.549075743846799025, 4.962709020481401723, -11.66216484053774138 ) ) ;
#37770=CARTESIAN_POINT ( 'NONE',  ( 1.547277799338547588, -11.66196709685588573, 4.961646058323668562 ) ) ;
#37776=VECTOR ( 'NONE', #51810, 999.9999999999998863 ) ;
#37779=CARTESIAN_POINT ( 'NONE',  ( 0.2657645697724709821, 11.55867655367626945, -4.045961170622892844 ) ) ;
#37780=ORIENTED_EDGE ( 'NONE', *, *, #40752, .T. ) ;
#37782=CARTESIAN_POINT ( 'NONE',  ( 1.937114397841932290, -5.226660192101668656, 11.72279974487461907 ) ) ;
#37784=CARTESIAN_POINT ( 'NONE',  ( 2.241506898688417238, 1.286963596520092956, -7.525229609709728429 ) ) ;
#37785=CARTESIAN_POINT ( 'NONE',  ( 5.514970785353741078, 0.003805873180274313254, -0.002796696073589883310 ) ) ;
#37788=CARTESIAN_POINT ( 'NONE',  ( 0.8320506296491576581, 12.30686996250300247, 1.781423711749617889 ) ) ;
#37795=CARTESIAN_POINT ( 'NONE',  ( 0.2653141334712566524, -6.084912053827412848, 10.62748186152495578 ) ) ;
#37799=CARTESIAN_POINT ( 'NONE',  ( 0.2650492433740059828, -11.54478237753289172, -4.084772052580713186 ) ) ;
#37810=CARTESIAN_POINT ( 'NONE',  ( 2.931247277082670966, 2.338794445044995118, 7.508560300462408854 ) ) ;
#37812=CARTESIAN_POINT ( 'NONE',  ( 0.2653141617321010948, -10.58343467791291737, -6.161204121352803931 ) ) ;
#37816=CARTESIAN_POINT ( 'NONE',  ( 0.3106921474978460718, 6.333448016104198608, -10.49891314301079071 ) ) ;
#37824=FACE_OUTER_BOUND ( 'NONE', #52574, .T. ) ;
#37826=EDGE_CURVE ( 'NONE', #4245, #32821, #51180, .T. ) ;
#37828=CARTESIAN_POINT ( 'NONE',  ( 1.020182472822681374, -8.370187102469690998, 9.280950437305071077 ) ) ;
#37835=DIRECTION ( 'NONE',  ( -1.000000000000000000, -0.000000000000000000, -0.000000000000000000 ) ) ;
#37838=DIRECTION ( 'NONE',  ( 0.000000000000000000, 0.000000000000000000, 1.000000000000000000 ) ) ;
#37841=CARTESIAN_POINT ( 'NONE',  ( 3.031336079627524605, 7.886784934834240701, -0.4165536638483573473 ) ) ;
#37842=EDGE_CURVE ( 'NONE', #4753, #807, #52646, .T. ) ;
#37843=CARTESIAN_POINT ( 'NONE',  ( 2.242418902651940549, -1.227462051872194815, 7.535443599794969138 ) ) ;
#37847=CARTESIAN_POINT ( 'NONE',  ( 1.633930747251779225, -5.718685543473577049, 11.34237452761324505 ) ) ;
#37850=CARTESIAN_POINT ( 'NONE',  ( 0.7446945582532709107, 8.243982823409844229, -9.270687147117392612 ) ) ;
#37857=VERTEX_POINT ( 'NONE', #12371 ) ;
#37859=DIRECTION ( 'NONE',  ( 0.000000000000000000, 0.000000000000000000, 1.000000000000000000 ) ) ;
#37873=ORIENTED_EDGE ( 'NONE', *, *, #59615, .F. ) ;
#37880=CARTESIAN_POINT ( 'NONE',  ( 2.305787727787084407, -3.971363876083918498, -6.545285700970570275 ) ) ;
#37881=CARTESIAN_POINT ( 'NONE',  ( 0.3006302518452078631, -11.59403866275563821, -3.979421585299229402 ) ) ;
#37885=DIRECTION ( 'NONE',  ( -1.000000000000000000, -0.000000000000000000, -0.000000000000000000 ) ) ;
#37887=CARTESIAN_POINT ( 'NONE',  ( 0.3223008802179254118, 10.74209118105756744, 5.919638939520617704 ) ) ;
#37890=CARTESIAN_POINT ( 'NONE',  ( 1.719304012341583476, 7.581471372739232883, -10.22720798541541498 ) ) ;
#37891=CARTESIAN_POINT ( 'NONE',  ( 2.430348790456736019, 7.611893186157221436, 1.144258029164500368 ) ) ;
#37902=CARTESIAN_POINT ( 'NONE',  ( 2.260457164927185847, -3.939659644572505393, -6.546788723198600835 ) ) ;
#37908=CARTESIAN_POINT ( 'NONE',  ( 2.244591118396559448, -6.558116599718194273, 3.910457279126699159 ) ) ;
#37915=EDGE_CURVE ( 'NONE', #22476, #50940, #12959, .T. ) ;
#37918=CARTESIAN_POINT ( 'NONE',  ( 2.284126774967663032, 7.240052432235682289, -2.466502196988892059 ) ) ;
#37920=CARTESIAN_POINT ( 'NONE',  ( 5.514970785353741078, 0.003262412238248228995, -0.003415090918276198536 ) ) ;
#37922=CARTESIAN_POINT ( 'NONE',  ( 1.719304012338199517, 0.000000000000000000, 0.000000000000000000 ) ) ;
#37927=CARTESIAN_POINT ( 'NONE',  ( 2.288423627607478750, -2.767471693622750362, -7.131972212895032470 ) ) ;
#37932=CARTESIAN_POINT ( 'NONE',  ( 2.259830038564998311, 2.483392345594764183, 7.225713255971552229 ) ) ;
#37936=CARTESIAN_POINT ( 'NONE',  ( 2.241352910868908754, 3.744764251556992996, 6.652881166698525028 ) ) ;
#37948=ORIENTED_EDGE ( 'NONE', *, *, #14814, .T. ) ;
#37950=CARTESIAN_POINT ( 'NONE',  ( 0.2872850955227766456, 12.02931961709053255, -2.333231805482862242 ) ) ;
#37951=CARTESIAN_POINT ( 'NONE',  ( 2.781367136451758260, -7.636197200465718815, 1.659348694504308552 ) ) ;
#37952=CIRCLE ( 'NONE', #14525, 12.73084802173761787 ) ;
#37957=CARTESIAN_POINT ( 'NONE',  ( 2.653899356900423001, -6.857477569908684956, -3.657605971842797565 ) ) ;
#37971=CARTESIAN_POINT ( 'NONE',  ( 0.8320506296491548826, 4.610676791972340816, 11.54877388447406616 ) ) ;
#37972=CARTESIAN_POINT ( 'NONE',  ( 2.705197763288554214, 5.217779042888522234, -5.783040721897881653 ) ) ;
#37975=CARTESIAN_POINT ( 'NONE',  ( 2.276198483117258586, -0.1540629821338843908, 7.644465698238557039 ) ) ;
#37982=CARTESIAN_POINT ( 'NONE',  ( 2.259830038566064125, 6.546987858512988367, 3.938923657570771564 ) ) ;
#37983=ORIENTED_EDGE ( 'NONE', *, *, #30256, .T. ) ;
#37990=CARTESIAN_POINT ( 'NONE',  ( 0.2911222467163573913, -12.02952766044174027, -2.338869407810991063 ) ) ;
#37995=CARTESIAN_POINT ( 'NONE',  ( 2.440552418640495436, -2.818488640081624474, 7.166505277347720693 ) ) ;
#38000=CARTESIAN_POINT ( 'NONE',  ( 1.452237505248552996, -6.833827325205392711, 10.65201107290465288 ) ) ;
#38006=ORIENTED_EDGE ( 'NONE', *, *, #55697, .T. ) ;
#38010=CARTESIAN_POINT ( 'NONE',  ( 0.3474126878361877835, -3.953748424960721319, 11.61929161290145451 ) ) ;
#38011=CARTESIAN_POINT ( 'NONE',  ( 0.2653141617321038703, -11.52265685897332048, 4.147035654172678498 ) ) ;
#38021=CARTESIAN_POINT ( 'NONE',  ( 0.3006302518452010353, -10.50091819089219847, 6.323626002161042869 ) ) ;
#38022=FACE_OUTER_BOUND ( 'NONE', #34952, .T. ) ;
#38025=EDGE_CURVE ( 'NONE', #31754, #57595, #22508, .T. ) ;
#38026=CARTESIAN_POINT ( 'NONE',  ( 0.4613984246114875565, -10.80075367333618352, -5.909164750631147989 ) ) ;
#38034=DIRECTION ( 'NONE',  ( -1.000000000000000000, -0.000000000000000000, -0.000000000000000000 ) ) ;
#38038=CARTESIAN_POINT ( 'NONE',  ( 1.452237505248555660, 12.34692280296795985, -2.778494755358929424 ) ) ;
#38040=EDGE_CURVE ( 'NONE', #39632, #23832, #55484, .T. ) ;
#38041=EDGE_LOOP ( 'NONE', ( #25418, #16148, #49109, #59787 ) ) ;
#38042=CARTESIAN_POINT ( 'NONE',  ( 0.2651627923886305527, 2.213220384814432951, -12.04449855907066436 ) ) ;
#38043=CARTESIAN_POINT ( 'NONE',  ( 0.3218525148189829710, -1.888670068297569449, -12.11874253990391637 ) ) ;
#38052=CARTESIAN_POINT ( 'NONE',  ( 5.530133899448235191, 0.01550764871776275436, -0.003876417824003384680 ) ) ;
#38064=ORIENTED_EDGE ( 'NONE', *, *, #35915, .T. ) ;
#38067=CARTESIAN_POINT ( 'NONE',  ( 0.2638984909335716500, -9.508791614589247487, 7.718810690099029870 ) ) ;
#38071=CARTESIAN_POINT ( 'NONE',  ( 2.257661810676419911, -7.546014018371154819, -1.193649218120667044 ) ) ;
#38082=VERTEX_POINT ( 'NONE', #48532 ) ;
#38095=VERTEX_POINT ( 'NONE', #22934 ) ;
#38097=CARTESIAN_POINT ( 'NONE',  ( 0.2869720083484389450, 0.2084396331388363444, -12.25163264065380453 ) ) ;
#38098=CARTESIAN_POINT ( 'NONE',  ( 0.3040950598368152291, 12.25911170648142701, -0.2511348647276077650 ) ) ;
#38103=CARTESIAN_POINT ( 'NONE',  ( 2.245754705088396364, 3.913944702466356063, -6.556487589645189296 ) ) ;
#38104=EDGE_CURVE ( 'NONE', #23316, #22231, #9765, .T. ) ;
#38110=CARTESIAN_POINT ( 'NONE',  ( 2.251139882113958990, -3.925854078924265966, 6.551456272498888289 ) ) ;
#38111=CARTESIAN_POINT ( 'NONE',  ( 0.2653141617321018164, -11.49253039221379957, -4.229807441322429362 ) ) ;
#38119=CARTESIAN_POINT ( 'NONE',  ( 2.276905613633648962, 1.479235344773160987, 7.501802783089481785 ) ) ;
#38123=CARTESIAN_POINT ( 'NONE',  ( 0.2653141334712582067, -6.161213243425185837, -10.58342934917118328 ) ) ;
#38129=CARTESIAN_POINT ( 'NONE',  ( 2.907497136250526637, -3.613027414876720300, 6.976431712756427928 ) ) ;
#38130=DIRECTION ( 'NONE',  ( -1.000000000000000000, -0.000000000000000000, -0.000000000000000000 ) ) ;
#38134=B_SPLINE_CURVE_WITH_KNOTS ( 'NONE', 3,
 ( #12548, #22558, #37841, #26546, #1301, #58132, #21581, #41844, #16587, #36853, #11580, #31850, #16901, #52164, #6616, #26884 ),
 .UNSPECIFIED., .F., .F.,
 ( 4, 3, 3, 3, 3, 4 ),
 ( 3.325020220743593725E-17, 0.0002126834539179991046, 0.0004253519300366846289, 0.0006380165497225060529, 0.0007442707582429298162, 0.0009453531351393624962 ),
 .UNSPECIFIED. ) ;
#38140=CARTESIAN_POINT ( 'NONE',  ( 5.520433897694421610, 0.005630909886752951364, 0.01397038704729916363 ) ) ;
#38141=CARTESIAN_POINT ( 'NONE',  ( 0.2872850955227749803, -11.44140577127595648, 4.386654201695106003 ) ) ;
#38144=ORIENTED_EDGE ( 'NONE', *, *, #5585, .F. ) ;
#38145=FACE_OUTER_BOUND ( 'NONE', #27145, .T. ) ;
#38153=CARTESIAN_POINT ( 'NONE',  ( 0.2638984909335720941, 0.1991813963113996944, 12.24571285024409129 ) ) ;
#38156=CARTESIAN_POINT ( 'NONE',  ( 0.2655924914740778742, -10.58356227062113675, 6.161287456391646877 ) ) ;
#38166=CARTESIAN_POINT ( 'NONE',  ( 3.047904605210427942, 1.788881754552641867, -7.698174516567096504 ) ) ;
#38175=EDGE_LOOP ( 'NONE', ( #41958, #5149, #22035, #26898 ) ) ;
#38179=CARTESIAN_POINT ( 'NONE',  ( 0.2676618633000460434, 7.994628339664956229, -9.277614237849192591 ) ) ;
#38180=CARTESIAN_POINT ( 'NONE',  ( 5.520433897694421610, 0.01397038704729859290, 0.005630909886752917537 ) ) ;
#38194=CARTESIAN_POINT ( 'NONE',  ( 2.655192694323949443, -9.584054627287619255, 0.5793947661801162052 ) ) ;
#38199=CARTESIAN_POINT ( 'NONE',  ( 2.305787727787083519, -7.135468203929965725, -2.774453000917220802 ) ) ;
#38202=CARTESIAN_POINT ( 'NONE',  ( 3.152665057733995191, 6.622010822086684456, 4.377619405892240856 ) ) ;
#38205=CARTESIAN_POINT ( 'NONE',  ( 3.152665057734040488, 0.000000000000000000, 0.000000000000000000 ) ) ;
#38206=CARTESIAN_POINT ( 'NONE',  ( 2.524535260911636936, 7.646662375930073807, 1.123794384999134754 ) ) ;
#38212=EDGE_CURVE ( 'NONE', #53630, #31059, #60125, .T. ) ;
#38216=FACE_OUTER_BOUND ( 'NONE', #41503, .T. ) ;
#38223=CARTESIAN_POINT ( 'NONE',  ( 2.257661810676204972, 5.013319178750904825, 5.764872664104674804 ) ) ;
#38228=VERTEX_POINT ( 'NONE', #39510 ) ;
#38234=DIRECTION ( 'NONE',  ( 0.000000000000000000, 0.000000000000000000, 1.000000000000000000 ) ) ;
#38237=EDGE_LOOP ( 'NONE', ( #52872, #31186, #24091, #53304 ) ) ;
#38242=( BOUNDED_SURFACE ( )  B_SPLINE_SURFACE ( 3, 1, ( 
 ( #17516, #36799 ),
 ( #47765, #48109 ),
 ( #62708, #11207 ),
 ( #37785, #57096 ) ),
 .UNSPECIFIED., .F., .F., .F. ) 
 B_SPLINE_SURFACE_WITH_KNOTS ( ( 4, 4 ),
 ( 2, 2 ),
 ( 0.000000000000000000, 1.000000000000000000 ),
 ( 0.000000000000000000, 1.000000000000000000 ),
 .UNSPECIFIED. ) 
 GEOMETRIC_REPRESENTATION_ITEM ( )  RATIONAL_B_SPLINE_SURFACE ( (
 ( 1.000000000000000000, 1.000000000000000000),
 ( 0.9942764183789327692, 0.8450855930916585379),
 ( 0.9942764183789327692, 0.8450855930916585379),
 ( 1.000000000000000000, 1.000000000000000000) ) ) 
 REPRESENTATION_ITEM ( '' )  SURFACE ( )  );
#38243=CARTESIAN_POINT ( 'NONE',  ( 2.244591118396556784, -2.712243649838657067, -7.137527852925281913 ) ) ;
#38251=CARTESIAN_POINT ( 'NONE',  ( 2.284126774967666584, 3.686252397487125965, 6.701756155761956713 ) ) ;
#38262=CARTESIAN_POINT ( 'NONE',  ( 2.241311220309554653, -7.141707286456110637, -2.698144003944865865 ) ) ;
#38266=CARTESIAN_POINT ( 'NONE',  ( 1.452237505248555660, -12.34692280296793676, 2.778494755359015134 ) ) ;
#38269=CARTESIAN_POINT ( 'NONE',  ( 0.3040950598368144520, -5.912066680610537972, -10.74226959800797587 ) ) ;
#38272=CARTESIAN_POINT ( 'NONE',  ( 0.2717059086739019858, -2.300075171420154163, -12.03041489115254414 ) ) ;
#38282=CARTESIAN_POINT ( 'NONE',  ( 0.2655924914740778742, -9.409507842005970346, -7.838010948425144342 ) ) ;
#38283=CARTESIAN_POINT ( 'NONE',  ( 2.241352910868908310, 4.970878533273838329, -5.794346703933798359 ) ) ;
#38292=EDGE_CURVE ( 'NONE', #37098, #8838, #60402, .T. ) ;
#38293=FACE_OUTER_BOUND ( 'NONE', #20530, .T. ) ;
#38295=CARTESIAN_POINT ( 'NONE',  ( 0.2651627923886329397, 7.803990550466305187, 9.437479615842670810 ) ) ;
#38318=EDGE_CURVE ( 'NONE', #46103, #62889, #111, .T. ) ;
#38330=CARTESIAN_POINT ( 'NONE',  ( 0.2646305136544065406, 6.008537389229564596, -10.67138229758223211 ) ) ;
#38337=CARTESIAN_POINT ( 'NONE',  ( 0.3341166715381294616, 3.958014133396767775, -11.61315925169690821 ) ) ;
#38339=CARTESIAN_POINT ( 'NONE',  ( 0.2958664285830416851, -3.984029505266645454, 11.59077733151254996 ) ) ;
#38357=CARTESIAN_POINT ( 'NONE',  ( 5.514970785353741078, 0.004532877335078711566, 0.001326349372336311627 ) ) ;
#38372=DIRECTION ( 'NONE',  ( 0.000000000000000000, 0.000000000000000000, 1.000000000000000000 ) ) ;
#38375=CARTESIAN_POINT ( 'NONE',  ( 2.241451721903214178, -2.553895636571891004, -7.194631024842671252 ) ) ;
#38381=CARTESIAN_POINT ( 'NONE',  ( 1.719304012339869514, -10.22720798541492471, 7.581471372739622794 ) ) ;
#38390=CARTESIAN_POINT ( 'NONE',  ( 0.2657645697724705380, 9.283243433323075777, 7.987126944299666853 ) ) ;
#38417=ORIENTED_EDGE ( 'NONE', *, *, #21341, .T. ) ;
#38418=EDGE_CURVE ( 'NONE', #38861, #28445, #33451, .T. ) ;
#38430=CARTESIAN_POINT ( 'NONE',  ( 2.288423627607479194, 5.755330594805035282, -5.039850887180206129 ) ) ;
#38437=CARTESIAN_POINT ( 'NONE',  ( 2.406456491625949656, -8.704497555693093247, 5.751891873091646623 ) ) ;
#38438=CARTESIAN_POINT ( 'NONE',  ( 3.152665057734040488, 0.000000000000000000, 0.000000000000000000 ) ) ;
#38439=EDGE_CURVE ( 'NONE', #27786, #44289, #3508, .T. ) ;
#38446=( BOUNDED_SURFACE ( )  B_SPLINE_SURFACE ( 3, 1, ( 
 ( #2136, #5848 ),
 ( #47379, #21099 ),
 ( #17098, #12106 ),
 ( #26108, #11448 ) ),
 .UNSPECIFIED., .F., .F., .F. ) 
 B_SPLINE_SURFACE_WITH_KNOTS ( ( 4, 4 ),
 ( 2, 2 ),
 ( 0.000000000000000000, 1.000000000000000000 ),
 ( 0.000000000000000000, 1.000000000000000000 ),
 .UNSPECIFIED. ) 
 GEOMETRIC_REPRESENTATION_ITEM ( )  RATIONAL_B_SPLINE_SURFACE ( (
 ( 1.000000000000000000, 1.000000000000000000),
 ( 0.9942764183789327692, 0.8450855930916585379),
 ( 0.9942764183789327692, 0.8450855930916585379),
 ( 1.000000000000000000, 1.000000000000000000) ) ) 
 REPRESENTATION_ITEM ( '' )  SURFACE ( )  );
#38449=CARTESIAN_POINT ( 'NONE',  ( 0.6511581176957895734, 3.919972364658811603, 11.73752429815098886 ) ) ;
#38450=CARTESIAN_POINT ( 'NONE',  ( 2.969415267404872161, 4.760005747566406598, -6.276215141898866534 ) ) ;
#38458=CARTESIAN_POINT ( 'NONE',  ( 0.3654063281920739148, 7.689576266239796176, -9.573804659448589049 ) ) ;
#38459=CARTESIAN_POINT ( 'NONE',  ( 5.515188684475870851, -0.002355816063606842176, 0.004804816249379301012 ) ) ;
#38463=CARTESIAN_POINT ( 'NONE',  ( 3.152665057736163678, 7.923639299009212600, -0.4801242025614006481 ) ) ;
#38465=CARTESIAN_POINT ( 'NONE',  ( 0.2653519991613825790, -6.104031847944945355, -10.61652626436034730 ) ) ;
#38467=CARTESIAN_POINT ( 'NONE',  ( 2.524535260912932344, -1.123794384998863416, 7.646662375930550759 ) ) ;
#38469=CARTESIAN_POINT ( 'NONE',  ( 2.251152103363648127, -0.1252683866804617796, -7.636644423939539905 ) ) ;
#38474=CARTESIAN_POINT ( 'NONE',  ( 5.514624014163232779, -0.001574979445069392804, -0.003830004412313170285 ) ) ;
#38482=CARTESIAN_POINT ( 'NONE',  ( 0.3109076770649024657, -11.43910935267335383, 4.414555973477779283 ) ) ;
#38485=ORIENTED_EDGE ( 'NONE', *, *, #38722, .F. ) ;
#38495=CARTESIAN_POINT ( 'NONE',  ( 2.247112776671466250, -1.211104213045427258, 7.539676020705981863 ) ) ;
#38500=CARTESIAN_POINT ( 'NONE',  ( 2.941278708680199916, 2.952340773940184349, -5.383216837018909295 ) ) ;
#38510=VERTEX_POINT ( 'NONE', #41664 ) ;
#38523=B_SPLINE_CURVE_WITH_KNOTS ( 'NONE', 3,
 ( #13696, #33981, #44288, #59274, #54633, #24029, #3440, #59599, #43976, #63577, #64559, #39296, #53643, #3101, #8081, #28670, #14027, #54295, #7751 ),
 .UNSPECIFIED., .F., .F.,
 ( 4, 3, 3, 3, 3, 3, 4 ),
 ( 1.029150036413375294E-17, 4.457896483014832405E-05, 6.639290541541954295E-05, 8.820687556478702977E-05, 0.0001100173248778896191, 0.0001545671401658089039, 0.0001830328308068576552 ),
 .UNSPECIFIED. ) ;
#38524=CARTESIAN_POINT ( 'NONE',  ( 0.2801149460245108691, 11.57793225195137055, 4.005169813315148097 ) ) ;
#38526=ORIENTED_EDGE ( 'NONE', *, *, #63145, .T. ) ;
#38529=CARTESIAN_POINT ( 'NONE',  ( 0.2652384529303155047, -9.338494547402444113, 7.922180393770638318 ) ) ;
#38531=VECTOR ( 'NONE', #10747, 999.9999999999998863 ) ;
#38560=VECTOR ( 'NONE', #63363, 1000.000000000000000 ) ;
#38570=CARTESIAN_POINT ( 'NONE',  ( 2.251152103363437185, 5.004701566804899748, 5.769488058190947122 ) ) ;
#38571=CARTESIAN_POINT ( 'NONE',  ( 2.507146904658099196, -3.672650549645619211, -6.793847219607487276 ) ) ;
#38573=CARTESIAN_POINT ( 'NONE',  ( 0.3006302518452059758, 9.243299516615135047, -8.051021221755679136 ) ) ;
#38574=CARTESIAN_POINT ( 'NONE',  ( 5.530133899448235191, -0.01111090067015095897, 0.01149180883054541115 ) ) ;
#38581=CARTESIAN_POINT ( 'NONE',  ( 5.516018279890452902, -0.005331956019561440684, -0.004180585980734585240 ) ) ;
#38588=CARTESIAN_POINT ( 'NONE',  ( 2.827825597296802496, -8.073505504738395899, 4.031992772938967740 ) ) ;
#38590=CARTESIAN_POINT ( 'NONE',  ( 2.931247277082684288, 7.255238984871627217, 3.034789039497215679 ) ) ;
#38596=CARTESIAN_POINT ( 'NONE',  ( 2.262775599886257538, 2.480428346600533906, 7.227769107232051127 ) ) ;
#38602=CARTESIAN_POINT ( 'NONE',  ( 0.2653519890518156177, -4.188437879978335054, 11.50766430042468080 ) ) ;
#38603=CARTESIAN_POINT ( 'NONE',  ( 0.2653519789438770204, 11.51519617080780655, 4.167744179923950298 ) ) ;
#38612=CARTESIAN_POINT ( 'NONE',  ( 2.276198483117258142, -2.759333101207195327, 7.130755363255154577 ) ) ;
#38614=FACE_OUTER_BOUND ( 'NONE', #27504, .T. ) ;
#38617=CARTESIAN_POINT ( 'NONE',  ( 0.3675815128205912052, 12.04510820461662668, -2.391755495700480516 ) ) ;
#38618=CARTESIAN_POINT ( 'NONE',  ( 0.3223008802179305743, -2.370176598416255054, -12.03398982086836355 ) ) ;
#38619=B_SPLINE_CURVE_WITH_KNOTS ( 'NONE', 3,
 ( #15949, #62823, #691, #46891, #31581, #56549, #36238, #6333, #31273, #6024, #1351, #51244, #21632, #41894, #26279, #32239 ),
 .UNSPECIFIED., .F., .F.,
 ( 4, 3, 3, 3, 3, 4 ),
 ( 8.673617379884034509E-19, 0.0002176109881720231839, 0.0004352086762394586066, 0.0006528017811446851226, 0.0007615147961451692411, 0.0009453342004947268718 ),
 .UNSPECIFIED. ) ;
#38623=CARTESIAN_POINT ( 'NONE',  ( 2.969415267404955650, -7.007431655063692588, -3.597837242549690284 ) ) ;
#38636=( BOUNDED_SURFACE ( )  B_SPLINE_SURFACE ( 3, 1, ( 
 ( #3901, #19172 ),
 ( #23518, #33798 ),
 ( #13210, #54442 ),
 ( #13516, #28825 ) ),
 .UNSPECIFIED., .F., .F., .F. ) 
 B_SPLINE_SURFACE_WITH_KNOTS ( ( 4, 4 ),
 ( 2, 2 ),
 ( 0.000000000000000000, 1.000000000000000000 ),
 ( 0.000000000000000000, 1.000000000000000000 ),
 .UNSPECIFIED. ) 
 GEOMETRIC_REPRESENTATION_ITEM ( )  RATIONAL_B_SPLINE_SURFACE ( (
 ( 1.000000000000000000, 1.000000000000000000),
 ( 0.6933888150995267674, 0.9895912004443193632),
 ( 0.6933888150995267674, 0.9895912004443193632),
 ( 1.000000000000000000, 1.000000000000000000) ) ) 
 REPRESENTATION_ITEM ( '' )  SURFACE ( )  );
#38647=VERTEX_POINT ( 'NONE', #13051 ) ;
#38649=VERTEX_POINT ( 'NONE', #12702 ) ;
#38652=EDGE_CURVE ( 'NONE', #7920, #3473, #28729, .T. ) ;
#38656=ORIENTED_EDGE ( 'NONE', *, *, #39099, .T. ) ;
#38657=CARTESIAN_POINT ( 'NONE',  ( 0.2650492594609234476, -12.24562116224018382, -0.1101156276918037469 ) ) ;
#38666=EDGE_CURVE ( 'NONE', #14988, #21432, #62075, .T. ) ;
#38676=CARTESIAN_POINT ( 'NONE',  ( 2.251152103363647683, -1.449454666117681256, -7.498874008626772003 ) ) ;
#38678=ORIENTED_EDGE ( 'NONE', *, *, #49379, .T. ) ;
#38679=CARTESIAN_POINT ( 'NONE',  ( 5.515188684475870851, -0.005140903460551146317, 0.001485678338381694451 ) ) ;
#38684=ORIENTED_EDGE ( 'NONE', *, *, #50955, .T. ) ;
#38685=CARTESIAN_POINT ( 'NONE',  ( 2.241451721903216399, 7.194631024842675693, -2.553895636571864802 ) ) ;
#38689=DIRECTION ( 'NONE',  ( 0.000000000000000000, 0.000000000000000000, 1.000000000000000000 ) ) ;
#38691=CARTESIAN_POINT ( 'NONE',  ( 1.719304012341585253, 11.38834240361577521, -5.690355757825364513 ) ) ;
#38695=EDGE_LOOP ( 'NONE', ( #3282, #7048, #57783, #39542 ) ) ;
#38697=ORIENTED_EDGE ( 'NONE', *, *, #12239, .F. ) ;
#38698=CARTESIAN_POINT ( 'NONE',  ( 1.283627346226881683, 1.641214790177954352, -12.47820286973621506 ) ) ;
#38699=CARTESIAN_POINT ( 'NONE',  ( 5.515188684475870851, -0.003154373509839927467, -0.004322737127823468931 ) ) ;
#38701=CARTESIAN_POINT ( 'NONE',  ( 0.3632410797595190810, -10.49990774419906181, 6.365652464380866959 ) ) ;
#38702=CARTESIAN_POINT ( 'NONE',  ( 0.2655924914740778742, -7.905499957109173970, -9.352877839710680874 ) ) ;
#38704=CARTESIAN_POINT ( 'NONE',  ( 2.241451721903216399, -7.507681056655368224, -1.385577012535832875 ) ) ;
#38709=CARTESIAN_POINT ( 'NONE',  ( 2.253265082352433168, -5.768060979107497488, -5.007416537586576233 ) ) ;
#38715=CARTESIAN_POINT ( 'NONE',  ( 2.241536586108912488, -2.617055111126402878, -7.171901127201320669 ) ) ;
#38717=ORIENTED_EDGE ( 'NONE', *, *, #58437, .T. ) ;
#38722=EDGE_CURVE ( 'NONE', #13729, #18751, #63252, .T. ) ;
#38725=FACE_OUTER_BOUND ( 'NONE', #35478, .T. ) ;
#38729=B_SPLINE_CURVE_WITH_KNOTS ( 'NONE', 3,
 ( #39473, #58472, #59134, #8565, #28852, #49163, #59774 ),
 .UNSPECIFIED., .F., .F.,
 ( 4, 3, 4 ),
 ( 0.000000000000000000, 0.001700533616330544926, 0.005002426799371471715 ),
 .UNSPECIFIED. ) ;
#38730=CARTESIAN_POINT ( 'NONE',  ( 0.2676618633000449332, -12.08777609394271657, 1.968216791520453368 ) ) ;
#38733=CARTESIAN_POINT ( 'NONE',  ( 0.2872850955227745917, 2.333231805482987475, 12.02931961709051834 ) ) ;
#38763=EDGE_CURVE ( 'NONE', #53630, #59129, #49381, .T. ) ;
#38769=FACE_OUTER_BOUND ( 'NONE', #10139, .T. ) ;
#38790=CARTESIAN_POINT ( 'NONE',  ( 2.350038591457881409, -1.210550722321041217, -10.55267716396152444 ) ) ;
#38795=CARTESIAN_POINT ( 'NONE',  ( 2.589278595513779813, -5.163950571302539316, -5.779442428606855309 ) ) ;
#38799=EDGE_CURVE ( 'NONE', #65794, #29543, #47000, .T. ) ;
#38800=CARTESIAN_POINT ( 'NONE',  ( 5.530133899448235191, 0.001124651387254987358, -0.01594518557925582447 ) ) ;
#38807=CARTESIAN_POINT ( 'NONE',  ( 0.2655924914740778742, -7.838010948425109703, 9.409507842005998768 ) ) ;
#38808=CARTESIAN_POINT ( 'NONE',  ( 1.937114397841935398, 11.53912442307255404, 5.620553190833015300 ) ) ;
#38811=CARTESIAN_POINT ( 'NONE',  ( 5.514970785353741078, -0.004324946436530291601, 0.001897634820904994845 ) ) ;
#38819=EDGE_LOOP ( 'NONE', ( #44504, #4020, #45514, #48268 ) ) ;
#38824=CARTESIAN_POINT ( 'NONE',  ( 2.368238019615414025, -4.795442552788031776, 5.994627685103054660 ) ) ;
#38831=CARTESIAN_POINT ( 'NONE',  ( 0.3665391374699464300, 12.13918562134721491, -1.872534962004675174 ) ) ;
#38832=B_SPLINE_CURVE_WITH_KNOTS ( 'NONE', 3,
 ( #12296, #32562, #52873, #58196, #12615, #32892, #7995 ),
 .UNSPECIFIED., .F., .F.,
 ( 4, 3, 4 ),
 ( 7.997016289651561525E-15, 0.002398160485435674606, 0.005002426799388316747 ),
 .UNSPECIFIED. ) ;
#38833=ORIENTED_EDGE ( 'NONE', *, *, #58159, .T. ) ;
#38849=EDGE_CURVE ( 'NONE', #4057, #21447, #24731, .T. ) ;
#38857=CARTESIAN_POINT ( 'NONE',  ( 0.3057689695767508153, 10.49983108339468707, -6.328747727191083250 ) ) ;
#38858=CARTESIAN_POINT ( 'NONE',  ( 0.2759803524722234669, 8.018167820447629879, -9.260954523383658099 ) ) ;
#38861=VERTEX_POINT ( 'NONE', #30615 ) ;
#38862=CARTESIAN_POINT ( 'NONE',  ( 2.249013661412228249, -1.444210756221599556, 7.499157010299432713 ) ) ;
#38873=ORIENTED_EDGE ( 'NONE', *, *, #16502, .T. ) ;
#38878=VERTEX_POINT ( 'NONE', #21307 ) ;
#38886=CARTESIAN_POINT ( 'NONE',  ( 2.288423627607476529, -3.684511167348244243, 6.704349683466405807 ) ) ;
#38888=DIRECTION ( 'NONE',  ( -1.000000000000000000, -0.000000000000000000, -0.000000000000000000 ) ) ;
#38895=CARTESIAN_POINT ( 'NONE',  ( 2.491965175173491698, 5.773748672881994892, -5.121563073453221371 ) ) ;
#38907=CARTESIAN_POINT ( 'NONE',  ( 1.452237505248552996, -11.67686475128076573, -4.880303821311127166 ) ) ;
#38919=CARTESIAN_POINT ( 'NONE',  ( 2.290907136833256530, -7.561169784528411597, 1.168459104840908314 ) ) ;
#38922=CARTESIAN_POINT ( 'NONE',  ( 2.241506898688417682, 6.591904579673283138, -3.851253041557037182 ) ) ;
#38927=CARTESIAN_POINT ( 'NONE',  ( 1.719304012341460908, 3.626341562669523011, -12.20344780066162649 ) ) ;
#38933=CARTESIAN_POINT ( 'NONE',  ( 2.261269890822074746, 3.699080366006695098, 6.685978463722140219 ) ) ;
#38936=LINE ( 'NONE', #33929, #46569 ) ;
#38938=CARTESIAN_POINT ( 'NONE',  ( 0.5572780756284594350, -0.3055340344620345872, 12.33974848088638687 ) ) ;
#38947=CARTESIAN_POINT ( 'NONE',  ( 2.844750968615431752, -7.651810733888697591, 1.686994672841962029 ) ) ;
#38949=ORIENTED_EDGE ( 'NONE', *, *, #49379, .F. ) ;
#38950=CARTESIAN_POINT ( 'NONE',  ( 2.263328370261528999, -7.640407877530317471, 0.1420109704215539170 ) ) ;
#38957=CARTESIAN_POINT ( 'NONE',  ( 1.372161826076366165, -9.274145586376226547, 8.551811013234654979 ) ) ;
#38961=CARTESIAN_POINT ( 'NONE',  ( 1.634816307075101838, 1.494046826342973588, 12.61459884933128350 ) ) ;
#38963=CARTESIAN_POINT ( 'NONE',  ( 2.507146904658100528, -7.565123178000297877, -1.553587269793135217 ) ) ;
#38964=CARTESIAN_POINT ( 'NONE',  ( 5.536195898058073439, 0.003145317580921152666, 0.007896796515810895062 ) ) ;
#38969=ORIENTED_EDGE ( 'NONE', *, *, #13250, .T. ) ;
#38982=CARTESIAN_POINT ( 'NONE',  ( 2.507146904658097863, -2.843654641958937912, 7.180414359940946234 ) ) ;
#38983=CARTESIAN_POINT ( 'NONE',  ( 0.3341166715381306274, -9.234320413907852299, 8.078283863465467007 ) ) ;
#38986=CARTESIAN_POINT ( 'NONE',  ( -14.47334165536099881, 0.000000000000000000, 0.000000000000000000 ) ) ;
#38988=LINE ( 'NONE', #12392, #25608 ) ;
#38989=CARTESIAN_POINT ( 'NONE',  ( 2.273267844204867938, -1.476347988307422199, -7.501135923490795498 ) ) ;
#38992=CARTESIAN_POINT ( 'NONE',  ( 5.515188684475870851, -0.004804816249378844779, 0.002355816063606914167 ) ) ;
#39000=CARTESIAN_POINT ( 'NONE',  ( 0.2915757698887279648, -3.989025639548713809, 11.58754481235185985 ) ) ;
#39002=CARTESIAN_POINT ( 'NONE',  ( 3.152665057734040488, 0.000000000000000000, 0.000000000000000000 ) ) ;
#39010=CARTESIAN_POINT ( 'NONE',  ( 1.719304012341412724, 1.452142814149018690, -12.64775761152637301 ) ) ;
#39012=DIRECTION ( 'NONE',  ( 0.000000000000000000, 0.000000000000000000, 1.000000000000000000 ) ) ;
#39013=CARTESIAN_POINT ( 'NONE',  ( 0.3654063281920718609, -10.50027211615251588, 6.366443614636645876 ) ) ;
#39015=CARTESIAN_POINT ( 'NONE',  ( 0.3106921474978457942, 10.73438344699978764, -5.925601485921557554 ) ) ;
#39018=SHAPE_REPRESENTATION ( 'straight bevel gear_iso_ISO - Straight bevel gear 0.7M 36GT 12PT 20PA 5FW ---36O12H20MD8.0S1', ( #24966 ), #48383 ) ;
#39023=CARTESIAN_POINT ( 'NONE',  ( 2.261269890822074302, -5.762737836065078056, -5.017604628138454537 ) ) ;
#39031=CARTESIAN_POINT ( 'NONE',  ( 2.241509619876138171, -2.575142053947820031, -7.187074272457178559 ) ) ;
#39035=FACE_BOUND ( 'NONE', #46529, .T. ) ;
#39050=CARTESIAN_POINT ( 'NONE',  ( 0.2650492433740077036, -4.291726136518470902, -11.46945725111971193 ) ) ;
#39056=DIRECTION ( 'NONE',  ( 0.000000000000000000, 0.000000000000000000, 1.000000000000000000 ) ) ;
#39059=CARTESIAN_POINT ( 'NONE',  ( 1.719304012338398246, 7.581471372739840398, 10.22720798541364395 ) ) ;
#39078=CARTESIAN_POINT ( 'NONE',  ( 2.655192694324496561, 9.204230091440560813, 2.733486750963942225 ) ) ;
#39081=CARTESIAN_POINT ( 'NONE',  ( 2.297017764050092836, -7.506328781223015945, 1.490897313050660644 ) ) ;
#39088=CARTESIAN_POINT ( 'NONE',  ( 2.298277635560276977, 3.968740875991644934, -6.543949079923893741 ) ) ;
#39090=ADVANCED_FACE ( 'NONE', ( #16974 ), #52410, .T. ) ;
#39096=B_SPLINE_CURVE_WITH_KNOTS ( 'NONE', 3,
 ( #16555, #55808, #20871, #61114, #30512, #56113, #41140 ),
 .UNSPECIFIED., .F., .F.,
 ( 4, 3, 4 ),
 ( 0.0001321430428584417424, 0.0001982171734706201821, 0.0002642860854759487171 ),
 .UNSPECIFIED. ) ;
#39099=EDGE_CURVE ( 'NONE', #32743, #60603, #5679, .T. ) ;
#39113=CARTESIAN_POINT ( 'NONE',  ( 2.266490820343228574, -0.1453321357832227656, -7.641399530653803396 ) ) ;
#39114=CARTESIAN_POINT ( 'NONE',  ( 2.259830038564998311, -5.940579220577209441, 4.804964945109168717 ) ) ;
#39116=VERTEX_POINT ( 'NONE', #4314 ) ;
#39120=ADVANCED_FACE ( 'NONE', ( #48568 ), #13758, .F. ) ;
#39121=ORIENTED_EDGE ( 'NONE', *, *, #46126, .T. ) ;
#39134=CARTESIAN_POINT ( 'NONE',  ( 2.290907136833256974, 7.561169784528423143, -1.168459104840855911 ) ) ;
#39137=CARTESIAN_POINT ( 'NONE',  ( 2.276905613632196790, 1.175741125185098213, -7.555317002491444889 ) ) ;
#39146=CARTESIAN_POINT ( 'NONE',  ( 3.152665057734040488, 0.000000000000000000, 0.000000000000000000 ) ) ;
#39149=CARTESIAN_POINT ( 'NONE',  ( 2.373367633546870969, 1.511052049480019255, -7.528269033630142104 ) ) ;
#39153=EDGE_LOOP ( 'NONE', ( #7811, #39666, #61159, #34497 ) ) ;
#39156=EDGE_CURVE ( 'NONE', #39116, #38647, #43680, .T. ) ;
#39165=EDGE_CURVE ( 'NONE', #2995, #48281, #26267, .T. ) ;
#39166=CARTESIAN_POINT ( 'NONE',  ( 3.152665057734086229, 4.725420687650732532, 6.378477742800449768 ) ) ;
#39169=CARTESIAN_POINT ( 'NONE',  ( 2.990245332647879284, -1.974808303407750154, 8.248134185053356049 ) ) ;
#39173=CARTESIAN_POINT ( 'NONE',  ( 0.2653141617321057577, -9.409385893408552803, 7.837919552760688191 ) ) ;
#39181=CARTESIAN_POINT ( 'NONE',  ( 1.719304012338401133, 5.690355757826538685, 11.38834240361399885 ) ) ;
#39184=VERTEX_POINT ( 'NONE', #60480 ) ;
#39188=CARTESIAN_POINT ( 'NONE',  ( 2.589278595513879733, 5.163950571302623693, 5.779442428606822446 ) ) ;
#39193=CARTESIAN_POINT ( 'NONE',  ( 0.6473888112830247232, 2.472751636945372145, 12.12394591856679860 ) ) ;
#39196=EDGE_CURVE ( 'NONE', #26844, #20926, #37314, .T. ) ;
#39203=CARTESIAN_POINT ( 'NONE',  ( 2.368238019615013012, 5.763545178420172554, -5.070835960312829016 ) ) ;
#39204=DIRECTION ( 'NONE',  ( -0.3865475372811021382, 0.6938894834606125217, -0.6075346789811091330 ) ) ;
#39210=B_SPLINE_CURVE_WITH_KNOTS ( 'NONE', 3,
 ( #16999, #37278, #27300, #57590, #41616, #62227, #31631, #57920, #51624, #26326 ),
 .UNSPECIFIED., .F., .F.,
 ( 4, 3, 3, 4 ),
 ( 4.336808689942017736E-19, 6.607638129004444159E-05, 9.911389841680550718E-05, 0.0001667630577588612270 ),
 .UNSPECIFIED. ) ;
#39212=CARTESIAN_POINT ( 'NONE',  ( 0.2638984909335716500, 4.375449752477288179, -11.43908195192325294 ) ) ;
#39213=( BOUNDED_SURFACE ( )  B_SPLINE_SURFACE ( 3, 1, ( 
 ( #24148, #44406 ),
 ( #65026, #35078 ),
 ( #65357, #25134 ),
 ( #19820, #50422 ) ),
 .UNSPECIFIED., .F., .F., .F. ) 
 B_SPLINE_SURFACE_WITH_KNOTS ( ( 4, 4 ),
 ( 2, 2 ),
 ( 0.000000000000000000, 1.000000000000000000 ),
 ( 0.000000000000000000, 1.000000000000000000 ),
 .UNSPECIFIED. ) 
 GEOMETRIC_REPRESENTATION_ITEM ( )  RATIONAL_B_SPLINE_SURFACE ( (
 ( 1.000000000000000000, 1.000000000000000000),
 ( 0.6933888150995267674, 0.9895912004443193632),
 ( 0.6933888150995267674, 0.9895912004443193632),
 ( 1.000000000000000000, 1.000000000000000000) ) ) 
 REPRESENTATION_ITEM ( '' )  SURFACE ( )  );
#39215=CARTESIAN_POINT ( 'NONE',  ( 2.889800649504073782, -4.732281052280337796, 3.882893708502031860 ) ) ;
#39216=CARTESIAN_POINT ( 'NONE',  ( 0.3654063281920751916, 9.235228056824031029, -8.093076148785947055 ) ) ;
#39217=CARTESIAN_POINT ( 'NONE',  ( 0.5572780756284481107, -12.33974848088638687, -0.3055340344620752768 ) ) ;
#39222=CARTESIAN_POINT ( 'NONE',  ( 5.514970785353741078, -0.004588761610584819045, -0.001117786416802158496 ) ) ;
#39230=CARTESIAN_POINT ( 'NONE',  ( 2.241528039335008327, 6.619488482362989146, -3.803597072146465585 ) ) ;
#39242=CARTESIAN_POINT ( 'NONE',  ( 0.2652384529303126182, 11.53005674806963121, 4.126283314267611857 ) ) ;
#39255=EDGE_CURVE ( 'NONE', #38647, #8430, #12687, .T. ) ;
#39259=CARTESIAN_POINT ( 'NONE',  ( 2.241352910868908754, -6.652881166698485949, -3.744764251557062718 ) ) ;
#39263=ORIENTED_EDGE ( 'NONE', *, *, #9295, .F. ) ;
#39265=ORIENTED_EDGE ( 'NONE', *, *, #28893, .F. ) ;
#39269=CARTESIAN_POINT ( 'NONE',  ( 2.969415267404248215, 4.269695207293191075, 6.619534278261581584 ) ) ;
#39271=ORIENTED_EDGE ( 'NONE', *, *, #14777, .T. ) ;
#39274=CARTESIAN_POINT ( 'NONE',  ( 2.406456491626281835, -9.333533259764168477, -4.662370073863471909 ) ) ;
#39276=B_SPLINE_CURVE_WITH_KNOTS ( 'NONE', 3,
 ( #37936, #7339, #48590, #3044, #48282, #3377, #52906, #32931, #33614, #58228, #27623, #38933, #17674, #22662, #47926, #38251, #12648, #2386, #2731 ),
 .UNSPECIFIED., .F., .F.,
 ( 4, 3, 3, 3, 3, 3, 4 ),
 ( 0.000000000000000000, 2.831840207499890458E-05, 4.217266859840865451E-05, 5.602024318396426049E-05, 6.290810167969416620E-05, 9.120440630945709744E-05, 0.0001153103026479752088 ),
 .UNSPECIFIED. ) ;
#39279=CARTESIAN_POINT ( 'NONE',  ( 2.373367633546870525, -5.072743978105275886, 5.764146204907447668 ) ) ;
#39292=CARTESIAN_POINT ( 'NONE',  ( 2.639814597422737386, -7.382549681340928593, 2.414168779979558810 ) ) ;
#39296=CARTESIAN_POINT ( 'NONE',  ( 0.2869720083484356143, -7.715523637151703973, -9.519277517057183502 ) ) ;
#39302=CARTESIAN_POINT ( 'NONE',  ( 0.3675815128205894289, -9.235491948680062180, 8.093875121226046687 ) ) ;
#39320=EDGE_CURVE ( 'NONE', #31123, #52583, #54767, .T. ) ;
#39322=CARTESIAN_POINT ( 'NONE',  ( 2.889800649504073782, 0.06738247734050435700, 6.121013568931506832 ) ) ;
#39323=CARTESIAN_POINT ( 'NONE',  ( 0.3106921474978455167, -3.971572160646677840, -11.60027394202202444 ) ) ;
#39328=FACE_OUTER_BOUND ( 'NONE', #45328, .T. ) ;
#39330=AXIS2_PLACEMENT_3D ( 'NONE', #54781, #7926, #23201 ) ;
#39331=EDGE_CURVE ( 'NONE', #58956, #47135, #38134, .T. ) ;
#39335=CARTESIAN_POINT ( 'NONE',  ( 1.452237505248555660, -2.778494755358972057, -12.34692280296794742 ) ) ;
#39339=CARTESIAN_POINT ( 'NONE',  ( 0.3675815128205894289, 10.76447900494948584, -5.910255304480332761 ) ) ;
#39346=CARTESIAN_POINT ( 'NONE',  ( 2.298277635560276533, -5.755367168477967255, -5.044791616846986848 ) ) ;
#39362=DIRECTION ( 'NONE',  ( -0.3865475372811021937, 0.1791957239473662700, 0.9046932595863054205 ) ) ;
#39381=CARTESIAN_POINT ( 'NONE',  ( 0.3401186441510199443, -6.355596563012379185, 10.49699112323340877 ) ) ;
#39386=CARTESIAN_POINT ( 'NONE',  ( 0.3675815128205912052, 7.689697408877274931, 9.574637318041988365 ) ) ;
#39391=CARTESIAN_POINT ( 'NONE',  ( 0.2650492594609234476, 10.66007682546625546, -6.027447650185258077 ) ) ;
#39392=ORIENTED_EDGE ( 'NONE', *, *, #2763, .F. ) ;
#39411=CARTESIAN_POINT ( 'NONE',  ( 0.2869720083484326167, -10.50600528807143164, -6.306330337780625683 ) ) ;
#39412=CARTESIAN_POINT ( 'NONE',  ( 5.515188684475870851, -0.003857086913166417504, -0.003709313826049733063 ) ) ;
#39422=LINE ( 'NONE', #30434, #24494 ) ;
#39431=CARTESIAN_POINT ( 'NONE',  ( 2.907497136251069314, -5.319973245618573543, -5.781215374755531933 ) ) ;
#39435=CARTESIAN_POINT ( 'NONE',  ( 5.520433897694421610, -0.002108682515300382403, -0.01491416502703810272 ) ) ;
#39438=AXIS2_PLACEMENT_3D ( 'NONE', #40160, #46167, #51156 ) ;
#39439=CARTESIAN_POINT ( 'NONE',  ( 2.440552418640497656, -6.568204543009798613, -4.020120046181113516 ) ) ;
#39440=CARTESIAN_POINT ( 'NONE',  ( 0.8320506296491623210, -4.610676791972267985, -11.54877388447409814 ) ) ;
#39442=CARTESIAN_POINT ( 'NONE',  ( 2.297017764050091948, -2.462009443075658943, 7.246120070222751508 ) ) ;
#39454=CARTESIAN_POINT ( 'NONE',  ( 1.283627346227448118, 12.28700367512568725, -2.725559306499256262 ) ) ;
#39456=CARTESIAN_POINT ( 'NONE',  ( 2.298277635560276089, -7.246601281227238900, 2.461898367585356961 ) ) ;
#39458=CARTESIAN_POINT ( 'NONE',  ( 0.2638984909335716500, 10.70468911391672684, -5.950360275954944989 ) ) ;
#39459=CARTESIAN_POINT ( 'NONE',  ( 0.3654063281920759687, -9.573804659448610366, -7.689576266239762425 ) ) ;
#39460=CARTESIAN_POINT ( 'NONE',  ( 3.152665057736233845, -4.725420687649230622, 6.378477742801980988 ) ) ;
#39470=CARTESIAN_POINT ( 'NONE',  ( 5.514970785353741078, -0.003415090918276162107, 0.003262412238248703009 ) ) ;
#39473=CARTESIAN_POINT ( 'NONE',  ( 3.152665057734062248, -7.609997527621111146, 2.258875078502258216 ) ) ;
#39476=EDGE_CURVE ( 'NONE', #54467, #7370, #3611, .T. ) ;
#39477=DIRECTION ( 'NONE',  ( 0.000000000000000000, 0.000000000000000000, 1.000000000000000000 ) ) ;
#39480=CARTESIAN_POINT ( 'NONE',  ( 2.835339799623981971, 1.682641786445544296, -7.649567297875980998 ) ) ;
#39482=EDGE_CURVE ( 'NONE', #58379, #21179, #53483, .T. ) ;
#39485=CARTESIAN_POINT ( 'NONE',  ( 2.266490820343224577, -7.230273269342692544, -2.476945027124343390 ) ) ;
#39489=VERTEX_POINT ( 'NONE', #19191 ) ;
#39490=CIRCLE ( 'NONE', #36316, 4.000000000000000000 ) ;
#39499=CARTESIAN_POINT ( 'NONE',  ( 1.719304012339893051, -12.70777170743898310, 0.7661785589588769874 ) ) ;
#39507=AXIS2_PLACEMENT_3D ( 'NONE', #60951, #16381, #36653 ) ;
#39510=CARTESIAN_POINT ( 'NONE',  ( 0.2648978790185584908, -9.295532325666394868, -7.972372351883127095 ) ) ;
#39516=CARTESIAN_POINT ( 'NONE',  ( 2.261269890822071194, -7.499479675451350857, -1.464004156081723185 ) ) ;
#39517=CARTESIAN_POINT ( 'NONE',  ( 5.514970785353741078, -0.004588761610585018538, 0.001117786416802603452 ) ) ;
#39518=CARTESIAN_POINT ( 'NONE',  ( 0.2648978790185619880, 9.465406350830608773, 7.769924372105235122 ) ) ;
#39521=CARTESIAN_POINT ( 'NONE',  ( 2.827825597296806048, 0.5449445831288285413, -9.007857251166427659 ) ) ;
#39522=CARTESIAN_POINT ( 'NONE',  ( 2.305787727787084407, 2.461236246751170142, -7.249469779319884566 ) ) ;
#39532=ORIENTED_EDGE ( 'NONE', *, *, #3489, .F. ) ;
#39533=CARTESIAN_POINT ( 'NONE',  ( 2.288423627607474753, 6.543055113184276017, -3.963881558061893351 ) ) ;
#39540=EDGE_CURVE ( 'NONE', #20729, #16846, #61939, .T. ) ;
#39542=ORIENTED_EDGE ( 'NONE', *, *, #53734, .F. ) ;
#39547=CARTESIAN_POINT ( 'NONE',  ( 0.3106921474978470155, 12.25904950202577659, 0.2354703039888528804 ) ) ;
#39548=CARTESIAN_POINT ( 'NONE',  ( 2.781367136452733924, 6.608147481822127745, -4.171010984503221053 ) ) ;
#39557=CARTESIAN_POINT ( 'NONE',  ( 5.514970785353741078, -0.001897634820904980750, -0.004324946436530298539 ) ) ;
#39573=AXIS2_PLACEMENT_3D ( 'NONE', #34048, #29085, #43366 ) ;
#39580=CIRCLE ( 'NONE', #14082, 7.938172270156617749 ) ;
#39586=CARTESIAN_POINT ( 'NONE',  ( 2.259830038564998311, -7.131511317046838272, -2.742210045659254192 ) ) ;
#39587=VERTEX_POINT ( 'NONE', #9201 ) ;
#39590=EDGE_CURVE ( 'NONE', #32821, #45493, #20506, .T. ) ;
#39592=CARTESIAN_POINT ( 'NONE',  ( 1.287602823388473983, 9.987902848014591939, -7.659913635101546880 ) ) ;
#39594=CARTESIAN_POINT ( 'NONE',  ( 0.2648321136542700627, 4.054947570138896396, 11.55519783395229005 ) ) ;
#39595=CARTESIAN_POINT ( 'NONE',  ( 2.251152103363641022, -6.676162264140654834, -3.709836606813393445 ) ) ;
#39596=ORIENTED_EDGE ( 'NONE', *, *, #4983, .F. ) ;
#39599=CARTESIAN_POINT ( 'NONE',  ( 0.5547464869798215403, 6.433541106625093597, 10.53334899235172983 ) ) ;
#39600=ORIENTED_EDGE ( 'NONE', *, *, #33501, .F. ) ;
#39603=CARTESIAN_POINT ( 'NONE',  ( 3.047904605210433271, 7.047014837597106229, -3.577928268981992233 ) ) ;
#39604=CARTESIAN_POINT ( 'NONE',  ( 0.2759803524722224677, -9.260954523383681192, -8.018167820447592575 ) ) ;
#39605=CARTESIAN_POINT ( 'NONE',  ( 1.547277799338546700, -9.261681528764437843, 8.651049845884134726 ) ) ;
#39614=CARTESIAN_POINT ( 'NONE',  ( 2.241317068080776131, -5.906676463196257387, -4.836852665784649119 ) ) ;
#39624=CARTESIAN_POINT ( 'NONE',  ( 0.3164563675027610712, 1.892265234253275530, -12.11636128244742494 ) ) ;
#39626=CARTESIAN_POINT ( 'NONE',  ( 2.963017218115625351, -7.522800244854591867, 2.328652339224321022 ) ) ;
#39632=VERTEX_POINT ( 'NONE', #34783 ) ;
#39641=CARTESIAN_POINT ( 'NONE',  ( 0.2915757698887310734, -9.248369946372577033, 8.040595355212914797 ) ) ;
#39648=CARTESIAN_POINT ( 'NONE',  ( 5.516018279890452902, 0.005042957932159071975, 0.004525000489649949435 ) ) ;
#39658=CARTESIAN_POINT ( 'NONE',  ( 0.7400311444011756778, -6.506979270898107792, -10.56075429936773880 ) ) ;
#39660=CARTESIAN_POINT ( 'NONE',  ( 0.3610902822527200517, -12.27530799859939314, 0.2623004149194189116 ) ) ;
#39662=CARTESIAN_POINT ( 'NONE',  ( 0.3002738374340822580, -3.979745968261130695, -11.59380198135586326 ) ) ;
#39665=EDGE_CURVE ( 'NONE', #51949, #32084, #16706, .T. ) ;
#39666=ORIENTED_EDGE ( 'NONE', *, *, #32416, .T. ) ;
#39672=CARTESIAN_POINT ( 'NONE',  ( 1.014383007554945149, 1.731118468094080987, -12.37541872618880312 ) ) ;
#39673=CONICAL_SURFACE ( 'NONE', #41802, 7.938172270156617749, 1.280189991382167047 ) ;
#39674=CARTESIAN_POINT ( 'NONE',  ( 3.152665057734040488, 0.000000000000000000, 0.000000000000000000 ) ) ;
#39679=CARTESIAN_POINT ( 'NONE',  ( 0.3537226245948368875, 10.75912040401517267, -5.910416419900417218 ) ) ;
#39681=CARTESIAN_POINT ( 'NONE',  ( 1.372161826076674362, -11.20801830616791328, -5.789954543171356605 ) ) ;
#39683=LINE ( 'NONE', #8442, #36055 ) ;
#39687=B_SPLINE_CURVE_WITH_KNOTS ( 'NONE', 3,
 ( #27478, #47779, #58089, #2230, #22509, #42770, #63065, #17528, #37795, #12504, #41685, #1475, #41024 ),
 .UNSPECIFIED., .F., .F.,
 ( 4, 3, 3, 3, 4 ),
 ( 8.673617379884035472E-19, 6.607593386745688247E-05, 0.0001321518677373530843, 0.0001982171734706230282, 0.0002642860854759495302 ),
 .UNSPECIFIED. ) ;
#39688=ORIENTED_EDGE ( 'NONE', *, *, #51338, .F. ) ;
#39689=CONICAL_SURFACE ( 'NONE', #64134, 7.938172270156617749, 1.280189991382167047 ) ;
#39700=DIRECTION ( 'NONE',  ( 0.000000000000000000, 0.000000000000000000, -1.000000000000000000 ) ) ;
#39702=CARTESIAN_POINT ( 'NONE',  ( 2.305787727787084407, 0.1666591538752685842, 7.654065630109507801 ) ) ;
#39705=ORIENTED_EDGE ( 'NONE', *, *, #58883, .F. ) ;
#39707=CARTESIAN_POINT ( 'NONE',  ( 2.241526690369557429, 6.620271521148430871, 3.802233103835192640 ) ) ;
#39713=ORIENTED_EDGE ( 'NONE', *, *, #40744, .F. ) ;
#39719=CARTESIAN_POINT ( 'NONE',  ( 1.109979610370702918, -12.24510427445497029, -2.646302643132570243 ) ) ;
#39723=AXIS2_PLACEMENT_3D ( 'NONE', #58034, #17131, #6506 ) ;
#39725=CARTESIAN_POINT ( 'NONE',  ( 2.241534463349551753, 9.451863027432619807E-16, 7.634462073473348376 ) ) ;
#39726=CARTESIAN_POINT ( 'NONE',  ( 1.549075743843701503, 7.618376504787362613, 10.12891450359415124 ) ) ;
#39727=ORIENTED_EDGE ( 'NONE', *, *, #47319, .T. ) ;
#39739=DIRECTION ( 'NONE',  ( 0.3865475372811021937, -0.2971585806051852408, -0.8730852074079749059 ) ) ;
#39742=ORIENTED_EDGE ( 'NONE', *, *, #343, .T. ) ;
#39748=CARTESIAN_POINT ( 'NONE',  ( 2.241528039335008771, -1.341200777944199674, 7.515727438419998130 ) ) ;
#39764=ADVANCED_FACE ( 'NONE', ( #37423 ), #57585, .T. ) ;
#39768=CARTESIAN_POINT ( 'NONE',  ( 2.556980015513344640, 6.074557383032630931, 4.795979673457624770 ) ) ;
#39774=CARTESIAN_POINT ( 'NONE',  ( 5.536195898058073439, 0.003145317580921150064, -0.007896796515810348624 ) ) ;
#39775=B_SPLINE_CURVE_WITH_KNOTS ( 'NONE', 3,
 ( #13935, #49548, #48890, #23617, #43888, #43218, #53214, #54198, #28270, #22632 ),
 .UNSPECIFIED., .F., .F.,
 ( 4, 3, 3, 4 ),
 ( 1.226634733346699542E-18, 6.607638129004514633E-05, 9.911389841680577823E-05, 0.0001667630577588626365 ),
 .UNSPECIFIED. ) ;
#39778=CARTESIAN_POINT ( 'NONE',  ( 2.770579946183333586, -6.607710183380604896, -4.165025702425915632 ) ) ;
#39782=CARTESIAN_POINT ( 'NONE',  ( 5.515188684475870851, 0.004442604682416481134, 0.002983184900674867857 ) ) ;
#39784=ORIENTED_EDGE ( 'NONE', *, *, #65034, .T. ) ;
#39789=EDGE_CURVE ( 'NONE', #59168, #18816, #43546, .T. ) ;
#39806=ORIENTED_EDGE ( 'NONE', *, *, #32624, .T. ) ;
#39823=CARTESIAN_POINT ( 'NONE',  ( 5.514624014163232779, 0.001255375129358076965, 0.003946330869975007462 ) ) ;
#39824=CARTESIAN_POINT ( 'NONE',  ( 2.247112776671470247, 7.135103076758483098, -2.720990995225236908 ) ) ;
#39830=CARTESIAN_POINT ( 'NONE',  ( 2.280717697723835258, 7.645922213779907217, -0.1564731737570369263 ) ) ;
#39831=CARTESIAN_POINT ( 'NONE',  ( 2.665405856346786617, 2.226920474533502059, -9.304623509366180656 ) ) ;
#39845=CARTESIAN_POINT ( 'NONE',  ( 5.514624014163232779, 0.004137701579365678402, 0.0001700579043834099459 ) ) ;
#39853=CARTESIAN_POINT ( 'NONE',  ( 5.516018279890452902, -0.006707902355168857828, -0.0009545156522405044090 ) ) ;
#39854=CARTESIAN_POINT ( 'NONE',  ( 2.251152103363644130, -3.709836606813365023, 6.676162264140674374 ) ) ;
#39866=CARTESIAN_POINT ( 'NONE',  ( 2.241352910868909643, -1.243507963608144751, 7.532448145350502777 ) ) ;
#39867=LINE ( 'NONE', #54531, #2289 ) ;
#39873=ORIENTED_EDGE ( 'NONE', *, *, #5267, .T. ) ;
#39875=LINE ( 'NONE', #35841, #5630 ) ;
#39878=CARTESIAN_POINT ( 'NONE',  ( 1.014383007554944705, 9.280879504741051278, -8.367379244277028505 ) ) ;
#39880=CARTESIAN_POINT ( 'NONE',  ( 0.4626703367445904047, -12.30872794628575839, -0.2831487465614367371 ) ) ;
#39884=VERTEX_POINT ( 'NONE', #11342 ) ;
#39893=CARTESIAN_POINT ( 'NONE',  ( 2.589278595513260672, 7.197074516942324252, -2.875840518181366434 ) ) ;
#39916=CARTESIAN_POINT ( 'NONE',  ( 0.2869720083484354478, 3.994435966590065057, 11.58405933820302103 ) ) ;
#39917=DIRECTION ( 'NONE',  ( 0.000000000000000000, 0.000000000000000000, 1.000000000000000000 ) ) ;
#39920=EDGE_CURVE ( 'NONE', #51949, #60783, #51924, .T. ) ;
#39922=CARTESIAN_POINT ( 'NONE',  ( 2.247112776671470247, -7.635437439951568095, 0.1165461824817482089 ) ) ;
#39925=CARTESIAN_POINT ( 'NONE',  ( 0.2647959493198542846, 10.67808515296911054, 5.995292100780825528 ) ) ;
#39926=CARTESIAN_POINT ( 'NONE',  ( 0.9232167919969169745, 9.809608956680866854, 7.691547553333150766 ) ) ;
#39927=DIRECTION ( 'NONE',  ( 0.3939253465568944290, 0.7910971609033170537, 0.4679616473074926231 ) ) ;
#39930=CARTESIAN_POINT ( 'NONE',  ( 1.283627346226609012, -9.278077665801919949, 8.503905436511940863 ) ) ;
#39938=CARTESIAN_POINT ( 'NONE',  ( 3.100650473569741994, -5.429218121582416678, 5.767490999797090900 ) ) ;
#39940=CARTESIAN_POINT ( 'NONE',  ( 5.520433897694421610, -0.007082458259338119365, -0.01329351892497969249 ) ) ;
#39955=CARTESIAN_POINT ( 'NONE',  ( 2.255723233589905785, -1.196143347837295146, -7.544965460066120677 ) ) ;
#39958=VERTEX_POINT ( 'NONE', #15350 ) ;
#39959=CARTESIAN_POINT ( 'NONE',  ( 2.835339799623986856, 2.985412098050598928, -7.241165502254415465 ) ) ;
#39960=CARTESIAN_POINT ( 'NONE',  ( 2.969415267404766912, 3.597837242549764003, -7.007431655063588671 ) ) ;
#39965=ORIENTED_EDGE ( 'NONE', *, *, #40794, .F. ) ;
#39970=EDGE_LOOP ( 'NONE', ( #55775, #61389, #26565, #30279 ) ) ;
#39973=CARTESIAN_POINT ( 'NONE',  ( 0.3675815128205894289, -9.574637318042015011, 7.689697408877242957 ) ) ;
#39976=DIRECTION ( 'NONE',  ( -0.3865475372811021382, 0.8598319252293163961, -0.3335716741247106154 ) ) ;
#39982=CARTESIAN_POINT ( 'NONE',  ( 0.2655924914740778187, -4.147079829127179984, -11.52280271232874753 ) ) ;
#39988=ORIENTED_EDGE ( 'NONE', *, *, #47808, .T. ) ;
#39994=CARTESIAN_POINT ( 'NONE',  ( 1.014383007554946925, -12.48801387563329612, 0.4441500209062635429 ) ) ;
#39998=CARTESIAN_POINT ( 'NONE',  ( 2.280717697722507875, 7.238333660706348205, 2.468022724684118874 ) ) ;
#40002=( BOUNDED_SURFACE ( )  B_SPLINE_SURFACE ( 3, 1, ( 
 ( #10835, #50753 ),
 ( #16492, #56052 ),
 ( #26138, #859 ),
 ( #46416, #25810 ) ),
 .UNSPECIFIED., .F., .F., .F. ) 
 B_SPLINE_SURFACE_WITH_KNOTS ( ( 4, 4 ),
 ( 2, 2 ),
 ( 0.000000000000000000, 1.000000000000000000 ),
 ( 0.000000000000000000, 1.000000000000000000 ),
 .UNSPECIFIED. ) 
 GEOMETRIC_REPRESENTATION_ITEM ( )  RATIONAL_B_SPLINE_SURFACE ( (
 ( 1.000000000000000000, 1.000000000000000000),
 ( 0.9942764183789327692, 0.8450855930916580938),
 ( 0.9942764183789327692, 0.8450855930916580938),
 ( 1.000000000000000000, 1.000000000000000000) ) ) 
 REPRESENTATION_ITEM ( '' )  SURFACE ( )  );
#40004=CARTESIAN_POINT ( 'NONE',  ( 3.031336079628712099, 0.4165536638489088506, 7.886784934834594196 ) ) ;
#40013=CARTESIAN_POINT ( 'NONE',  ( 2.305787727787083519, 6.711944854845874886, -3.682701754025442753 ) ) ;
#40020=VERTEX_POINT ( 'NONE', #12981 ) ;
#40022=CARTESIAN_POINT ( 'NONE',  ( 2.241317068080781016, 0.09149433816015992149, 7.633845645378816158 ) ) ;
#40023=CARTESIAN_POINT ( 'NONE',  ( 0.3278977287071249136, -12.12129679591847164, 1.885359334311925705 ) ) ;
#40049=CARTESIAN_POINT ( 'NONE',  ( 1.948354844647129269, 9.612178954895149730, 7.125078658758032368 ) ) ;
#40054=EDGE_CURVE ( 'NONE', #58956, #22574, #44893, .T. ) ;
#40061=CARTESIAN_POINT ( 'NONE',  ( 2.241506898688417238, 1.364429914801517318, 7.511570207700565938 ) ) ;
#40067=ORIENTED_EDGE ( 'NONE', *, *, #5585, .T. ) ;
#40081=CARTESIAN_POINT ( 'NONE',  ( 2.653899356899585893, 6.118160465318848829, 4.792827201941034510 ) ) ;
#40083=CARTESIAN_POINT ( 'NONE',  ( 2.507146904658100084, -0.2163149345877113661, 7.719969556433168734 ) ) ;
#40085=CARTESIAN_POINT ( 'NONE',  ( 2.827825597296800719, 6.550135365664094600, 6.207590800588408619 ) ) ;
#40087=EDGE_CURVE ( 'NONE', #23349, #45003, #46989, .T. ) ;
#40090=ORIENTED_EDGE ( 'NONE', *, *, #41500, .F. ) ;
#40091=CARTESIAN_POINT ( 'NONE',  ( 2.256373768223413734, -2.487510024221220473, 7.223078030710456510 ) ) ;
#40092=CARTESIAN_POINT ( 'NONE',  ( 0.2646305136544065406, -12.03696649559616105, 2.256625640822277568 ) ) ;
#40106=CIRCLE ( 'NONE', #12484, 12.73084802173761787 ) ;
#40114=ORIENTED_EDGE ( 'NONE', *, *, #14917, .F. ) ;
#40115=CARTESIAN_POINT ( 'NONE',  ( 2.268878695253354394, -5.025754889199090414, 5.759001817705848403 ) ) ;
#40118=( NAMED_UNIT ( * ) PLANE_ANGLE_UNIT ( ) SI_UNIT ( $, .RADIAN. ) );
#40130=CARTESIAN_POINT ( 'NONE',  ( 5.520433897694421610, 0.01329351892497962311, -0.007082458259338250336 ) ) ;
#40132=CARTESIAN_POINT ( 'NONE',  ( 0.3675815128205912052, -2.391755495700685241, 12.04510820461658582 ) ) ;
#40134=CARTESIAN_POINT ( 'NONE',  ( 2.931247277082674962, -4.248542803114378152, 6.618030015945717714 ) ) ;
#40139=CARTESIAN_POINT ( 'NONE',  ( 1.375507693218858574, -12.04466556545208178, 3.754650692913366505 ) ) ;
#40141=ADVANCED_FACE ( 'NONE', ( #47910 ), #20590, .F. ) ;
#40143=CARTESIAN_POINT ( 'NONE',  ( 2.241528039335009659, -7.521191296022424311, 1.310213701658565100 ) ) ;
#40157=CARTESIAN_POINT ( 'NONE',  ( 0.2657645697724692058, -0.1513403555226406350, 12.24540328300721903 ) ) ;
#40160=CARTESIAN_POINT ( 'NONE',  ( 3.152665057734040488, 0.000000000000000000, 0.000000000000000000 ) ) ;
#40161=CARTESIAN_POINT ( 'NONE',  ( 2.297017764050034661, 2.462009443075729109, -7.246120070222707099 ) ) ;
#40164=CARTESIAN_POINT ( 'NONE',  ( 2.260457164927185847, -3.699855525213191942, 6.685239696063469239 ) ) ;
#40167=CARTESIAN_POINT ( 'NONE',  ( 2.034671305879537151, 6.436604249851601622, -9.742055912617745506 ) ) ;
#40170=LINE ( 'NONE', #60461, #63770 ) ;
#40171=( BOUNDED_SURFACE ( )  B_SPLINE_SURFACE ( 3, 1, ( 
 ( #1973, #671 ),
 ( #42179, #16933 ),
 ( #20930, #26577 ),
 ( #46870, #10968 ) ),
 .UNSPECIFIED., .F., .F., .F. ) 
 B_SPLINE_SURFACE_WITH_KNOTS ( ( 4, 4 ),
 ( 2, 2 ),
 ( 0.000000000000000000, 1.000000000000000000 ),
 ( 0.000000000000000000, 1.000000000000000000 ),
 .UNSPECIFIED. ) 
 GEOMETRIC_REPRESENTATION_ITEM ( )  RATIONAL_B_SPLINE_SURFACE ( (
 ( 1.000000000000000000, 1.000000000000000000),
 ( 0.6933888150995267674, 0.9895912004443193632),
 ( 0.6933888150995267674, 0.9895912004443193632),
 ( 1.000000000000000000, 1.000000000000000000) ) ) 
 REPRESENTATION_ITEM ( '' )  SURFACE ( )  );
#40172=ORIENTED_EDGE ( 'NONE', *, *, #14814, .F. ) ;
#40175=CARTESIAN_POINT ( 'NONE',  ( 0.3223008802179234134, -0.2444878876722378358, -12.26274332232494579 ) ) ;
#40176=CARTESIAN_POINT ( 'NONE',  ( 2.941278708680199916, 4.615461433467311636, -4.048809123187888659 ) ) ;
#40177=CARTESIAN_POINT ( 'NONE',  ( 2.889800649504073782, -6.016320774579815733, 1.129261637821590947 ) ) ;
#40185=CARTESIAN_POINT ( 'NONE',  ( 0.3040950598368152291, -0.2511348647274793677, -12.25911170648142701 ) ) ;
#40187=CARTESIAN_POINT ( 'NONE',  ( 0.2911222467163546712, 12.25291251554515526, 0.2144311696656072685 ) ) ;
#40189=CARTESIAN_POINT ( 'NONE',  ( 2.430348790457637964, 6.566563360302426489, -4.016278121583773952 ) ) ;
#40193=CARTESIAN_POINT ( 'NONE',  ( 0.3675815128205912052, -10.76447900494944321, 5.910255304480407368 ) ) ;
#40194=ORIENTED_EDGE ( 'NONE', *, *, #3078, .F. ) ;
#40206=CARTESIAN_POINT ( 'NONE',  ( 5.536195898058073439, -0.001224473329857533226, -0.008411485181668796121 ) ) ;
#40213=EDGE_CURVE ( 'NONE', #38510, #8110, #28596, .T. ) ;
#40216=ORIENTED_EDGE ( 'NONE', *, *, #7397, .T. ) ;
#40220=CARTESIAN_POINT ( 'NONE',  ( 2.368238019615030776, -5.763545178420138804, 5.070835960312876090 ) ) ;
#40221=CARTESIAN_POINT ( 'NONE',  ( 1.549075743843499886, 11.66216484053741276, 4.962709020479369570 ) ) ;
#40233=CARTESIAN_POINT ( 'NONE',  ( 0.3278977287071211943, -10.74546228373870704, 5.917385921415761807 ) ) ;
#40238=CARTESIAN_POINT ( 'NONE',  ( 2.241352910868908310, 7.633946224498473931, -0.08337961031706911386 ) ) ;
#40244=CARTESIAN_POINT ( 'NONE',  ( 2.305787727787083519, 6.711944854845874886, -3.682701754025442753 ) ) ;
#40250=LINE ( 'NONE', #10012, #36411 ) ;
#40257=CARTESIAN_POINT ( 'NONE',  ( 2.256373768223411957, -5.936694589811224887, -4.807932997207762682 ) ) ;
#40267=CARTESIAN_POINT ( 'NONE',  ( 2.241311220309654129, -1.234192392742715860, -7.533971938435956694 ) ) ;
#40275=CYLINDRICAL_SURFACE ( 'NONE', #6925, 4.000000000000000000 ) ;
#40276=B_SPLINE_CURVE_WITH_KNOTS ( 'NONE', 3,
 ( #27151, #11517, #36472, #37110, #17170, #11204, #41781, #62077, #10525, #30801, #31787, #52096, #26821, #1574, #21848, #42093 ),
 .UNSPECIFIED., .F., .F.,
 ( 4, 3, 3, 3, 3, 4 ),
 ( 2.178818782297515178E-15, 0.0002126834539179851184, 0.0004253519300366563854, 0.0006380165497224616006, 0.0007442707582428764734, 0.0009453531351414631379 ),
 .UNSPECIFIED. ) ;
#40296=CARTESIAN_POINT ( 'NONE',  ( 1.459561108993791434, -6.861308540877895545, -10.62073135189161199 ) ) ;
#40298=CARTESIAN_POINT ( 'NONE',  ( 0.3341166715381305719, -12.26652061402056049, 0.2526177176099637656 ) ) ;
#40300=EDGE_CURVE ( 'NONE', #44356, #58956, #53936, .T. ) ;
#40311=CARTESIAN_POINT ( 'NONE',  ( 0.2915757698887279648, 8.040595355212950324, 9.248369946372557493 ) ) ;
#40317=CARTESIAN_POINT ( 'NONE',  ( 0.2646305136544072623, 10.67138229758237777, -6.008537389229307024 ) ) ;
#40319=EDGE_CURVE ( 'NONE', #14103, #28435, #62623, .T. ) ;
#40320=ORIENTED_EDGE ( 'NONE', *, *, #13930, .T. ) ;
#40321=CARTESIAN_POINT ( 'NONE',  ( 2.899286259009673739, -6.239228647238591385, 4.769992516330216148 ) ) ;
#40324=CARTESIAN_POINT ( 'NONE',  ( 1.549075743843931097, 12.34675572956519218, 2.862200647101266870 ) ) ;
#40340=ORIENTED_EDGE ( 'NONE', *, *, #28308, .F. ) ;
#40341=CARTESIAN_POINT ( 'NONE',  ( 2.273267844204866162, 0.1513603614830498212, 7.643541951623946673 ) ) ;
#40347=ORIENTED_EDGE ( 'NONE', *, *, #43612, .T. ) ;
#40355=CARTESIAN_POINT ( 'NONE',  ( 0.2653519890518156177, 6.123091032184292182, -10.60552241699060794 ) ) ;
#40357=CARTESIAN_POINT ( 'NONE',  ( 0.2651627923886321070, 4.271101819784510312, -11.47719387551881987 ) ) ;
#40360=CARTESIAN_POINT ( 'NONE',  ( 0.2650492594609249464, -12.04046128294316631, -2.234872523101302466 ) ) ;
#40367=ORIENTED_EDGE ( 'NONE', *, *, #40388, .T. ) ;
#40371=VECTOR ( 'NONE', #2606, 1000.000000000000114 ) ;
#40372=CARTESIAN_POINT ( 'NONE',  ( 2.507146904658100972, 7.640248566386913076, -1.127530020444418746 ) ) ;
#40374=CARTESIAN_POINT ( 'NONE',  ( 0.9296196016823207176, -2.573053270830310435, 12.19921892949957964 ) ) ;
#40375=CARTESIAN_POINT ( 'NONE',  ( 2.305787727787083519, 5.970480882365222897, 4.792270232040915623 ) ) ;
#40385=CARTESIAN_POINT ( 'NONE',  ( 0.3675815128205894289, 10.50067073900660652, -6.367184624550055183 ) ) ;
#40386=CARTESIAN_POINT ( 'NONE',  ( 2.241509619876138171, 1.287997509666571005, 7.525055189891909357 ) ) ;
#40388=EDGE_CURVE ( 'NONE', #64491, #38510, #56275, .T. ) ;
#40397=ADVANCED_FACE ( 'NONE', ( #11590 ), #49535, .F. ) ;
#40399=CARTESIAN_POINT ( 'NONE',  ( 2.260457164927184071, 7.499412009325160611, -1.462935478981523207 ) ) ;
#40404=AXIS2_PLACEMENT_3D ( 'NONE', #16520, #31475, #58313 ) ;
#40406=CARTESIAN_POINT ( 'NONE',  ( 2.241352910868910531, 5.901537464758519036, -4.843133558968066410 ) ) ;
#40410=CARTESIAN_POINT ( 'NONE',  ( 2.573738926104376823, -0.2352053552897994393, 7.741646296020606499 ) ) ;
#40418=CARTESIAN_POINT ( 'NONE',  ( 2.305787727787083519, -7.135468203930003028, 2.774453000917123990 ) ) ;
#40419=EDGE_LOOP ( 'NONE', ( #38485, #53645, #14026, #46720 ) ) ;
#40422=CARTESIAN_POINT ( 'NONE',  ( 5.515539859299206427, 0.004509673239148338786, 0.004037661319610840079 ) ) ;
#40434=FACE_OUTER_BOUND ( 'NONE', #45271, .T. ) ;
#40442=CARTESIAN_POINT ( 'NONE',  ( 0.3053067050349180800, -11.43920902168903631, -4.409108891833770194 ) ) ;
#40444=CARTESIAN_POINT ( 'NONE',  ( 2.241509619876138171, 2.647089031563667483, -7.160887714159589912 ) ) ;
#40449=EDGE_LOOP ( 'NONE', ( #22842, #39392, #45066, #7404 ) ) ;
#40450=( NAMED_UNIT ( * ) SI_UNIT ( $, .STERADIAN. ) SOLID_ANGLE_UNIT ( ) );
#40458=CARTESIAN_POINT ( 'NONE',  ( 2.260457164927723639, -5.016645293558778640, -5.763213574030600306 ) ) ;
#40461=DIRECTION ( 'NONE',  ( -1.000000000000000000, 0.000000000000000000, 0.000000000000000000 ) ) ;
#40465=DIRECTION ( 'NONE',  ( -1.000000000000000000, -0.000000000000000000, -0.000000000000000000 ) ) ;
#40467=EDGE_CURVE ( 'NONE', #281, #60006, #13545, .T. ) ;
#40468=CARTESIAN_POINT ( 'NONE',  ( 2.241317068080780128, 7.142175514530117120, -2.696905536171223083 ) ) ;
#40470=CARTESIAN_POINT ( 'NONE',  ( 2.241352910868908310, 7.202080440908741998, 2.532612177304466972 ) ) ;
#40475=EDGE_LOOP ( 'NONE', ( #2174, #28585, #61966, #10760 ) ) ;
#40476=CARTESIAN_POINT ( 'NONE',  ( 0.7446945582518929019, -11.77484212699360455, 3.906659168236906954 ) ) ;
#40482=CARTESIAN_POINT ( 'NONE',  ( 0.2648978790185602672, 4.312320170909236694, 11.46165506714229565 ) ) ;
#40496=CARTESIAN_POINT ( 'NONE',  ( 2.781367136452037592, -7.743208838465379884, -1.052455537429842769 ) ) ;
#40498=ORIENTED_EDGE ( 'NONE', *, *, #65634, .T. ) ;
#40504=CARTESIAN_POINT ( 'NONE',  ( 2.241528039335008327, -6.603755931420462133, -3.830846649711583840 ) ) ;
#40508=CARTESIAN_POINT ( 'NONE',  ( 0.3665391374699467075, 12.13918562134721668, -1.872534962004676728 ) ) ;
#40512=CARTESIAN_POINT ( 'NONE',  ( 0.3675815128205894289, -0.2638082659427565813, -12.27743992903066328 ) ) ;
#40524=FACE_OUTER_BOUND ( 'NONE', #9448, .T. ) ;
#40527=CARTESIAN_POINT ( 'NONE',  ( 1.719304012338836563, -7.017415949612288095, 10.62216384465580710 ) ) ;
#40528=CARTESIAN_POINT ( 'NONE',  ( 1.287602823388476647, 11.16629420487894642, -5.809161206979844394 ) ) ;
#40529=CARTESIAN_POINT ( 'NONE',  ( 0.6511581176963597839, -12.37037447926123690, -0.3309006379877566517 ) ) ;
#40530=VERTEX_POINT ( 'NONE', #7939 ) ;
#40532=CARTESIAN_POINT ( 'NONE',  ( 3.152665057734079568, -2.258875078502220024, -7.609997527621126245 ) ) ;
#40534=CARTESIAN_POINT ( 'NONE',  ( 0.9232167919969109793, -2.570564963838065431, -12.19756235544081591 ) ) ;
#40546=CARTESIAN_POINT ( 'NONE',  ( 2.368238019615203971, 7.150288915654831712, -2.793778585134612413 ) ) ;
#40564=CARTESIAN_POINT ( 'NONE',  ( 1.633930747250415205, 11.34237452761254694, 5.718685543473949195 ) ) ;
#40569=ORIENTED_EDGE ( 'NONE', *, *, #14469, .T. ) ;
#40570=CARTESIAN_POINT ( 'NONE',  ( 0.2648321136542706733, -10.67551415837654361, 5.999882851577440057 ) ) ;
#40585=CARTESIAN_POINT ( 'NONE',  ( 2.290907136832899482, -3.684064771923272197, -6.705538900522698853 ) ) ;
#40593=EDGE_CURVE ( 'NONE', #38861, #57898, #29189, .T. ) ;
#40594=CARTESIAN_POINT ( 'NONE',  ( 0.3006302518451990924, 12.25587491745531032, -0.2259616664572675626 ) ) ;
#40595=CONICAL_SURFACE ( 'NONE', #11923, 7.938172270156617749, 1.280189991382167047 ) ;
#40597=EDGE_CURVE ( 'NONE', #29543, #30254, #38729, .T. ) ;
#40598=CARTESIAN_POINT ( 'NONE',  ( 0.2650492594609225594, -2.234872523101260278, 12.04046128294317342 ) ) ;
#40599=CARTESIAN_POINT ( 'NONE',  ( 1.948354844646953188, -1.364409644999331039, 11.88693049004095670 ) ) ;
#40600=CARTESIAN_POINT ( 'NONE',  ( 2.261269890822069861, 0.1394916642590906530, -7.639767381742373686 ) ) ;
#40609=CARTESIAN_POINT ( 'NONE',  ( 2.298277635560819654, -1.166137492762092887, -7.564013289873369850 ) ) ;
#40615=CARTESIAN_POINT ( 'NONE',  ( 5.515188684475870851, 0.0003622115669626745408, 0.005339000964282161928 ) ) ;
#40621=CARTESIAN_POINT ( 'NONE',  ( 2.941278708680199916, -0.1348063076487378276, 6.138172921908580548 ) ) ;
#40627=ORIENTED_EDGE ( 'NONE', *, *, #55234, .T. ) ;
#40632=CARTESIAN_POINT ( 'NONE',  ( 0.4613984246114877785, -8.128335150814447019, -9.246873830555978557 ) ) ;
#40634=CARTESIAN_POINT ( 'NONE',  ( 5.514970785353741078, 0.002796696073589870733, 0.003805873180274323229 ) ) ;
#40638=CARTESIAN_POINT ( 'NONE',  ( 0.3109076770649020771, -12.25911371383827841, 0.2359198520040733382 ) ) ;
#40639=CARTESIAN_POINT ( 'NONE',  ( 1.719304012341583476, 7.581471372739232883, -10.22720798541541498 ) ) ;
#40641=CARTESIAN_POINT ( 'NONE',  ( 2.034671305879987013, -4.647127512369094937, 10.71175679137298609 ) ) ;
#40643=ORIENTED_EDGE ( 'NONE', *, *, #56850, .F. ) ;
#40646=ORIENTED_EDGE ( 'NONE', *, *, #17127, .T. ) ;
#40652=CARTESIAN_POINT ( 'NONE',  ( 0.3675815128205894289, -12.27743992903066328, 0.2638082659427993804 ) ) ;
#40653=CARTESIAN_POINT ( 'NONE',  ( 0.2671309869109484980, 6.263183022891178453, 10.52409658627918532 ) ) ;
#40658=ORIENTED_EDGE ( 'NONE', *, *, #47038, .T. ) ;
#40661=CARTESIAN_POINT ( 'NONE',  ( 2.491965175173379343, 0.2120508241295852025, 7.715025372670630155 ) ) ;
#40677=CARTESIAN_POINT ( 'NONE',  ( 0.2653519991613807472, 2.148211862903072866, -12.05632699103096783 ) ) ;
#40679=CARTESIAN_POINT ( 'NONE',  ( 1.634816307077032960, -3.661851000130445399, -12.16351623921555181 ) ) ;
#40683=B_SPLINE_CURVE_WITH_KNOTS ( 'NONE', 3,
 ( #22931, #43185, #63458, #23242, #43503, #63785, #59800, #19572, #64441, #34819, #34187, #19234, #4615, #43851, #54495, #49193 ),
 .UNSPECIFIED., .F., .F.,
 ( 4, 3, 3, 3, 3, 4 ),
 ( 0.000000000000000000, 0.0002999043160757414064, 0.0005998071753051159626, 0.0008997092107374784131, 0.001204458948196456295, 0.001510329163478117687 ),
 .UNSPECIFIED. ) ;
#40691=ORIENTED_EDGE ( 'NONE', *, *, #10949, .F. ) ;
#40702=CARTESIAN_POINT ( 'NONE',  ( 2.889800649504073782, -6.039722463373545125, 0.9965440656173527589 ) ) ;
#40704=CARTESIAN_POINT ( 'NONE',  ( 5.515188684475870851, -0.004804816249379324430, -0.002355816063606793170 ) ) ;
#40711=VECTOR ( 'NONE', #64401, 1000.000000000000000 ) ;
#40721=CARTESIAN_POINT ( 'NONE',  ( 2.080613030138687147, 0.000000000000000000, 0.000000000000000000 ) ) ;
#40728=CIRCLE ( 'NONE', #46061, 12.73084802173761787 ) ;
#40732=DIRECTION ( 'NONE',  ( -0.3939253465568944290, -0.7103112711423410497, -0.5833358547425164797 ) ) ;
#40733=CARTESIAN_POINT ( 'NONE',  ( 2.941278708680199916, -2.952340773940071550, -5.383216837018973244 ) ) ;
#40734=CARTESIAN_POINT ( 'NONE',  ( 1.014383007554945815, -12.22116704270658971, 2.605923236272090993 ) ) ;
#40744=EDGE_CURVE ( 'NONE', #48793, #42095, #45443, .T. ) ;
#40748=EDGE_CURVE ( 'NONE', #64826, #30538, #62501, .T. ) ;
#40750=B_SPLINE_CURVE_WITH_KNOTS ( 'NONE', 3,
 ( #14687, #5403, #424, #9717, #4772, #30004, #35312, #45968, #5748, #10059, #45303, #20693, #24700, #40638, #61247, #35642, #40298, #64915, #39660, #55624, #55937, #9378 ),
 .UNSPECIFIED., .F., .F.,
 ( 4, 3, 3, 3, 3, 3, 3, 4 ),
 ( 1.149970062512530604E-18, 4.449119708436735838E-05, 6.626296329540299560E-05, 8.803456484962497708E-05, 0.0001098060367612783733, 0.0001315774408628487678, 0.0001760698110411146094, 0.0001829697163287828600 ),
 .UNSPECIFIED. ) ;
#40751=CARTESIAN_POINT ( 'NONE',  ( 5.514970785353741078, 0.004694330894494710971, 0.0005190732562555225478 ) ) ;
#40752=EDGE_CURVE ( 'NONE', #5409, #16864, #25167, .T. ) ;
#40763=B_SPLINE_CURVE_WITH_KNOTS ( 'NONE', 3,
 ( #52561, #63804, #37576, #16957, #8296, #28566, #27927, #48236, #7987, #52864, #23256, #22615, #2685, #58870, #6989, #63167 ),
 .UNSPECIFIED., .F., .F.,
 ( 4, 3, 3, 3, 3, 4 ),
 ( 2.710505431213761085E-19, 0.0003017745587525226449, 0.0006035491769808692952, 0.0009053241094668096345, 0.001207275924541012166, 0.001510325902535038321 ),
 .UNSPECIFIED. ) ;
#40769=DIRECTION ( 'NONE',  ( 0.000000000000000000, 0.000000000000000000, 1.000000000000000000 ) ) ;
#40770=CARTESIAN_POINT ( 'NONE',  ( 3.100650473569588783, 6.622643684997381541, 4.345221797103435257 ) ) ;
#40771=EDGE_CURVE ( 'NONE', #29925, #59870, #5415, .T. ) ;
#40784=CARTESIAN_POINT ( 'NONE',  ( 2.781367136452309818, -7.442815111163310959, -2.381060477055452651 ) ) ;
#40787=ADVANCED_FACE ( 'NONE', ( #26473 ), #56296, .F. ) ;
#40792=( BOUNDED_SURFACE ( )  B_SPLINE_SURFACE ( 3, 1, ( 
 ( #62007, #37041 ),
 ( #58009, #31720 ),
 ( #53004, #7434 ),
 ( #51714, #6155 ) ),
 .UNSPECIFIED., .F., .F., .F. ) 
 B_SPLINE_SURFACE_WITH_KNOTS ( ( 4, 4 ),
 ( 2, 2 ),
 ( 0.000000000000000000, 1.000000000000000000 ),
 ( 0.000000000000000000, 1.000000000000000000 ),
 .UNSPECIFIED. ) 
 GEOMETRIC_REPRESENTATION_ITEM ( )  RATIONAL_B_SPLINE_SURFACE ( (
 ( 1.000000000000000000, 1.000000000000000000),
 ( 0.6933888150995267674, 0.9895912004443193632),
 ( 0.6933888150995267674, 0.9895912004443193632),
 ( 1.000000000000000000, 1.000000000000000000) ) ) 
 REPRESENTATION_ITEM ( '' )  SURFACE ( )  );
#40794=EDGE_CURVE ( 'NONE', #59884, #41431, #23673, .T. ) ;
#40796=CARTESIAN_POINT ( 'NONE',  ( 0.2646305136544072623, 10.53923716745246963, 6.237419468587114046 ) ) ;
#40801=CARTESIAN_POINT ( 'NONE',  ( 2.844750968616289732, 1.686994672842381693, 7.651810733888897431 ) ) ;
#40810=CARTESIAN_POINT ( 'NONE',  ( 2.280717697723834814, -7.238333660707024109, -2.468022724683533564 ) ) ;
#40817=CARTESIAN_POINT ( 'NONE',  ( 2.257661810676420799, 7.131864446283263881, -2.739276463085611901 ) ) ;
#40818=EDGE_CURVE ( 'NONE', #48048, #5162, #62368, .T. ) ;
#40819=CARTESIAN_POINT ( 'NONE',  ( 0.2653141334712582622, -10.58342934917116018, 6.161213243425222252 ) ) ;
#40820=CARTESIAN_POINT ( 'NONE',  ( 0.3675815128205894289, 11.62724744438065727, 3.951233083390508050 ) ) ;
#40824=CARTESIAN_POINT ( 'NONE',  ( 5.530133899448235191, 0.006998616117864070972, -0.01437126147332074694 ) ) ;
#40840=CARTESIAN_POINT ( 'NONE',  ( 5.514970785353741078, 0.002619824551223701864, 0.003929719953530115030 ) ) ;
#40841=CARTESIAN_POINT ( 'NONE',  ( 2.491965175173920688, -7.634639040875003779, -1.130870800982851865 ) ) ;
#40844=ORIENTED_EDGE ( 'NONE', *, *, #46160, .T. ) ;
#40852=CARTESIAN_POINT ( 'NONE',  ( 2.241352910868908310, 2.689314586382351546, 7.145045428366586293 ) ) ;
#40855=ORIENTED_EDGE ( 'NONE', *, *, #33952, .T. ) ;
#40856=CARTESIAN_POINT ( 'NONE',  ( 0.2648978790185602672, -0.1321385342561549048, -12.24533305150758267 ) ) ;
#40861=ORIENTED_EDGE ( 'NONE', *, *, #5390, .F. ) ;
#40863=CARTESIAN_POINT ( 'NONE',  ( 0.2638984909335716500, -1.930290337333974593, -12.09426044257626209 ) ) ;
#40865=ORIENTED_EDGE ( 'NONE', *, *, #24074, .T. ) ;
#40867=CARTESIAN_POINT ( 'NONE',  ( 2.241352910868909643, -7.145045428366594287, 2.689314586382326677 ) ) ;
#40868=CARTESIAN_POINT ( 'NONE',  ( 1.937114397841932290, 10.63710405811933946, 7.182898292393801398 ) ) ;
#40869=CARTESIAN_POINT ( 'NONE',  ( 1.287602823384980555, 9.277923463524217595, 8.506034117234060332 ) ) ;
#40872=CARTESIAN_POINT ( 'NONE',  ( 0.5572780756290610649, 10.83930267798936420, -5.905274004878195093 ) ) ;
#40891=CARTESIAN_POINT ( 'NONE',  ( 3.152665057734129750, -7.102135024645910732, 3.546019893116286958 ) ) ;
#40893=CARTESIAN_POINT ( 'NONE',  ( 0.9232167919969109793, -11.84868134597554423, -3.872606616958390369 ) ) ;
#40913=CARTESIAN_POINT ( 'NONE',  ( 0.8375941296816821202, -10.57337970710580599, -6.548446001456700749 ) ) ;
#40921=CARTESIAN_POINT ( 'NONE',  ( 2.241311220309521790, -3.736531646286333164, -6.657499176698745913 ) ) ;
#40928=CARTESIAN_POINT ( 'NONE',  ( 2.903928887688524529, 2.041797854847264393, 8.528865300111828418 ) ) ;
#40929=CARTESIAN_POINT ( 'NONE',  ( 1.719304012339844867, -12.64775761152577971, 1.452142814149586902 ) ) ;
#40930=EDGE_CURVE ( 'NONE', #46588, #646, #33259, .T. ) ;
#40931=CARTESIAN_POINT ( 'NONE',  ( 0.2834382757448002943, 12.25055062943084927, -0.2027202995057415524 ) ) ;
#40932=CARTESIAN_POINT ( 'NONE',  ( 1.937114397841935398, -5.226660192101514113, -11.72279974487468834 ) ) ;
#40933=CARTESIAN_POINT ( 'NONE',  ( 0.2652384770603652409, -2.191555293694056328, 12.04846497255942062 ) ) ;
#40934=FACE_OUTER_BOUND ( 'NONE', #10598, .T. ) ;
#40939=EDGE_CURVE ( 'NONE', #3105, #18651, #45091, .T. ) ;
#40944=CARTESIAN_POINT ( 'NONE',  ( 2.249013661412873066, -1.207748565001795393, -7.540851674529120530 ) ) ;
#40961=CARTESIAN_POINT ( 'NONE',  ( 1.462291587750005561, -10.08151577214924188, 7.633056170898021797 ) ) ;
#40962=EDGE_LOOP ( 'NONE', ( #16353, #39596, #27888, #55806 ) ) ;
#40966=CARTESIAN_POINT ( 'NONE',  ( 2.276905613633651182, 3.955794200962202911, 6.543460433228652562 ) ) ;
#40971=LINE ( 'NONE', #26996, #13991 ) ;
#40973=ORIENTED_EDGE ( 'NONE', *, *, #22089, .F. ) ;
#40976=( BOUNDED_SURFACE ( )  B_SPLINE_SURFACE ( 3, 1, ( 
 ( #49427, #60036 ),
 ( #34729, #44081 ),
 ( #64662, #13795 ),
 ( #48434, #43748 ) ),
 .UNSPECIFIED., .F., .F., .F. ) 
 B_SPLINE_SURFACE_WITH_KNOTS ( ( 4, 4 ),
 ( 2, 2 ),
 ( 0.000000000000000000, 1.000000000000000000 ),
 ( 0.000000000000000000, 1.000000000000000000 ),
 .UNSPECIFIED. ) 
 GEOMETRIC_REPRESENTATION_ITEM ( )  RATIONAL_B_SPLINE_SURFACE ( (
 ( 1.000000000000000000, 1.000000000000000000),
 ( 0.6933888150995267674, 0.9895912004443193632),
 ( 0.6933888150995267674, 0.9895912004443193632),
 ( 1.000000000000000000, 1.000000000000000000) ) ) 
 REPRESENTATION_ITEM ( '' )  SURFACE ( )  );
#40980=CARTESIAN_POINT ( 'NONE',  ( 2.963017218115631124, -5.778072204777605414, -5.350609950027729766 ) ) ;
#40983=CARTESIAN_POINT ( 'NONE',  ( 0.3675815128205912052, 11.62724744438071056, -3.951233083390353062 ) ) ;
#40990=ORIENTED_EDGE ( 'NONE', *, *, #17864, .F. ) ;
#40991=CARTESIAN_POINT ( 'NONE',  ( 3.092491956584988877, 0.4473002062003109680, 7.905533744258577578 ) ) ;
#41004=CARTESIAN_POINT ( 'NONE',  ( 0.8375941296809052972, -3.890418817177767163, -11.81283813871897692 ) ) ;
#41013=FACE_OUTER_BOUND ( 'NONE', #60229, .T. ) ;
#41014=CARTESIAN_POINT ( 'NONE',  ( 3.152665057735501097, 6.622010822086128456, -4.377619405893580229 ) ) ;
#41024=CARTESIAN_POINT ( 'NONE',  ( 0.2648978790185610999, -6.008231198269058382, 10.67083876753489946 ) ) ;
#41038=CARTESIAN_POINT ( 'NONE',  ( 2.994568964204212591, 7.825096839971888762, -0.9739368093813937088 ) ) ;
#41040=CARTESIAN_POINT ( 'NONE',  ( 1.549075743844145370, -2.862200647101428075, 12.34675572956523304 ) ) ;
#41044=ORIENTED_EDGE ( 'NONE', *, *, #29940, .F. ) ;
#41051=CARTESIAN_POINT ( 'NONE',  ( 0.9232167919969163083, -10.58277433962385494, 6.587352952801118100 ) ) ;
#41053=CARTESIAN_POINT ( 'NONE',  ( 2.241352910868908310, 1.243507963608194045, -7.532448145350496560 ) ) ;
#41054=CARTESIAN_POINT ( 'NONE',  ( 2.253265082352433613, 7.637296367516833939, 0.1282654837134977743 ) ) ;
#41058=ADVANCED_FACE ( 'NONE', ( #20108 ), #39673, .T. ) ;
#41067=CARTESIAN_POINT ( 'NONE',  ( 1.375507693220370919, 2.770709900327031239, -12.30831170622617243 ) ) ;
#41070=CARTESIAN_POINT ( 'NONE',  ( 0.2650492433740076481, 10.66007796911768857, 6.027445608088885187 ) ) ;
#41071=CARTESIAN_POINT ( 'NONE',  ( 2.969415267405037806, 0.9841783286029369693, -7.815364626284241112 ) ) ;
#41089=CARTESIAN_POINT ( 'NONE',  ( 2.491965175174208014, -7.322278065136096359, -2.439431489055742475 ) ) ;
#41090=EDGE_LOOP ( 'NONE', ( #2555, #43299, #16946, #11969 ) ) ;
#41094=CARTESIAN_POINT ( 'NONE',  ( 1.719304012341272836, -1.452142814148833949, -12.64775761152634281 ) ) ;
#41095=CARTESIAN_POINT ( 'NONE',  ( 0.3401186441510236635, -11.44115600261388188, -4.436257390736940920 ) ) ;
#41097=DIRECTION ( 'NONE',  ( 0.3939253465568944290, 0.8603393047164938912, 0.3234796780324392107 ) ) ;
#41102=CARTESIAN_POINT ( 'NONE',  ( 0.3160775863651062445, 11.43919651388225667, 4.419114254409931775 ) ) ;
#41104=CARTESIAN_POINT ( 'NONE',  ( -14.47334165536100059, 0.000000000000000000, 0.000000000000000000 ) ) ;
#41105=ORIENTED_EDGE ( 'NONE', *, *, #4315, .F. ) ;
#41118=CARTESIAN_POINT ( 'NONE',  ( 0.3665391374699464300, -8.095513416941292562, 9.237363111276737371 ) ) ;
#41124=CARTESIAN_POINT ( 'NONE',  ( 2.305787727787084407, 7.508843116234155346, 1.493241775258449255 ) ) ;
#41130=DIRECTION ( 'NONE',  ( -1.000000000000000000, -0.000000000000000000, -0.000000000000000000 ) ) ;
#41134=CARTESIAN_POINT ( 'NONE',  ( 0.2646305136544065406, 4.312539723326135110, 11.46223899740601304 ) ) ;
#41138=EDGE_CURVE ( 'NONE', #12885, #64920, #59335, .T. ) ;
#41140=CARTESIAN_POINT ( 'NONE',  ( 0.2648978790185602672, 0.1321385342562404197, 12.24533305150758089 ) ) ;
#41142=EDGE_CURVE ( 'NONE', #47440, #57990, #17304, .T. ) ;
#41143=CARTESIAN_POINT ( 'NONE',  ( 0.2653519789438765208, -12.05632450344284301, 2.148225749114954564 ) ) ;
#41144=CARTESIAN_POINT ( 'NONE',  ( 2.247112776671284173, 2.501955819907980771, -7.214825360831188306 ) ) ;
#41154=( BOUNDED_SURFACE ( )  B_SPLINE_SURFACE ( 3, 1, ( 
 ( #39853, #59486 ),
 ( #34836, #49212 ),
 ( #35170, #9251 ),
 ( #54515, #55477 ) ),
 .UNSPECIFIED., .F., .F., .F. ) 
 B_SPLINE_SURFACE_WITH_KNOTS ( ( 4, 4 ),
 ( 2, 2 ),
 ( 0.000000000000000000, 1.000000000000000000 ),
 ( 0.000000000000000000, 1.000000000000000000 ),
 .UNSPECIFIED. ) 
 GEOMETRIC_REPRESENTATION_ITEM ( )  RATIONAL_B_SPLINE_SURFACE ( (
 ( 1.000000000000000000, 1.000000000000000000),
 ( 0.9942764183789327692, 0.8450855930916585379),
 ( 0.9942764183789327692, 0.8450855930916585379),
 ( 1.000000000000000000, 1.000000000000000000) ) ) 
 REPRESENTATION_ITEM ( '' )  SURFACE ( )  );
#41155=ORIENTED_EDGE ( 'NONE', *, *, #29690, .F. ) ;
#41178=CARTESIAN_POINT ( 'NONE',  ( 2.373367633546871414, -2.455525055524842237, -7.275198254387436059 ) ) ;
#41182=CARTESIAN_POINT ( 'NONE',  ( 0.2638984909335716500, 9.508791614589302554, -7.718810690098965921 ) ) ;
#41184=EDGE_CURVE ( 'NONE', #22716, #42272, #22844, .T. ) ;
#41189=CARTESIAN_POINT ( 'NONE',  ( 5.520433897694421610, -0.009283255140285096713, -0.01186170453199835231 ) ) ;
#41190=CARTESIAN_POINT ( 'NONE',  ( 2.305787727787084407, 2.774453000917148415, 7.135468203929992370 ) ) ;
#41204=FACE_OUTER_BOUND ( 'NONE', #5376, .T. ) ;
#41215=CARTESIAN_POINT ( 'NONE',  ( 0.2647959493198551728, -7.983607158780263724, -9.285851961022039802 ) ) ;
#41217=CARTESIAN_POINT ( 'NONE',  ( 2.507146904658097863, -7.719969556433177615, -0.2163149345877387331 ) ) ;
#41232=CARTESIAN_POINT ( 'NONE',  ( 1.283627346226907884, 5.810034161408880848, -11.16434663959580398 ) ) ;
#41239=CARTESIAN_POINT ( 'NONE',  ( 1.549075743846074271, -5.743768701986616598, -11.29795072957547575 ) ) ;
#41241=CARTESIAN_POINT ( 'NONE',  ( 5.516018279890452902, -0.006707902355168857828, -0.0009545156522405044090 ) ) ;
#41248=ORIENTED_EDGE ( 'NONE', *, *, #27856, .F. ) ;
#41249=CARTESIAN_POINT ( 'NONE',  ( 0.2648978790185593790, 1.996248716311628479, 12.08224454301449313 ) ) ;
#41253=CARTESIAN_POINT ( 'NONE',  ( 0.3675815128205894289, -1.872154644482166397, 12.13672785388549613 ) ) ;
#41256=VERTEX_POINT ( 'NONE', #53977 ) ;
#41259=CARTESIAN_POINT ( 'NONE',  ( 2.639814597422739606, 7.763021810282392465, 0.2564041122425372854 ) ) ;
#41272=CARTESIAN_POINT ( 'NONE',  ( 1.459561108994217316, 7.633517148169352673, -10.08002506399590104 ) ) ;
#41275=EDGE_CURVE ( 'NONE', #44872, #53953, #31180, .T. ) ;
#41276=CARTESIAN_POINT ( 'NONE',  ( 2.889800649504073782, 1.129261637821610709, 6.016320774579811292 ) ) ;
#41289=CARTESIAN_POINT ( 'NONE',  ( 0.2911222467163508965, -4.392242282524938091, 11.44063169461054486 ) ) ;
#41292=CARTESIAN_POINT ( 'NONE',  ( 0.2647959493198550618, 7.983607158780327673, 9.285851961021984735 ) ) ;
#41296=VECTOR ( 'NONE', #63731, 1000.000000000000000 ) ;
#41303=VERTEX_POINT ( 'NONE', #20353 ) ;
#41324=CARTESIAN_POINT ( 'NONE',  ( 0.3675815128205894289, 10.50067073900651771, 6.367184624550202621 ) ) ;
#41327=ORIENTED_EDGE ( 'NONE', *, *, #33046, .F. ) ;
#41328=DIRECTION ( 'NONE',  ( 0.000000000000000000, 0.000000000000000000, 1.000000000000000000 ) ) ;
#41338=CARTESIAN_POINT ( 'NONE',  ( 2.406456491626836502, 9.333533259762544887, 4.662370073862575737 ) ) ;
#41342=ORIENTED_EDGE ( 'NONE', *, *, #42483, .T. ) ;
#41344=CARTESIAN_POINT ( 'NONE',  ( 5.514970785353741078, -0.003805873180274802012, -0.002796696073589725016 ) ) ;
#41347=CARTESIAN_POINT ( 'NONE',  ( 0.2653519789438754661, -12.06397564829376101, -2.104833950422703825 ) ) ;
#41349=CARTESIAN_POINT ( 'NONE',  ( 2.241537034860907163, -2.615577641485573146, 7.172440248506149807 ) ) ;
#41353=ORIENTED_EDGE ( 'NONE', *, *, #38040, .T. ) ;
#41360=CARTESIAN_POINT ( 'NONE',  ( 2.305787727787085295, 7.566723232958088019, -1.164987321564654676 ) ) ;
#41368=CARTESIAN_POINT ( 'NONE',  ( 5.536195898058073439, 0.006344799443923436130, 0.005656495196970911903 ) ) ;
#41375=VECTOR ( 'NONE', #25534, 1000.000000000000000 ) ;
#41387=CARTESIAN_POINT ( 'NONE',  ( 0.8375941296815080372, 2.537217542322766750, -12.17542732751335777 ) ) ;
#41397=ORIENTED_EDGE ( 'NONE', *, *, #55416, .T. ) ;
#41402=EDGE_CURVE ( 'NONE', #23822, #14988, #18004, .T. ) ;
#41405=FACE_OUTER_BOUND ( 'NONE', #30696, .T. ) ;
#41407=EDGE_LOOP ( 'NONE', ( #46414, #12819, #39121, #12174 ) ) ;
#41414=CARTESIAN_POINT ( 'NONE',  ( 5.514970785353741078, 0.004233694591582517000, -0.002093325033904037177 ) ) ;
#41415=CARTESIAN_POINT ( 'NONE',  ( 0.2648978790185584908, -7.972372351883092456, 9.295532325666423290 ) ) ;
#41418=CARTESIAN_POINT ( 'NONE',  ( 2.241506898688418126, 2.574154135948788280, -7.187425579579779011 ) ) ;
#41419=CARTESIAN_POINT ( 'NONE',  ( 1.014383007554947591, 0.4441500209063078408, 12.48801387563330145 ) ) ;
#41428=B_SPLINE_CURVE_WITH_KNOTS ( 'NONE', 3,
 ( #22403, #8431, #14391, #53675, #4100, #44014, #29365, #39672, #43336, #19405, #38698, #18086, #44320, #48368, #64286, #39010 ),
 .UNSPECIFIED., .F., .F.,
 ( 4, 3, 3, 3, 3, 4 ),
 ( 5.421010862427522170E-19, 0.0003017745587525240002, 0.0006035491769808742826, 0.0009053241094668172239, 0.001207275924540914154, 0.001510325902534833623 ),
 .UNSPECIFIED. ) ;
#41431=VERTEX_POINT ( 'NONE', #61559 ) ;
#41464=CARTESIAN_POINT ( 'NONE',  ( 5.516018279890452902, -0.003580555109620835435, 0.005752102158674384652 ) ) ;
#41465=CARTESIAN_POINT ( 'NONE',  ( 3.152665057736256493, -0.9030954876717440793, 7.886634106564762270 ) ) ;
#41466=CARTESIAN_POINT ( 'NONE',  ( 1.372161826076670588, -10.03232826862084082, -7.648244077827061282 ) ) ;
#41469=CARTESIAN_POINT ( 'NONE',  ( 5.516018279890452902, 0.0009545156522404378389, -0.006707902355168868236 ) ) ;
#41476=CARTESIAN_POINT ( 'NONE',  ( 0.2648978790185584908, 6.237101853238694815, -10.53870023327857197 ) ) ;
#41484=CARTESIAN_POINT ( 'NONE',  ( 2.241449424704146764, 7.194804211893846002, 2.553400830064003646 ) ) ;
#41485=CARTESIAN_POINT ( 'NONE',  ( 5.514970785353741078, -0.003929719953530087274, -0.002619824551223206600 ) ) ;
#41492=CARTESIAN_POINT ( 'NONE',  ( 0.2655924914740778187, 7.905499957109361375, -9.352877839710522778 ) ) ;
#41497=CARTESIAN_POINT ( 'NONE',  ( 2.080613030138687147, 0.000000000000000000, 0.000000000000000000 ) ) ;
#41500=EDGE_CURVE ( 'NONE', #48647, #39184, #52165, .T. ) ;
#41503=EDGE_LOOP ( 'NONE', ( #50875, #12456, #39727, #7288 ) ) ;
#41505=CARTESIAN_POINT ( 'NONE',  ( 2.770579946183338471, -2.384572752174033639, -7.437949029067715934 ) ) ;
#41526=EDGE_LOOP ( 'NONE', ( #18194, #26643, #370, #6788 ) ) ;
#41531=CARTESIAN_POINT ( 'NONE',  ( 0.4626703367442792092, 11.46957824750455046, 4.475905684073717694 ) ) ;
#41534=CARTESIAN_POINT ( 'NONE',  ( 2.258463476536644254, 2.740340677911331291, -7.131741622455316509 ) ) ;
#41545=CARTESIAN_POINT ( 'NONE',  ( 0.3537226245948356662, -2.388187631842599412, 12.04110684114372276 ) ) ;
#41554=CARTESIAN_POINT ( 'NONE',  ( 2.177405672432020545, 4.457418613955601572, 10.27382588316165624 ) ) ;
#41557=VECTOR ( 'NONE', #4076, 1000.000000000000114 ) ;
#41564=CARTESIAN_POINT ( 'NONE',  ( 0.2648321136542706178, 2.265911310221971231, -12.03456865502703188 ) ) ;
#41575=B_SPLINE_CURVE_WITH_KNOTS ( 'NONE', 3,
 ( #52263, #43232, #57577, #62866, #21981, #52595, #62213, #11996, #27290, #47276, #42234, #52894, #1717 ),
 .UNSPECIFIED., .F., .F.,
 ( 4, 3, 3, 3, 4 ),
 ( 3.878959614448865017E-18, 6.607593386745471407E-05, 0.0001321518677373519459, 0.0001982171734706200195, 0.0002642860854759489881 ),
 .UNSPECIFIED. ) ;
#41577=CARTESIAN_POINT ( 'NONE',  ( 5.530133899448235191, -0.01149180883054537645, -0.01111090067015099367 ) ) ;
#41583=CARTESIAN_POINT ( 'NONE',  ( 2.556980015514067173, -6.584367695372273843, 4.067895092073629648 ) ) ;
#41588=CARTESIAN_POINT ( 'NONE',  ( 0.3610902822527252143, -1.873269382026075291, 12.13436647668549995 ) ) ;
#41592=ORIENTED_EDGE ( 'NONE', *, *, #19539, .T. ) ;
#41604=CARTESIAN_POINT ( 'NONE',  ( 2.280717697724240267, 4.794838658390990105, -5.957695241725613933 ) ) ;
#41606=CARTESIAN_POINT ( 'NONE',  ( 2.241311220309654129, 7.141707286456011161, 2.698144003945220692 ) ) ;
#41607=ORIENTED_EDGE ( 'NONE', *, *, #22497, .F. ) ;
#41609=CARTESIAN_POINT ( 'NONE',  ( 2.241352910868910531, 5.901537464758454199, 4.843133558968147234 ) ) ;
#41611=CARTESIAN_POINT ( 'NONE',  ( 2.889800649504073782, -5.774917447012985150, -2.030191121417194378 ) ) ;
#41616=CARTESIAN_POINT ( 'NONE',  ( 2.241536586108913376, -6.608496983003814940, 3.822683724643440417 ) ) ;
#41628=CARTESIAN_POINT ( 'NONE',  ( 1.459561108993356005, -12.62847742794678929, 0.6317018236574121204 ) ) ;
#41629=CARTESIAN_POINT ( 'NONE',  ( 1.020182472824462394, 11.88926988382094230, -3.852445298735137857 ) ) ;
#41631=LINE ( 'NONE', #33214, #47594 ) ;
#41645=B_SPLINE_CURVE_WITH_KNOTS ( 'NONE', 3,
 ( #52110, #51136, #61744, #46785, #26498, #1586, #52454, #6891, #31173, #46457, #10883, #6566, #21859, #20540, #51481, #11217 ),
 .UNSPECIFIED., .F., .F.,
 ( 4, 3, 3, 3, 3, 4 ),
 ( 0.000000000000000000, 0.0003017745587525255181, 0.0006035491769808753668, 0.0009053241094668198260, 0.001207275924539022221, 0.001510325902531028074 ),
 .UNSPECIFIED. ) ;
#41650=DIRECTION ( 'NONE',  ( 0.3939253465568943180, -0.7103112711423530401, 0.5833358547425019358 ) ) ;
#41656=ADVANCED_FACE ( 'NONE', ( #43486 ), #30848, .F. ) ;
#41661=CARTESIAN_POINT ( 'NONE',  ( 0.3106921474978480147, -12.25904950202577481, -0.2354703039889393112 ) ) ;
#41663=CARTESIAN_POINT ( 'NONE',  ( 2.889800649504073782, -2.156828754871430665, -5.728825117897728525 ) ) ;
#41664=CARTESIAN_POINT ( 'NONE',  ( 0.3675815128205912052, 8.093875121226199454, -9.235491948679927177 ) ) ;
#41666=ORIENTED_EDGE ( 'NONE', *, *, #33870, .T. ) ;
#41670=ORIENTED_EDGE ( 'NONE', *, *, #52571, .T. ) ;
#41674=COLOUR_RGB ( '', 0.40784314, 0.44705882, 0.49803922) ;
#41682=DIRECTION ( 'NONE',  ( 0.000000000000000000, 0.000000000000000000, 1.000000000000000000 ) ) ;
#41685=CARTESIAN_POINT ( 'NONE',  ( 0.2651627682582908263, -6.046625184671059472, 10.64925413290591827 ) ) ;
#41689=ORIENTED_EDGE ( 'NONE', *, *, #62921, .T. ) ;
#41693=CARTESIAN_POINT ( 'NONE',  ( 2.827825597296800275, 4.031992772939004155, 8.073505504738395899 ) ) ;
#41699=CARTESIAN_POINT ( 'NONE',  ( 0.5547464869798242049, 8.164898018378810463, 9.256151063740572837 ) ) ;
#41702=CARTESIAN_POINT ( 'NONE',  ( 0.3341166715381320151, -12.03629799686216373, 2.378838837789055471 ) ) ;
#41706=CARTESIAN_POINT ( 'NONE',  ( 2.440552418640494547, 7.547055375260062426, 1.531218882877318999 ) ) ;
#41712=CARTESIAN_POINT ( 'NONE',  ( 2.241509619876138171, -7.160887714159601458, -2.647089031563641726 ) ) ;
#41718=EDGE_CURVE ( 'NONE', #28421, #13640, #4591, .T. ) ;
#41724=VECTOR ( 'NONE', #22964, 1000.000000000000114 ) ;
#41725=CARTESIAN_POINT ( 'NONE',  ( 0.3675815128205894289, 4.447030445008336663, -11.44679196252404729 ) ) ;
#41727=CARTESIAN_POINT ( 'NONE',  ( 5.516018279890452902, 0.006440244342253413461, -0.002104829434641034870 ) ) ;
#41728=CARTESIAN_POINT ( 'NONE',  ( 0.5572780756289984483, 2.443667122521743451, -12.09922454589811025 ) ) ;
#41731=EDGE_CURVE ( 'NONE', #61002, #34346, #27524, .T. ) ;
#41740=CARTESIAN_POINT ( 'NONE',  ( 1.937114397841935398, -7.182898292393691264, -10.63710405811941229 ) ) ;
#41741=( BOUNDED_SURFACE ( )  B_SPLINE_SURFACE ( 3, 1, ( 
 ( #39470, #8898 ),
 ( #18229, #9206 ),
 ( #34486, #8561 ),
 ( #43469, #38831 ) ),
 .UNSPECIFIED., .F., .F., .F. ) 
 B_SPLINE_SURFACE_WITH_KNOTS ( ( 4, 4 ),
 ( 2, 2 ),
 ( 0.000000000000000000, 1.000000000000000000 ),
 ( 0.000000000000000000, 1.000000000000000000 ),
 .UNSPECIFIED. ) 
 GEOMETRIC_REPRESENTATION_ITEM ( )  RATIONAL_B_SPLINE_SURFACE ( (
 ( 1.000000000000000000, 1.000000000000000000),
 ( 0.9942764183789327692, 0.8450855930916580938),
 ( 0.9942764183789327692, 0.8450855930916580938),
 ( 1.000000000000000000, 1.000000000000000000) ) ) 
 REPRESENTATION_ITEM ( '' )  SURFACE ( )  );
#41742=ORIENTED_EDGE ( 'NONE', *, *, #27161, .F. ) ;
#41743=CARTESIAN_POINT ( 'NONE',  ( 2.241536586108913820, 7.634468130435847932, -0.006292724672674973423 ) ) ;
#41747=CARTESIAN_POINT ( 'NONE',  ( 3.092491956585722512, 7.070043156103611892, 3.565393530441222314 ) ) ;
#41749=CARTESIAN_POINT ( 'NONE',  ( 5.514970785353741078, 0.004713149585127533910, -0.0003039746380528451919 ) ) ;
#41756=ORIENTED_EDGE ( 'NONE', *, *, #26334, .F. ) ;
#41757=CARTESIAN_POINT ( 'NONE',  ( 0.2759803524722189705, -9.504501710971656081, 7.727919584673414555 ) ) ;
#41763=CARTESIAN_POINT ( 'NONE',  ( 5.514624014163232779, -0.003946330869975260731, -0.001255375129357653909 ) ) ;
#41766=CARTESIAN_POINT ( 'NONE',  ( 2.241534463349553086, -0.005244187652451783553, 7.634462073473345711 ) ) ;
#41768=FILL_AREA_STYLE_COLOUR ( '', #6972 ) ;
#41772=CARTESIAN_POINT ( 'NONE',  ( 0.2655924914740778187, 4.229867354073712171, -11.49267051747963997 ) ) ;
#41774=CARTESIAN_POINT ( 'NONE',  ( 1.937114397841932290, 8.920887662793592909, -9.228205347192362851 ) ) ;
#41775=CARTESIAN_POINT ( 'NONE',  ( 0.2646305136544072623, 11.46223899740606100, -4.312539723326019647 ) ) ;
#41781=CARTESIAN_POINT ( 'NONE',  ( 2.781367136452208122, 7.636197200465840496, -1.659348694504450217 ) ) ;
#41784=B_SPLINE_CURVE_WITH_KNOTS ( 'NONE', 3,
 ( #47237, #1684, #21950, #27257, #42198, #1993, #62488 ),
 .UNSPECIFIED., .F., .F.,
 ( 4, 3, 4 ),
 ( 0.000000000000000000, 0.001700533616330544059, 0.005002426799371351152 ),
 .UNSPECIFIED. ) ;
#41791=CARTESIAN_POINT ( 'NONE',  ( 2.255723233588951437, 7.499053486174019234, 1.456523090672637410 ) ) ;
#41800=CARTESIAN_POINT ( 'NONE',  ( 2.262775599886258426, -3.942403752832051467, 6.546038779272026709 ) ) ;
#41802=AXIS2_PLACEMENT_3D ( 'NONE', #60674, #10780, #24429 ) ;
#41809=VERTEX_POINT ( 'NONE', #36165 ) ;
#41813=CARTESIAN_POINT ( 'NONE',  ( 0.2646305136544065406, -4.064188116014473273, -11.55263159009962592 ) ) ;
#41819=DIRECTION ( 'NONE',  ( 0.000000000000000000, 0.000000000000000000, 1.000000000000000000 ) ) ;
#41820=CARTESIAN_POINT ( 'NONE',  ( 0.4613984246114875010, -1.858723191796552987, 12.17044190070616771 ) ) ;
#41824=CARTESIAN_POINT ( 'NONE',  ( 0.2911222467163535610, 6.312159098066323359, -10.50411792397751576 ) ) ;
#41825=CARTESIAN_POINT ( 'NONE',  ( 2.263328370261528999, 2.746620058315294433, 7.131064289852348637 ) ) ;
#41828=CARTESIAN_POINT ( 'NONE',  ( 1.452237505248552996, 12.55261342181978002, -1.611965288198602408 ) ) ;
#41831=CARTESIAN_POINT ( 'NONE',  ( 2.241506898688419458, 7.187425579579805657, 2.574154135948715005 ) ) ;
#41833=CARTESIAN_POINT ( 'NONE',  ( 5.514970785353741078, 0.004694330894494369230, -0.0005190732562558711188 ) ) ;
#41836=VERTEX_POINT ( 'NONE', #26530 ) ;
#41841=DIRECTION ( 'NONE',  ( -1.000000000000000000, -0.000000000000000000, -0.000000000000000000 ) ) ;
#41844=CARTESIAN_POINT ( 'NONE',  ( 2.717984159217651907, 7.788152353088505286, -0.2836133496094412898 ) ) ;
#41845=CARTESIAN_POINT ( 'NONE',  ( 5.516018279890452902, 0.006707902355169300182, -0.0009545156522407284051 ) ) ;
#41846=CARTESIAN_POINT ( 'NONE',  ( 1.719304012343089161, 12.64775761152706401, -1.452142814147889816 ) ) ;
#41868=ORIENTED_EDGE ( 'NONE', *, *, #51474, .F. ) ;
#41870=CARTESIAN_POINT ( 'NONE',  ( 0.3654063281920718054, 4.446369912832507154, 11.44627072062580808 ) ) ;
#41884=CARTESIAN_POINT ( 'NONE',  ( 0.3401186441510233305, -2.382124782498441284, 12.03768714635923942 ) ) ;
#41885=CARTESIAN_POINT ( 'NONE',  ( 0.3665391374699472626, 11.62960183138726933, 3.952034409876334475 ) ) ;
#41894=CARTESIAN_POINT ( 'NONE',  ( 3.047904605210422169, 6.318654123925978361, -4.747272783555583686 ) ) ;
#41897=ORIENTED_EDGE ( 'NONE', *, *, #18021, .T. ) ;
#41913=CARTESIAN_POINT ( 'NONE',  ( 2.368238019615342971, -6.556525400300611928, 3.992969450835649248 ) ) ;
#41916=CARTESIAN_POINT ( 'NONE',  ( 0.3057689695767503157, -1.901059295890996870, 12.11137787899271601 ) ) ;
#41920=CARTESIAN_POINT ( 'NONE',  ( 3.047904605209668549, 7.891858004695730067, 0.4249306449412027509 ) ) ;
#41937=CARTESIAN_POINT ( 'NONE',  ( 2.241526690369556096, 4.920579984890965264, 5.837196604699864899 ) ) ;
#41942=CARTESIAN_POINT ( 'NONE',  ( 1.719304012340733934, -11.67935079956419031, -5.066286238786891438 ) ) ;
#41944=CARTESIAN_POINT ( 'NONE',  ( 0.2651627682582892165, 4.271106202749272107, 11.47719223137561961 ) ) ;
#41949=CARTESIAN_POINT ( 'NONE',  ( 5.516018279890452902, 0.006286471671801929263, -0.002527316374434327665 ) ) ;
#41951=CARTESIAN_POINT ( 'NONE',  ( 2.440552418640498100, -5.770332237304409695, -5.099602138956265129 ) ) ;
#41955=CARTESIAN_POINT ( 'NONE',  ( 5.515188684475870851, -0.001485678338381749095, -0.005140903460551130705 ) ) ;
#41958=ORIENTED_EDGE ( 'NONE', *, *, #32927, .T. ) ;
#41968=B_SPLINE_CURVE_WITH_KNOTS ( 'NONE', 3,
 ( #47248, #1694, #51254, #1026, #15961, #36252, #5360, #40931, #10999, #25631, #45923, #40594, #60887, #31284, #61860, #10649, #51585, #35603, #50913, #56210, #6032, #21292 ),
 .UNSPECIFIED., .F., .F.,
 ( 4, 3, 3, 3, 3, 3, 3, 4 ),
 ( 1.230521702633870283E-18, 4.449119708436748713E-05, 6.626296329540296850E-05, 8.803456484962499063E-05, 0.0001098060367612792814, 0.0001315774408628494997, 0.0001760698110411141487, 0.0001829697163287829684 ),
 .UNSPECIFIED. ) ;
#41969=CARTESIAN_POINT ( 'NONE',  ( 0.2915757698887307403, -4.392559307431826099, -11.44067056871812760 ) ) ;
#41977=CARTESIAN_POINT ( 'NONE',  ( 0.3401186441510253844, -5.912862694513639994, -10.75260364139051639 ) ) ;
#41987=CARTESIAN_POINT ( 'NONE',  ( 1.462291587748181465, 10.62080802716765682, 6.862867011840884324 ) ) ;
#41988=CARTESIAN_POINT ( 'NONE',  ( 0.4626703367448722348, -9.247028139127534629, -8.128802338754541168 ) ) ;
#41990=CARTESIAN_POINT ( 'NONE',  ( 2.241352910868908310, 6.569501556381442953, 3.889181972941473386 ) ) ;
#41997=ADVANCED_FACE ( 'NONE', ( #7563 ), #60573, .F. ) ;
#42000=CARTESIAN_POINT ( 'NONE',  ( 5.516018279890452902, 0.006707902355168863032, 0.0009545156522404598482 ) ) ;
#42002=CARTESIAN_POINT ( 'NONE',  ( 0.7400311444011703488, -0.3548322008126197358, -12.39937114182724720 ) ) ;
#42013=EDGE_LOOP ( 'NONE', ( #60663, #4054, #62865, #6210 ) ) ;
#42015=CARTESIAN_POINT ( 'NONE',  ( 2.241506898688419458, -4.937416071751796309, -5.822995664778306768 ) ) ;
#42022=FACE_OUTER_BOUND ( 'NONE', #13830, .T. ) ;
#42023=ORIENTED_EDGE ( 'NONE', *, *, #10374, .T. ) ;
#42024=ORIENTED_EDGE ( 'NONE', *, *, #17943, .F. ) ;
#42028=B_SPLINE_CURVE_WITH_KNOTS ( 'NONE', 3,
 ( #63454, #37553, #22249, #47535, #58499, #12931, #11617, #42510, #62809, #31887, #52206, #33212, #42186, #16940, #53523, #12271 ),
 .UNSPECIFIED., .F., .F.,
 ( 4, 3, 3, 3, 3, 4 ),
 ( 8.673617379884035472E-19, 0.0002176109881719744219, 0.0004352086762393612995, 0.0006528017811445412490, 0.0007615147961449995635, 0.0009453342004946792753 ),
 .UNSPECIFIED. ) ;
#42032=CARTESIAN_POINT ( 'NONE',  ( 1.014383007554952032, -10.59286224865785542, 6.628652139012873867 ) ) ;
#42034=DIRECTION ( 'NONE',  ( -1.000000000000000000, -0.000000000000000000, -0.000000000000000000 ) ) ;
#42044=CARTESIAN_POINT ( 'NONE',  ( 0.3106921474978497355, 4.414111574791988346, -11.43920276778352907 ) ) ;
#42045=LINE ( 'NONE', #62327, #25787 ) ;
#42048=EDGE_CURVE ( 'NONE', #20926, #27786, #54403, .T. ) ;
#42053=CARTESIAN_POINT ( 'NONE',  ( 0.3040950598368152291, -12.25911170648142701, 0.2511348647275222223 ) ) ;
#42062=CARTESIAN_POINT ( 'NONE',  ( 2.717984159219797302, 6.886544461123903282, 3.648459810929759684 ) ) ;
#42068=VECTOR ( 'NONE', #55679, 1000.000000000000114 ) ;
#42070=VERTEX_POINT ( 'NONE', #24485 ) ;
#42078=CARTESIAN_POINT ( 'NONE',  ( 0.3218525148189828045, 5.919623386703340984, 10.74192973049790645 ) ) ;
#42079=CARTESIAN_POINT ( 'NONE',  ( 0.3057689695767490945, 11.43929056598612171, -4.409323295154093714 ) ) ;
#42086=CARTESIAN_POINT ( 'NONE',  ( 2.034671305879990566, 1.331347915349286204, 11.60021725667403203 ) ) ;
#42090=CARTESIAN_POINT ( 'NONE',  ( 1.014383007554948701, -3.853787798429482603, 11.88680274101310630 ) ) ;
#42093=CARTESIAN_POINT ( 'NONE',  ( 2.305787727787085295, 7.508843116234176662, -1.493241775258346227 ) ) ;
#42095=VERTEX_POINT ( 'NONE', #19521 ) ;
#42097=CARTESIAN_POINT ( 'NONE',  ( 5.516018279890452902, -0.006771744149385743039, -0.0002248006052446425063 ) ) ;
#42102=CARTESIAN_POINT ( 'NONE',  ( 2.276198483117263027, 7.501576331167730594, 1.479169956994091706 ) ) ;
#42112=CARTESIAN_POINT ( 'NONE',  ( 0.2651627923886318294, -11.47719387551883941, -4.271101819784471232 ) ) ;
#42121=CARTESIAN_POINT ( 'NONE',  ( 0.3223008802179250232, 7.695050880595616150, -9.550960164375519312 ) ) ;
#42123=FACE_OUTER_BOUND ( 'NONE', #63033, .T. ) ;
#42130=B_SPLINE_CURVE_WITH_KNOTS ( 'NONE', 3,
 ( #57673, #48361, #7423, #2811, #7108, #17428, #63286, #48674, #22071, #23072 ),
 .UNSPECIFIED., .F., .F.,
 ( 4, 3, 3, 4 ),
 ( 2.453269466693398698E-18, 6.607638129004548514E-05, 9.911389841680599507E-05, 0.0001667630577588613897 ),
 .UNSPECIFIED. ) ;
#42134=CARTESIAN_POINT ( 'NONE',  ( 0.3665391374699464300, 6.368473106897276637, -10.50279796150429945 ) ) ;
#42138=CARTESIAN_POINT ( 'NONE',  ( 5.514624014163232779, -0.004045310349816146414, -0.0008859786816841948168 ) ) ;
#42139=CARTESIAN_POINT ( 'NONE',  ( 3.152665057734129750, 3.161213418913565221, -7.281573230474259972 ) ) ;
#42143=CARTESIAN_POINT ( 'NONE',  ( 0.3002738374340830352, 1.906042098269019824, 12.10874171309340497 ) ) ;
#42151=CARTESIAN_POINT ( 'NONE',  ( 2.288423627607476973, -1.169285315515829371, 7.560204962263195938 ) ) ;
#42154=CARTESIAN_POINT ( 'NONE',  ( 2.990245332647867738, -5.834301250882223400, 6.155689586375181044 ) ) ;
#42159=CARTESIAN_POINT ( 'NONE',  ( 5.536195898058073439, 0.007896796515810928022, -0.003145317580921069833 ) ) ;
#42162=CARTESIAN_POINT ( 'NONE',  ( 3.152665057734128862, 2.258875078502223133, 7.609997527621164437 ) ) ;
#42176=EDGE_CURVE ( 'NONE', #46588, #35243, #36938, .T. ) ;
#42179=CARTESIAN_POINT ( 'NONE',  ( 5.520433897694421610, -0.01397038704729910638, 0.005630909886753099683 ) ) ;
#42181=B_SPLINE_CURVE_WITH_KNOTS ( 'NONE', 3,
 ( #5718, #52250, #1377, #21662, #35925, #11015, #46584, #36270, #7008, #47264, #46273, #56913, #41916, #6690, #62515, #27278, #2017, #26303, #41588, #51598, #1704, #41253 ),
 .UNSPECIFIED., .F., .F.,
 ( 4, 3, 3, 3, 3, 3, 3, 4 ),
 ( 8.741117365843378158E-19, 4.449119708436956745E-05, 6.626296329540612624E-05, 8.803456484962883955E-05, 0.0001098060367612828321, 0.0001315774408628544599, 0.0001760698110411208165, 0.0001829697163287820740 ),
 .UNSPECIFIED. ) ;
#42182=ORIENTED_EDGE ( 'NONE', *, *, #47973, .T. ) ;
#42186=CARTESIAN_POINT ( 'NONE',  ( 2.994568964204062489, 4.756002438591091064, 6.289764245798157738 ) ) ;
#42187=CARTESIAN_POINT ( 'NONE',  ( 2.244591118396912055, 3.724266936772022696, -6.665613643997293281 ) ) ;
#42188=CARTESIAN_POINT ( 'NONE',  ( 0.3006302518452043104, -8.051021221755712887, -9.243299516615106626 ) ) ;
#42189=CARTESIAN_POINT ( 'NONE',  ( 20.00005080000000035, 0.000000000000000000, 1.000000000000000000 ) ) ;
#42194=CARTESIAN_POINT ( 'NONE',  ( 0.2646305136544072623, 12.08286001766538398, -1.996350543472872996 ) ) ;
#42195=AXIS2_PLACEMENT_3D ( 'NONE', #44170, #49186, #47860 ) ;
#42196=ORIENTED_EDGE ( 'NONE', *, *, #13468, .T. ) ;
#42198=CARTESIAN_POINT ( 'NONE',  ( 2.350038591457881409, 10.18214835919976302, -3.024612895785611766 ) ) ;
#42203=CARTESIAN_POINT ( 'NONE',  ( 0.3537226245948345005, 2.388187631842678016, -12.04110684114370677 ) ) ;
#42211=VERTEX_POINT ( 'NONE', #1197 ) ;
#42212=CARTESIAN_POINT ( 'NONE',  ( 3.031336079628962121, -0.4165536638489777954, -7.886784934834683014 ) ) ;
#42213=CARTESIAN_POINT ( 'NONE',  ( 1.462291587750754296, -5.766456054323672475, -11.25382118863359260 ) ) ;
#42228=EDGE_CURVE ( 'NONE', #12898, #11089, #12323, .T. ) ;
#42230=CARTESIAN_POINT ( 'NONE',  ( 3.152665057734079568, -2.258875078502220024, -7.609997527621126245 ) ) ;
#42234=CARTESIAN_POINT ( 'NONE',  ( 0.2651627682582922141, 11.47719223137565869, -4.271106202749156644 ) ) ;
#42237=VERTEX_POINT ( 'NONE', #11479 ) ;
#42241=EDGE_CURVE ( 'NONE', #53890, #8677, #58398, .T. ) ;
#42243=AXIS2_PLACEMENT_3D ( 'NONE', #18757, #22763, #43340 ) ;
#42245=CARTESIAN_POINT ( 'NONE',  ( 1.719304012340734822, -3.626341562669572305, -12.20344780066098345 ) ) ;
#42251=ORIENTED_EDGE ( 'NONE', *, *, #35784, .F. ) ;
#42255=CARTESIAN_POINT ( 'NONE',  ( 5.530133899448235191, 0.01550764871776215935, 0.003876417824003496135 ) ) ;
#42256=CARTESIAN_POINT ( 'NONE',  ( 2.263328370259784172, 6.687792802425356342, 3.697218830765363951 ) ) ;
#42258=CARTESIAN_POINT ( 'NONE',  ( 1.633930747251838511, -12.68212725188740286, 0.7186603069036878733 ) ) ;
#42261=B_SPLINE_CURVE_WITH_KNOTS ( 'NONE', 3,
 ( #57533, #53537, #53850, #23251, #7980, #28246, #47872, #48540, #2990, #28561, #48863, #32237, #62822, #22259, #3318, #52554, #40157, #44491, #54169 ),
 .UNSPECIFIED., .F., .F.,
 ( 4, 3, 3, 3, 3, 3, 4 ),
 ( 7.884170296961029399E-18, 4.457896483014810721E-05, 6.639290541542139964E-05, 8.820687556478942857E-05, 0.0001100173248778936035, 0.0001545671401658124818, 0.0001830328308068588749 ),
 .UNSPECIFIED. ) ;
#42264=FACE_OUTER_BOUND ( 'NONE', #33469, .T. ) ;
#42267=CARTESIAN_POINT ( 'NONE',  ( 3.152665057735657861, -7.609997527621795932, -2.258875078500884204 ) ) ;
#42271=CARTESIAN_POINT ( 'NONE',  ( 2.889800649504073782, 6.039722463373554007, -0.9965440656173106815 ) ) ;
#42272=VERTEX_POINT ( 'NONE', #47725 ) ;
#42273=CARTESIAN_POINT ( 'NONE',  ( 5.514970785353741078, -0.004324946436530292468, 0.001897634820904997880 ) ) ;
#42277=CARTESIAN_POINT ( 'NONE',  ( 1.719304012338836563, 0.7661785589583339773, 12.70777170743865980 ) ) ;
#42281=CARTESIAN_POINT ( 'NONE',  ( 5.514624014163232779, -0.002216125254993689137, -0.003498325728817801728 ) ) ;
#42282=CARTESIAN_POINT ( 'NONE',  ( 1.104777566491138785, 4.729982681549531165, 11.59867774809546148 ) ) ;
#42292=CARTESIAN_POINT ( 'NONE',  ( 1.719304012339819332, -7.581471372739574832, 10.22720798541442555 ) ) ;
#42293=CARTESIAN_POINT ( 'NONE',  ( 1.020182472824409547, -9.280950437305058642, -8.370187102470554308 ) ) ;
#42309=EDGE_LOOP ( 'NONE', ( #46029, #59271, #10708, #28674 ) ) ;
#42310=CARTESIAN_POINT ( 'NONE',  ( 0.3675815128205894289, -7.689697408877338880, 9.574637318041938627 ) ) ;
#42314=CARTESIAN_POINT ( 'NONE',  ( 1.937114397841932290, -7.182898292393840478, 10.63710405811931459 ) ) ;
#42319=CARTESIAN_POINT ( 'NONE',  ( 0.2652384529303148941, 9.338494547402500956, -7.922180393770576146 ) ) ;
#42326=CARTESIAN_POINT ( 'NONE',  ( 1.283627346226357879, 8.503905436511839611, 9.278077665801896856 ) ) ;
#42332=ORIENTED_EDGE ( 'NONE', *, *, #23821, .F. ) ;
#42333=CARTESIAN_POINT ( 'NONE',  ( 0.2706063244538028933, 12.03021891034991064, 2.299194104693123020 ) ) ;
#42339=CARTESIAN_POINT ( 'NONE',  ( 1.104777566491149221, -10.60111489796739193, 6.672212870706169419 ) ) ;
#42340=CARTESIAN_POINT ( 'NONE',  ( 2.241449424704145876, -7.194804211893830015, -2.553400830064051164 ) ) ;
#42348=CARTESIAN_POINT ( 'NONE',  ( 0.2676618633000484859, 4.339362305359601990, -11.45242956837282655 ) ) ;
#42353=VECTOR ( 'NONE', #2668, 999.9999999999998863 ) ;
#42354=CARTESIAN_POINT ( 'NONE',  ( 0.2652384529303158933, 12.04846370803831412, -2.191562200667060978 ) ) ;
#42356=ORIENTED_EDGE ( 'NONE', *, *, #29940, .T. ) ;
#42358=CARTESIAN_POINT ( 'NONE',  ( 0.2648978790185584908, -1.996248716311547433, -12.08224454301450734 ) ) ;
#42361=CARTESIAN_POINT ( 'NONE',  ( 2.305787727787084407, -1.493241775258372872, -7.508843116234172221 ) ) ;
#42371=CARTESIAN_POINT ( 'NONE',  ( 1.459561108993789880, -12.54631635028882286, -1.570807238540975037 ) ) ;
#42374=CARTESIAN_POINT ( 'NONE',  ( 0.2646305136544072623, -10.67138229758225343, -6.008537389229529957 ) ) ;
#42375=EDGE_CURVE ( 'NONE', #33979, #11407, #23406, .T. ) ;
#42384=CARTESIAN_POINT ( 'NONE',  ( 2.241537034860907607, 7.519304283075095796, -1.321063441155912788 ) ) ;
#42385=CARTESIAN_POINT ( 'NONE',  ( 2.941278708680199916, -1.972702289976042023, 5.814102272488581136 ) ) ;
#42399=CARTESIAN_POINT ( 'NONE',  ( 2.889800649504073782, 3.882893708502110908, -4.732281052280274736 ) ) ;
#42408=EDGE_LOOP ( 'NONE', ( #22091, #34705, #56183, #33989 ) ) ;
#42422=CARTESIAN_POINT ( 'NONE',  ( 1.719304012338199517, 0.000000000000000000, 0.000000000000000000 ) ) ;
#42426=CARTESIAN_POINT ( 'NONE',  ( 2.242819959140646802, -3.905785747113969641, 6.560218843829765056 ) ) ;
#42427=B_SPLINE_CURVE_WITH_KNOTS ( 'NONE', 3,
 ( #60792, #9566, #65432, #45482, #65747, #20219, #40496, #15229, #35512, #55811, #10237, #30514, #40841, #50817, #25533, #21875 ),
 .UNSPECIFIED., .F., .F.,
 ( 4, 3, 3, 3, 3, 4 ),
 ( 2.346432215325189512E-15, 0.0002126834539179932228, 0.0004253519300366710764, 0.0006380165497224839352, 0.0007442707582429045543, 0.0009453531351412929181 ),
 .UNSPECIFIED. ) ;
#42438=CARTESIAN_POINT ( 'NONE',  ( 5.515539859299206427, 0.005751553894235443033, 0.001886660928063796675 ) ) ;
#42439=CARTESIAN_POINT ( 'NONE',  ( 2.259830038564998755, 1.462175769136944581, -7.499347412930710277 ) ) ;
#42441=CARTESIAN_POINT ( 'NONE',  ( 0.2647959493198550618, 12.08462848595695149, 1.981611532097588446 ) ) ;
#42443=ADVANCED_FACE ( 'NONE', ( #53212 ), #13011, .F. ) ;
#42454=CARTESIAN_POINT ( 'NONE',  ( 2.034671305880519476, 11.35598636043232190, 2.716450156983679420 ) ) ;
#42457=CARTESIAN_POINT ( 'NONE',  ( 1.462291587748163257, 12.62932306616532152, 0.6330131614645532201 ) ) ;
#42458=ADVANCED_FACE ( 'NONE', ( #2359 ), #37201, .T. ) ;
#42459=CARTESIAN_POINT ( 'NONE',  ( 0.2759803524722214130, -11.57441428600635902, 4.011137970318905843 ) ) ;
#42462=ORIENTED_EDGE ( 'NONE', *, *, #6213, .F. ) ;
#42469=CARTESIAN_POINT ( 'NONE',  ( 1.719304012342639965, 12.38166659047149487, -2.961219984262613458 ) ) ;
#42472=CARTESIAN_POINT ( 'NONE',  ( 2.266490820343226797, 7.550546162186920540, 1.183790889241755018 ) ) ;
#42476=CARTESIAN_POINT ( 'NONE',  ( 3.152665057734113319, -5.461013642405577073, 5.761241965769066553 ) ) ;
#42483=EDGE_CURVE ( 'NONE', #24280, #19299, #9149, .T. ) ;
#42487=CARTESIAN_POINT ( 'NONE',  ( 0.3665391374699465965, -0.2638605131386297376, -12.27992639892678639 ) ) ;
#42489=CARTESIAN_POINT ( 'NONE',  ( 2.080613030138687147, 0.000000000000000000, -7.580821595991582562 ) ) ;
#42504=CARTESIAN_POINT ( 'NONE',  ( 2.241311220309555985, 2.698144003944889846, -7.141707286456099091 ) ) ;
#42508=( BOUNDED_SURFACE ( )  B_SPLINE_SURFACE ( 3, 1, ( 
 ( #13177, #13481 ),
 ( #8184, #38098 ),
 ( #39412, #28456 ),
 ( #28146, #54068 ) ),
 .UNSPECIFIED., .F., .F., .F. ) 
 B_SPLINE_SURFACE_WITH_KNOTS ( ( 4, 4 ),
 ( 2, 2 ),
 ( 0.000000000000000000, 1.000000000000000000 ),
 ( 0.000000000000000000, 1.000000000000000000 ),
 .UNSPECIFIED. ) 
 GEOMETRIC_REPRESENTATION_ITEM ( )  RATIONAL_B_SPLINE_SURFACE ( (
 ( 1.000000000000000000, 1.000000000000000000),
 ( 0.9942764183789327692, 0.8450855930916585379),
 ( 0.9942764183789327692, 0.8450855930916585379),
 ( 1.000000000000000000, 1.000000000000000000) ) ) 
 REPRESENTATION_ITEM ( '' )  SURFACE ( )  );
#42510=CARTESIAN_POINT ( 'NONE',  ( 2.770579946183230113, 4.784693811915898820, 6.173813901927509562 ) ) ;
#42514=CARTESIAN_POINT ( 'NONE',  ( 0.3341166715381381214, -11.61315925169691177, -3.958014133396720702 ) ) ;
#42516=VERTEX_POINT ( 'NONE', #20744 ) ;
#42519=AXIS2_PLACEMENT_3D ( 'NONE', #48158, #44427, #7565 ) ;
#42520=ADVANCED_FACE ( 'NONE', ( #41013 ), #29137, .F. ) ;
#42522=CARTESIAN_POINT ( 'NONE',  ( 1.948354844646956963, 4.761851831282559289, 10.97658859989492086 ) ) ;
#42523=CARTESIAN_POINT ( 'NONE',  ( 2.284126774967658147, 5.959830409747719493, -4.793997684221303679 ) ) ;
#42526=CARTESIAN_POINT ( 'NONE',  ( 2.276198483117258586, -6.697332984100285991, 3.688810392808530736 ) ) ;
#42531=DIRECTION ( 'NONE',  ( 0.000000000000000000, 0.000000000000000000, 1.000000000000000000 ) ) ;
#42535=DIRECTION ( 'NONE',  ( 0.3865475372811021382, 0.7888450329201709410, 0.4778122177792122338 ) ) ;
#42542=CIRCLE ( 'NONE', #54268, 12.73084802173761787 ) ;
#42544=ORIENTED_EDGE ( 'NONE', *, *, #7352, .F. ) ;
#42545=CARTESIAN_POINT ( 'NONE',  ( 5.516018279890452902, -0.005042957932159101465, -0.004525000489649917343 ) ) ;
#42548=CARTESIAN_POINT ( 'NONE',  ( 1.014383007554957139, -7.686901933424216793, 9.851867765302158020 ) ) ;
#42553=CARTESIAN_POINT ( 'NONE',  ( 2.305787727787084407, 7.654065630109506913, 0.1666591538752955071 ) ) ;
#42555=EDGE_CURVE ( 'NONE', #36274, #44559, #49677, .T. ) ;
#42560=VECTOR ( 'NONE', #20132, 1000.000000000000000 ) ;
#42569=DIRECTION ( 'NONE',  ( 0.000000000000000000, 0.000000000000000000, 1.000000000000000000 ) ) ;
#42584=ORIENTED_EDGE ( 'NONE', *, *, #47962, .F. ) ;
#42586=CARTESIAN_POINT ( 'NONE',  ( 2.259025283526324479, 6.683966451871405035, 3.701170455112714475 ) ) ;
#42590=CARTESIAN_POINT ( 'NONE',  ( 0.3164563675027631806, 12.03284811452140346, -2.365891945210687020 ) ) ;
#42598=CARTESIAN_POINT ( 'NONE',  ( 2.931247277082670077, -6.255823895766985387, 4.765826751677415984 ) ) ;
#42604=CARTESIAN_POINT ( 'NONE',  ( 0.2638984909335716500, 12.02508546958696911, 2.322601104020707741 ) ) ;
#42612=CARTESIAN_POINT ( 'NONE',  ( 1.719304012338836563, -3.626341562670527985, 12.20344780066003487 ) ) ;
#42616=CARTESIAN_POINT ( 'NONE',  ( 2.260457164927182738, -5.763213574030888964, 5.016645293558183560 ) ) ;
#42621=CARTESIAN_POINT ( 'NONE',  ( 0.2956976708475462234, -12.25433786972505779, -0.2200030809426881950 ) ) ;
#42625=CARTESIAN_POINT ( 'NONE',  ( 1.462291587751586297, -9.267729738232038272, -8.602888600422598842 ) ) ;
#42634=AXIS2_PLACEMENT_3D ( 'NONE', #51751, #36766, #10180 ) ;
#42638=CARTESIAN_POINT ( 'NONE',  ( 3.047904605210309814, -3.098478597269290535, 7.270585891216595265 ) ) ;
#42640=FACE_OUTER_BOUND ( 'NONE', #2094, .T. ) ;
#42644=CARTESIAN_POINT ( 'NONE',  ( 2.305787727787084407, -7.654065630109508689, 0.1666591538752418555 ) ) ;
#42659=LINE ( 'NONE', #12738, #49485 ) ;
#42667=ORIENTED_EDGE ( 'NONE', *, *, #31732, .F. ) ;
#42690=EDGE_CURVE ( 'NONE', #64984, #39958, #20339, .T. ) ;
#42697=CARTESIAN_POINT ( 'NONE',  ( 0.2648321136542697296, -1.986804758684036276, -12.08378267055567434 ) ) ;
#42699=CARTESIAN_POINT ( 'NONE',  ( 2.941278708680199916, -6.138172921908580548, -0.1348063076487592271 ) ) ;
#42709=CARTESIAN_POINT ( 'NONE',  ( 2.298277635560095788, -4.791911337974128493, -5.967558917212117287 ) ) ;
#42711=CARTESIAN_POINT ( 'NONE',  ( 0.6473888112830246122, -12.23851338376148590, -1.823007254467082339 ) ) ;
#42712=EDGE_LOOP ( 'NONE', ( #17743, #33761, #61030, #65465 ) ) ;
#42714=CARTESIAN_POINT ( 'NONE',  ( 0.2652384529303120075, -4.250461213012467709, -11.48485968917278299 ) ) ;
#42715=VERTEX_POINT ( 'NONE', #55164 ) ;
#42717=B_SPLINE_CURVE_WITH_KNOTS ( 'NONE', 3,
 ( #22681, #62892, #53605, #38272, #17359, #58932, #63223, #27994, #48938, #48300, #8047, #48606, #23323, #43587, #33630, #38618, #18355, #53918, #28633, #3394, #23664, #64846 ),
 .UNSPECIFIED., .F., .F.,
 ( 4, 3, 3, 3, 3, 3, 3, 4 ),
 ( 8.824766327896537836E-19, 4.449119708436899146E-05, 6.626296329540649216E-05, 8.803456484963045230E-05, 0.0001098060367612840654, 0.0001315774408628553544, 0.0001760698110411230662, 0.0001829697163287824805 ),
 .UNSPECIFIED. ) ;
#42720=ORIENTED_EDGE ( 'NONE', *, *, #58535, .F. ) ;
#42721=CARTESIAN_POINT ( 'NONE',  ( 0.2911222467163543381, -9.524109243548023684, 7.711756541611659799 ) ) ;
#42727=CARTESIAN_POINT ( 'NONE',  ( 0.2911222467163552263, 5.940753417478925158, 10.71854909364320463 ) ) ;
#42730=CARTESIAN_POINT ( 'NONE',  ( 1.287602823388335427, 4.819820779360716401, -11.62763122280001582 ) ) ;
#42733=CARTESIAN_POINT ( 'NONE',  ( 2.241528039335008327, -0.01573255094247159869, 7.634443721858077403 ) ) ;
#42738=CARTESIAN_POINT ( 'NONE',  ( 1.719304012339893051, -12.70777170743897422, -0.7661785589590540679 ) ) ;
#42753=EDGE_CURVE ( 'NONE', #8323, #55428, #29072, .T. ) ;
#42757=CARTESIAN_POINT ( 'NONE',  ( 0.3665391374699464300, 5.911453292029603013, 10.76665847464314751 ) ) ;
#42764=CARTESIAN_POINT ( 'NONE',  ( 2.276198483117258586, 3.955655305430065383, -6.543270001966361882 ) ) ;
#42769=VECTOR ( 'NONE', #63686, 1000.000000000000114 ) ;
#42770=CARTESIAN_POINT ( 'NONE',  ( 0.2653519991613804141, -6.142165520908248411, 10.59450977800980453 ) ) ;
#42773=CARTESIAN_POINT ( 'NONE',  ( 2.276198483117258142, -3.955655305430017865, 6.543270001966392080 ) ) ;
#42775=B_SPLINE_CURVE_WITH_KNOTS ( 'NONE', 3,
 ( #23048, #2789, #18728, #54636, #58642, #13383, #43308, #63582, #24338, #19373, #33668, #13699, #28353, #28675, #44603, #58296 ),
 .UNSPECIFIED., .F., .F.,
 ( 4, 3, 3, 3, 3, 4 ),
 ( 4.336808689942017736E-19, 0.0002176109881720207173, 0.0004352086762394531856, 0.0006528017811446789427, 0.0007615147961451612180, 0.0009453342004947423759 ),
 .UNSPECIFIED. ) ;
#42776=ORIENTED_EDGE ( 'NONE', *, *, #64750, .F. ) ;
#42784=CARTESIAN_POINT ( 'NONE',  ( 2.241352910868908310, 1.407733736974966288, -7.503490710578218703 ) ) ;
#42788=CARTESIAN_POINT ( 'NONE',  ( 0.3654063281920738038, 12.13594617907221540, 1.872466061177124885 ) ) ;
#42797=CARTESIAN_POINT ( 'NONE',  ( 2.305787727787084407, 1.493241775258423720, 7.508843116234161563 ) ) ;
#42798=B_SPLINE_CURVE_WITH_KNOTS ( 'NONE', 3,
 ( #12352, #43942, #48942, #38623, #52928, #22324, #23670, #27998, #37957, #64220, #8050, #48612, #48303, #58936, #12028, #58251 ),
 .UNSPECIFIED., .F., .F.,
 ( 4, 3, 3, 3, 3, 4 ),
 ( 2.536682445082988549E-15, 0.0002126834539179670665, 0.0004253519300366167036, 0.0006380165497224025116, 0.0007442707582428092529, 0.0009453531351419345490 ),
 .UNSPECIFIED. ) ;
#42799=ORIENTED_EDGE ( 'NONE', *, *, #28699, .F. ) ;
#42806=CARTESIAN_POINT ( 'NONE',  ( 1.109979610370630754, -8.414317452282139342, 9.281420052101156060 ) ) ;
#42815=ORIENTED_EDGE ( 'NONE', *, *, #35784, .T. ) ;
#42817=CARTESIAN_POINT ( 'NONE',  ( 3.047904605210274731, 7.561255571389346564, -2.299870214474515340 ) ) ;
#42822=CARTESIAN_POINT ( 'NONE',  ( 2.263328370261528555, 7.548992860189821741, 1.186889399881216223 ) ) ;
#42835=CARTESIAN_POINT ( 'NONE',  ( 2.705197763288549329, -1.627208841526513350, 7.617149697727738200 ) ) ;
#42838=CARTESIAN_POINT ( 'NONE',  ( 3.152665057734040488, 0.000000000000000000, 0.000000000000000000 ) ) ;
#42848=CARTESIAN_POINT ( 'NONE',  ( 1.719304012338199517, 0.000000000000000000, 0.000000000000000000 ) ) ;
#42851=CARTESIAN_POINT ( 'NONE',  ( 0.2648978790185584908, -7.769924372105139199, -9.465406350830686932 ) ) ;
#42859=CARTESIAN_POINT ( 'NONE',  ( 0.2646305136544072623, -0.1321451301298671999, 12.24595685781654630 ) ) ;
#42864=CARTESIAN_POINT ( 'NONE',  ( 0.2717059086739035956, -11.56868249951478589, -4.023283916512541580 ) ) ;
#42865=CARTESIAN_POINT ( 'NONE',  ( 1.375507693217275840, 5.789143338282538132, 11.20969178069527139 ) ) ;
#42871=CARTESIAN_POINT ( 'NONE',  ( 0.3164563675027642353, 10.73846246126249149, 5.922187299605671029 ) ) ;
#42876=CARTESIAN_POINT ( 'NONE',  ( 2.994568964204213923, -4.756002438591021786, -6.289764245798271425 ) ) ;
#42877=ORIENTED_EDGE ( 'NONE', *, *, #60809, .F. ) ;
#42882=EDGE_CURVE ( 'NONE', #7766, #30254, #4383, .T. ) ;
#42887=LINE ( 'NONE', #62503, #54083 ) ;
#42895=( BOUNDED_SURFACE ( )  B_SPLINE_SURFACE ( 3, 1, ( 
 ( #50282, #25000 ),
 ( #45273, #20667 ),
 ( #15341, #35922 ),
 ( #45936, #11333 ) ),
 .UNSPECIFIED., .F., .F., .F. ) 
 B_SPLINE_SURFACE_WITH_KNOTS ( ( 4, 4 ),
 ( 2, 2 ),
 ( 0.000000000000000000, 1.000000000000000000 ),
 ( 0.000000000000000000, 1.000000000000000000 ),
 .UNSPECIFIED. ) 
 GEOMETRIC_REPRESENTATION_ITEM ( )  RATIONAL_B_SPLINE_SURFACE ( (
 ( 1.000000000000000000, 1.000000000000000000),
 ( 0.9942764183789327692, 0.8450855930916585379),
 ( 0.9942764183789327692, 0.8450855930916585379),
 ( 1.000000000000000000, 1.000000000000000000) ) ) 
 REPRESENTATION_ITEM ( '' )  SURFACE ( )  );
#42897=CARTESIAN_POINT ( 'NONE',  ( 2.251152103363646795, -6.550893877460178594, 3.926807817126177547 ) ) ;
#42898=CARTESIAN_POINT ( 'NONE',  ( 2.639814597422736941, -3.659458430304299181, -6.851176153958514981 ) ) ;
#42899=AXIS2_PLACEMENT_3D ( 'NONE', #56382, #15154, #40769 ) ;
#42907=CARTESIAN_POINT ( 'NONE',  ( 5.515539859299206427, -0.005142293699651617929, -0.003193223631738859817 ) ) ;
#42908=VECTOR ( 'NONE', #52049, 1000.000000000000114 ) ;
#42914=ADVANCED_FACE ( 'NONE', ( #22886 ), #8348, .F. ) ;
#42917=( BOUNDED_SURFACE ( )  B_SPLINE_SURFACE ( 3, 1, ( 
 ( #18351, #18005 ),
 ( #17007, #38266 ),
 ( #58927, #53912 ),
 ( #13014, #33297 ) ),
 .UNSPECIFIED., .F., .F., .F. ) 
 B_SPLINE_SURFACE_WITH_KNOTS ( ( 4, 4 ),
 ( 2, 2 ),
 ( 0.000000000000000000, 1.000000000000000000 ),
 ( 0.000000000000000000, 1.000000000000000000 ),
 .UNSPECIFIED. ) 
 GEOMETRIC_REPRESENTATION_ITEM ( )  RATIONAL_B_SPLINE_SURFACE ( (
 ( 1.000000000000000000, 1.000000000000000000),
 ( 0.6933888150995267674, 0.9895912004443193632),
 ( 0.6933888150995267674, 0.9895912004443193632),
 ( 1.000000000000000000, 1.000000000000000000) ) ) 
 REPRESENTATION_ITEM ( '' )  SURFACE ( )  );
#42928=CARTESIAN_POINT ( 'NONE',  ( 5.515539859299206427, 0.004759416711442177560, 0.003740028639278364028 ) ) ;
#42934=CARTESIAN_POINT ( 'NONE',  ( 1.462291587751620714, 6.862867011842961773, -10.62080802716768524 ) ) ;
#42939=CARTESIAN_POINT ( 'NONE',  ( 2.245754705088393255, -2.715960966012146649, 7.136529175883355336 ) ) ;
#42944=CARTESIAN_POINT ( 'NONE',  ( 2.781367136452501221, 7.442815111163411324, 2.381060477055354507 ) ) ;
#42945=CARTESIAN_POINT ( 'NONE',  ( 0.3632410797595206353, 6.365652464380907816, 10.49990774419904227 ) ) ;
#42946=CARTESIAN_POINT ( 'NONE',  ( 0.2653519890518172830, -9.381137101569615666, -7.871697161810781829 ) ) ;
#42957=CARTESIAN_POINT ( 'NONE',  ( 5.515188684475870851, -0.004442604682416595625, 0.002983184900675373528 ) ) ;
#42961=ADVANCED_FACE ( 'NONE', ( #63416 ), #15131, .F. ) ;
#42970=CARTESIAN_POINT ( 'NONE',  ( 2.245754705088395475, -0.1113317465207330631, 7.635057163463321750 ) ) ;
#42971=CARTESIAN_POINT ( 'NONE',  ( 0.2648321136542695631, -12.24520788540325711, -0.1417061099916042954 ) ) ;
#42973=FACE_OUTER_BOUND ( 'NONE', #2727, .T. ) ;
#42985=CARTESIAN_POINT ( 'NONE',  ( 0.3218525148189839702, -12.03385614540603044, -2.370084734146341798 ) ) ;
#42994=CARTESIAN_POINT ( 'NONE',  ( 0.2647959493198549508, -7.758440170207231645, 9.474789498086966688 ) ) ;
#42996=FACE_OUTER_BOUND ( 'NONE', #44618, .T. ) ;
#43004=CARTESIAN_POINT ( 'NONE',  ( 2.241526690369556984, 7.168108047190872689, -2.627393882429245320 ) ) ;
#43005=CARTESIAN_POINT ( 'NONE',  ( 0.2647959493198541736, 4.049980114636526629, -11.55693259385002492 ) ) ;
#43008=CARTESIAN_POINT ( 'NONE',  ( 0.2834382757448030699, -3.999440312567289713, 11.58108645293229166 ) ) ;
#43010=CARTESIAN_POINT ( 'NONE',  ( 1.372161826075867230, 8.551811013234416947, 9.274145586376221218 ) ) ;
#43020=CARTESIAN_POINT ( 'NONE',  ( 0.9232058338315058954, -2.536181247095282476, -12.21058493388775901 ) ) ;
#43021=CARTESIAN_POINT ( 'NONE',  ( 5.516018279890452902, -0.002104829434640716982, 0.006440244342253021413 ) ) ;
#43033=FACE_OUTER_BOUND ( 'NONE', #11774, .T. ) ;
#43035=CARTESIAN_POINT ( 'NONE',  ( 5.530133899448235191, -0.001661287012793933454, -0.01589823604557703135 ) ) ;
#43043=CARTESIAN_POINT ( 'NONE',  ( 0.3675815128205912052, 3.951233083390468526, 11.62724744438066971 ) ) ;
#43047=CARTESIAN_POINT ( 'NONE',  ( 0.3160775863651122397, 9.237902461149245070, 8.065044686487343739 ) ) ;
#43048=CARTESIAN_POINT ( 'NONE',  ( 2.290907136833257862, 1.168459104840932961, 7.561169784528408933 ) ) ;
#43056=DIRECTION ( 'NONE',  ( -1.000000000000000000, -0.000000000000000000, -0.000000000000000000 ) ) ;
#43064=CARTESIAN_POINT ( 'NONE',  ( 2.241352910868909643, -0.08337961031709527349, 7.633946224498472155 ) ) ;
#43065=B_SPLINE_CURVE_WITH_KNOTS ( 'NONE', 3,
 ( #58219, #32922, #37927, #53578, #57910, #49250, #53234, #12990, #43561, #2377, #7680, #28287, #8329, #18663, #27965, #38243, #22295, #33915, #12324 ),
 .UNSPECIFIED., .F., .F.,
 ( 4, 3, 3, 3, 3, 3, 4 ),
 ( 6.269651592512720910E-18, 2.825908398831147194E-05, 4.208813692483879805E-05, 5.591713746943844775E-05, 6.279584083231875386E-05, 9.105792820296639836E-05, 0.0001153131102488859876 ),
 .UNSPECIFIED. ) ;
#43067=ORIENTED_EDGE ( 'NONE', *, *, #57375, .T. ) ;
#43069=CARTESIAN_POINT ( 'NONE',  ( 0.8375941296815332393, 4.612912274496897780, -11.54987202580294969 ) ) ;
#43085=ORIENTED_EDGE ( 'NONE', *, *, #64847, .F. ) ;
#43087=CARTESIAN_POINT ( 'NONE',  ( 0.3665391374699467075, -4.447929964102923961, 11.44911061034385291 ) ) ;
#43090=CARTESIAN_POINT ( 'NONE',  ( 0.2911222467163554484, 0.2144311696657358324, -12.25291251554514815 ) ) ;
#43095=EDGE_CURVE ( 'NONE', #42211, #51152, #42542, .T. ) ;
#43096=CARTESIAN_POINT ( 'NONE',  ( 2.268878695253353950, 3.949362208797156271, -6.544222817598178032 ) ) ;
#43098=( BOUNDED_SURFACE ( )  B_SPLINE_SURFACE ( 3, 1, ( 
 ( #37631, #11052 ),
 ( #42255, #62546 ),
 ( #21006, #11365 ),
 ( #41949, #57598 ) ),
 .UNSPECIFIED., .F., .F., .F. ) 
 B_SPLINE_SURFACE_WITH_KNOTS ( ( 4, 4 ),
 ( 2, 2 ),
 ( 0.000000000000000000, 1.000000000000000000 ),
 ( 0.000000000000000000, 1.000000000000000000 ),
 .UNSPECIFIED. ) 
 GEOMETRIC_REPRESENTATION_ITEM ( )  RATIONAL_B_SPLINE_SURFACE ( (
 ( 1.000000000000000000, 1.000000000000000000),
 ( 0.6933888150995267674, 0.9895912004443193632),
 ( 0.6933888150995267674, 0.9895912004443193632),
 ( 1.000000000000000000, 1.000000000000000000) ) ) 
 REPRESENTATION_ITEM ( '' )  SURFACE ( )  );
#43102=CARTESIAN_POINT ( 'NONE',  ( 2.781367136452001620, -2.960151187464810540, -7.232043329634134210 ) ) ;
#43111=CARTESIAN_POINT ( 'NONE',  ( 2.255723233588950549, 1.456523090672709797, -7.499053486174006800 ) ) ;
#43119=CARTESIAN_POINT ( 'NONE',  ( 2.969415267404411196, -3.597837242549799974, 7.007431655063433240 ) ) ;
#43124=CARTESIAN_POINT ( 'NONE',  ( 5.536195898058073439, 0.006672323185952712399, -0.005266167600747622204 ) ) ;
#43128=CARTESIAN_POINT ( 'NONE',  ( 1.549075743845145015, -8.652116335901308020, 9.261503792573748228 ) ) ;
#43130=FACE_OUTER_BOUND ( 'NONE', #7475, .T. ) ;
#43133=VERTEX_POINT ( 'NONE', #30466 ) ;
#43135=CARTESIAN_POINT ( 'NONE',  ( 0.2648321136542695076, 1.986804758684115990, 12.08378267055565658 ) ) ;
#43138=CARTESIAN_POINT ( 'NONE',  ( 0.2717059086739027629, -9.494961435243642001, -7.737372654246677861 ) ) ;
#43143=CARTESIAN_POINT ( 'NONE',  ( 0.3040950598368152291, 0.2511348647275649659, 12.25911170648142701 ) ) ;
#43158=CARTESIAN_POINT ( 'NONE',  ( 5.530133899448235191, -0.006510401266731719039, 0.01459891979722816729 ) ) ;
#43165=CARTESIAN_POINT ( 'NONE',  ( 2.280717697723837922, 3.958470850374305350, 6.543326285614636362 ) ) ;
#43170=CARTESIAN_POINT ( 'NONE',  ( 0.2801149460245140888, 4.374013318106550585, 11.44368419510487378 ) ) ;
#43171=CARTESIAN_POINT ( 'NONE',  ( 2.253265082352144955, 5.007416537586165006, -5.768060979107731967 ) ) ;
#43172=CARTESIAN_POINT ( 'NONE',  ( 0.2648978790185593790, 12.08224454301451445, -1.996248716311504801 ) ) ;
#43173=CARTESIAN_POINT ( 'NONE',  ( 0.2869720083484385009, 8.034871682535227322, -9.251312689958684388 ) ) ;
#43174=CARTESIAN_POINT ( 'NONE',  ( 0.2646305136544072623, -2.256625640822234047, -12.03696649559617171 ) ) ;
#43178=ORIENTED_EDGE ( 'NONE', *, *, #10015, .T. ) ;
#43179=DIRECTION ( 'NONE',  ( 0.000000000000000000, 0.000000000000000000, 1.000000000000000000 ) ) ;
#43185=CARTESIAN_POINT ( 'NONE',  ( 1.634816307077576081, 0.7191532042408318448, -12.68239325670243822 ) ) ;
#43186=CARTESIAN_POINT ( 'NONE',  ( 2.491965175174250202, -4.041154086925277333, -6.575382551509628470 ) ) ;
#43187=CARTESIAN_POINT ( 'NONE',  ( 0.2648978790185602672, -11.55204314799261311, -4.063980959785162383 ) ) ;
#43189=EDGE_LOOP ( 'NONE', ( #24363, #7011 ) ) ;
#43192=CARTESIAN_POINT ( 'NONE',  ( 2.034671305880103809, 9.742055912616228497, 6.436604249850454984 ) ) ;
#43195=B_SPLINE_CURVE_WITH_KNOTS ( 'NONE', 3,
 ( #63701, #2899, #29140, #64044, #33775, #64365, #8196, #18531, #9162, #3880, #59082, #34096, #38449, #19490, #49742, #18180 ),
 .UNSPECIFIED., .F., .F.,
 ( 4, 3, 3, 3, 3, 4 ),
 ( 0.000000000000000000, 0.0002999043160757258481, 0.0005998071753050843039, 0.0008997092107374322261, 0.001204458948194995658, 0.001510329163475229806 ),
 .UNSPECIFIED. ) ;
#43196=CARTESIAN_POINT ( 'NONE',  ( 0.2651627923886314409, 9.324231535593115794, 7.938954356958122460 ) ) ;
#43197=CARTESIAN_POINT ( 'NONE',  ( 2.241352910868908754, -6.652881166698538351, 3.744764251556969903 ) ) ;
#43204=ADVANCED_FACE ( 'NONE', ( #1210 ), #54182, .F. ) ;
#43218=CARTESIAN_POINT ( 'NONE',  ( 2.241537034860906275, -5.845308934728745243, -4.910958050585496615 ) ) ;
#43220=CARTESIAN_POINT ( 'NONE',  ( 0.4613984246114889998, -7.694922453052204681, 9.610550265395824354 ) ) ;
#43226=CARTESIAN_POINT ( 'NONE',  ( 2.290907136833254309, 7.243397831411281906, -2.463690939638600419 ) ) ;
#43232=CARTESIAN_POINT ( 'NONE',  ( 0.2650492594609233366, 11.54478160586242907, -4.084774262245968401 ) ) ;
#43248=CARTESIAN_POINT ( 'NONE',  ( 0.8320506296491577691, 11.54877388447410702, -4.610676791972224464 ) ) ;
#43254=VERTEX_POINT ( 'NONE', #49071 ) ;
#43260=CARTESIAN_POINT ( 'NONE',  ( 0.3057689695767449312, 6.328747727191191608, 10.49983108339462845 ) ) ;
#43270=CARTESIAN_POINT ( 'NONE',  ( 2.241352910868908754, -1.243507963608043498, -7.532448145350521429 ) ) ;
#43277=( BOUNDED_SURFACE ( )  B_SPLINE_SURFACE ( 3, 1, ( 
 ( #43124, #38808 ),
 ( #49462, #3247 ),
 ( #28183, #18853 ),
 ( #63402, #59106 ) ),
 .UNSPECIFIED., .F., .F., .F. ) 
 B_SPLINE_SURFACE_WITH_KNOTS ( ( 4, 4 ),
 ( 2, 2 ),
 ( 0.000000000000000000, 1.000000000000000000 ),
 ( 0.000000000000000000, 1.000000000000000000 ),
 .UNSPECIFIED. ) 
 GEOMETRIC_REPRESENTATION_ITEM ( )  RATIONAL_B_SPLINE_SURFACE ( (
 ( 1.000000000000000000, 1.000000000000000000),
 ( 0.6933888150995267674, 0.9895912004443193632),
 ( 0.6933888150995267674, 0.9895912004443193632),
 ( 1.000000000000000000, 1.000000000000000000) ) ) 
 REPRESENTATION_ITEM ( '' )  SURFACE ( )  );
#43280=CARTESIAN_POINT ( 'NONE',  ( 0.2646305136544065406, -1.996350543473074390, 12.08286001766534667 ) ) ;
#43287=CARTESIAN_POINT ( 'NONE',  ( 2.261269890822071194, -0.1394916642590379452, 7.639767381742377239 ) ) ;
#43289=EDGE_LOOP ( 'NONE', ( #46515, #26784, #57409, #29044 ) ) ;
#43290=CARTESIAN_POINT ( 'NONE',  ( 0.3057689695767459304, 1.901059295891078804, -12.11137787899271245 ) ) ;
#43299=ORIENTED_EDGE ( 'NONE', *, *, #43531, .F. ) ;
#43301=VERTEX_POINT ( 'NONE', #12464 ) ;
#43304=CARTESIAN_POINT ( 'NONE',  ( 2.269879328256731554, -7.130835954829864320, 2.753278809616085177 ) ) ;
#43305=B_SPLINE_CURVE_WITH_KNOTS ( 'NONE', 3,
 ( #1536, #22112, #12449, #7146, #21812, #17467, #57371 ),
 .UNSPECIFIED., .F., .F.,
 ( 4, 3, 4 ),
 ( 8.074120965598165776E-15, 0.002398160485434909592, 0.005002426799384971333 ),
 .UNSPECIFIED. ) ;
#43308=CARTESIAN_POINT ( 'NONE',  ( 2.705197763288543111, 5.783040721897930503, 5.217779042888458285 ) ) ;
#43309=CARTESIAN_POINT ( 'NONE',  ( 2.963017218115624463, -3.051711603120581984, 7.259628195185923616 ) ) ;
#43313=CARTESIAN_POINT ( 'NONE',  ( 0.3109076770649005228, -7.699281309344391921, 9.542672295796789328 ) ) ;
#43318=CARTESIAN_POINT ( 'NONE',  ( 0.2638984909335720941, 4.001111175853898416, -11.57533005135174875 ) ) ;
#43327=CARTESIAN_POINT ( 'NONE',  ( 0.3223008802179294641, 9.550960164375604577, 7.695050880595522003 ) ) ;
#43331=VERTEX_POINT ( 'NONE', #22805 ) ;
#43334=ADVANCED_FACE ( 'NONE', ( #49406 ), #58876, .F. ) ;
#43336=CARTESIAN_POINT ( 'NONE',  ( 1.104777566491144558, 1.703053712365489858, -12.40974092093470382 ) ) ;
#43338=CARTESIAN_POINT ( 'NONE',  ( 5.516018279890452902, -0.005042957932158615743, 0.004525000489649755146 ) ) ;
#43340=DIRECTION ( 'NONE',  ( 0.000000000000000000, 0.000000000000000000, 1.000000000000000000 ) ) ;
#43342=CARTESIAN_POINT ( 'NONE',  ( 1.452237505248555660, 12.08199618361513039, 3.767214359061165307 ) ) ;
#43347=CARTESIAN_POINT ( 'NONE',  ( 0.2646305136544065406, 2.256625640822475631, -12.03696649559612375 ) ) ;
#43352=CARTESIAN_POINT ( 'NONE',  ( 2.247112776671472467, -4.818685025480685447, 5.923998863713047847 ) ) ;
#43354=EDGE_CURVE ( 'NONE', #13777, #9473, #32101, .T. ) ;
#43357=ORIENTED_EDGE ( 'NONE', *, *, #32732, .F. ) ;
#43358=DIRECTION ( 'NONE',  ( 1.000000000000000000, 0.000000000000000000, 0.000000000000000000 ) ) ;
#43364=ORIENTED_EDGE ( 'NONE', *, *, #26432, .F. ) ;
#43366=DIRECTION ( 'NONE',  ( 0.000000000000000000, 0.000000000000000000, 1.000000000000000000 ) ) ;
#43380=CARTESIAN_POINT ( 'NONE',  ( 5.514970785353741078, 0.001326349372336293846, -0.004532877335078717637 ) ) ;
#43388=CARTESIAN_POINT ( 'NONE',  ( 0.4626703367448694038, 4.475905684074013458, -11.46957824750464638 ) ) ;
#43413=EDGE_CURVE ( 'NONE', #20510, #35691, #29723, .T. ) ;
#43414=CARTESIAN_POINT ( 'NONE',  ( 5.536195898058073439, -0.006344799443923397099, -0.005656495196970955271 ) ) ;
#43423=CARTESIAN_POINT ( 'NONE',  ( 2.430348790457534935, 4.796903114819468072, -6.019963855523847940 ) ) ;
#43432=CARTESIAN_POINT ( 'NONE',  ( 0.2834382757448023482, 7.719209397492100777, -9.514772331577340481 ) ) ;
#43437=CARTESIAN_POINT ( 'NONE',  ( 0.2648978790185602672, -6.237101853238473659, -10.53870023327869987 ) ) ;
#43438=DIRECTION ( 'NONE',  ( 0.3865475372811021382, 0.8730852074079760161, -0.2971585806051821321 ) ) ;
#43443=CARTESIAN_POINT ( 'NONE',  ( 2.288423627607479194, -0.1612945702821226845, -7.648392725410196213 ) ) ;
#43452=CARTESIAN_POINT ( 'NONE',  ( 2.941278708680199916, -5.248410529370246991, 3.185832147968428618 ) ) ;
#43458=B_SPLINE_CURVE_WITH_KNOTS ( 'NONE', 3,
 ( #49886, #24946, #35562, #20613, #51212, #29919, #65480, #30255, #4337, #24610, #55856, #10286, #30565, #45882, #44887, #40891 ),
 .UNSPECIFIED., .F., .F.,
 ( 4, 3, 3, 3, 3, 4 ),
 ( 8.673617379884035472E-19, 0.0002176109881720219099, 0.0004352086762394569803, 0.0006528017811446825205, 0.0007615147961451645790, 0.0009453342004947430264 ),
 .UNSPECIFIED. ) ;
#43460=CARTESIAN_POINT ( 'NONE',  ( 1.452237505248552996, -2.778494755359138146, 12.34692280296791189 ) ) ;
#43461=CARTESIAN_POINT ( 'NONE',  ( 0.2767916011545398236, -9.504925141026303592, -7.727819755721567319 ) ) ;
#43463=CARTESIAN_POINT ( 'NONE',  ( 0.9232167919969144210, 3.872606616958433445, -11.84868134597554246 ) ) ;
#43465=CARTESIAN_POINT ( 'NONE',  ( 2.273267844204862165, -1.178226273332996898, 7.553702825375862240 ) ) ;
#43466=CARTESIAN_POINT ( 'NONE',  ( 5.515188684475870851, -0.005320786921497683807, -0.0005703990286339872965 ) ) ;
#43469=CARTESIAN_POINT ( 'NONE',  ( 5.516018279890452902, -0.002527316374434336339, 0.006286471671802434068 ) ) ;
#43476=CONICAL_SURFACE ( 'NONE', #37121, 7.938172270156617749, 1.280189991382167047 ) ;
#43477=ORIENTED_EDGE ( 'NONE', *, *, #34159, .F. ) ;
#43478=CARTESIAN_POINT ( 'NONE',  ( 0.3223008802179238019, 5.919638939520732279, -10.74209118105750882 ) ) ;
#43480=CARTESIAN_POINT ( 'NONE',  ( 2.931247277082681180, 1.728824746592373840, -7.672001188570248154 ) ) ;
#43486=FACE_OUTER_BOUND ( 'NONE', #34272, .T. ) ;
#43493=CARTESIAN_POINT ( 'NONE',  ( 0.3006302518452048100, 10.50091819089224288, -6.323626002160976256 ) ) ;
#43495=CARTESIAN_POINT ( 'NONE',  ( 0.2655924914740778742, -2.169924872617981393, -12.05257978623656001 ) ) ;
#43496=CARTESIAN_POINT ( 'NONE',  ( 2.034671305880000336, 6.953089744304945974, 9.380408876023668796 ) ) ;
#43498=DIRECTION ( 'NONE',  ( 0.3865475372811021382, -0.1791957239473782881, 0.9046932595863030890 ) ) ;
#43500=CARTESIAN_POINT ( 'NONE',  ( 3.152665057734040488, 0.000000000000000000, 0.000000000000000000 ) ) ;
#43503=CARTESIAN_POINT ( 'NONE',  ( 1.375507693220225702, 0.5913006932469592192, -12.60244951981792561 ) ) ;
#43504=CARTESIAN_POINT ( 'NONE',  ( 2.524535260912557533, -4.054303386867513126, -6.580044328001104503 ) ) ;
#43505=CARTESIAN_POINT ( 'NONE',  ( 0.3632410797595283514, -11.62558329798848433, -3.951633449031027201 ) ) ;
#43511=CARTESIAN_POINT ( 'NONE',  ( 2.931247277082680736, -7.255238984871605012, -3.034789039497262308 ) ) ;
#43512=AXIS2_PLACEMENT_3D ( 'NONE', #36813, #41130, #48379 ) ;
#43515=DIRECTION ( 'NONE',  ( -1.000000000000000000, -0.000000000000000000, -0.000000000000000000 ) ) ;
#43520=CARTESIAN_POINT ( 'NONE',  ( 2.241311220309555097, -6.657499176698812526, 3.736531646286240793 ) ) ;
#43525=CARTESIAN_POINT ( 'NONE',  ( 1.633930747250948334, 2.909970528250789723, 12.36466318969054790 ) ) ;
#43530=ORIENTED_EDGE ( 'NONE', *, *, #26051, .T. ) ;
#43531=EDGE_CURVE ( 'NONE', #42516, #51949, #9840, .T. ) ;
#43532=CARTESIAN_POINT ( 'NONE',  ( 5.514624014163232779, 0.002529391395135005636, -0.003278974416024992272 ) ) ;
#43533=CARTESIAN_POINT ( 'NONE',  ( 0.6473888112830246122, -8.203438694127592967, -9.263269341114870770 ) ) ;
#43534=CARTESIAN_POINT ( 'NONE',  ( 2.247112776671468470, -3.918650674719057481, -6.554209700764013213 ) ) ;
#43536=B_SPLINE_CURVE_WITH_KNOTS ( 'NONE', 3,
 ( #19047, #58985, #13712, #33998, #54312, #12728, #63596, #8751, #14043, #34335, #15668, #61241, #4764, #14373, #45611, #44616, #9708, #20023, #24351, #15019, #10360, #20347 ),
 .UNSPECIFIED., .F., .F.,
 ( 4, 3, 3, 3, 3, 3, 3, 4 ),
 ( 5.421010862427522170E-20, 4.449119708437038737E-05, 6.626296329540639729E-05, 8.803456484963022191E-05, 0.0001098060367612849870, 0.0001315774408628578751, 0.0001760698110411264815, 0.0001829697163287849471 ),
 .UNSPECIFIED. ) ;
#43540=EDGE_CURVE ( 'NONE', #11296, #29095, #11297, .T. ) ;
#43543=CARTESIAN_POINT ( 'NONE',  ( 2.770579946183330478, -3.639932028439770484, -6.910873157406271616 ) ) ;
#43545=CARTESIAN_POINT ( 'NONE',  ( 0.2801149460245141998, 9.257544930777269698, -8.024198546827383538 ) ) ;
#43546=B_SPLINE_CURVE_WITH_KNOTS ( 'NONE', 3,
 ( #4748, #9692, #25009, #39960, #55255, #12467, #45282, #29982, #60243, #14664, #65540, #50293, #58376, #22808, #8157, #58052 ),
 .UNSPECIFIED., .F., .F.,
 ( 4, 3, 3, 3, 3, 4 ),
 ( 2.923441161686954018E-15, 0.0002126834539179695872, 0.0004253519300366267325, 0.0006380165497224176904, 0.0007442707582428259496, 0.0009453531351417306106 ),
 .UNSPECIFIED. ) ;
#43549=EDGE_LOOP ( 'NONE', ( #32044, #58623, #36687, #54058 ) ) ;
#43558=CARTESIAN_POINT ( 'NONE',  ( 2.249013661412227361, -7.540851674528683546, 1.207748565003212482 ) ) ;
#43561=CARTESIAN_POINT ( 'NONE',  ( 2.263328370261530775, -2.746620058315247359, -7.131064289852364624 ) ) ;
#43562=LINE ( 'NONE', #53579, #5922 ) ;
#43566=VERTEX_POINT ( 'NONE', #25742 ) ;
#43569=CARTESIAN_POINT ( 'NONE',  ( 0.2652384770603659070, -4.250454630553642588, 11.48486213386624755 ) ) ;
#43575=CARTESIAN_POINT ( 'NONE',  ( 1.547277799340754711, 11.66196709685618416, -4.961646058324859609 ) ) ;
#43576=DIRECTION ( 'NONE',  ( 0.000000000000000000, 0.000000000000000000, 1.000000000000000000 ) ) ;
#43581=CARTESIAN_POINT ( 'NONE',  ( 2.244591118395372398, 6.665613643994186432, 3.724266936776519987 ) ) ;
#43585=CARTESIAN_POINT ( 'NONE',  ( 0.3610902822527179978, 6.364812822043165674, 10.49957835860565503 ) ) ;
#43586=CIRCLE ( 'NONE', #14893, 12.73084802173761787 ) ;
#43587=CARTESIAN_POINT ( 'NONE',  ( 0.3109076770649110144, -2.361108455562764163, -12.03190317807025700 ) ) ;
#43599=ADVANCED_FACE ( 'NONE', ( #61303 ), #22313, .F. ) ;
#43600=LINE ( 'NONE', #42271, #5567 ) ;
#43605=EDGE_CURVE ( 'NONE', #54859, #12885, #51683, .T. ) ;
#43612=EDGE_CURVE ( 'NONE', #11073, #51152, #45598, .T. ) ;
#43617=CARTESIAN_POINT ( 'NONE',  ( 2.241352910868909643, -0.08337961031709527349, 7.633946224498472155 ) ) ;
#43628=EDGE_CURVE ( 'NONE', #57528, #26284, #3524, .T. ) ;
#43632=ORIENTED_EDGE ( 'NONE', *, *, #59977, .T. ) ;
#43635=CARTESIAN_POINT ( 'NONE',  ( 2.266490820343225909, -7.130860233521867819, 2.750080098241490134 ) ) ;
#43639=CARTESIAN_POINT ( 'NONE',  ( 0.2648978790185619880, -9.295532325666501450, 7.972372351882998309 ) ) ;
#43648=CARTESIAN_POINT ( 'NONE',  ( 5.514970785353741078, -0.003805873180274332770, 0.002796696073589857289 ) ) ;
#43650=EDGE_LOOP ( 'NONE', ( #52594, #51500, #51693, #23929 ) ) ;
#43652=ORIENTED_EDGE ( 'NONE', *, *, #64847, .T. ) ;
#43653=CARTESIAN_POINT ( 'NONE',  ( 2.241509619876139059, 7.187074272457187440, -2.575142053947795606 ) ) ;
#43663=VERTEX_POINT ( 'NONE', #59278 ) ;
#43669=CARTESIAN_POINT ( 'NONE',  ( 0.3665391374699472626, 12.13918562134718826, 1.872534962004840597 ) ) ;
#43671=CARTESIAN_POINT ( 'NONE',  ( 0.3341166715381246322, -10.49680960898231064, 6.352033667906565206 ) ) ;
#43672=CARTESIAN_POINT ( 'NONE',  ( 5.514970785353741078, 0.0005190732562558549642, 0.004694330894494371832 ) ) ;
#43673=CIRCLE ( 'NONE', #30948, 6.000000000000000888 ) ;
#43676=CARTESIAN_POINT ( 'NONE',  ( 0.7400311444011724582, -10.91558650018038001, -5.892391870929129638 ) ) ;
#43678=( BOUNDED_SURFACE ( )  B_SPLINE_SURFACE ( 3, 1, ( 
 ( #8612, #65115 ),
 ( #45170, #44837 ),
 ( #34201, #23928 ),
 ( #60135, #13284 ) ),
 .UNSPECIFIED., .F., .F., .F. ) 
 B_SPLINE_SURFACE_WITH_KNOTS ( ( 4, 4 ),
 ( 2, 2 ),
 ( 0.000000000000000000, 1.000000000000000000 ),
 ( 0.000000000000000000, 1.000000000000000000 ),
 .UNSPECIFIED. ) 
 GEOMETRIC_REPRESENTATION_ITEM ( )  RATIONAL_B_SPLINE_SURFACE ( (
 ( 1.000000000000000000, 1.000000000000000000),
 ( 0.9942764183789327692, 0.8450855930916585379),
 ( 0.9942764183789327692, 0.8450855930916585379),
 ( 1.000000000000000000, 1.000000000000000000) ) ) 
 REPRESENTATION_ITEM ( '' )  SURFACE ( )  );
#43679=ORIENTED_EDGE ( 'NONE', *, *, #24762, .T. ) ;
#43680=B_SPLINE_CURVE_WITH_KNOTS ( 'NONE', 3,
 ( #54200, #8972, #53877, #9275, #8315, #3350, #43545, #43890, #63828, #64175, #18309, #38573, #13937, #18647, #59197, #14277, #29558, #8642, #13613, #28927, #39216, #44521 ),
 .UNSPECIFIED., .F., .F.,
 ( 4, 3, 3, 3, 3, 3, 3, 4 ),
 ( 2.501313391450904306E-18, 4.449119708436507478E-05, 6.626296329540233153E-05, 8.803456484962373025E-05, 0.0001098060367612770181, 0.0001315774408628485239, 0.0001760698110411154768, 0.0001829697163287807187 ),
 .UNSPECIFIED. ) ;
#43696=CARTESIAN_POINT ( 'NONE',  ( 0.2650492594609241137, 2.234872523101338881, -12.04046128294315920 ) ) ;
#43709=CARTESIAN_POINT ( 'NONE',  ( 0.2869720083484391115, 9.251312689958767876, 8.034871682535136728 ) ) ;
#43713=CARTESIAN_POINT ( 'NONE',  ( 0.3654063281920730821, 2.391195511198650259, 12.04448018134536369 ) ) ;
#43715=EDGE_LOOP ( 'NONE', ( #61818, #48188, #34828, #25040 ) ) ;
#43722=CARTESIAN_POINT ( 'NONE',  ( 0.9296196016834358256, -12.19921892949987274, -2.573053270830791384 ) ) ;
#43724=CARTESIAN_POINT ( 'NONE',  ( 0.2648978790185619880, -7.972372351882965447, -9.295532325666529871 ) ) ;
#43725=CARTESIAN_POINT ( 'NONE',  ( 2.251152103363645907, -7.542379262759450143, -1.202724109297157451 ) ) ;
#43730=CARTESIAN_POINT ( 'NONE',  ( 5.515188684475870851, -0.005339000964282158458, 0.0003622115669627282630 ) ) ;
#43735=ORIENTED_EDGE ( 'NONE', *, *, #13121, .T. ) ;
#43738=B_SPLINE_CURVE_WITH_KNOTS ( 'NONE', 3,
 ( #17237, #52807, #23202, #16899, #47818, #52503, #43463, #11904, #57479, #12547, #2277, #63743, #17571, #32825, #1941, #58461 ),
 .UNSPECIFIED., .F., .F.,
 ( 4, 3, 3, 3, 3, 4 ),
 ( 1.084202172485504434E-19, 0.0003017745587525269275, 0.0006035491769808807878, 0.0009053241094668276322, 0.001207275924541018237, 0.001510325902535035285 ),
 .UNSPECIFIED. ) ;
#43745=EDGE_CURVE ( 'NONE', #49132, #50940, #55258, .T. ) ;
#43748=CARTESIAN_POINT ( 'NONE',  ( 1.937114397841932290, 1.334979369128424853, 12.76557247858998778 ) ) ;
#43749=ORIENTED_EDGE ( 'NONE', *, *, #57506, .T. ) ;
#43753=CARTESIAN_POINT ( 'NONE',  ( 2.242418902651939661, -7.500817491983891472, 1.423836467585327448 ) ) ;
#43759=CIRCLE ( 'NONE', #52278, 12.73084802173761787 ) ;
#43777=CARTESIAN_POINT ( 'NONE',  ( 3.152665057734129306, -7.923639299008720549, -0.4801242025592799556 ) ) ;
#43779=VECTOR ( 'NONE', #48585, 1000.000000000000227 ) ;
#43780=CARTESIAN_POINT ( 'NONE',  ( 2.241317068080781016, 1.415707718487511757, 7.501982551779186714 ) ) ;
#43783=CARTESIAN_POINT ( 'NONE',  ( 3.152665057735613008, -6.378477742801520023, -4.725420687649700469 ) ) ;
#43792=VERTEX_POINT ( 'NONE', #19374 ) ;
#43793=CARTESIAN_POINT ( 'NONE',  ( 2.241317068080785013, -2.524952427345706241, 7.204761327832128082 ) ) ;
#43801=CARTESIAN_POINT ( 'NONE',  ( 0.4626703367442810966, 12.30872794628565892, 0.2831487465612879117 ) ) ;
#43808=CARTESIAN_POINT ( 'NONE',  ( 5.516018279890452902, -0.0002248006052447136570, 0.006771744149385739570 ) ) ;
#43809=CARTESIAN_POINT ( 'NONE',  ( 0.2958664285830429064, -9.529149585189895078, -7.708042451272270945 ) ) ;
#43810=CARTESIAN_POINT ( 'NONE',  ( 2.717984159220105500, -4.788867404453539756, 6.148373979319240235 ) ) ;
#43815=ORIENTED_EDGE ( 'NONE', *, *, #54926, .T. ) ;
#43817=( NAMED_UNIT ( * ) PLANE_ANGLE_UNIT ( ) SI_UNIT ( $, .RADIAN. ) );
#43825=CARTESIAN_POINT ( 'NONE',  ( 0.3474126878361826209, 5.911350916722190263, -10.75620725594709803 ) ) ;
#43829=CARTESIAN_POINT ( 'NONE',  ( 2.899286259009689282, -1.713434346771278038, 7.664525129300153061 ) ) ;
#43843=CARTESIAN_POINT ( 'NONE',  ( 3.152665057734104437, -3.546019893116280741, -7.102135024645891193 ) ) ;
#43850=CARTESIAN_POINT ( 'NONE',  ( 0.3610902822527225497, -8.091349661862569320, -9.234828023175179368 ) ) ;
#43851=CARTESIAN_POINT ( 'NONE',  ( 0.5572780756289488213, 0.3055340344622364257, -12.33974848088654319 ) ) ;
#43861=CARTESIAN_POINT ( 'NONE',  ( 2.305787727787084407, 7.508843116234155346, 1.493241775258449255 ) ) ;
#43864=CARTESIAN_POINT ( 'NONE',  ( 0.2651627682582904932, 9.437482589529976096, 7.803986935114045842 ) ) ;
#43865=CARTESIAN_POINT ( 'NONE',  ( 2.556980015514285220, 5.149458076504937587, 5.777953785406889864 ) ) ;
#43869=CARTESIAN_POINT ( 'NONE',  ( 2.266490820343223689, -3.694838443752345825, 6.690312181904310762 ) ) ;
#43872=CIRCLE ( 'NONE', #6717, 7.938172270156617749 ) ;
#43878=CARTESIAN_POINT ( 'NONE',  ( 3.092491956585066148, 5.768471164323067946, -5.424230976133981308 ) ) ;
#43879=CARTESIAN_POINT ( 'NONE',  ( 2.244591118396558116, -3.910457279126670738, -6.558116599718206707 ) ) ;
#43883=ORIENTED_EDGE ( 'NONE', *, *, #34760, .F. ) ;
#43888=CARTESIAN_POINT ( 'NONE',  ( 2.241536586108913820, -5.852386772940035620, -4.902521014023387913 ) ) ;
#43889=CARTESIAN_POINT ( 'NONE',  ( 0.3160775863651093531, 12.26075464248084046, 0.2401734240703286283 ) ) ;
#43890=CARTESIAN_POINT ( 'NONE',  ( 0.2834382757448009049, 9.254160138069064345, -8.029794915379463660 ) ) ;
#43896=ORIENTED_EDGE ( 'NONE', *, *, #61940, .F. ) ;
#43905=ORIENTED_EDGE ( 'NONE', *, *, #22672, .T. ) ;
#43906=CARTESIAN_POINT ( 'NONE',  ( 2.573738926104374158, 7.194322927777959897, 2.868819712476736949 ) ) ;
#43915=ORIENTED_EDGE ( 'NONE', *, *, #60376, .F. ) ;
#43927=CARTESIAN_POINT ( 'NONE',  ( 1.719304012338517706, -0.7661785589593724799, 12.70777170744426243 ) ) ;
#43937=CARTESIAN_POINT ( 'NONE',  ( 0.3675815128205912052, -10.76447900494944321, 5.910255304480407368 ) ) ;
#43938=CARTESIAN_POINT ( 'NONE',  ( 0.3278977287071228042, 3.961557589215610520, 11.60975784853193460 ) ) ;
#43940=VERTEX_POINT ( 'NONE', #56235 ) ;
#43942=CARTESIAN_POINT ( 'NONE',  ( 3.092491956585922797, -7.070043156103695381, -3.565393530441119285 ) ) ;
#43948=CARTESIAN_POINT ( 'NONE',  ( 0.3160775863651091311, -9.237902461149193556, -8.065044686487407688 ) ) ;
#43953=B_SPLINE_CURVE_WITH_KNOTS ( 'NONE', 3,
 ( #5698, #15633, #21637, #61853, #55891, #31585, #25625 ),
 .UNSPECIFIED., .F., .F.,
 ( 4, 3, 4 ),
 ( 7.377595983537455577E-15, 0.002398160485434805075, 0.005002426799384204585 ),
 .UNSPECIFIED. ) ;
#43954=CARTESIAN_POINT ( 'NONE',  ( 3.152665057736261822, -7.102135024647099115, -3.546019893114602972 ) ) ;
#43959=PRODUCT_DEFINITION_SHAPE ( 'NONE', 'NONE',  #65283 ) ;
#43960=CARTESIAN_POINT ( 'NONE',  ( 5.520433897694421610, 0.007971295965052600102, 0.01278034823632019125 ) ) ;
#43968=CARTESIAN_POINT ( 'NONE',  ( 0.2872850955227764236, 1.921748909352319012, -12.10187515377841017 ) ) ;
#43973=VERTEX_POINT ( 'NONE', #21671 ) ;
#43975=ORIENTED_EDGE ( 'NONE', *, *, #1681, .T. ) ;
#43976=CARTESIAN_POINT ( 'NONE',  ( 0.3002738374340846450, -7.705051734330212732, -9.533456882268719568 ) ) ;
#43977=CARTESIAN_POINT ( 'NONE',  ( 2.244591118396558116, -7.137527852925273031, 2.712243649838676163 ) ) ;
#43980=ORIENTED_EDGE ( 'NONE', *, *, #57993, .T. ) ;
#43984=CARTESIAN_POINT ( 'NONE',  ( 5.514970785353741078, 0.002796696073589740195, -0.003805873180274790303 ) ) ;
#43985=VERTEX_POINT ( 'NONE', #42230 ) ;
#43989=CARTESIAN_POINT ( 'NONE',  ( 2.256373768223416842, -1.457292142211169539, -7.499124080223150912 ) ) ;
#43994=ORIENTED_EDGE ( 'NONE', *, *, #9099, .F. ) ;
#43995=AXIS2_PLACEMENT_3D ( 'NONE', #11731, #1123, #62279 ) ;
#44001=CARTESIAN_POINT ( 'NONE',  ( 1.719304012341317467, -0.7661785589597189805, -12.70777170743969009 ) ) ;
#44002=CARTESIAN_POINT ( 'NONE',  ( 2.080613030138688480, 0.000000000000000000, 0.000000000000000000 ) ) ;
#44011=EDGE_CURVE ( 'NONE', #49256, #9187, #52778, .T. ) ;
#44014=CARTESIAN_POINT ( 'NONE',  ( 0.8320506296491561038, 1.781423711749740235, -12.30686996250299359 ) ) ;
#44019=CARTESIAN_POINT ( 'NONE',  ( 5.514624014163232779, 0.003278974416024983164, 0.002529391395135016912 ) ) ;
#44025=DIRECTION ( 'NONE',  ( -0.3939253465568944290, 0.9190910618577644575, -0.009718094113436451242 ) ) ;
#44027=CARTESIAN_POINT ( 'NONE',  ( 2.242819959140646358, -5.782321801516506099, -4.985618132689735305 ) ) ;
#44031=CARTESIAN_POINT ( 'NONE',  ( 2.241526690369556096, -2.627393882429269301, -7.168108047190864696 ) ) ;
#44032=DIRECTION ( 'NONE',  ( -1.000000000000000000, 0.000000000000000000, -0.000000000000000000 ) ) ;
#44038=EDGE_CURVE ( 'NONE', #40020, #35019, #50655, .T. ) ;
#44043=CARTESIAN_POINT ( 'NONE',  ( 0.3665391374699467075, -1.872534962004718473, -12.13918562134720602 ) ) ;
#44059=CARTESIAN_POINT ( 'NONE',  ( 0.3278977287071176416, -6.347150352417378905, 10.49733767381180449 ) ) ;
#44074=LINE ( 'NONE', #13790, #9470 ) ;
#44078=( BOUNDED_SURFACE ( )  B_SPLINE_SURFACE ( 3, 1, ( 
 ( #59287, #53657 ),
 ( #23380, #8410 ),
 ( #23058, #28686 ),
 ( #49000, #3785 ) ),
 .UNSPECIFIED., .F., .F., .F. ) 
 B_SPLINE_SURFACE_WITH_KNOTS ( ( 4, 4 ),
 ( 2, 2 ),
 ( 0.000000000000000000, 1.000000000000000000 ),
 ( 0.000000000000000000, 1.000000000000000000 ),
 .UNSPECIFIED. ) 
 GEOMETRIC_REPRESENTATION_ITEM ( )  RATIONAL_B_SPLINE_SURFACE ( (
 ( 1.000000000000000000, 1.000000000000000000),
 ( 0.9942764183789327692, 0.8450855930916580938),
 ( 0.9942764183789327692, 0.8450855930916580938),
 ( 1.000000000000000000, 1.000000000000000000) ) ) 
 REPRESENTATION_ITEM ( '' )  SURFACE ( )  );
#44081=CARTESIAN_POINT ( 'NONE',  ( 0.9232058338315048962, 1.793035206307345808, 12.34162163148534219 ) ) ;
#44084=CARTESIAN_POINT ( 'NONE',  ( 2.260457164927188511, -7.499412009325147288, 1.462935478981580051 ) ) ;
#44089=CARTESIAN_POINT ( 'NONE',  ( 3.152665057733881504, -7.719888720907738922, -1.848755561851823881 ) ) ;
#44098=CARTESIAN_POINT ( 'NONE',  ( 2.368238019615359402, 4.795442552788066415, -5.994627685103000481 ) ) ;
#44104=CARTESIAN_POINT ( 'NONE',  ( 2.241451721903215955, 5.887257931662910337, -4.860585618235909955 ) ) ;
#44105=CARTESIAN_POINT ( 'NONE',  ( 2.297017764050092836, 1.490897313050684847, 7.506328781223009727 ) ) ;
#44110=CARTESIAN_POINT ( 'NONE',  ( 2.665405856346782620, 6.944580094494342326, 6.580881457836746939 ) ) ;
#44111=B_SPLINE_CURVE_WITH_KNOTS ( 'NONE', 3,
 ( #37483, #21550, #31822, #933, #11237, #21199, #26855 ),
 .UNSPECIFIED., .F., .F.,
 ( 4, 3, 4 ),
 ( 9.486769009248163798E-19, 6.607638129004467199E-05, 8.338150981373126328E-05 ),
 .UNSPECIFIED. ) ;
#44114=CARTESIAN_POINT ( 'NONE',  ( 2.305787727787083519, -6.545285700970500109, -3.971363876084033961 ) ) ;
#44116=CARTESIAN_POINT ( 'NONE',  ( 1.719304012340749033, -5.066286238787660601, -11.67935079956571087 ) ) ;
#44125=PRODUCT_DEFINITION_FORMATION_WITH_SPECIFIED_SOURCE ( 'ANY', '', #54043, .NOT_KNOWN. ) ;
#44127=CARTESIAN_POINT ( 'NONE',  ( 0.2911222467163514516, -8.040284153519429822, 9.248441845564659758 ) ) ;
#44130=CARTESIAN_POINT ( 'NONE',  ( 2.261269890822072082, -7.226741992146805238, 2.481875047312914528 ) ) ;
#44134=CARTESIAN_POINT ( 'NONE',  ( 2.430348790457645070, -4.796903114819432545, 6.019963855523926988 ) ) ;
#44135=CARTESIAN_POINT ( 'NONE',  ( 2.262775599886258426, 7.548684916004849477, -1.187656132455193081 ) ) ;
#44141=ORIENTED_EDGE ( 'NONE', *, *, #6757, .T. ) ;
#44142=FILL_AREA_STYLE ('',( #7935 ) ) ;
#44144=B_SPLINE_CURVE_WITH_KNOTS ( 'NONE', 3,
 ( #49525, #45825, #29228, #55138, #19584, #14248, #3963, #34831, #24226, #9247 ),
 .UNSPECIFIED., .F., .F.,
 ( 4, 3, 3, 4 ),
 ( 0.000000000000000000, 6.607638129004591882E-05, 9.911389841680699796E-05, 0.0001667630577588627449 ),
 .UNSPECIFIED. ) ;
#44152=CARTESIAN_POINT ( 'NONE',  ( 0.2767916011545374366, 5.959903879715737318, -10.70244578860289053 ) ) ;
#44164=CARTESIAN_POINT ( 'NONE',  ( 0.2767916011545381028, 10.51265105824871426, -6.288637995698005412 ) ) ;
#44170=CARTESIAN_POINT ( 'NONE',  ( -14.47334165536100059, 0.000000000000000000, 0.000000000000000000 ) ) ;
#44178=CARTESIAN_POINT ( 'NONE',  ( 1.020182472821187014, 5.858468047366232057, 11.03967505355296552 ) ) ;
#44186=CARTESIAN_POINT ( 'NONE',  ( 1.719304012338517706, -0.7661785589593724799, 12.70777170744426243 ) ) ;
#44197=EDGE_LOOP ( 'NONE', ( #7963, #63101, #25291, #54143 ) ) ;
#44198=CARTESIAN_POINT ( 'NONE',  ( 5.514624014163232779, 0.001255375129357668438, -0.003946330869975257262 ) ) ;
#44201=CARTESIAN_POINT ( 'NONE',  ( 2.276905613633650738, -3.955794200962162943, -6.543460433228690754 ) ) ;
#44202=DIRECTION ( 'NONE',  ( -0.3939253465568944290, -0.9034404741085565460, 0.1691689424289735677 ) ) ;
#44209=CARTESIAN_POINT ( 'NONE',  ( 2.835339799623981527, -3.628068688271626208, -6.941489812670562642 ) ) ;
#44210=CARTESIAN_POINT ( 'NONE',  ( 0.2869720083484362805, 12.25163264065381696, 0.2084396331387086132 ) ) ;
#44211=CARTESIAN_POINT ( 'NONE',  ( 3.031336079629822322, 6.621879275826772826, -4.304138522350520191 ) ) ;
#44212=CARTESIAN_POINT ( 'NONE',  ( 1.549075743845217179, -12.65619669351034915, -0.6747257554048951000 ) ) ;
#44217=CARTESIAN_POINT ( 'NONE',  ( 2.259830038564998755, 7.225713255971581539, -2.483392345594692685 ) ) ;
#44220=VERTEX_POINT ( 'NONE', #13949 ) ;
#44227=CARTESIAN_POINT ( 'NONE',  ( 5.514624014163232779, -0.001574979445068916189, 0.003830004412313241843 ) ) ;
#44241=CARTESIAN_POINT ( 'NONE',  ( 1.014383007554946037, 11.58298623339620548, -4.688516792764495733 ) ) ;
#44242=CARTESIAN_POINT ( 'NONE',  ( 0.3675815128205894289, -0.2638082659429279997, 12.27743992903066150 ) ) ;
#44244=CARTESIAN_POINT ( 'NONE',  ( 2.290907136833251201, -7.132394668149370176, -2.768669624188762945 ) ) ;
#44255=CARTESIAN_POINT ( 'NONE',  ( 1.283627346226426713, 6.763590725840804119, 10.61381050043330632 ) ) ;
#44256=VERTEX_POINT ( 'NONE', #15825 ) ;
#44257=CARTESIAN_POINT ( 'NONE',  ( 2.350038591457883630, 4.227970903881152154, -9.744161863087125397 ) ) ;
#44260=CARTESIAN_POINT ( 'NONE',  ( 0.3675815128205912052, -9.235491948679950269, -8.093875121226169256 ) ) ;
#44265=CARTESIAN_POINT ( 'NONE',  ( 1.719304012340734378, -11.38834240361519612, -5.690355757825884986 ) ) ;
#44282=DIRECTION ( 'NONE',  ( 0.3865475372811021382, 0.1791957239473723762, -0.9046932595863041993 ) ) ;
#44284=ORIENTED_EDGE ( 'NONE', *, *, #51535, .T. ) ;
#44286=VERTEX_POINT ( 'NONE', #64186 ) ;
#44288=CARTESIAN_POINT ( 'NONE',  ( 0.3401186441510243852, -7.690203051555953628, -9.562489599411604146 ) ) ;
#44289=VERTEX_POINT ( 'NONE', #18658 ) ;
#44293=CARTESIAN_POINT ( 'NONE',  ( 0.2911222467163550043, 10.50411792397758326, 6.312159098066215890 ) ) ;
#44301=ORIENTED_EDGE ( 'NONE', *, *, #56603, .F. ) ;
#44307=CARTESIAN_POINT ( 'NONE',  ( 2.241449424704145876, 7.152834201978796713, -2.668712484599891077 ) ) ;
#44310=CARTESIAN_POINT ( 'NONE',  ( 0.2652384529303142280, -11.48485968917276168, 4.250461213012500572 ) ) ;
#44313=CARTESIAN_POINT ( 'NONE',  ( 0.2648321136542690080, -4.054947570138820900, -11.55519783395232203 ) ) ;
#44320=CARTESIAN_POINT ( 'NONE',  ( 1.459561108994131606, 1.570807238540870232, -12.54631635028895786 ) ) ;
#44321=DIRECTION ( 'NONE',  ( 0.000000000000000000, 0.000000000000000000, 1.000000000000000000 ) ) ;
#44322=CARTESIAN_POINT ( 'NONE',  ( 1.937114397841935398, -3.111612666689993922, -12.45230409340484634 ) ) ;
#44323=CARTESIAN_POINT ( 'NONE',  ( 0.2872850955227719827, -10.50585060073184884, 6.306790329742891110 ) ) ;
#44326=CARTESIAN_POINT ( 'NONE',  ( 0.2648321136542690080, 10.67551415837658801, -5.999882851577366338 ) ) ;
#44330=CARTESIAN_POINT ( 'NONE',  ( 2.251139882113958990, -5.770207524085861905, -5.003859976903250129 ) ) ;
#44332=VERTEX_POINT ( 'NONE', #42738 ) ;
#44335=AXIS2_PLACEMENT_3D ( 'NONE', #12582, #2663, #43179 ) ;
#44336=CARTESIAN_POINT ( 'NONE',  ( 2.241449424704146320, -2.668712484599915058, -7.152834201978786943 ) ) ;
#44346=CARTESIAN_POINT ( 'NONE',  ( 3.152665057735657861, -7.609997527621795932, -2.258875078500884204 ) ) ;
#44349=CARTESIAN_POINT ( 'NONE',  ( 2.251152103363646795, 0.1252683866805144597, 7.636644423939547011 ) ) ;
#44351=CARTESIAN_POINT ( 'NONE',  ( 0.2833330754217391889, -12.09951353627562298, 1.928200609300433355 ) ) ;
#44355=CARTESIAN_POINT ( 'NONE',  ( 2.241506898688419458, 6.631235260227164474, 3.783130304541451050 ) ) ;
#44356=VERTEX_POINT ( 'NONE', #37435 ) ;
#44357=ORIENTED_EDGE ( 'NONE', *, *, #1936, .F. ) ;
#44363=CARTESIAN_POINT ( 'NONE',  ( 0.2648321136542702847, -6.245325033825803729, 10.53380804838496232 ) ) ;
#44377=CARTESIAN_POINT ( 'NONE',  ( 1.719304012338199517, 0.000000000000000000, 0.000000000000000000 ) ) ;
#44386=ORIENTED_EDGE ( 'NONE', *, *, #64284, .F. ) ;
#44399=EDGE_CURVE ( 'NONE', #51119, #54308, #6759, .T. ) ;
#44406=CARTESIAN_POINT ( 'NONE',  ( 1.937114397841935398, -12.76557247858997890, -1.334979369128554305 ) ) ;
#44409=ORIENTED_EDGE ( 'NONE', *, *, #28208, .T. ) ;
#44412=CARTESIAN_POINT ( 'NONE',  ( 5.516018279890452902, -0.003580555109620837603, -0.005752102158673828673 ) ) ;
#44413=VECTOR ( 'NONE', #52537, 1000.000000000000114 ) ;
#44415=CARTESIAN_POINT ( 'NONE',  ( 2.276198483117258142, -5.955030244776311044, 4.795748742147491583 ) ) ;
#44418=ORIENTED_EDGE ( 'NONE', *, *, #21371, .F. ) ;
#44427=DIRECTION ( 'NONE',  ( -1.000000000000000000, -0.000000000000000000, -0.000000000000000000 ) ) ;
#44430=CARTESIAN_POINT ( 'NONE',  ( 0.8375941296786580947, 12.43103843093986427, 0.3844307390181883610 ) ) ;
#44433=CARTESIAN_POINT ( 'NONE',  ( 0.9232167919969100911, 12.19756235544082834, -2.570564963838022354 ) ) ;
#44438=( BOUNDED_SURFACE ( )  B_SPLINE_SURFACE ( 3, 1, ( 
 ( #61921, #6086 ),
 ( #25697, #26033 ),
 ( #21017, #46631 ),
 ( #10714, #40317 ) ),
 .UNSPECIFIED., .F., .F., .F. ) 
 B_SPLINE_SURFACE_WITH_KNOTS ( ( 4, 4 ),
 ( 2, 2 ),
 ( 0.000000000000000000, 1.000000000000000000 ),
 ( 0.000000000000000000, 1.000000000000000000 ),
 .UNSPECIFIED. ) 
 GEOMETRIC_REPRESENTATION_ITEM ( )  RATIONAL_B_SPLINE_SURFACE ( (
 ( 1.000000000000000000, 1.000000000000000000),
 ( 0.9856612449720755231, 0.9999558406602322425),
 ( 0.9856612449720755231, 0.9999558406602322425),
 ( 1.000000000000000000, 1.000000000000000000) ) ) 
 REPRESENTATION_ITEM ( '' )  SURFACE ( )  );
#44441=CARTESIAN_POINT ( 'NONE',  ( 2.261269890822073414, 7.547924622047993637, -1.189259211195865529 ) ) ;
#44442=CARTESIAN_POINT ( 'NONE',  ( 2.941278708680199916, -6.021511413163954884, -1.198640839021370974 ) ) ;
#44449=ORIENTED_EDGE ( 'NONE', *, *, #44767, .F. ) ;
#44453=CARTESIAN_POINT ( 'NONE',  ( 0.9232058338315048962, 3.908895078357520703, 11.84276737136202051 ) ) ;
#44455=CARTESIAN_POINT ( 'NONE',  ( 0.3654063281920715833, 5.910280591919207183, -10.76363796011279206 ) ) ;
#44456=CARTESIAN_POINT ( 'NONE',  ( 2.259025283528082184, 6.547290863799087646, -3.937899517809406280 ) ) ;
#44471=CARTESIAN_POINT ( 'NONE',  ( 0.3665391374699465965, -5.911453292029679396, 10.76665847464310843 ) ) ;
#44472=DIRECTION ( 'NONE',  ( -1.000000000000000000, -0.000000000000000000, -0.000000000000000000 ) ) ;
#44478=CARTESIAN_POINT ( 'NONE',  ( 0.2648978790185584908, -9.465406350830660287, 7.769924372105172949 ) ) ;
#44487=VERTEX_POINT ( 'NONE', #61006 ) ;
#44488=CARTESIAN_POINT ( 'NONE',  ( 5.536195898058073439, 0.001224473329857592423, 0.008411485181668789182 ) ) ;
#44490=CARTESIAN_POINT ( 'NONE',  ( 1.719304012338210619, 10.62216384465585328, 7.017415949611872428 ) ) ;
#44491=CARTESIAN_POINT ( 'NONE',  ( 0.2648321136542718390, -0.1417061099915604971, 12.24520788540325178 ) ) ;
#44504=ORIENTED_EDGE ( 'NONE', *, *, #8547, .T. ) ;
#44506=ORIENTED_EDGE ( 'NONE', *, *, #59472, .T. ) ;
#44507=CARTESIAN_POINT ( 'NONE',  ( 2.305787727787083519, 6.545285700970583598, -3.971363876083895850 ) ) ;
#44518=CARTESIAN_POINT ( 'NONE',  ( 2.260457164926971796, 5.016645293557960628, 5.763213574030991992 ) ) ;
#44519=CARTESIAN_POINT ( 'NONE',  ( 5.514970785353741078, -0.002619824551223247366, 0.003929719953530060386 ) ) ;
#44521=CARTESIAN_POINT ( 'NONE',  ( 0.3675815128205894289, 9.235491948680119023, -8.093875121225982738 ) ) ;
#44525=ORIENTED_EDGE ( 'NONE', *, *, #17917, .F. ) ;
#44532=EDGE_CURVE ( 'NONE', #19799, #47363, #1918, .T. ) ;
#44536=CARTESIAN_POINT ( 'NONE',  ( 2.899286259009687061, 7.250549018622942654, 3.018334250363109206 ) ) ;
#44541=CARTESIAN_POINT ( 'NONE',  ( 2.253265082352432724, 2.491579069691589154, 7.220580418434027870 ) ) ;
#44559=VERTEX_POINT ( 'NONE', #36708 ) ;
#44561=CARTESIAN_POINT ( 'NONE',  ( 0.2706063244538043921, 4.023948952279264191, 11.56807224179754279 ) ) ;
#44569=CARTESIAN_POINT ( 'NONE',  ( 2.034671305879535819, 4.647127512369766400, -10.71175679137433612 ) ) ;
#44577=CARTESIAN_POINT ( 'NONE',  ( 2.241536586108914264, 3.811784405792441710, -6.614789707676422381 ) ) ;
#44580=CARTESIAN_POINT ( 'NONE',  ( 0.2717059086739048723, -12.09156413799788510, -1.953280559502818647 ) ) ;
#44581=CARTESIAN_POINT ( 'NONE',  ( 2.835339799623985080, -5.281994181469023886, 5.783398714696532217 ) ) ;
#44582=CARTESIAN_POINT ( 'NONE',  ( 2.241352910868908310, -5.901537464758421336, -4.843133558968188979 ) ) ;
#44593=CARTESIAN_POINT ( 'NONE',  ( 2.931247277082682068, -7.508560300462421289, 2.338794445044965808 ) ) ;
#44594=CARTESIAN_POINT ( 'NONE',  ( 2.241528039335006994, 3.803597072146535751, 6.619488482362950954 ) ) ;
#44598=CARTESIAN_POINT ( 'NONE',  ( 2.770579946183335807, 2.954332771348919362, -7.230573341413116140 ) ) ;
#44603=CARTESIAN_POINT ( 'NONE',  ( 3.100650473569742438, 5.767490999797108664, 5.429218121582397139 ) ) ;
#44606=CARTESIAN_POINT ( 'NONE',  ( 0.2759803524722215795, 10.51260004517012270, 6.288205958087823788 ) ) ;
#44607=CARTESIAN_POINT ( 'NONE',  ( 3.152665057734108878, -7.886634106564198277, 0.9030954876737806725 ) ) ;
#44611=CARTESIAN_POINT ( 'NONE',  ( 2.242418902651940993, -1.423836467585299914, -7.500817491983890584 ) ) ;
#44612=CARTESIAN_POINT ( 'NONE',  ( -14.47334165536100059, 0.000000000000000000, -6.000000000000000888 ) ) ;
#44616=CARTESIAN_POINT ( 'NONE',  ( 0.3223008802179271326, -6.343104382804245489, -10.49760329338526432 ) ) ;
#44618=EDGE_LOOP ( 'NONE', ( #58573, #12526, #16798, #11165 ) ) ;
#44625=CARTESIAN_POINT ( 'NONE',  ( 0.3537226245948357217, -3.952322262392311103, -11.62199823003437871 ) ) ;
#44640=CARTESIAN_POINT ( 'NONE',  ( 2.305787727787084407, 7.249469779319909435, 2.461236246751095536 ) ) ;
#44649=DIRECTION ( 'NONE',  ( -0.3939253465568944290, 0.8669868725995557579, 0.3052156353794350796 ) ) ;
#44650=CARTESIAN_POINT ( 'NONE',  ( 1.020182472821379527, 12.22263240120502026, 2.608319446514492324 ) ) ;
#44657=AXIS2_PLACEMENT_3D ( 'NONE', #1287, #47173, #62423 ) ;
#44680=VERTEX_POINT ( 'NONE', #23065 ) ;
#44686=CARTESIAN_POINT ( 'NONE',  ( 1.634816307076185193, -12.36483956257026939, -2.910502128620845674 ) ) ;
#44691=CARTESIAN_POINT ( 'NONE',  ( 0.3474126878361846749, -10.75620725594711580, -5.911350916722150295 ) ) ;
#44692=CARTESIAN_POINT ( 'NONE',  ( 2.241526690369556096, 0.01730530154276703134, 7.634439869182785721 ) ) ;
#44695=CARTESIAN_POINT ( 'NONE',  ( 5.514970785353741078, -0.004694330894494715307, -0.0005190732562554894796 ) ) ;
#44707=CARTESIAN_POINT ( 'NONE',  ( 5.536195898058073439, -0.001726268814999567603, -0.008323005098841091201 ) ) ;
#44714=EDGE_CURVE ( 'NONE', #27543, #3865, #64545, .T. ) ;
#44721=CARTESIAN_POINT ( 'NONE',  ( 2.251152103363646351, -7.498874008626767562, 1.449454666117707236 ) ) ;
#44722=LINE ( 'NONE', #32381, #57440 ) ;
#44724=CARTESIAN_POINT ( 'NONE',  ( 2.255723233588951882, 7.638048593862505342, 0.1321982600347512971 ) ) ;
#44727=CARTESIAN_POINT ( 'NONE',  ( 2.406456491625821759, 1.188938370543313860, -10.36527681096184672 ) ) ;
#44729=VERTEX_POINT ( 'NONE', #8753 ) ;
#44732=CONICAL_SURFACE ( 'NONE', #16064, 7.580821595991582562, 0.3217505529694035249 ) ;
#44748=CARTESIAN_POINT ( 'NONE',  ( 0.2650492433740059273, 12.07870441534856631, 2.017984765249114076 ) ) ;
#44755=CARTESIAN_POINT ( 'NONE',  ( 2.284126774967659923, -5.959830409747688407, 4.793997684221343647 ) ) ;
#44757=CARTESIAN_POINT ( 'NONE',  ( 0.2646305136544072623, -7.770320294339239098, 9.465888453932937097 ) ) ;
#44766=CARTESIAN_POINT ( 'NONE',  ( 2.080613030138688480, 4.898587196589412829E-16, -4.000000000000000000 ) ) ;
#44767=EDGE_CURVE ( 'NONE', #46970, #9266, #19353, .T. ) ;
#44771=CARTESIAN_POINT ( 'NONE',  ( 2.251139882113957658, -7.218573619021352528, 2.495216312514858981 ) ) ;
#44778=CARTESIAN_POINT ( 'NONE',  ( 0.3675815128205894289, 5.910255304480445560, 10.76447900494942367 ) ) ;
#44779=CARTESIAN_POINT ( 'NONE',  ( 2.260457164925433027, 1.190240296004817511, -7.547495527592634090 ) ) ;
#44791=ORIENTED_EDGE ( 'NONE', *, *, #47699, .T. ) ;
#44801=EDGE_LOOP ( 'NONE', ( #37873, #43994, #41689, #12395 ) ) ;
#44802=CARTESIAN_POINT ( 'NONE',  ( 0.3675815128205894289, 2.391755495700603973, 12.04510820461660003 ) ) ;
#44813=CARTESIAN_POINT ( 'NONE',  ( 2.257661810676419467, 7.638648121130928281, -0.1348365785571233599 ) ) ;
#44824=B_SPLINE_CURVE_WITH_KNOTS ( 'NONE', 3,
 ( #49508, #39169, #50485, #55120, #59461, #54490, #19880 ),
 .UNSPECIFIED., .F., .F.,
 ( 4, 3, 4 ),
 ( 0.000000000000000000, 0.001700533616330542541, 0.005002426799371243599 ),
 .UNSPECIFIED. ) ;
#44825=CARTESIAN_POINT ( 'NONE',  ( 0.3278977287071236923, 9.235688435081733871, 8.073566434006613335 ) ) ;
#44828=CARTESIAN_POINT ( 'NONE',  ( 0.3223008802179229693, 0.2444878876723223515, 12.26274332232494224 ) ) ;
#44833=CARTESIAN_POINT ( 'NONE',  ( 2.298277635560282750, -7.506689984432316720, -1.491234112749268759 ) ) ;
#44837=CARTESIAN_POINT ( 'NONE',  ( 0.3040950598368152291, -4.428852722102656791, -11.43390362554257322 ) ) ;
#44852=CARTESIAN_POINT ( 'NONE',  ( 0.2648978790185602672, 12.24533305150758089, -0.1321385342562831633 ) ) ;
#44856=DIRECTION ( 'NONE',  ( 0.000000000000000000, 0.000000000000000000, -1.000000000000000000 ) ) ;
#44858=ORIENTED_EDGE ( 'NONE', *, *, #43095, .T. ) ;
#44864=CARTESIAN_POINT ( 'NONE',  ( 2.276198483118645921, 6.543270001966289939, 3.955655305431081015 ) ) ;
#44866=CARTESIAN_POINT ( 'NONE',  ( 2.556980015514263460, 6.584367695372324469, -4.067895092073666952 ) ) ;
#44871=ORIENTED_EDGE ( 'NONE', *, *, #17547, .T. ) ;
#44872=VERTEX_POINT ( 'NONE', #45614 ) ;
#44875=EDGE_CURVE ( 'NONE', #5276, #63698, #36767, .T. ) ;
#44877=B_SPLINE_CURVE_WITH_KNOTS ( 'NONE', 3,
 ( #12186, #27473, #11215, #1583, #7192, #36480, #1246, #904, #41791, #5926, #51479, #52765, #47773, #62085, #42102, #56793, #57102, #20856, #41124 ),
 .UNSPECIFIED., .F., .F.,
 ( 4, 3, 3, 3, 3, 3, 4 ),
 ( 0.000000000000000000, 2.831840207499747818E-05, 4.217266859840622183E-05, 5.602024318396007954E-05, 6.290810167969113043E-05, 9.120440630945109367E-05, 0.0001153103026479756967 ),
 .UNSPECIFIED. ) ;
#44882=CARTESIAN_POINT ( 'NONE',  ( 0.3665391374699465965, 10.50279796150445755, -6.368473106897019065 ) ) ;
#44884=CARTESIAN_POINT ( 'NONE',  ( 3.092491956585503132, 7.275786042219460015, -3.124176487320081019 ) ) ;
#44887=CARTESIAN_POINT ( 'NONE',  ( 3.100650473569750876, -7.074394303868237976, 3.562766772868519727 ) ) ;
#44893=CIRCLE ( 'NONE', #12998, 7.938172270156617749 ) ;
#44907=CARTESIAN_POINT ( 'NONE',  ( 0.8375941296816566961, 9.769835228044911446, -7.696026447556128858 ) ) ;
#44914=CARTESIAN_POINT ( 'NONE',  ( 1.719304012338439325, 7.017415949612858306, 10.62216384465677521 ) ) ;
#44917=CARTESIAN_POINT ( 'NONE',  ( 0.2648978790185593790, 10.67083876753491900, 6.008231198269021078 ) ) ;
#44924=ORIENTED_EDGE ( 'NONE', *, *, #8539, .T. ) ;
#44926=CARTESIAN_POINT ( 'NONE',  ( 1.719304012341537957, 12.20344780066137602, -3.626341562669237906 ) ) ;
#44928=AXIS2_PLACEMENT_3D ( 'NONE', #60057, #20139, #50421 ) ;
#44931=CARTESIAN_POINT ( 'NONE',  ( 2.251152103363643242, -5.930529991878042750, -4.812779263775083471 ) ) ;
#44932=CARTESIAN_POINT ( 'NONE',  ( 3.152665057736256493, -0.9030954876717440793, 7.886634106564762270 ) ) ;
#44945=CARTESIAN_POINT ( 'NONE',  ( 0.2648978790185584908, 6.008231198268983775, 10.67083876753494032 ) ) ;
#44950=EDGE_CURVE ( 'NONE', #7261, #11247, #1042, .T. ) ;
#44962=VECTOR ( 'NONE', #13884, 1000.000000000000114 ) ;
#44968=EDGE_CURVE ( 'NONE', #48281, #22893, #32688, .T. ) ;
#44969=EDGE_CURVE ( 'NONE', #32172, #20267, #223, .T. ) ;
#44971=CARTESIAN_POINT ( 'NONE',  ( 0.5572780756284869685, -9.649189244958623846, 7.697784780878684785 ) ) ;
#44980=CARTESIAN_POINT ( 'NONE',  ( 2.259025283528087513, 5.764013728792251712, -5.014999102875807857 ) ) ;
#44991=CARTESIAN_POINT ( 'NONE',  ( 0.3223008802179207488, 8.069628056118119730, 9.236652594547164696 ) ) ;
#44993=FACE_OUTER_BOUND ( 'NONE', #60419, .T. ) ;
#45003=VERTEX_POINT ( 'NONE', #23218 ) ;
#45004=CARTESIAN_POINT ( 'NONE',  ( 2.034671305879419467, -8.476347594674740193, -8.030508024280845092 ) ) ;
#45020=CARTESIAN_POINT ( 'NONE',  ( 2.941278708680199916, 1.198640839021308357, 6.021511413163964654 ) ) ;
#45025=CARTESIAN_POINT ( 'NONE',  ( 0.2648321136542700072, -12.08378267055566013, 1.986804758684075578 ) ) ;
#45034=ORIENTED_EDGE ( 'NONE', *, *, #31825, .F. ) ;
#45048=ADVANCED_FACE ( 'NONE', ( #48191 ), #49148, .F. ) ;
#45063=( BOUNDED_SURFACE ( )  B_SPLINE_SURFACE ( 3, 1, ( 
 ( #53101, #58429 ),
 ( #38459, #23167 ),
 ( #63710, #33480 ),
 ( #53769, #22179 ) ),
 .UNSPECIFIED., .F., .F., .F. ) 
 B_SPLINE_SURFACE_WITH_KNOTS ( ( 4, 4 ),
 ( 2, 2 ),
 ( 0.000000000000000000, 1.000000000000000000 ),
 ( 0.000000000000000000, 1.000000000000000000 ),
 .UNSPECIFIED. ) 
 GEOMETRIC_REPRESENTATION_ITEM ( )  RATIONAL_B_SPLINE_SURFACE ( (
 ( 1.000000000000000000, 1.000000000000000000),
 ( 0.9942764183789327692, 0.8450855930916580938),
 ( 0.9942764183789327692, 0.8450855930916580938),
 ( 1.000000000000000000, 1.000000000000000000) ) ) 
 REPRESENTATION_ITEM ( '' )  SURFACE ( )  );
#45066=ORIENTED_EDGE ( 'NONE', *, *, #37842, .T. ) ;
#45070=CARTESIAN_POINT ( 'NONE',  ( 2.273267844204866162, -7.501135923490791946, 1.476347988307447734 ) ) ;
#45073=CARTESIAN_POINT ( 'NONE',  ( 0.3675815128205894289, -12.04510820461660892, 2.391755495700564449 ) ) ;
#45088=CARTESIAN_POINT ( 'NONE',  ( 2.305787727787084407, -5.970480882365253983, 4.792270232040873879 ) ) ;
#45091=B_SPLINE_CURVE_WITH_KNOTS ( 'NONE', 3,
 ( #50392, #40049, #55022, #24778, #45700, #60337, #15756 ),
 .UNSPECIFIED., .F., .F.,
 ( 4, 3, 4 ),
 ( 3.893818994016422208E-15, 0.002398160485434589102, 0.005002426799381067338 ),
 .UNSPECIFIED. ) ;
#45096=CARTESIAN_POINT ( 'NONE',  ( 0.2653141334712571520, 12.06772877558523227, 2.083134085643086220 ) ) ;
#45106=CARTESIAN_POINT ( 'NONE',  ( 2.899286259009568045, 6.616268644969683699, 4.231523595108440894 ) ) ;
#45113=CARTESIAN_POINT ( 'NONE',  ( 1.287602823384977446, 12.57487505104494119, 0.5522659225141822725 ) ) ;
#45118=CARTESIAN_POINT ( 'NONE',  ( 2.305787727787083519, -7.654065630109506913, -0.1666591538753489643 ) ) ;
#45122=CARTESIAN_POINT ( 'NONE',  ( 0.3537226245948363323, -11.44347094181049229, -4.442821955543915458 ) ) ;
#45128=CARTESIAN_POINT ( 'NONE',  ( 2.251139882113958102, -5.003859976903235030, 5.770207524085884110 ) ) ;
#45134=EDGE_LOOP ( 'NONE', ( #13052, #43883, #37666, #55349 ) ) ;
#45147=CARTESIAN_POINT ( 'NONE',  ( 2.297017764050092836, 7.133399178907352756, -2.771707546665520994 ) ) ;
#45153=CARTESIAN_POINT ( 'NONE',  ( 0.2648978790185602672, 7.769924372105329269, -9.465406350830530613 ) ) ;
#45154=CARTESIAN_POINT ( 'NONE',  ( 0.2650492433740071485, -9.309907554970028087, 7.955688793816054982 ) ) ;
#45155=CARTESIAN_POINT ( 'NONE',  ( 1.452237505248552996, -10.65201107290462623, -6.833827325205429126 ) ) ;
#45164=CARTESIAN_POINT ( 'NONE',  ( 0.3109076770649027432, 0.2359198520041151936, 12.25911371383827309 ) ) ;
#45167=CARTESIAN_POINT ( 'NONE',  ( 2.259830038564996091, -7.499347412930715606, -1.462175769136920156 ) ) ;
#45169=DIRECTION ( 'NONE',  ( -1.000000000000000000, -0.000000000000000000, -0.000000000000000000 ) ) ;
#45170=CARTESIAN_POINT ( 'NONE',  ( 5.515539859299206427, -0.003193223631738841602, 0.005142293699651627470 ) ) ;
#45171=ORIENTED_EDGE ( 'NONE', *, *, #52998, .T. ) ;
#45172=CARTESIAN_POINT ( 'NONE',  ( 2.241352910868909643, -2.532612177304395029, -7.202080440908765979 ) ) ;
#45173=CARTESIAN_POINT ( 'NONE',  ( 2.717984159219170692, 2.397195612260841102, -7.415470774236799123 ) ) ;
#45183=ADVANCED_FACE ( 'NONE', ( #65712 ), #31636, .F. ) ;
#45184=CARTESIAN_POINT ( 'NONE',  ( 0.3341166715381287955, -0.2526177176099212440, -12.26652061402056404 ) ) ;
#45189=EDGE_LOOP ( 'NONE', ( #62482, #44386, #19330, #482 ) ) ;
#45206=CARTESIAN_POINT ( 'NONE',  ( 2.406456491626046912, -8.382123850278466293, -6.212289237905048722 ) ) ;
#45211=ADVANCED_FACE ( 'NONE', ( #56418 ), #17685, .F. ) ;
#45221=CARTESIAN_POINT ( 'NONE',  ( 2.655192694323576852, 2.733486750964913892, -9.204230091443479367 ) ) ;
#45223=CARTESIAN_POINT ( 'NONE',  ( 0.3278977287071236923, 11.60975784853197545, -3.961557589215493280 ) ) ;
#45238=ORIENTED_EDGE ( 'NONE', *, *, #9691, .T. ) ;
#45239=CARTESIAN_POINT ( 'NONE',  ( 0.2657645697724667633, -10.68050050043095567, 5.991637049003212034 ) ) ;
#45240=CARTESIAN_POINT ( 'NONE',  ( 0.3053067050349170808, 3.975408458060513794, 11.59706307017084193 ) ) ;
#45241=CARTESIAN_POINT ( 'NONE',  ( 2.266490820343221468, -6.690312181904289446, -3.694838443752371582 ) ) ;
#45246=CARTESIAN_POINT ( 'NONE',  ( 2.889800649504073782, -3.002151847318954125, 5.334644486274186193 ) ) ;
#45248=ORIENTED_EDGE ( 'NONE', *, *, #26032, .T. ) ;
#45251=CARTESIAN_POINT ( 'NONE',  ( 2.835339799623982859, 6.941489812670579518, -3.628068688271603559 ) ) ;
#45252=CARTESIAN_POINT ( 'NONE',  ( 2.258463476536300973, -3.701774005561162095, -6.683417898966597548 ) ) ;
#45261=CARTESIAN_POINT ( 'NONE',  ( 0.3223008802179238019, -12.11889957318022937, -1.888629463821808852 ) ) ;
#45268=ORIENTED_EDGE ( 'NONE', *, *, #8860, .T. ) ;
#45271=EDGE_LOOP ( 'NONE', ( #52251, #41155, #22272, #25937 ) ) ;
#45273=CARTESIAN_POINT ( 'NONE',  ( 5.515539859299206427, -0.0001942659352248233629, 0.006049968793488396702 ) ) ;
#45274=DIRECTION ( 'NONE',  ( 0.000000000000000000, 0.000000000000000000, 1.000000000000000000 ) ) ;
#45276=CARTESIAN_POINT ( 'NONE',  ( 5.515539859299206427, -0.004759416711442203581, -0.003740028639278331068 ) ) ;
#45282=CARTESIAN_POINT ( 'NONE',  ( 2.781367136452478572, 3.637318098960558022, -6.916275212954685614 ) ) ;
#45286=CARTESIAN_POINT ( 'NONE',  ( 3.031336079629378677, -2.306006909710469621, 7.553623348802286586 ) ) ;
#45287=ORIENTED_EDGE ( 'NONE', *, *, #38418, .F. ) ;
#45288=LINE ( 'NONE', #409, #6735 ) ;
#45295=ORIENTED_EDGE ( 'NONE', *, *, #8860, .F. ) ;
#45301=CARTESIAN_POINT ( 'NONE',  ( 1.283627346226769328, -6.763590725840913365, -10.61381050043338448 ) ) ;
#45303=CARTESIAN_POINT ( 'NONE',  ( 0.2958664285830425733, -12.25438626999990355, 0.2205161970873960042 ) ) ;
#45313=VERTEX_POINT ( 'NONE', #13473 ) ;
#45319=CARTESIAN_POINT ( 'NONE',  ( 2.241352910868908310, 7.202080440908741998, 2.532612177304466972 ) ) ;
#45322=CARTESIAN_POINT ( 'NONE',  ( 3.152665057734040488, 0.000000000000000000, 0.000000000000000000 ) ) ;
#45325=CARTESIAN_POINT ( 'NONE',  ( 2.770579946183323372, -6.173813901927566405, 4.784693811915867734 ) ) ;
#45327=CARTESIAN_POINT ( 'NONE',  ( 0.2653519789438750220, -7.888580323518811888, -9.366970421692856874 ) ) ;
#45328=EDGE_LOOP ( 'NONE', ( #47474, #40990, #24229, #54221 ) ) ;
#45334=B_SPLINE_CURVE_WITH_KNOTS ( 'NONE', 3,
 ( #45073, #35726, #50721, #177, #65008, #20458, #30737, #40734, #65340, #51050, #34735, #5509, #25776, #15771, #31086, #19481 ),
 .UNSPECIFIED., .F., .F.,
 ( 4, 3, 3, 3, 3, 4 ),
 ( 4.336808689942017736E-19, 0.0003017745587525235665, 0.0006035491769808712468, 0.0009053241094668126702, 0.001207275924540017736, 0.001510325902533037534 ),
 .UNSPECIFIED. ) ;
#45337=CARTESIAN_POINT ( 'NONE',  ( 2.268878695253353950, 6.692359410363658334, -3.692782103667214155 ) ) ;
#45360=CARTESIAN_POINT ( 'NONE',  ( 0.3610902822527242151, -10.76187877352508870, -5.910495176556292307 ) ) ;
#45362=CARTESIAN_POINT ( 'NONE',  ( 2.305787727787084407, -1.493241775258372872, -7.508843116234172221 ) ) ;
#45370=CARTESIAN_POINT ( 'NONE',  ( 0.3106921474978561748, 9.542334142800575236, -7.699584408545789849 ) ) ;
#45383=CARTESIAN_POINT ( 'NONE',  ( 0.3632410797595246321, 10.49990774419911155, -6.365652464380801234 ) ) ;
#45386=CARTESIAN_POINT ( 'NONE',  ( 1.719304012338199517, 12.20344780065974888, 3.626341562670754914 ) ) ;
#45406=CARTESIAN_POINT ( 'NONE',  ( 2.639814597422739162, -0.2564041122425642083, 7.763021810282391577 ) ) ;
#45407=CARTESIAN_POINT ( 'NONE',  ( 0.3665391374699472626, 10.50279796150445577, -6.368473106897019953 ) ) ;
#45411=CARTESIAN_POINT ( 'NONE',  ( 5.516018279890452902, -0.004525000489649900863, 0.005042957932159117078 ) ) ;
#45413=CARTESIAN_POINT ( 'NONE',  ( 2.241509619876138171, -3.784042210004660678, -6.630717740088888590 ) ) ;
#45426=CARTESIAN_POINT ( 'NONE',  ( 2.907497136250727365, -7.497839665536855769, -2.346692756478276021 ) ) ;
#45427=ORIENTED_EDGE ( 'NONE', *, *, #832, .F. ) ;
#45428=CARTESIAN_POINT ( 'NONE',  ( 0.2648978790185584908, 7.769924372105204036, 9.465406350830633642 ) ) ;
#45433=( BOUNDED_SURFACE ( )  B_SPLINE_SURFACE ( 3, 1, ( 
 ( #39517, #35511 ),
 ( #50815, #34199 ),
 ( #19249, #45480 ),
 ( #4282, #59481 ) ),
 .UNSPECIFIED., .F., .F., .F. ) 
 B_SPLINE_SURFACE_WITH_KNOTS ( ( 4, 4 ),
 ( 2, 2 ),
 ( 0.000000000000000000, 1.000000000000000000 ),
 ( 0.000000000000000000, 1.000000000000000000 ),
 .UNSPECIFIED. ) 
 GEOMETRIC_REPRESENTATION_ITEM ( )  RATIONAL_B_SPLINE_SURFACE ( (
 ( 1.000000000000000000, 1.000000000000000000),
 ( 0.9942764183789327692, 0.8450855930916580938),
 ( 0.9942764183789327692, 0.8450855930916580938),
 ( 1.000000000000000000, 1.000000000000000000) ) ) 
 REPRESENTATION_ITEM ( '' )  SURFACE ( )  );
#45434=CARTESIAN_POINT ( 'NONE',  ( 0.3218525148189834151, -11.43947393562873849, -4.423735011438943765 ) ) ;
#45436=CARTESIAN_POINT ( 'NONE',  ( 2.266490820341529044, 1.183790889243382383, -7.550546162186090982 ) ) ;
#45438=ORIENTED_EDGE ( 'NONE', *, *, #5390, .T. ) ;
#45443=LINE ( 'NONE', #55096, #8823 ) ;
#45449=EDGE_LOOP ( 'NONE', ( #166, #63193, #39742, #9533 ) ) ;
#45459=CARTESIAN_POINT ( 'NONE',  ( 0.2653519991613820794, -10.61652626436032953, 6.104031847944984435 ) ) ;
#45463=CARTESIAN_POINT ( 'NONE',  ( 0.9296196016834894493, -11.85136013469028704, 3.871279966919827675 ) ) ;
#45477=EDGE_LOOP ( 'NONE', ( #56322, #49158, #60274, #15748 ) ) ;
#45480=CARTESIAN_POINT ( 'NONE',  ( 0.3040950598368144520, 11.43390362554253237, 4.428852722102769590 ) ) ;
#45482=CARTESIAN_POINT ( 'NONE',  ( 2.969415267404351244, -7.815364626283974658, -0.9841783286031883238 ) ) ;
#45487=CARTESIAN_POINT ( 'NONE',  ( 2.247112776671466694, -3.716786765232484857, 6.670755883245758966 ) ) ;
#45490=CARTESIAN_POINT ( 'NONE',  ( 2.241449424704146320, -6.642105568284079276, -3.763973574060608840 ) ) ;
#45493=VERTEX_POINT ( 'NONE', #26652 ) ;
#45495=EDGE_LOOP ( 'NONE', ( #9372, #61316, #7336, #49697 ) ) ;
#45503=EDGE_LOOP ( 'NONE', ( #47760, #1093, #9161, #63764 ) ) ;
#45504=CARTESIAN_POINT ( 'NONE',  ( 0.2646305136544072623, 7.770320294339302158, -9.465888453932885582 ) ) ;
#45505=ORIENTED_EDGE ( 'NONE', *, *, #29588, .T. ) ;
#45509=CARTESIAN_POINT ( 'NONE',  ( 0.7446945582506564465, 9.270687147117307347, 8.243982823408627425 ) ) ;
#45514=ORIENTED_EDGE ( 'NONE', *, *, #48710, .T. ) ;
#45529=CARTESIAN_POINT ( 'NONE',  ( 2.524535260912363466, 7.184101064217870203, -2.850096701925667109 ) ) ;
#45540=CARTESIAN_POINT ( 'NONE',  ( 2.305787727787084407, -5.756228004061490822, 5.047606869483037606 ) ) ;
#45541=CARTESIAN_POINT ( 'NONE',  ( 1.375507693217066008, 11.64019206974653642, 4.865932489130583072 ) ) ;
#45543=CARTESIAN_POINT ( 'NONE',  ( 3.047904605210430162, -0.9519317672906252303, -7.845751380824991017 ) ) ;
#45546=EDGE_LOOP ( 'NONE', ( #6734, #6928, #43915, #57119 ) ) ;
#45547=CARTESIAN_POINT ( 'NONE',  ( 2.276198483116796289, -2.469789406312446811, -7.236140649716140238 ) ) ;
#45553=ORIENTED_EDGE ( 'NONE', *, *, #48710, .F. ) ;
#45554=CARTESIAN_POINT ( 'NONE',  ( 0.3218525148189824159, -10.74192973049792066, 5.919623386703301904 ) ) ;
#45555=CARTESIAN_POINT ( 'NONE',  ( 0.3675815128205894289, 7.689697408877401941, -9.574637318041888889 ) ) ;
#45560=CARTESIAN_POINT ( 'NONE',  ( 2.260457164927186291, -7.639515169785726201, 0.1384509728648797844 ) ) ;
#45562=VERTEX_POINT ( 'NONE', #63525 ) ;
#45565=CARTESIAN_POINT ( 'NONE',  ( 0.5547464869798253151, 9.648168635481845001, 7.697709668896102642 ) ) ;
#45566=CARTESIAN_POINT ( 'NONE',  ( 2.373367633546870525, 6.738274194514266568, -3.681545031436583848 ) ) ;
#45568=CARTESIAN_POINT ( 'NONE',  ( 2.241449424704146320, 7.528892370271791812, 1.265244293929113972 ) ) ;
#45571=CARTESIAN_POINT ( 'NONE',  ( 1.194176325881334710, 5.827386336993033211, -11.12159247766666326 ) ) ;
#45573=CARTESIAN_POINT ( 'NONE',  ( 2.305787727787083519, 3.682701754025512919, 6.711944854845837583 ) ) ;
#45574=VECTOR ( 'NONE', #28830, 1000.000000000000227 ) ;
#45579=CARTESIAN_POINT ( 'NONE',  ( 0.3057689695767519256, -12.11137787899270002, -1.901059295891038836 ) ) ;
#45582=CARTESIAN_POINT ( 'NONE',  ( 2.244591118396555451, -5.917635828475942716, -4.825158615932966910 ) ) ;
#45584=CARTESIAN_POINT ( 'NONE',  ( 2.941278708680199916, 0.1348063076487806822, -6.138172921908579660 ) ) ;
#45598=B_SPLINE_CURVE_WITH_KNOTS ( 'NONE', 3,
 ( #18403, #12716, #28040, #53647, #7757, #8087, #48652 ),
 .UNSPECIFIED., .F., .F.,
 ( 4, 3, 4 ),
 ( 0.000000000000000000, 0.001700533616330600437, 0.005002426799370906195 ),
 .UNSPECIFIED. ) ;
#45600=CARTESIAN_POINT ( 'NONE',  ( 2.305787727787085295, -7.249469779319927198, 2.461236246751046242 ) ) ;
#45603=ORIENTED_EDGE ( 'NONE', *, *, #40930, .T. ) ;
#45610=EDGE_LOOP ( 'NONE', ( #53465, #62266, #53713, #39600 ) ) ;
#45611=CARTESIAN_POINT ( 'NONE',  ( 0.3164563675027652345, -6.338687639235967453, -10.49799587805937229 ) ) ;
#45614=CARTESIAN_POINT ( 'NONE',  ( 2.080613030138688480, 3.872983346207417021, 1.000000000000000000 ) ) ;
#45622=CARTESIAN_POINT ( 'NONE',  ( 1.719304012341582588, 5.690355757825640737, -11.38834240361563488 ) ) ;
#45637=DIRECTION ( 'NONE',  ( -1.000000000000000000, -0.000000000000000000, -0.000000000000000000 ) ) ;
#45640=CYLINDRICAL_SURFACE ( 'NONE', #50773, 6.000000000000000888 ) ;
#45658=EDGE_CURVE ( 'NONE', #33142, #55082, #59881, .T. ) ;
#45662=CARTESIAN_POINT ( 'NONE',  ( 0.2653141334712560417, 2.083134085643206568, -12.06772877558521806 ) ) ;
#45670=CARTESIAN_POINT ( 'NONE',  ( 2.257661810676420355, 0.1348365785570998787, 7.638648121130935387 ) ) ;
#45672=CARTESIAN_POINT ( 'NONE',  ( 5.520433897694421610, -0.01397038704729854953, -0.005630909886753013814 ) ) ;
#45675=LINE ( 'NONE', #9119, #49001 ) ;
#45684=CARTESIAN_POINT ( 'NONE',  ( 3.152665057736204535, -4.377619405894248139, -6.622010822085805160 ) ) ;
#45693=VERTEX_POINT ( 'NONE', #58918 ) ;
#45700=CARTESIAN_POINT ( 'NONE',  ( 2.655192694324109759, 7.714239566599824016, 5.716669423974572339 ) ) ;
#45707=CARTESIAN_POINT ( 'NONE',  ( 0.3223008802179264110, -12.03398982086835112, 2.370176598416293245 ) ) ;
#45715=CARTESIAN_POINT ( 'NONE',  ( 0.2872850955227737590, 10.50585060073189680, -6.306790329742824497 ) ) ;
#45737=CARTESIAN_POINT ( 'NONE',  ( 2.844750968615535669, 6.210802026112107299, 4.777247819183539690 ) ) ;
#45740=CARTESIAN_POINT ( 'NONE',  ( 2.931247277082685176, -0.3703309885897361209, 7.855653518374115407 ) ) ;
#45746=CARTESIAN_POINT ( 'NONE',  ( 2.994568964204213479, -6.620406464816364966, -4.283796412555548550 ) ) ;
#45748=ORIENTED_EDGE ( 'NONE', *, *, #48878, .F. ) ;
#45749=CARTESIAN_POINT ( 'NONE',  ( 2.241526690369556096, -3.832206765347542010, -6.602966219605680642 ) ) ;
#45757=VERTEX_POINT ( 'NONE', #344 ) ;
#45763=CARTESIAN_POINT ( 'NONE',  ( 3.031336079629428859, -7.553623348802302573, -2.306006909710477171 ) ) ;
#45766=CARTESIAN_POINT ( 'NONE',  ( 0.3160775863651080764, 7.697077652699450212, 9.546663463486071421 ) ) ;
#45767=EDGE_CURVE ( 'NONE', #43301, #64826, #46977, .T. ) ;
#45776=CARTESIAN_POINT ( 'NONE',  ( 2.276198483117261251, -5.031786924855515153, 5.756970692722257255 ) ) ;
#45780=SURFACE_STYLE_USAGE ( .BOTH. , #51768 ) ;
#45782=CARTESIAN_POINT ( 'NONE',  ( 3.031336079629727731, 1.779751109289623434, 7.694633165537369202 ) ) ;
#45789=ORIENTED_EDGE ( 'NONE', *, *, #31745, .F. ) ;
#45800=CARTESIAN_POINT ( 'NONE',  ( 2.889800649504073782, -3.118861721612602889, 5.267262008933660589 ) ) ;
#45807=CARTESIAN_POINT ( 'NONE',  ( 2.263328370261529887, 7.640407877530305925, -0.1420109704216046820 ) ) ;
#45821=EDGE_CURVE ( 'NONE', #35612, #8110, #914, .T. ) ;
#45825=CARTESIAN_POINT ( 'NONE',  ( 2.241449424704146320, -4.860179885671838562, 5.887589908049627674 ) ) ;
#45827=CARTESIAN_POINT ( 'NONE',  ( 0.000000000000000000, 0.000000000000000000, 0.000000000000000000 ) ) ;
#45834=CARTESIAN_POINT ( 'NONE',  ( 2.350038591457883186, 5.855794476068868271, -8.861946706686296693 ) ) ;
#45844=CARTESIAN_POINT ( 'NONE',  ( 0.3632410797595224117, -0.2628628737172604701, -12.27601307605977965 ) ) ;
#45856=CARTESIAN_POINT ( 'NONE',  ( 2.903928887688506322, 4.835706109686078058, 7.316175791235219883 ) ) ;
#45859=CARTESIAN_POINT ( 'NONE',  ( 0.6511581176954504002, 9.263557799002967386, 8.205008037406312127 ) ) ;
#45860=CARTESIAN_POINT ( 'NONE',  ( 2.990245332647883281, -4.676740826320302524, 7.075286609974379637 ) ) ;
#45861=CARTESIAN_POINT ( 'NONE',  ( 0.3675815128205894289, 10.76447900494948584, -5.910255304480332761 ) ) ;
#45863=ORIENTED_EDGE ( 'NONE', *, *, #62654, .F. ) ;
#45864=CARTESIAN_POINT ( 'NONE',  ( 0.9296196016833910836, -10.99907063288863540, 5.870433615766981639 ) ) ;
#45865=ORIENTED_EDGE ( 'NONE', *, *, #9151, .T. ) ;
#45871=ORIENTED_EDGE ( 'NONE', *, *, #40748, .F. ) ;
#45873=CARTESIAN_POINT ( 'NONE',  ( 1.719304012340734378, -7.581471372739226666, -10.22720798541506682 ) ) ;
#45878=CARTESIAN_POINT ( 'NONE',  ( 2.305787727787083519, 7.135468203930020792, -2.774453000917077805 ) ) ;
#45882=CARTESIAN_POINT ( 'NONE',  ( 3.047904605210427942, -7.047014837597081360, 3.577928268982043747 ) ) ;
#45885=CARTESIAN_POINT ( 'NONE',  ( 0.4613984246114875010, -11.66278164635732217, -3.943860067443764716 ) ) ;
#45889=ORIENTED_EDGE ( 'NONE', *, *, #60975, .T. ) ;
#45890=CARTESIAN_POINT ( 'NONE',  ( 2.969415267404014624, -5.777543886622418690, 5.354299007565158419 ) ) ;
#45896=CARTESIAN_POINT ( 'NONE',  ( 2.259830038564644816, -2.483392345595102579, -7.225713255971310645 ) ) ;
#45901=CARTESIAN_POINT ( 'NONE',  ( 0.2833330754217375791, -10.71034013638382021, 5.950193237802373858 ) ) ;
#45902=CARTESIAN_POINT ( 'NONE',  ( 5.536195898058073439, 0.002666509901870070445, -0.008071068258923577710 ) ) ;
#45903=CARTESIAN_POINT ( 'NONE',  ( 1.549075743847115660, -10.62322497417014411, -6.912427991524592308 ) ) ;
#45904=AXIS2_PLACEMENT_3D ( 'NONE', #57391, #32099, #27131 ) ;
#45905=B_SPLINE_CURVE_WITH_KNOTS ( 'NONE', 3,
 ( #54709, #9130, #4156, #44692, #64982, #19455, #39725 ),
 .UNSPECIFIED., .F., .F.,
 ( 4, 3, 4 ),
 ( 9.486769009248163798E-19, 6.607638129004464488E-05, 8.338150981378363025E-05 ),
 .UNSPECIFIED. ) ;
#45906=EDGE_CURVE ( 'NONE', #29286, #11102, #37952, .T. ) ;
#45911=ORIENTED_EDGE ( 'NONE', *, *, #18326, .F. ) ;
#45913=CARTESIAN_POINT ( 'NONE',  ( 2.639814597422738718, 6.851176153958525639, -3.659458430304273868 ) ) ;
#45923=CARTESIAN_POINT ( 'NONE',  ( 0.2958664285830414076, 12.25438626999990710, -0.2205161970874815469 ) ) ;
#45936=CARTESIAN_POINT ( 'NONE',  ( 5.514970785353741078, 0.001326349372336578557, 0.004532877335078321253 ) ) ;
#45938=CARTESIAN_POINT ( 'NONE',  ( 2.247206125383336417, -1.211896144125592878, -7.539576157880987672 ) ) ;
#45945=CARTESIAN_POINT ( 'NONE',  ( 2.373367633546871414, 2.795365972209170824, -7.151506276328599476 ) ) ;
#45958=CARTESIAN_POINT ( 'NONE',  ( 0.3665391374699472626, -10.50279796150441136, 6.368473106897092784 ) ) ;
#45965=CARTESIAN_POINT ( 'NONE',  ( 0.2655924914740778742, -11.52280271232868003, -4.147079829127369166 ) ) ;
#45968=CARTESIAN_POINT ( 'NONE',  ( 0.2834382757448027368, -12.25055062943084394, 0.2027202995056558987 ) ) ;
#45969=CARTESIAN_POINT ( 'NONE',  ( 2.256373768223416842, 5.765785888499285861, -5.011614056001876705 ) ) ;
#45971=CARTESIAN_POINT ( 'NONE',  ( 0.2638984909335716500, 1.930290337334056749, 12.09426044257624788 ) ) ;
#45973=ORIENTED_EDGE ( 'NONE', *, *, #11757, .T. ) ;
#45982=CARTESIAN_POINT ( 'NONE',  ( 0.2648978790185602672, 7.972372351883029395, 9.295532325666474804 ) ) ;
#45987=ORIENTED_EDGE ( 'NONE', *, *, #58535, .T. ) ;
#45995=VECTOR ( 'NONE', #65706, 1000.000000000000000 ) ;
#46000=B_SPLINE_CURVE_WITH_KNOTS ( 'NONE', 3,
 ( #58681, #38026, #8122, #59312, #43676, #13738, #58334, #23407, #13103, #63963, #18444, #39681, #14397, #15392, #14072, #55957 ),
 .UNSPECIFIED., .F., .F.,
 ( 4, 3, 3, 3, 3, 4 ),
 ( 5.421010862427522170E-20, 0.0003017745587525248675, 0.0006035491769808740657, 0.0009053241094668204765, 0.001207275924540515818, 0.001510325902534030229 ),
 .UNSPECIFIED. ) ;
#46003=CARTESIAN_POINT ( 'NONE',  ( 2.241352910868908310, 0.08337961031714861970, -7.633946224498473043 ) ) ;
#46008=CARTESIAN_POINT ( 'NONE',  ( 1.020182472823635500, -3.852445298735368784, -11.88926988382057282 ) ) ;
#46012=FACE_OUTER_BOUND ( 'NONE', #38237, .T. ) ;
#46013=CARTESIAN_POINT ( 'NONE',  ( 0.2646305136544065406, -10.67138229758225343, -6.008537389229527292 ) ) ;
#46022=CARTESIAN_POINT ( 'NONE',  ( 2.305787727787084407, -6.545285700970554288, 3.971363876083942035 ) ) ;
#46026=ORIENTED_EDGE ( 'NONE', *, *, #53397, .F. ) ;
#46029=ORIENTED_EDGE ( 'NONE', *, *, #63412, .T. ) ;
#46035=CARTESIAN_POINT ( 'NONE',  ( 2.889800649504073782, -2.156828754871506604, 5.728825117897699215 ) ) ;
#46037=CARTESIAN_POINT ( 'NONE',  ( 0.3341166715381324592, -10.74942732659227751, -5.914486946114021926 ) ) ;
#46046=ORIENTED_EDGE ( 'NONE', *, *, #2463, .F. ) ;
#46047=CARTESIAN_POINT ( 'NONE',  ( 0.3160775863651184570, 9.546663463486153134, -7.697077652699344519 ) ) ;
#46055=CARTESIAN_POINT ( 'NONE',  ( 0.2915757698887282423, -12.02962099476165392, 2.339174865979246398 ) ) ;
#46061=AXIS2_PLACEMENT_3D ( 'NONE', #22256, #37885, #12942 ) ;
#46062=EDGE_CURVE ( 'NONE', #15837, #46970, #4102, .T. ) ;
#46067=CARTESIAN_POINT ( 'NONE',  ( 1.372161826076370383, -10.61825687422744124, 6.811451307636625430 ) ) ;
#46068=CARTESIAN_POINT ( 'NONE',  ( 0.2657645697724685951, 0.1513403555227276764, -12.24540328300721725 ) ) ;
#46070=CARTESIAN_POINT ( 'NONE',  ( 2.245754705088395031, 7.635057163463317309, 0.1113317465207070839 ) ) ;
#46077=CARTESIAN_POINT ( 'NONE',  ( 2.241317068080785901, 7.501982551779192043, -1.415707718487429823 ) ) ;
#46078=CARTESIAN_POINT ( 'NONE',  ( 1.719304012343089161, 12.64775761152706401, -1.452142814147889816 ) ) ;
#46079=EDGE_CURVE ( 'NONE', #49417, #16846, #34809, .T. ) ;
#46083=CARTESIAN_POINT ( 'NONE',  ( 0.3665391374699464300, -9.237363111276710725, -8.095513416941326312 ) ) ;
#46084=CARTESIAN_POINT ( 'NONE',  ( 0.7446945582529461705, 2.504154979876664910, -12.15064199164638126 ) ) ;
#46087=CIRCLE ( 'NONE', #5759, 12.73084802173761787 ) ;
#46088=CARTESIAN_POINT ( 'NONE',  ( 0.2653519991613820239, 10.59450977800982230, 6.142165520908205778 ) ) ;
#46089=CARTESIAN_POINT ( 'NONE',  ( 2.556980015514295435, 1.116161541731621520, -7.658710847181731118 ) ) ;
#46098=ORIENTED_EDGE ( 'NONE', *, *, #3843, .T. ) ;
#46103=VERTEX_POINT ( 'NONE', #55449 ) ;
#46104=CARTESIAN_POINT ( 'NONE',  ( 1.719304012339833099, -9.242227816401946683, 8.755325027794301107 ) ) ;
#46109=CARTESIAN_POINT ( 'NONE',  ( 2.705197763288543555, 1.076142490489871317, 7.714317563576063463 ) ) ;
#46115=CARTESIAN_POINT ( 'NONE',  ( 0.3053067050349148603, 7.702091166066015404, 9.538004819224376263 ) ) ;
#46117=CARTESIAN_POINT ( 'NONE',  ( 0.2653141617321028156, -7.905395731875554333, 9.352766656400028467 ) ) ;
#46121=CARTESIAN_POINT ( 'NONE',  ( 0.3675815128205912052, 11.44679196252415210, -4.447030445008065769 ) ) ;
#46126=EDGE_CURVE ( 'NONE', #57990, #57528, #15526, .T. ) ;
#46127=CARTESIAN_POINT ( 'NONE',  ( 0.3278977287071177527, 11.44003061923231535, 4.427879319182928874 ) ) ;
#46128=CONICAL_SURFACE ( 'NONE', #12118, 7.938172270156617749, 1.280189991382167047 ) ;
#46132=CARTESIAN_POINT ( 'NONE',  ( 0.2638984909335716500, -10.50550771760515545, -6.295352574289097447 ) ) ;
#46141=ORIENTED_EDGE ( 'NONE', *, *, #26334, .T. ) ;
#46143=CARTESIAN_POINT ( 'NONE',  ( 5.530133899448235191, 0.01536822665454895542, -0.004396748047611278437 ) ) ;
#46156=CARTESIAN_POINT ( 'NONE',  ( 0.3057689695767532578, -10.73077184758787617, -5.928746590069690292 ) ) ;
#46157=CARTESIAN_POINT ( 'NONE',  ( 2.034671305880252135, 10.71175679137217784, 4.647127512368699698 ) ) ;
#46160=EDGE_CURVE ( 'NONE', #60006, #42211, #62724, .T. ) ;
#46167=DIRECTION ( 'NONE',  ( -1.000000000000000000, -0.000000000000000000, -0.000000000000000000 ) ) ;
#46173=CARTESIAN_POINT ( 'NONE',  ( 3.031336079629786795, -0.9593005538805217114, 7.839300734793265057 ) ) ;
#46188=CARTESIAN_POINT ( 'NONE',  ( 0.3053067050349194678, -11.59706307017085791, 3.975408458060472938 ) ) ;
#46190=ORIENTED_EDGE ( 'NONE', *, *, #14415, .T. ) ;
#46192=ORIENTED_EDGE ( 'NONE', *, *, #17607, .F. ) ;
#46193=CARTESIAN_POINT ( 'NONE',  ( 2.241311220309555541, -6.564680916077770156, -3.897297589552050301 ) ) ;
#46199=CARTESIAN_POINT ( 'NONE',  ( 0.6511581176972721652, 10.87850887236121977, -5.898618881004612291 ) ) ;
#46200=CARTESIAN_POINT ( 'NONE',  ( 1.287602823390032958, 12.47973441446294807, -1.639728374784856113 ) ) ;
#46203=ORIENTED_EDGE ( 'NONE', *, *, #9759, .T. ) ;
#46207=CARTESIAN_POINT ( 'NONE',  ( 0.2958664285830445717, -9.245659426743934262, 8.045892866065326388 ) ) ;
#46213=CARTESIAN_POINT ( 'NONE',  ( 1.948354844648340745, 11.88693049003635238, 1.364409644998757276 ) ) ;
#46215=CARTESIAN_POINT ( 'NONE',  ( 2.781367136452389310, 2.960151187465042355, 7.232043329634182172 ) ) ;
#46222=CARTESIAN_POINT ( 'NONE',  ( 0.2676618633000479863, 11.56235835488945973, -4.037335446657117188 ) ) ;
#46225=ORIENTED_EDGE ( 'NONE', *, *, #23729, .T. ) ;
#46227=CARTESIAN_POINT ( 'NONE',  ( 1.198791140417288847, 11.61358959650646483, 4.776130053251955943 ) ) ;
#46232=CARTESIAN_POINT ( 'NONE',  ( 2.258463476536303638, -2.484972401833594358, -7.224688073723371851 ) ) ;
#46239=CARTESIAN_POINT ( 'NONE',  ( 5.520433897694421610, 0.01186170453199860732, 0.009283255140285660498 ) ) ;
#46262=CARTESIAN_POINT ( 'NONE',  ( 5.520433897694421610, 0.007082458259338205234, 0.01329351892497965086 ) ) ;
#46264=CARTESIAN_POINT ( 'NONE',  ( 1.937114397841935398, 9.228205347192574237, -8.920887662793379747 ) ) ;
#46265=CARTESIAN_POINT ( 'NONE',  ( 5.536195898058073439, -0.004027525919832385289, -0.007485416011287845603 ) ) ;
#46272=CARTESIAN_POINT ( 'NONE',  ( 3.100650473569671828, -7.585586315875718633, 2.280184661131201107 ) ) ;
#46273=CARTESIAN_POINT ( 'NONE',  ( 0.2958664285830423513, -1.910785783655658765, 12.10650684287254464 ) ) ;
#46277=CARTESIAN_POINT ( 'NONE',  ( 2.899286259009686617, 7.845618522360458869, 0.3564726075923687620 ) ) ;
#46285=CARTESIAN_POINT ( 'NONE',  ( 2.241317068080786346, 4.836852665784303618, -5.906676463196497195 ) ) ;
#46291=CARTESIAN_POINT ( 'NONE',  ( 0.6473888112830226138, 7.698027285532596409, -9.687359867659717239 ) ) ;
#46296=CARTESIAN_POINT ( 'NONE',  ( 2.273267844204863497, 3.952852893982297555, 6.543821324256898109 ) ) ;
#46309=B_SPLINE_CURVE_WITH_KNOTS ( 'NONE', 3,
 ( #56866, #51220, #50876, #45890, #6311, #60851, #989, #50559, #15290, #35569, #11290, #5003, #19949, #60508, #40220, #45540 ),
 .UNSPECIFIED., .F., .F.,
 ( 4, 3, 3, 3, 3, 4 ),
 ( 2.641088042841306632E-15, 0.0002126834539180078596, 0.0004253519300367007835, 0.0006380165497225274117, 0.0007442707582429536686, 0.0009453531351409383840 ),
 .UNSPECIFIED. ) ;
#46320=CARTESIAN_POINT ( 'NONE',  ( 2.524535260911693335, 0.2211075636757951768, 7.725637239510134258 ) ) ;
#46331=CARTESIAN_POINT ( 'NONE',  ( 0.2706063244538051693, -5.971590789837440738, -10.69357582853952948 ) ) ;
#46332=CARTESIAN_POINT ( 'NONE',  ( 0.2651627682582902712, 2.039709641845743437, -12.07509313786331084 ) ) ;
#46336=ORIENTED_EDGE ( 'NONE', *, *, #1642, .T. ) ;
#46340=CARTESIAN_POINT ( 'NONE',  ( 2.406456491625306615, -6.212289237906496453, 8.382123850280477129 ) ) ;
#46342=CARTESIAN_POINT ( 'NONE',  ( 5.536195898058073439, -0.005266167600747551948, -0.006672323185952767910 ) ) ;
#46353=CARTESIAN_POINT ( 'NONE',  ( 0.3675815128205912052, -3.951233083390393030, -11.62724744438069635 ) ) ;
#46354=CARTESIAN_POINT ( 'NONE',  ( 1.459561108994131162, -0.6317018236577405244, -12.62847742794703443 ) ) ;
#46361=CARTESIAN_POINT ( 'NONE',  ( 2.241536586108913820, -2.605228657247397717, 7.176205604390200499 ) ) ;
#46363=CARTESIAN_POINT ( 'NONE',  ( 2.034671305879988790, 5.218565780488984451, 10.44529075078584590 ) ) ;
#46365=ORIENTED_EDGE ( 'NONE', *, *, #54796, .T. ) ;
#46368=CARTESIAN_POINT ( 'NONE',  ( 2.242819959140645469, -7.634209046698942736, -0.1024002568250162587 ) ) ;
#46373=CARTESIAN_POINT ( 'NONE',  ( 0.5572780756280651948, -2.443667122521392177, 12.09922454589786156 ) ) ;
#46376=CARTESIAN_POINT ( 'NONE',  ( 0.2956976708475452797, 12.02996380804954057, 2.344604179391455823 ) ) ;
#46382=CARTESIAN_POINT ( 'NONE',  ( 2.305787727787084407, -1.164987321564681100, -7.566723232958083578 ) ) ;
#46385=B_SPLINE_CURVE_WITH_KNOTS ( 'NONE', 3,
 ( #42469, #58130, #37169, #2625, #32824, #52806, #2276 ),
 .UNSPECIFIED., .F., .F.,
 ( 4, 3, 4 ),
 ( 4.352182061961988653E-15, 0.002398160485435415698, 0.005002426799387886536 ),
 .UNSPECIFIED. ) ;
#46390=EDGE_CURVE ( 'NONE', #36996, #20105, #19868, .T. ) ;
#46404=B_SPLINE_CURVE_WITH_KNOTS ( 'NONE', 3,
 ( #41360, #9796, #61646, #40372, #65330, #5834, #60676, #15110, #50050, #50394, #61322, #15757, #41038, #60338, #14764, #162 ),
 .UNSPECIFIED., .F., .F.,
 ( 4, 3, 3, 3, 3, 4 ),
 ( 4.336808689942017255E-19, 0.0002176109881720239428, 0.0004352086762394593656, 0.0006528017811446864237, 0.0007615147961451704337, 0.0009453342004946751554 ),
 .UNSPECIFIED. ) ;
#46409=ORIENTED_EDGE ( 'NONE', *, *, #44011, .F. ) ;
#46410=CARTESIAN_POINT ( 'NONE',  ( 2.241509619876138171, 7.634391113243451876, 0.03828218718772713469 ) ) ;
#46414=ORIENTED_EDGE ( 'NONE', *, *, #14830, .F. ) ;
#46416=CARTESIAN_POINT ( 'NONE',  ( 5.516018279890452902, 0.003580555109620875767, -0.005752102158674359499 ) ) ;
#46419=VERTEX_POINT ( 'NONE', #45386 ) ;
#46427=CARTESIAN_POINT ( 'NONE',  ( 0.2706063244538050583, -11.44820198696412739, -4.353289770698342664 ) ) ;
#46428=CARTESIAN_POINT ( 'NONE',  ( 2.241528039335008327, 2.625917297988483945, -7.168649579907096836 ) ) ;
#46429=CARTESIAN_POINT ( 'NONE',  ( 0.7400311444011723472, 0.3548322008127070548, 12.39937114182724542 ) ) ;
#46430=ORIENTED_EDGE ( 'NONE', *, *, #5525, .F. ) ;
#46432=CARTESIAN_POINT ( 'NONE',  ( 2.298277635560276089, -5.044791616846968196, 5.755367168477987683 ) ) ;
#46435=CARTESIAN_POINT ( 'NONE',  ( 2.941278708680199916, -4.788765081995656203, 3.842273877444545960 ) ) ;
#46439=CARTESIAN_POINT ( 'NONE',  ( 3.152665057734040488, 0.000000000000000000, 0.000000000000000000 ) ) ;
#46447=CARTESIAN_POINT ( 'NONE',  ( 0.2638984909335720941, 2.322601104020666885, 12.02508546958697266 ) ) ;
#46452=CARTESIAN_POINT ( 'NONE',  ( 2.770579946183334474, -7.739026583264747572, 1.056759439485547514 ) ) ;
#46457=CARTESIAN_POINT ( 'NONE',  ( 1.194176325881340706, 12.54527478469375623, -0.5141316333311681808 ) ) ;
#46458=CARTESIAN_POINT ( 'NONE',  ( 2.373367633546871858, 3.994744114396181267, -6.557448619657597177 ) ) ;
#46459=ADVANCED_FACE ( 'NONE', ( #5510 ), #38446, .F. ) ;
#46466=B_SPLINE_CURVE_WITH_KNOTS ( 'NONE', 3,
 ( #57365, #30757, #51419, #41071, #61350, #26773, #47071, #11789, #6498, #1183, #46089, #1529, #26126, #10481, #1839, #10818 ),
 .UNSPECIFIED., .F., .F.,
 ( 4, 3, 3, 3, 3, 4 ),
 ( 3.697854792267728832E-15, 0.0002126834539179605613, 0.0004253519300366067832, 0.0006380165497223873328, 0.0007442707582427906046, 0.0009453531351420190083 ),
 .UNSPECIFIED. ) ;
#46473=CARTESIAN_POINT ( 'NONE',  ( 2.241352910868910531, 5.901537464758519036, -4.843133558968066410 ) ) ;
#46474=CARTESIAN_POINT ( 'NONE',  ( 5.536195898058073439, 0.005266167600748165173, -0.006672323185952934443 ) ) ;
#46480=CARTESIAN_POINT ( 'NONE',  ( 1.109979610370654290, -12.41172293674659421, 1.701361252868953455 ) ) ;
#46481=CARTESIAN_POINT ( 'NONE',  ( 1.719304012341582588, 7.017415949614099979, -10.62216384465570762 ) ) ;
#46482=EDGE_CURVE ( 'NONE', #34740, #51848, #36403, .T. ) ;
#46485=CARTESIAN_POINT ( 'NONE',  ( 0.3278977287071215274, 6.347150352417455288, -10.49733767381175653 ) ) ;
#46494=B_SPLINE_CURVE_WITH_KNOTS ( 'NONE', 3,
 ( #24361, #20361, #9077, #35645, #19057, #40641, #4092 ),
 .UNSPECIFIED., .F., .F.,
 ( 4, 3, 4 ),
 ( 0.000000000000000000, 0.001700533616330624290, 0.005002426799371293906 ),
 .UNSPECIFIED. ) ;
#46497=CARTESIAN_POINT ( 'NONE',  ( 0.3218525148189880225, -11.60666749448226120, 3.964374483810605643 ) ) ;
#46500=CARTESIAN_POINT ( 'NONE',  ( 5.516018279890452902, 0.006286471671802441874, 0.002527316374434314221 ) ) ;
#46506=CARTESIAN_POINT ( 'NONE',  ( 0.3675815128205894289, -7.689697408877210094, -9.574637318042043432 ) ) ;
#46515=ORIENTED_EDGE ( 'NONE', *, *, #48874, .F. ) ;
#46529=EDGE_LOOP ( 'NONE', ( #64420, #27044 ) ) ;
#46532=CARTESIAN_POINT ( 'NONE',  ( 0.5572780756278360448, 11.49107179558535385, 4.507550621618145570 ) ) ;
#46534=CARTESIAN_POINT ( 'NONE',  ( 0.2655924914740778742, -4.147079829127330974, 11.52280271232869424 ) ) ;
#46535=DIRECTION ( 'NONE',  ( -1.000000000000000000, -0.000000000000000000, -0.000000000000000000 ) ) ;
#46546=B_SPLINE_CURVE_WITH_KNOTS ( 'NONE', 3,
 ( #51162, #5617, #46173, #51503, #26207, #6912, #62742, #2913, #63717, #52787, #18197, #38467, #58108, #8213, #11880, #52477 ),
 .UNSPECIFIED., .F., .F.,
 ( 4, 3, 3, 3, 3, 4 ),
 ( 2.559284012420599289E-15, 0.0002126834539179633531, 0.0004253519300366116079, 0.0006380165497223953559, 0.0007442707582428000372, 0.0009453531351419522215 ),
 .UNSPECIFIED. ) ;
#46547=CARTESIAN_POINT ( 'NONE',  ( 0.2648978790185593790, -2.256510822326224464, 12.03635331166811540 ) ) ;
#46555=CARTESIAN_POINT ( 'NONE',  ( 5.516018279890452902, -0.004180585980735018921, -0.005331956019561697423 ) ) ;
#46559=CARTESIAN_POINT ( 'NONE',  ( 2.241537034860906275, 7.517665055736011404, 1.330359961362312493 ) ) ;
#46568=CARTESIAN_POINT ( 'NONE',  ( 0.9232058338315048962, -10.98407661738932894, 5.905985151448110315 ) ) ;
#46569=VECTOR ( 'NONE', #3720, 1000.000000000000114 ) ;
#46570=CARTESIAN_POINT ( 'NONE',  ( 5.536195898058073439, -0.008496323383586251374, -0.0002547682446687694544 ) ) ;
#46577=ORIENTED_EDGE ( 'NONE', *, *, #57768, .F. ) ;
#46580=CARTESIAN_POINT ( 'NONE',  ( 2.969415267404832193, -6.619534278261622440, 4.269695207293495720 ) ) ;
#46584=CARTESIAN_POINT ( 'NONE',  ( 0.2801149460245125900, -1.933835447580712685, 12.09752788490058073 ) ) ;
#46588=VERTEX_POINT ( 'NONE', #37042 ) ;
#46591=VERTEX_POINT ( 'NONE', #11768 ) ;
#46596=( BOUNDED_SURFACE ( )  B_SPLINE_SURFACE ( 3, 1, ( 
 ( #58354, #41740 ),
 ( #11471, #48395 ),
 ( #31747, #12775 ),
 ( #57050, #22440 ) ),
 .UNSPECIFIED., .F., .F., .F. ) 
 B_SPLINE_SURFACE_WITH_KNOTS ( ( 4, 4 ),
 ( 2, 2 ),
 ( 0.000000000000000000, 1.000000000000000000 ),
 ( 0.000000000000000000, 1.000000000000000000 ),
 .UNSPECIFIED. ) 
 GEOMETRIC_REPRESENTATION_ITEM ( )  RATIONAL_B_SPLINE_SURFACE ( (
 ( 1.000000000000000000, 1.000000000000000000),
 ( 0.6933888150995267674, 0.9895912004443193632),
 ( 0.6933888150995267674, 0.9895912004443193632),
 ( 1.000000000000000000, 1.000000000000000000) ) ) 
 REPRESENTATION_ITEM ( '' )  SURFACE ( )  );
#46597=CARTESIAN_POINT ( 'NONE',  ( 2.288423627607774957, 4.792733268640427369, -5.962686897379307460 ) ) ;
#46611=CARTESIAN_POINT ( 'NONE',  ( 3.152665057734040488, 0.000000000000000000, 0.000000000000000000 ) ) ;
#46612=CARTESIAN_POINT ( 'NONE',  ( 0.9296196016852266153, 6.590257778218349571, -10.58347995892882487 ) ) ;
#46613=CARTESIAN_POINT ( 'NONE',  ( 5.514970785353741078, -0.003262412238248737269, -0.003415090918276127412 ) ) ;
#46620=DIRECTION ( 'NONE',  ( 0.000000000000000000, 0.000000000000000000, 1.000000000000000000 ) ) ;
#46622=ADVANCED_FACE ( 'NONE', ( #59002 ), #35896, .F. ) ;
#46624=CARTESIAN_POINT ( 'NONE',  ( 2.305787727787084407, 7.249469779319909435, 2.461236246751095536 ) ) ;
#46625=CARTESIAN_POINT ( 'NONE',  ( 1.462291587751557653, 12.08418494300955004, -3.724645088506112423 ) ) ;
#46631=CARTESIAN_POINT ( 'NONE',  ( 0.2655924914740778187, 10.62761259256425284, -6.084990060696399361 ) ) ;
#46643=CARTESIAN_POINT ( 'NONE',  ( 1.948354844646952744, 0.7204626209691127325, 11.94326855455485514 ) ) ;
#46645=CARTESIAN_POINT ( 'NONE',  ( 0.3537226245948364434, -5.910416419900456297, -10.75912040401515313 ) ) ;
#46647=CARTESIAN_POINT ( 'NONE',  ( 2.297017764050090616, -5.755222757172079540, 5.044319338147345455 ) ) ;
#46655=CARTESIAN_POINT ( 'NONE',  ( 1.948354844646782214, -7.125078658760747530, 9.612178954899706085 ) ) ;
#46659=CARTESIAN_POINT ( 'NONE',  ( 2.247112776671470247, -6.554209700764000779, 3.918650674719086346 ) ) ;
#46662=CARTESIAN_POINT ( 'NONE',  ( 0.3223008802179245236, -5.919638939520659449, 10.74209118105755145 ) ) ;
#46671=CARTESIAN_POINT ( 'NONE',  ( 0.4613984246114872789, -0.2828900474739520221, -12.30830943644279962 ) ) ;
#46673=ORIENTED_EDGE ( 'NONE', *, *, #27161, .T. ) ;
#46680=CARTESIAN_POINT ( 'NONE',  ( 5.536195898058073439, -0.005656495196971037670, -0.006344799443924007722 ) ) ;
#46686=CARTESIAN_POINT ( 'NONE',  ( 3.152665057735335452, -7.719888720907720270, 1.848755561853250295 ) ) ;
#46692=CARTESIAN_POINT ( 'NONE',  ( 0.2646305136544065406, -11.55263159009961527, 4.064188116014508800 ) ) ;
#46694=B_SPLINE_CURVE_WITH_KNOTS ( 'NONE', 3,
 ( #54263, #6489, #8705, #26767, #44577, #19341, #25, #65514, #4043, #30293 ),
 .UNSPECIFIED., .F., .F.,
 ( 4, 3, 3, 4 ),
 ( 1.563658610346375379E-18, 6.607638129004486172E-05, 9.911389841680535810E-05, 0.0001667630577588616607 ),
 .UNSPECIFIED. ) ;
#46701=CARTESIAN_POINT ( 'NONE',  ( 2.241352910868908754, -7.202080440908725123, -2.532612177304514933 ) ) ;
#46710=CARTESIAN_POINT ( 'NONE',  ( 2.941278708680199916, -5.383216837018920842, -2.952340773940166141 ) ) ;
#46717=CARTESIAN_POINT ( 'NONE',  ( 5.515188684475870851, 0.005339000964282161060, -0.0003622115669626908038 ) ) ;
#46720=ORIENTED_EDGE ( 'NONE', *, *, #48774, .F. ) ;
#46722=ADVANCED_FACE ( 'NONE', ( #2822 ), #29536, .T. ) ;
#46723=CARTESIAN_POINT ( 'NONE',  ( 3.152665057735194232, -3.161213418914472051, -7.281573230474045921 ) ) ;
#46729=CARTESIAN_POINT ( 'NONE',  ( 2.781367136452508326, -7.232043329634210593, 2.960151187465072109 ) ) ;
#46733=CARTESIAN_POINT ( 'NONE',  ( 1.633930747252547944, -12.61425129500178421, -1.494486044209151432 ) ) ;
#46735=CARTESIAN_POINT ( 'NONE',  ( 2.844750968616099662, 6.946006365803938820, 3.626176236708051004 ) ) ;
#46741=VECTOR ( 'NONE', #33884, 1000.000000000000000 ) ;
#46742=ADVANCED_FACE ( 'NONE', ( #38022 ), #6613, .F. ) ;
#46745=CARTESIAN_POINT ( 'NONE',  ( 0.2655924914740778742, 9.352877839710711072, -7.905499957109142883 ) ) ;
#46749=CARTESIAN_POINT ( 'NONE',  ( 0.2653519789438758547, -7.854827495960873485, 9.395292406847904232 ) ) ;
#46762=CARTESIAN_POINT ( 'NONE',  ( 5.516018279890452902, -0.0009545156522407517155, -0.006707902355169297580 ) ) ;
#46775=CIRCLE ( 'NONE', #18111, 7.938172270156617749 ) ;
#46777=CARTESIAN_POINT ( 'NONE',  ( 0.2646305136544065406, 6.008537389229416270, 10.67138229758231738 ) ) ;
#46784=VERTEX_POINT ( 'NONE', #34668 ) ;
#46785=CARTESIAN_POINT ( 'NONE',  ( 0.6473888112830267216, 12.36914475328377350, -0.3298838684459264869 ) ) ;
#46786=VERTEX_POINT ( 'NONE', #64929 ) ;
#46788=DIRECTION ( 'NONE',  ( 0.3939253465568944290, -0.5833358547425091523, -0.7103112711423471559 ) ) ;
#46789=CARTESIAN_POINT ( 'NONE',  ( 0.3665391374699464300, 2.392238720110619443, -12.04754782681754932 ) ) ;
#46790=CARTESIAN_POINT ( 'NONE',  ( 3.092491956585373014, -3.124176487319987761, -7.275786042219477778 ) ) ;
#46794=EDGE_LOOP ( 'NONE', ( #58241, #19365, #50345, #27460 ) ) ;
#46797=( BOUNDED_SURFACE ( )  B_SPLINE_SURFACE ( 3, 1, ( 
 ( #3420, #23688 ),
 ( #43960, #53284 ),
 ( #64233, #13682 ),
 ( #2768, #28017 ) ),
 .UNSPECIFIED., .F., .F., .F. ) 
 B_SPLINE_SURFACE_WITH_KNOTS ( ( 4, 4 ),
 ( 2, 2 ),
 ( 0.000000000000000000, 1.000000000000000000 ),
 ( 0.000000000000000000, 1.000000000000000000 ),
 .UNSPECIFIED. ) 
 GEOMETRIC_REPRESENTATION_ITEM ( )  RATIONAL_B_SPLINE_SURFACE ( (
 ( 1.000000000000000000, 1.000000000000000000),
 ( 0.6933888150995267674, 0.9895912004443193632),
 ( 0.6933888150995267674, 0.9895912004443193632),
 ( 1.000000000000000000, 1.000000000000000000) ) ) 
 REPRESENTATION_ITEM ( '' )  SURFACE ( )  );
#46800=CARTESIAN_POINT ( 'NONE',  ( 2.305787727787083519, 5.756228004061526349, -5.047606869482997638 ) ) ;
#46801=CARTESIAN_POINT ( 'NONE',  ( 2.241311220309556429, 4.835827934491015334, 5.907514893712945359 ) ) ;
#46802=CARTESIAN_POINT ( 'NONE',  ( 0.9232058338315048962, -5.905985151448073012, -10.98407661738934848 ) ) ;
#46806=CARTESIAN_POINT ( 'NONE',  ( 0.8375941296801170388, -12.30893872205250439, 1.780036797758517864 ) ) ;
#46813=VECTOR ( 'NONE', #39976, 1000.000000000000114 ) ;
#46814=CARTESIAN_POINT ( 'NONE',  ( 2.241317068080776576, 2.696905536171296358, 7.142175514530098468 ) ) ;
#46816=FACE_OUTER_BOUND ( 'NONE', #21869, .T. ) ;
#46822=CARTESIAN_POINT ( 'NONE',  ( 0.2638984909335720941, -9.252728947331126719, 8.023974293733148855 ) ) ;
#46831=CARTESIAN_POINT ( 'NONE',  ( 2.305787727787083519, 3.971363876084056166, -6.545285700970486786 ) ) ;
#46837=DIRECTION ( 'NONE',  ( 0.000000000000000000, 0.000000000000000000, 1.000000000000000000 ) ) ;
#46841=CARTESIAN_POINT ( 'NONE',  ( 0.3675815128205894289, -5.910255304480521055, 10.76447900494938459 ) ) ;
#46845=CARTESIAN_POINT ( 'NONE',  ( 1.719304012341629884, 8.755325027796281745, -9.242227816402079910 ) ) ;
#46858=ADVANCED_FACE ( 'NONE', ( #10076 ), #45640, .T. ) ;
#46859=ORIENTED_EDGE ( 'NONE', *, *, #8355, .T. ) ;
#46861=ORIENTED_EDGE ( 'NONE', *, *, #46079, .T. ) ;
#46867=CARTESIAN_POINT ( 'NONE',  ( 2.268878695252937394, 5.025754889198752906, -5.759001817705959425 ) ) ;
#46869=CARTESIAN_POINT ( 'NONE',  ( 5.514624014163232779, 0.0005510299962881775801, -0.004104370840204391718 ) ) ;
#46870=CARTESIAN_POINT ( 'NONE',  ( 5.536195898058073439, -0.005266167600748119203, 0.006672323185952970005 ) ) ;
#46882=CARTESIAN_POINT ( 'NONE',  ( 0.2869720083484330053, -2.332746648244278465, 12.02930764912520445 ) ) ;
#46883=CARTESIAN_POINT ( 'NONE',  ( 1.719304012340734822, -5.690355757825686922, -11.38834240361529737 ) ) ;
#46884=CARTESIAN_POINT ( 'NONE',  ( 1.719304012340549859, -10.62216384465898500, -7.017415949616274240 ) ) ;
#46886=CARTESIAN_POINT ( 'NONE',  ( 0.2646305136544072623, 12.03696649559618059, -2.256625640822192747 ) ) ;
#46891=CARTESIAN_POINT ( 'NONE',  ( 2.507146904658098752, 6.052884339496489297, -4.796593924427919653 ) ) ;
#46893=CARTESIAN_POINT ( 'NONE',  ( 1.948354844646345452, 7.125078658759951722, -9.612178954897759198 ) ) ;
#46898=CARTESIAN_POINT ( 'NONE',  ( 0.3002738374340817029, 2.350339881555103982, -12.03040002643109574 ) ) ;
#46900=CARTESIAN_POINT ( 'NONE',  ( 2.507146904658097419, 3.672650549645667617, 6.793847219607461518 ) ) ;
#46904=VECTOR ( 'NONE', #36512, 1000.000000000000114 ) ;
#46906=CARTESIAN_POINT ( 'NONE',  ( 2.241536586108913376, 2.617055111126449063, 7.171901127201301129 ) ) ;
#46907=CARTESIAN_POINT ( 'NONE',  ( 1.719304012340734822, -5.690355757825686922, -11.38834240361529737 ) ) ;
#46909=CARTESIAN_POINT ( 'NONE',  ( 2.305787727787084407, -4.792270232040854339, -5.970480882365271746 ) ) ;
#46915=B_SPLINE_CURVE_WITH_KNOTS ( 'NONE', 3,
 ( #39339, #39679, #34020, #34359, #64292, #18759, #39015, #54672, #13737, #59976, #54338, #8773, #59643, #29059, #3812, #24065, #34987, #44326, #64597 ),
 .UNSPECIFIED., .F., .F.,
 ( 4, 3, 3, 3, 3, 3, 4 ),
 ( 7.470971189404981089E-18, 4.457896483015255922E-05, 6.639290541542495041E-05, 8.820687556479337235E-05, 0.0001100173248778935222, 0.0001545671401658117229, 0.0001830328308068584142 ),
 .UNSPECIFIED. ) ;
#46917=CARTESIAN_POINT ( 'NONE',  ( 2.589278595513663461, -6.588350318048504128, 4.081908913132012984 ) ) ;
#46922=EDGE_CURVE ( 'NONE', #23985, #62968, #41631, .T. ) ;
#46926=CARTESIAN_POINT ( 'NONE',  ( 2.705197763288548440, 7.783989928191466845, 0.2797837188786633789 ) ) ;
#46940=B_SPLINE_CURVE_WITH_KNOTS ( 'NONE', 3,
 ( #17022, #37302, #32311, #52626, #44257, #44569, #2756 ),
 .UNSPECIFIED., .F., .F.,
 ( 4, 3, 4 ),
 ( 0.000000000000000000, 0.001700533616330547528, 0.005002426799371374570 ),
 .UNSPECIFIED. ) ;
#46947=CARTESIAN_POINT ( 'NONE',  ( 5.515188684475870851, -0.005339000964281801972, -0.0003622115669623841372 ) ) ;
#46951=CARTESIAN_POINT ( 'NONE',  ( 0.2653141334712546540, 4.229817350136413800, 11.49252672845885037 ) ) ;
#46957=CARTESIAN_POINT ( 'NONE',  ( 2.705197763288551549, -5.783040721897899417, -5.217779042888505359 ) ) ;
#46959=VERTEX_POINT ( 'NONE', #26342 ) ;
#46961=CARTESIAN_POINT ( 'NONE',  ( 5.530133899448235191, 0.01111090067015088091, -0.01149180883054549095 ) ) ;
#46967=CARTESIAN_POINT ( 'NONE',  ( 2.781367136452345790, -4.171010984503056740, -6.608147481822085112 ) ) ;
#46968=ORIENTED_EDGE ( 'NONE', *, *, #3804, .F. ) ;
#46970=VERTEX_POINT ( 'NONE', #56622 ) ;
#46972=AXIS2_PLACEMENT_3D ( 'NONE', #47590, #2035, #42569 ) ;
#46974=B_SPLINE_CURVE_WITH_KNOTS ( 'NONE', 3,
 ( #61563, #22307, #21994, #56604, #61906, #21687, #41942 ),
 .UNSPECIFIED., .F., .F.,
 ( 4, 3, 4 ),
 ( 0.000000000000000000, 0.001700533616330530615, 0.005002426799371309518 ),
 .UNSPECIFIED. ) ;
#46977=B_SPLINE_CURVE_WITH_KNOTS ( 'NONE', 3,
 ( #56520, #35874, #40221, #5670, #45541, #25941, #46227, #10964, #31251, #668, #60509, #20928, #51556, #46532, #41531, #58158 ),
 .UNSPECIFIED., .F., .F.,
 ( 4, 3, 3, 3, 3, 4 ),
 ( 0.000000000000000000, 0.0002999043160757217824, 0.0005998071753050755218, 0.0008997092107374187820, 0.001204458948194616187, 0.001510329163474478670 ),
 .UNSPECIFIED. ) ;
#46985=CARTESIAN_POINT ( 'NONE',  ( 0.2648321136542687859, -5.999882851577401865, -10.67551415837656492 ) ) ;
#46989=CIRCLE ( 'NONE', #60798, 12.73084802173761787 ) ;
#46999=CARTESIAN_POINT ( 'NONE',  ( 1.375507693220495042, -9.273955665125749093, -8.553661013313396566 ) ) ;
#47000=B_SPLINE_CURVE_WITH_KNOTS ( 'NONE', 3,
 ( #29009, #4060, #24023, #64552, #19027, #39292, #59591, #14020, #34308, #9044, #44593, #39626, #50283, #29974, #46272, #20000 ),
 .UNSPECIFIED., .F., .F.,
 ( 4, 3, 3, 3, 3, 4 ),
 ( 8.673617379884035472E-19, 0.0002176109881720227231, 0.0004352086762394592571, 0.0006528017811446877247, 0.0007615147961451714095, 0.0009453342004946414367 ),
 .UNSPECIFIED. ) ;
#47006=CARTESIAN_POINT ( 'NONE',  ( 0.3675815128205894289, -5.910255304480521055, 10.76447900494938459 ) ) ;
#47011=CARTESIAN_POINT ( 'NONE',  ( 2.305787727787083519, -7.135468203930003028, 2.774453000917123990 ) ) ;
#47014=DIRECTION ( 'NONE',  ( 0.000000000000000000, 0.000000000000000000, 1.000000000000000000 ) ) ;
#47017=ORIENTED_EDGE ( 'NONE', *, *, #56725, .F. ) ;
#47022=DIRECTION ( 'NONE',  ( -0.3865475372811021937, 0.1410344188397524012, -0.9114221272958256126 ) ) ;
#47032=CARTESIAN_POINT ( 'NONE',  ( 2.290907136833252089, -7.649199419879184170, -0.1622757685885879708 ) ) ;
#47036=CARTESIAN_POINT ( 'NONE',  ( 0.2648978790185602672, -12.03635331166813494, 2.256510822326103671 ) ) ;
#47037=VERTEX_POINT ( 'NONE', #3302 ) ;
#47038=EDGE_CURVE ( 'NONE', #32432, #44286, #4268, .T. ) ;
#47041=CARTESIAN_POINT ( 'NONE',  ( 2.373367633546869637, 7.528269033630156315, 1.511052049479944648 ) ) ;
#47044=ORIENTED_EDGE ( 'NONE', *, *, #54845, .F. ) ;
#47048=CARTESIAN_POINT ( 'NONE',  ( 2.990245332647878840, -7.075286609974364538, -4.676740826320321176 ) ) ;
#47056=ORIENTED_EDGE ( 'NONE', *, *, #1681, .F. ) ;
#47062=CARTESIAN_POINT ( 'NONE',  ( 0.2648978790185593790, 4.312320170909392125, -11.46165506714223703 ) ) ;
#47065=CARTESIAN_POINT ( 'NONE',  ( 0.2650492433740059828, 12.04046084639676373, -2.234874822562773478 ) ) ;
#47070=CARTESIAN_POINT ( 'NONE',  ( 0.2759803524722213575, -1.940323823244580081, -12.09509972435083114 ) ) ;
#47071=CARTESIAN_POINT ( 'NONE',  ( 2.781367136452763233, 1.052455537429629606, -7.743208838465648114 ) ) ;
#47072=CARTESIAN_POINT ( 'NONE',  ( 2.969415267405037362, -1.748187016698512952, -7.680649281077315038 ) ) ;
#47088=CARTESIAN_POINT ( 'NONE',  ( 0.2652384529303140615, -12.24598125395191417, 0.06607367983849406212 ) ) ;
#47098=CARTESIAN_POINT ( 'NONE',  ( 0.2652384770603670727, -7.922175044417039125, 9.338499095996397159 ) ) ;
#47102=CARTESIAN_POINT ( 'NONE',  ( 0.2833330754217406877, 5.950193237802404944, 10.71034013638380067 ) ) ;
#47103=CARTESIAN_POINT ( 'NONE',  ( 0.2801149460245167533, 11.44368419510491108, -4.374013318106434234 ) ) ;
#47110=CARTESIAN_POINT ( 'NONE',  ( 1.194176325881340039, -11.61285876598809175, 4.773862381874691252 ) ) ;
#47113=CARTESIAN_POINT ( 'NONE',  ( 2.827825597296805160, 1.027532345921684742, 8.965636292765712057 ) ) ;
#47124=CARTESIAN_POINT ( 'NONE',  ( 2.241526690369555208, 1.308664175663869500, -7.521460607153586331 ) ) ;
#47127=CARTESIAN_POINT ( 'NONE',  ( 1.459561108992491141, 12.54631635028832548, 1.570807238541433115 ) ) ;
#47135=VERTEX_POINT ( 'NONE', #24212 ) ;
#47140=CARTESIAN_POINT ( 'NONE',  ( 2.247206125382828823, -3.917979829727955110, 6.554642244888448488 ) ) ;
#47141=CARTESIAN_POINT ( 'NONE',  ( 0.2717059086739051499, -10.69429229731972519, -5.971041827598930318 ) ) ;
#47153=CARTESIAN_POINT ( 'NONE',  ( 2.258463476536662462, 4.806099079317524669, 5.939075453322714360 ) ) ;
#47158=CARTESIAN_POINT ( 'NONE',  ( 0.2801149460245144773, 12.09752788490057895, 1.933835447580672495 ) ) ;
#47160=CARTESIAN_POINT ( 'NONE',  ( 0.6473888112830256114, -1.823007254467038596, 12.23851338376148234 ) ) ;
#47164=EDGE_CURVE ( 'NONE', #36560, #39587, #64757, .T. ) ;
#47166=CARTESIAN_POINT ( 'NONE',  ( 3.152665057733966769, 0.9030954876739563097, 7.886634106564108571 ) ) ;
#47172=CARTESIAN_POINT ( 'NONE',  ( 2.241537034860904942, 7.172440248506164018, 2.615577641485550497 ) ) ;
#47173=DIRECTION ( 'NONE',  ( -1.000000000000000000, -0.000000000000000000, -0.000000000000000000 ) ) ;
#47185=CARTESIAN_POINT ( 'NONE',  ( 2.241534463349552198, 0.005244187652470188102, -7.634462073473343935 ) ) ;
#47186=CARTESIAN_POINT ( 'NONE',  ( 1.634816307077033182, -7.601181930720684043, -10.17753964889855567 ) ) ;
#47187=CARTESIAN_POINT ( 'NONE',  ( 2.297017764050091504, -1.166330442180224747, 7.563558677601593061 ) ) ;
#47188=CARTESIAN_POINT ( 'NONE',  ( 1.462291587753156152, 12.54737685278498738, -1.569662666435215126 ) ) ;
#47191=B_SPLINE_CURVE_WITH_KNOTS ( 'NONE', 3,
 ( #8519, #51069, #9172, #30753, #49751, #45737, #60058, #15144, #40081, #35427, #39768, #55731, #65668, #24810, #10161, #34754 ),
 .UNSPECIFIED., .F., .F.,
 ( 4, 3, 3, 3, 3, 4 ),
 ( 2.030687410393290492E-15, 0.0002126834539180011104, 0.0004253519300366869599, 0.0006380165497225099560, 0.0007442707582429343698, 0.0009453531351411225900 ),
 .UNSPECIFIED. ) ;
#47197=CARTESIAN_POINT ( 'NONE',  ( 0.6511581176974240437, 8.205008037407228727, -9.263557799003033111 ) ) ;
#47204=ORIENTED_EDGE ( 'NONE', *, *, #10910, .F. ) ;
#47209=VERTEX_POINT ( 'NONE', #15211 ) ;
#47211=CARTESIAN_POINT ( 'NONE',  ( 0.3341166715381296282, 4.432780143632490066, 11.44035855572976423 ) ) ;
#47213=CARTESIAN_POINT ( 'NONE',  ( 2.247206125382661845, 4.996658593544773375, -5.774712443419645957 ) ) ;
#47214=ADVANCED_FACE ( 'NONE', ( #24880 ), #13388, .F. ) ;
#47217=FACE_OUTER_BOUND ( 'NONE', #59035, .T. ) ;
#47222=FACE_BOUND ( 'NONE', #6080, .T. ) ;
#47225=CARTESIAN_POINT ( 'NONE',  ( 2.241352910868909643, 3.744764251557084922, -6.652881166698471738 ) ) ;
#47227=FACE_OUTER_BOUND ( 'NONE', #17725, .T. ) ;
#47228=CARTESIAN_POINT ( 'NONE',  ( 2.931247277082682512, -7.855653518374111854, -0.3703309885897621556 ) ) ;
#47230=EDGE_CURVE ( 'NONE', #52387, #26102, #64269, .T. ) ;
#47231=ORIENTED_EDGE ( 'NONE', *, *, #14242, .F. ) ;
#47237=CARTESIAN_POINT ( 'NONE',  ( 3.152665057734130638, 7.609997527621177760, -2.258875078502145861 ) ) ;
#47240=CARTESIAN_POINT ( 'NONE',  ( 2.639814597422738718, -4.793557287999591132, -6.111633106000479820 ) ) ;
#47248=CARTESIAN_POINT ( 'NONE',  ( 0.2648978790185602672, 12.24533305150758089, -0.1321385342562831633 ) ) ;
#47252=CARTESIAN_POINT ( 'NONE',  ( 2.907497136250241976, -0.3592423305251857268, -7.848280798452723417 ) ) ;
#47253=CARTESIAN_POINT ( 'NONE',  ( 0.2653519890518185043, -2.126521162241138185, 12.06015162724940382 ) ) ;
#47254=AXIS2_PLACEMENT_3D ( 'NONE', #33289, #3050, #43576 ) ;
#47257=ORIENTED_EDGE ( 'NONE', *, *, #21113, .T. ) ;
#47264=CARTESIAN_POINT ( 'NONE',  ( 0.2915757698887287974, -1.916267336493256757, 12.10419100255479563 ) ) ;
#47266=B_SPLINE_CURVE_WITH_KNOTS ( 'NONE', 3,
 ( #35143, #5589, #24531, #60112, #55453, #45459, #34508, #65727, #40819, #56093, #20197, #9889, #35489 ),
 .UNSPECIFIED., .F., .F.,
 ( 4, 3, 3, 3, 4 ),
 ( 3.878959614448864246E-18, 6.607593386745442947E-05, 0.0001321518677373505364, 0.0001982171734706177969, 0.0002642860854759470366 ),
 .UNSPECIFIED. ) ;
#47276=CARTESIAN_POINT ( 'NONE',  ( 0.2652384529303143390, 11.48485968917279365, -4.250461213012427741 ) ) ;
#47290=CARTESIAN_POINT ( 'NONE',  ( 1.719304012338199517, 0.000000000000000000, 0.000000000000000000 ) ) ;
#47291=CARTESIAN_POINT ( 'NONE',  ( 0.2646305136544065406, -6.237419468587153126, 10.53923716745244832 ) ) ;
#47292=CARTESIAN_POINT ( 'NONE',  ( 5.516018279890452902, -0.006286471671802459221, -0.002527316374434270853 ) ) ;
#47301=CARTESIAN_POINT ( 'NONE',  ( 3.092491956585768254, 7.581757403488332159, 2.283527081234053568 ) ) ;
#47302=CARTESIAN_POINT ( 'NONE',  ( 0.2648978790185602672, 6.237101853238547378, 10.53870023327865901 ) ) ;
#47303=DIRECTION ( 'NONE',  ( -1.000000000000000000, -0.000000000000000000, -0.000000000000000000 ) ) ;
#47308=ORIENTED_EDGE ( 'NONE', *, *, #24219, .F. ) ;
#47319=EDGE_CURVE ( 'NONE', #28687, #34363, #26501, .T. ) ;
#47321=CARTESIAN_POINT ( 'NONE',  ( 0.3218525148189865237, -5.919623386703263712, -10.74192973049794375 ) ) ;
#47334=CARTESIAN_POINT ( 'NONE',  ( 1.634816307076947695, -9.253014110596202713, -8.702988562442458331 ) ) ;
#47335=ORIENTED_EDGE ( 'NONE', *, *, #23088, .F. ) ;
#47339=CARTESIAN_POINT ( 'NONE',  ( 0.3341166715381302943, -5.914486946113987287, 10.74942732659230238 ) ) ;
#47344=ORIENTED_EDGE ( 'NONE', *, *, #27047, .F. ) ;
#47350=CARTESIAN_POINT ( 'NONE',  ( 0.2717059086739005425, -7.737372654246648551, 9.494961435243668646 ) ) ;
#47357=CARTESIAN_POINT ( 'NONE',  ( 0.2653519789438749110, 9.366970421692881743, -7.888580323518779025 ) ) ;
#47361=CARTESIAN_POINT ( 'NONE',  ( 0.7446945582510989814, -4.576048078258570406, 11.53120448859754887 ) ) ;
#47363=VERTEX_POINT ( 'NONE', #22169 ) ;
#47366=CARTESIAN_POINT ( 'NONE',  ( 0.3040950598368152291, 12.02925914197708757, -2.376091969481093358 ) ) ;
#47371=CARTESIAN_POINT ( 'NONE',  ( 2.899286259009684397, 7.664525129300157502, 1.713434346771250283 ) ) ;
#47377=CARTESIAN_POINT ( 'NONE',  ( 2.241528039335008327, -7.168649579907108382, -2.625917297988457744 ) ) ;
#47379=CARTESIAN_POINT ( 'NONE',  ( 5.515539859299206427, -0.002251761459665569190, 0.005618668168217179175 ) ) ;
#47380=CARTESIAN_POINT ( 'NONE',  ( 5.536195898058073439, 0.005656495196970890219, -0.006344799443923454345 ) ) ;
#47389=B_SPLINE_CURVE_WITH_KNOTS ( 'NONE', 3,
 ( #36508, #51812, #25886, #15870, #292, #30519, #31511, #46480, #6259, #50823, #46806, #31198, #21880, #56120, #6590, #36154 ),
 .UNSPECIFIED., .F., .F.,
 ( 4, 3, 3, 3, 3, 4 ),
 ( 0.000000000000000000, 0.0002999043160757332749, 0.0005998071753050982901, 0.0008997092107374523922, 0.001204458948195600426, 0.001510329163476426982 ),
 .UNSPECIFIED. ) ;
#47391=VECTOR ( 'NONE', #4091, 1000.000000000000114 ) ;
#47392=CARTESIAN_POINT ( 'NONE',  ( 0.2759803524722223012, 4.367180139677484085, -11.44482553421627280 ) ) ;
#47394=CARTESIAN_POINT ( 'NONE',  ( 0.9232058338315058954, -9.306586124266649662, 8.301689855530135276 ) ) ;
#47395=( BOUNDED_SURFACE ( )  B_SPLINE_SURFACE ( 3, 1, ( 
 ( #11699, #6741 ),
 ( #16700, #52629 ),
 ( #36661, #12036 ),
 ( #26040, #31014 ) ),
 .UNSPECIFIED., .F., .F., .F. ) 
 B_SPLINE_SURFACE_WITH_KNOTS ( ( 4, 4 ),
 ( 2, 2 ),
 ( 0.000000000000000000, 1.000000000000000000 ),
 ( 0.000000000000000000, 1.000000000000000000 ),
 .UNSPECIFIED. ) 
 GEOMETRIC_REPRESENTATION_ITEM ( )  RATIONAL_B_SPLINE_SURFACE ( (
 ( 1.000000000000000000, 1.000000000000000000),
 ( 0.6933888150995267674, 0.9895912004443193632),
 ( 0.6933888150995267674, 0.9895912004443193632),
 ( 1.000000000000000000, 1.000000000000000000) ) ) 
 REPRESENTATION_ITEM ( '' )  SURFACE ( )  );
#47396=CARTESIAN_POINT ( 'NONE',  ( 0.2650492594609233366, 12.07870403910584223, -2.017987075343835368 ) ) ;
#47398=VERTEX_POINT ( 'NONE', #23489 ) ;
#47400=CARTESIAN_POINT ( 'NONE',  ( 2.941278708680199916, -5.383216837018962586, 2.952340773940090646 ) ) ;
#47402=CARTESIAN_POINT ( 'NONE',  ( 3.031336079629848523, -1.779751109289636979, -7.694633165537411834 ) ) ;
#47410=CARTESIAN_POINT ( 'NONE',  ( 2.242819959140598840, -4.828731837260408888, -5.913965034148014333 ) ) ;
#47413=EDGE_CURVE ( 'NONE', #3865, #60104, #43195, .T. ) ;
#47414=CARTESIAN_POINT ( 'NONE',  ( 0.2717059086739021523, 2.300075171420234099, 12.03041489115252638 ) ) ;
#47422=VERTEX_POINT ( 'NONE', #8849 ) ;
#47429=CARTESIAN_POINT ( 'NONE',  ( 0.3106921474978465714, 5.925601485921673905, 10.73438344699973435 ) ) ;
#47435=ORIENTED_EDGE ( 'NONE', *, *, #2863, .F. ) ;
#47436=CARTESIAN_POINT ( 'NONE',  ( 1.633930747251797211, -11.67150509329678698, 5.012862767614018722 ) ) ;
#47437=CARTESIAN_POINT ( 'NONE',  ( 5.536195898058073439, -0.007485416011288131832, -0.004027525919832926522 ) ) ;
#47440=VERTEX_POINT ( 'NONE', #54077 ) ;
#47443=CARTESIAN_POINT ( 'NONE',  ( 2.269879328256731554, 5.759117113708073887, -5.026125315665156634 ) ) ;
#47446=CARTESIAN_POINT ( 'NONE',  ( 2.242418902651939216, -7.207816731001386756, -2.517330194228364793 ) ) ;
#47449=B_SPLINE_CURVE_WITH_KNOTS ( 'NONE', 3,
 ( #25257, #34887, #50227, #45223, #4687, #24949, #65799, #35227, #55529, #9976, #30258, #31556, #17826, #33109, #20615, #46222, #37779, #61819, #58073 ),
 .UNSPECIFIED., .F., .F.,
 ( 4, 3, 3, 3, 3, 3, 4 ),
 ( 9.891822368120406898E-18, 4.457896483014692814E-05, 6.639290541541845875E-05, 8.820687556478574228E-05, 0.0001100173248778870305, 0.0001545671401658038353, 0.0001830328308068570318 ),
 .UNSPECIFIED. ) ;
#47453=CARTESIAN_POINT ( 'NONE',  ( 5.516018279890452902, -0.006629829924290480368, 0.001397286410094396563 ) ) ;
#47454=LINE ( 'NONE', #52449, #49811 ) ;
#47462=CARTESIAN_POINT ( 'NONE',  ( 2.241352910868910531, -3.889181972941495147, 6.569501556381427854 ) ) ;
#47473=CARTESIAN_POINT ( 'NONE',  ( 0.2653141435805210224, -0.04404957080773672096, -12.24612531649368030 ) ) ;
#47474=ORIENTED_EDGE ( 'NONE', *, *, #40593, .F. ) ;
#47475=CARTESIAN_POINT ( 'NONE',  ( 0.3341166715381312935, 12.12403120948088109, 1.881279064087884256 ) ) ;
#47482=ORIENTED_EDGE ( 'NONE', *, *, #19662, .F. ) ;
#47484=ORIENTED_EDGE ( 'NONE', *, *, #12239, .T. ) ;
#47493=CARTESIAN_POINT ( 'NONE',  ( 0.3218525148189838592, 1.888670068297651383, 12.11874253990390038 ) ) ;
#47494=ORIENTED_EDGE ( 'NONE', *, *, #26258, .T. ) ;
#47497=DIRECTION ( 'NONE',  ( -0.3939253465568944290, 0.3052156353794439614, -0.8669868725995526493 ) ) ;
#47503=ORIENTED_EDGE ( 'NONE', *, *, #46079, .F. ) ;
#47506=ORIENTED_EDGE ( 'NONE', *, *, #25721, .F. ) ;
#47515=EDGE_CURVE ( 'NONE', #61407, #48793, #14760, .T. ) ;
#47523=ORIENTED_EDGE ( 'NONE', *, *, #44011, .T. ) ;
#47526=CARTESIAN_POINT ( 'NONE',  ( 0.3006302518452020345, 4.404090606399880592, 11.43947177966003537 ) ) ;
#47529=CARTESIAN_POINT ( 'NONE',  ( 2.284126774967661255, 2.764365694977889198, -7.131638985093283090 ) ) ;
#47530=EDGE_CURVE ( 'NONE', #58982, #23316, #9449, .T. ) ;
#47535=CARTESIAN_POINT ( 'NONE',  ( 2.507146904658053455, 4.796593924427980049, 6.052884339496421795 ) ) ;
#47538=CARTESIAN_POINT ( 'NONE',  ( 0.2676618633000437675, -2.284744117040155675, 12.03196378632210362 ) ) ;
#47547=CARTESIAN_POINT ( 'NONE',  ( 2.241352910868910531, 5.901537464758519036, -4.843133558968066410 ) ) ;
#47551=ORIENTED_EDGE ( 'NONE', *, *, #32455, .F. ) ;
#47556=CARTESIAN_POINT ( 'NONE',  ( 0.2652384529303135619, -2.191562200667102722, -12.04846370803831235 ) ) ;
#47559=CARTESIAN_POINT ( 'NONE',  ( 2.889800649504073782, -2.030191121417175726, 5.774917447012991367 ) ) ;
#47560=CARTESIAN_POINT ( 'NONE',  ( 1.287602823387599571, -5.809161206980071768, -11.16629420487849345 ) ) ;
#47561=B_SPLINE_CURVE_WITH_KNOTS ( 'NONE', 3,
 ( #27448, #41766, #36782, #42733, #58058, #26806, #37097 ),
 .UNSPECIFIED., .F., .F.,
 ( 4, 3, 4 ),
 ( 8.338150981378363025E-05, 9.911389841680508705E-05, 0.0001667630577588621215 ),
 .UNSPECIFIED. ) ;
#47564=( BOUNDED_SURFACE ( )  B_SPLINE_SURFACE ( 3, 1, ( 
 ( #21387, #25727 ),
 ( #26704, #62267 ),
 ( #61956, #62584 ),
 ( #20740, #21735 ) ),
 .UNSPECIFIED., .F., .F., .F. ) 
 B_SPLINE_SURFACE_WITH_KNOTS ( ( 4, 4 ),
 ( 2, 2 ),
 ( 0.000000000000000000, 1.000000000000000000 ),
 ( 0.000000000000000000, 1.000000000000000000 ),
 .UNSPECIFIED. ) 
 GEOMETRIC_REPRESENTATION_ITEM ( )  RATIONAL_B_SPLINE_SURFACE ( (
 ( 1.000000000000000000, 1.000000000000000000),
 ( 0.6933888150995267674, 0.9895912004443193632),
 ( 0.6933888150995267674, 0.9895912004443193632),
 ( 1.000000000000000000, 1.000000000000000000) ) ) 
 REPRESENTATION_ITEM ( '' )  SURFACE ( )  );
#47568=CARTESIAN_POINT ( 'NONE',  ( 0.6473888112830271657, -7.698027285532536013, 9.687359867659774082 ) ) ;
#47570=VERTEX_POINT ( 'NONE', #9817 ) ;
#47573=CARTESIAN_POINT ( 'NONE',  ( 2.963017218115628459, 7.865565884553440412, 0.3847317984105586564 ) ) ;
#47579=CARTESIAN_POINT ( 'NONE',  ( 2.251139882113957658, -7.542197031254636030, 1.203816215709523796 ) ) ;
#47583=( BOUNDED_SURFACE ( )  B_SPLINE_SURFACE ( 3, 1, ( 
 ( #43021, #63295 ),
 ( #34667, #30915 ),
 ( #61190, #49664 ),
 ( #15937, #35889 ) ),
 .UNSPECIFIED., .F., .F., .F. ) 
 B_SPLINE_SURFACE_WITH_KNOTS ( ( 4, 4 ),
 ( 2, 2 ),
 ( 0.000000000000000000, 1.000000000000000000 ),
 ( 0.000000000000000000, 1.000000000000000000 ),
 .UNSPECIFIED. ) 
 GEOMETRIC_REPRESENTATION_ITEM ( )  RATIONAL_B_SPLINE_SURFACE ( (
 ( 1.000000000000000000, 1.000000000000000000),
 ( 0.9942764183789327692, 0.8450855930916585379),
 ( 0.9942764183789327692, 0.8450855930916585379),
 ( 1.000000000000000000, 1.000000000000000000) ) ) 
 REPRESENTATION_ITEM ( '' )  SURFACE ( )  );
#47590=CARTESIAN_POINT ( 'NONE',  ( 3.152665057734040488, 0.000000000000000000, 0.000000000000000000 ) ) ;
#47594=VECTOR ( 'NONE', #36315, 1000.000000000000000 ) ;
#47598=CARTESIAN_POINT ( 'NONE',  ( 0.2648978790185602672, 0.1321385342562404197, 12.24533305150758089 ) ) ;
#47601=CARTESIAN_POINT ( 'NONE',  ( 5.514970785353741078, -0.0003039746380528647075, -0.004713149585127535644 ) ) ;
#47603=ORIENTED_EDGE ( 'NONE', *, *, #28990, .F. ) ;
#47604=FACE_OUTER_BOUND ( 'NONE', #30350, .T. ) ;
#47625=CIRCLE ( 'NONE', #18964, 7.938172270156617749 ) ;
#47629=CARTESIAN_POINT ( 'NONE',  ( 2.903928887688517424, -2.496183838365630514, 8.407112942776095110 ) ) ;
#47630=CARTESIAN_POINT ( 'NONE',  ( 0.2648978790185584908, 12.03635331166812250, 2.256510822326184940 ) ) ;
#47642=CARTESIAN_POINT ( 'NONE',  ( 0.3675815128205912052, -9.235491948679950269, -8.093875121226169256 ) ) ;
#47643=ORIENTED_EDGE ( 'NONE', *, *, #19213, .F. ) ;
#47647=CARTESIAN_POINT ( 'NONE',  ( 0.3654063281920725270, -5.910280591919130799, 10.76363796011283469 ) ) ;
#47657=CARTESIAN_POINT ( 'NONE',  ( 1.104777566491144114, -0.4777483965052850556, -12.51694124543052133 ) ) ;
#47659=CARTESIAN_POINT ( 'NONE',  ( 0.2915757698887281313, -7.711631695122908248, 9.524403232224839755 ) ) ;
#47669=CARTESIAN_POINT ( 'NONE',  ( 5.514624014163232779, -0.001255375129358104504, -0.003946330869974997921 ) ) ;
#47672=CARTESIAN_POINT ( 'NONE',  ( 2.241526690369557429, -4.920579984890920855, -5.837196604699895985 ) ) ;
#47674=CARTESIAN_POINT ( 'NONE',  ( 2.241311220309554209, -7.633829235838274663, -0.09281826062103946950 ) ) ;
#47682=CARTESIAN_POINT ( 'NONE',  ( 2.994568964204206818, 7.686291764591511644, 1.761139509856855856 ) ) ;
#47692=ADVANCED_FACE ( 'NONE', ( #62324 ), #8742, .F. ) ;
#47694=CARTESIAN_POINT ( 'NONE',  ( 5.520433897694421610, 0.003119431460922221164, -0.01473594271720233932 ) ) ;
#47696=CARTESIAN_POINT ( 'NONE',  ( 2.941278708680199916, 4.788765081995683737, -3.842273877444514429 ) ) ;
#47699=EDGE_CURVE ( 'NONE', #23038, #54088, #11776, .T. ) ;
#47707=CARTESIAN_POINT ( 'NONE',  ( 0.2653141617321017609, 12.06772699408311489, -2.083144498805149514 ) ) ;
#47711=CARTESIAN_POINT ( 'NONE',  ( 0.3002738374340833682, -1.906042098268937446, -12.10874171309341563 ) ) ;
#47713=CARTESIAN_POINT ( 'NONE',  ( 2.524535260913002510, -1.559291270914674232, -7.569872524929103008 ) ) ;
#47722=CARTESIAN_POINT ( 'NONE',  ( 0.2706063244538063350, 9.268878137104398007, 8.006269958070639348 ) ) ;
#47724=ORIENTED_EDGE ( 'NONE', *, *, #29507, .F. ) ;
#47725=CARTESIAN_POINT ( 'NONE',  ( 0.3675815128205894289, -3.951233083390547129, 11.62724744438064306 ) ) ;
#47726=CARTESIAN_POINT ( 'NONE',  ( 5.514970785353741078, 0.002093325033904021564, 0.004233694591582523939 ) ) ;
#47735=CARTESIAN_POINT ( 'NONE',  ( 0.2706063244538005619, -9.494160524941746004, 7.737788863017279972 ) ) ;
#47736=B_SPLINE_CURVE_WITH_KNOTS ( 'NONE', 3,
 ( #51223, #42504, #21929, #11294, #51866, #15930, #61827, #15611, #52536, #41534, #6965, #35877, #27235, #36215, #36565, #47529, #5673, #56523, #25943 ),
 .UNSPECIFIED., .F., .F.,
 ( 4, 3, 3, 3, 3, 3, 4 ),
 ( 4.336808689942017736E-19, 2.831840207499626523E-05, 4.217266859840494790E-05, 5.602024318396020829E-05, 6.290810167969150990E-05, 9.120440630945391260E-05, 0.0001153103026479759813 ),
 .UNSPECIFIED. ) ;
#47750=CARTESIAN_POINT ( 'NONE',  ( 0.3675815128205912052, -11.44679196252412368, 4.447030445008141264 ) ) ;
#47752=CARTESIAN_POINT ( 'NONE',  ( 3.152665057733966769, 0.9030954876739563097, 7.886634106564108571 ) ) ;
#47759=CARTESIAN_POINT ( 'NONE',  ( 1.719304012338836563, -3.626341562670527985, 12.20344780066003487 ) ) ;
#47760=ORIENTED_EDGE ( 'NONE', *, *, #33076, .F. ) ;
#47763=EDGE_LOOP ( 'NONE', ( #41248, #46190, #64848, #38144 ) ) ;
#47765=CARTESIAN_POINT ( 'NONE',  ( 5.515539859299206427, 0.005751553894234952106, -0.001886660928063908999 ) ) ;
#47768=CARTESIAN_POINT ( 'NONE',  ( 1.719304012338199295, 12.64775761152512423, 1.452142814150486183 ) ) ;
#47773=CARTESIAN_POINT ( 'NONE',  ( 2.262775599886257538, 7.499645832851604688, 1.465770593192917470 ) ) ;
#47779=CARTESIAN_POINT ( 'NONE',  ( 0.2650492594609251684, -6.218173512054836927, 10.54996119777443297 ) ) ;
#47781=CARTESIAN_POINT ( 'NONE',  ( 2.589278595513088366, -2.875840518181322913, -7.197074516942284284 ) ) ;
#47788=CARTESIAN_POINT ( 'NONE',  ( 0.2872850955227761460, 7.715220952083361006, -9.519656861923639468 ) ) ;
#47791=CARTESIAN_POINT ( 'NONE',  ( 2.305787727787083519, 1.493241775258524084, -7.508843116234142911 ) ) ;
#47793=CARTESIAN_POINT ( 'NONE',  ( 0.3164563675027646794, 12.11636128244742672, 1.892265234253155182 ) ) ;
#47808=EDGE_CURVE ( 'NONE', #54991, #44256, #61484, .T. ) ;
#47810=CARTESIAN_POINT ( 'NONE',  ( 0.2717059086739033180, -11.44824199474646420, 4.354191483751232106 ) ) ;
#47818=CARTESIAN_POINT ( 'NONE',  ( 0.7400311444011756778, 3.907401494355078331, -11.77295732453929844 ) ) ;
#47820=CARTESIAN_POINT ( 'NONE',  ( 2.269879328256732443, 7.552124491910172210, 1.181008584585979682 ) ) ;
#47830=EDGE_CURVE ( 'NONE', #27180, #19660, #33390, .T. ) ;
#47841=DIRECTION ( 'NONE',  ( -1.000000000000000000, -0.000000000000000000, -0.000000000000000000 ) ) ;
#47842=VECTOR ( 'NONE', #17149, 999.9999999999998863 ) ;
#47860=DIRECTION ( 'NONE',  ( 0.000000000000000000, 0.000000000000000000, 1.000000000000000000 ) ) ;
#47867=CARTESIAN_POINT ( 'NONE',  ( 2.573738926104373714, -7.194322927777932364, -2.868819712476781358 ) ) ;
#47872=CARTESIAN_POINT ( 'NONE',  ( 0.3106921474978496800, -0.2354703039888949578, 12.25904950202576416 ) ) ;
#47873=FACE_OUTER_BOUND ( 'NONE', #20974, .T. ) ;
#47876=CARTESIAN_POINT ( 'NONE',  ( 2.899286259009687505, -4.769992516330196608, -6.239228647238621583 ) ) ;
#47898=CARTESIAN_POINT ( 'NONE',  ( 0.3665391374699464300, 10.50279796150436695, 6.368473106897166502 ) ) ;
#47899=CARTESIAN_POINT ( 'NONE',  ( 5.515539859299206427, -0.004037661319611337077, -0.004509673239148472360 ) ) ;
#47910=FACE_OUTER_BOUND ( 'NONE', #6010, .T. ) ;
#47915=ORIENTED_EDGE ( 'NONE', *, *, #56603, .T. ) ;
#47920=VERTEX_POINT ( 'NONE', #54004 ) ;
#47926=CARTESIAN_POINT ( 'NONE',  ( 2.276198483117263915, 3.688810392808549832, 6.697332984100271780 ) ) ;
#47932=CARTESIAN_POINT ( 'NONE',  ( 0.7446945582530690722, 6.508900271376239388, -10.56139717223440933 ) ) ;
#47938=CARTESIAN_POINT ( 'NONE',  ( 2.242819959140644137, -2.707278038035121792, 7.138786956204155487 ) ) ;
#47942=CARTESIAN_POINT ( 'NONE',  ( 1.372161826076382374, -12.60140585080803177, 0.5897614319403238214 ) ) ;
#47943=CARTESIAN_POINT ( 'NONE',  ( 0.2648978790185619880, 12.03635331166815270, -2.256510822326019738 ) ) ;
#47950=ORIENTED_EDGE ( 'NONE', *, *, #6223, .T. ) ;
#47953=CARTESIAN_POINT ( 'NONE',  ( 3.047904605210380424, -6.318654123925923294, 4.747272783555632536 ) ) ;
#47957=B_SPLINE_CURVE_WITH_KNOTS ( 'NONE', 3,
 ( #56238, #31617, #46597, #41604, #25016, #55608, #10681, #65546, #10045, #15356, #61235, #20015, #726, #51283, #5733, #56587, #26001, #46285, #50941 ),
 .UNSPECIFIED., .F., .F.,
 ( 4, 3, 3, 3, 3, 3, 4 ),
 ( 5.502793334042459344E-18, 2.825908398782625081E-05, 4.208813692417807169E-05, 5.591713746860116585E-05, 6.279584083139550150E-05, 9.105792820166967901E-05, 0.0001153131102489458491 ),
 .UNSPECIFIED. ) ;
#47962=EDGE_CURVE ( 'NONE', #49787, #21262, #24128, .T. ) ;
#47971=CARTESIAN_POINT ( 'NONE',  ( 1.719304012338210619, 10.62216384465585328, 7.017415949611872428 ) ) ;
#47973=EDGE_CURVE ( 'NONE', #29718, #40530, #55927, .T. ) ;
#48000=CARTESIAN_POINT ( 'NONE',  ( 0.2872850955227740366, -7.715220952083302386, 9.519656861923696312 ) ) ;
#48009=CARTESIAN_POINT ( 'NONE',  ( 2.241352910868909643, 7.145045428366612050, -2.689314586382279604 ) ) ;
#48011=CARTESIAN_POINT ( 'NONE',  ( 0.3675815128205894289, 3.951233083390626177, -11.62724744438061641 ) ) ;
#48012=CARTESIAN_POINT ( 'NONE',  ( 0.2739690278137243973, -4.016979056590845865, 11.57167385487631961 ) ) ;
#48015=CARTESIAN_POINT ( 'NONE',  ( 2.655192694323964098, -9.539062147542258785, -1.093661162899928430 ) ) ;
#48020=CARTESIAN_POINT ( 'NONE',  ( 0.2833330754217378566, 12.02930703389100131, 2.326361469893271305 ) ) ;
#48035=CARTESIAN_POINT ( 'NONE',  ( 0.2638984909335720941, 6.295352574288986425, 10.50550771760521940 ) ) ;
#48038=CARTESIAN_POINT ( 'NONE',  ( 2.276905613633655623, -4.795880183929603469, 5.955225895210576326 ) ) ;
#48040=B_SPLINE_CURVE_WITH_KNOTS ( 'NONE', 3,
 ( #41990, #62270, #62588, #36997, #32007, #52328, #17050, #18047, #33338, #59846, #37982, #9273, #7745, #58631, #44864, #17396, #28031, #22717, #37672 ),
 .UNSPECIFIED., .F., .F.,
 ( 4, 3, 3, 3, 3, 3, 4 ),
 ( 4.336808689942017736E-19, 2.831840207625253706E-05, 4.217266860012148388E-05, 5.602024318565883461E-05, 6.290810168138159136E-05, 9.120440631110341779E-05, 0.0001153103026478300612 ),
 .UNSPECIFIED. ) ;
#48043=DIRECTION ( 'NONE',  ( -1.000000000000000000, 0.000000000000000000, 0.000000000000000000 ) ) ;
#48048=VERTEX_POINT ( 'NONE', #31981 ) ;
#48061=FACE_OUTER_BOUND ( 'NONE', #22789, .T. ) ;
#48062=ADVANCED_FACE ( 'NONE', ( #1092 ), #47395, .F. ) ;
#48064=CARTESIAN_POINT ( 'NONE',  ( 3.152665057735613008, -6.378477742801520023, -4.725420687649700469 ) ) ;
#48073=VERTEX_POINT ( 'NONE', #763 ) ;
#48082=CARTESIAN_POINT ( 'NONE',  ( 0.3053067050349160261, 5.928821939311931466, 10.73055518945190023 ) ) ;
#48084=ORIENTED_EDGE ( 'NONE', *, *, #7609, .T. ) ;
#48085=CARTESIAN_POINT ( 'NONE',  ( 0.7446945582529681529, 4.576048078259359109, -11.53120448859789882 ) ) ;
#48086=ORIENTED_EDGE ( 'NONE', *, *, #40388, .F. ) ;
#48095=CARTESIAN_POINT ( 'NONE',  ( 2.368238019615373169, 1.509700170844646250, 7.526794520527686494 ) ) ;
#48109=CARTESIAN_POINT ( 'NONE',  ( 0.3040950598368152291, -3.956873563689608631, 11.60568999039893257 ) ) ;
#48136=CARTESIAN_POINT ( 'NONE',  ( 2.251139882113958546, 1.448366094935513937, -7.499076289418090013 ) ) ;
#48140=CARTESIAN_POINT ( 'NONE',  ( 2.440552418640494103, 2.447453236303825719, 7.301551120181771992 ) ) ;
#48147=CARTESIAN_POINT ( 'NONE',  ( 2.244591118396558116, -0.1074970442783618058, -7.634724215899730382 ) ) ;
#48148=CARTESIAN_POINT ( 'NONE',  ( 3.152665057736261822, -7.102135024647099115, -3.546019893114602972 ) ) ;
#48157=CARTESIAN_POINT ( 'NONE',  ( 0.8375941296801004965, -8.285008510335032383, 9.275620596396437989 ) ) ;
#48158=CARTESIAN_POINT ( 'NONE',  ( 3.152665057734040488, 0.000000000000000000, 0.000000000000000000 ) ) ;
#48160=B_SPLINE_CURVE_WITH_KNOTS ( 'NONE', 3,
 ( #15379, #35650, #10377, #51307, #30653, #5412, #20702, #61255, #56613, #32608, #41289, #21693, #7038, #27307, #747, #6078, #11685, #32298, #52917 ),
 .UNSPECIFIED., .F., .F.,
 ( 4, 3, 3, 3, 3, 3, 4 ),
 ( 8.911587868699592868E-18, 4.457896483015155633E-05, 6.639290541542550606E-05, 8.820687556479513418E-05, 0.0001100173248778960430, 0.0001545671401658155718, 0.0001830328308068577907 ),
 .UNSPECIFIED. ) ;
#48162=CARTESIAN_POINT ( 'NONE',  ( 0.2956976708475475002, -11.59055635407404594, 3.984495122852534710 ) ) ;
#48174=CARTESIAN_POINT ( 'NONE',  ( 2.241536586108913820, -3.811784405792396857, 6.614789707676452579 ) ) ;
#48188=ORIENTED_EDGE ( 'NONE', *, *, #32247, .F. ) ;
#48190=( BOUNDED_SURFACE ( )  B_SPLINE_SURFACE ( 3, 1, ( 
 ( #32969, #33321 ),
 ( #23343, #53283 ),
 ( #18029, #7727 ),
 ( #23025, #43280 ) ),
 .UNSPECIFIED., .F., .F., .F. ) 
 B_SPLINE_SURFACE_WITH_KNOTS ( ( 4, 4 ),
 ( 2, 2 ),
 ( 0.000000000000000000, 1.000000000000000000 ),
 ( 0.000000000000000000, 1.000000000000000000 ),
 .UNSPECIFIED. ) 
 GEOMETRIC_REPRESENTATION_ITEM ( )  RATIONAL_B_SPLINE_SURFACE ( (
 ( 1.000000000000000000, 1.000000000000000000),
 ( 0.9942764183789327692, 0.8450855930916585379),
 ( 0.9942764183789327692, 0.8450855930916585379),
 ( 1.000000000000000000, 1.000000000000000000) ) ) 
 REPRESENTATION_ITEM ( '' )  SURFACE ( )  );
#48191=FACE_OUTER_BOUND ( 'NONE', #3272, .T. ) ;
#48201=CARTESIAN_POINT ( 'NONE',  ( 2.241526690369558317, -7.168108047190856702, 2.627393882429291061 ) ) ;
#48204=ADVANCED_FACE ( 'NONE', ( #15278 ), #7371, .T. ) ;
#48206=CARTESIAN_POINT ( 'NONE',  ( 0.3401186441510247738, 8.081824149807820490, -9.233880480307224303 ) ) ;
#48208=CARTESIAN_POINT ( 'NONE',  ( 0.2958664285830391316, 11.59077733151255352, 3.984029505266609039 ) ) ;
#48217=LINE ( 'NONE', #8275, #42353 ) ;
#48221=CARTESIAN_POINT ( 'NONE',  ( 0.2958664285830437390, -11.59077733151253398, -3.984029505266682758 ) ) ;
#48228=CARTESIAN_POINT ( 'NONE',  ( 5.516018279890452902, 0.002104829434640673614, -0.006440244342253036158 ) ) ;
#48233=CARTESIAN_POINT ( 'NONE',  ( 2.440552418640494992, -4.797131306497530723, -6.024135401262425304 ) ) ;
#48236=CARTESIAN_POINT ( 'NONE',  ( 1.014383007554942262, 10.59286224865790338, -6.628652139012797484 ) ) ;
#48238=DIRECTION ( 'NONE',  ( 0.9486832985018464059, 3.872673197958701185E-17, 0.3162277646628405270 ) ) ;
#48240=ADVANCED_FACE ( 'NONE', ( #61471 ), #1938, .F. ) ;
#48244=CARTESIAN_POINT ( 'NONE',  ( 3.152665057736049103, -0.4801242025610908959, -7.923639299008895520 ) ) ;
#48245=CARTESIAN_POINT ( 'NONE',  ( 1.194176325881338263, -8.457794872459055924, -9.279760592562180221 ) ) ;
#48246=CARTESIAN_POINT ( 'NONE',  ( 2.280717697723837922, -3.958470850374266270, -6.543326285614674553 ) ) ;
#48259=DIRECTION ( 'NONE',  ( -1.000000000000000000, -0.000000000000000000, -0.000000000000000000 ) ) ;
#48268=ORIENTED_EDGE ( 'NONE', *, *, #20451, .F. ) ;
#48281=VERTEX_POINT ( 'NONE', #26900 ) ;
#48282=CARTESIAN_POINT ( 'NONE',  ( 2.247206125382828379, 3.717496781928092631, 6.670391186503657366 ) ) ;
#48288=CARTESIAN_POINT ( 'NONE',  ( 1.462291587750105260, -0.6330131614655301053, 12.62932306616591482 ) ) ;
#48291=CARTESIAN_POINT ( 'NONE',  ( 0.4613984246114875565, 10.80075367333622260, 5.909164750631071605 ) ) ;
#48300=CARTESIAN_POINT ( 'NONE',  ( 0.2915757698887310734, -2.339174865979208207, -12.02962099476165925 ) ) ;
#48303=CARTESIAN_POINT ( 'NONE',  ( 2.491965175174603697, -6.787433375639562172, -3.673871285745604620 ) ) ;
#48304=ORIENTED_EDGE ( 'NONE', *, *, #47515, .T. ) ;
#48307=CARTESIAN_POINT ( 'NONE',  ( 2.241528039335009215, -1.310213701658539343, -7.521191296022434081 ) ) ;
#48319=CARTESIAN_POINT ( 'NONE',  ( 3.100650473569707355, 5.429218121582431777, -5.767490999797057150 ) ) ;
#48323=CARTESIAN_POINT ( 'NONE',  ( 2.253265082352433168, -0.1282654837135236425, 7.637296367516834827 ) ) ;
#48325=CARTESIAN_POINT ( 'NONE',  ( 0.2671309869109499413, 1.966882337881849407, -12.08782215308009711 ) ) ;
#48327=CARTESIAN_POINT ( 'NONE',  ( 1.719304012340653998, -9.242227816403676854, -8.755325027797448811 ) ) ;
#48329=CARTESIAN_POINT ( 'NONE',  ( 2.241352910868908754, 4.843133558968205854, -5.901537464758406237 ) ) ;
#48347=CARTESIAN_POINT ( 'NONE',  ( 2.241317068080777908, -1.415707718487463351, -7.501982551779205366 ) ) ;
#48350=CARTESIAN_POINT ( 'NONE',  ( 5.514970785353741078, -0.004233694591582531745, 0.002093325033904006385 ) ) ;
#48355=CARTESIAN_POINT ( 'NONE',  ( 0.2801149460245144773, 4.005169813315260008, -11.57793225195133147 ) ) ;
#48356=VECTOR ( 'NONE', #10433, 1000.000000000000000 ) ;
#48359=CARTESIAN_POINT ( 'NONE',  ( 0.2653519789438770760, -11.50012635727058452, 4.209148152332875981 ) ) ;
#48360=CARTESIAN_POINT ( 'NONE',  ( 0.2646305136544065406, 12.03696649559617882, -2.256625640822194079 ) ) ;
#48361=CARTESIAN_POINT ( 'NONE',  ( 2.241449424704146320, -5.808712090826644747, 4.954182807723320536 ) ) ;
#48364=CARTESIAN_POINT ( 'NONE',  ( 5.530133899448235191, -0.003876417824003439323, -0.01550764871776274222 ) ) ;
#48368=CARTESIAN_POINT ( 'NONE',  ( 1.547277799339609405, 1.534072017332309246, -12.58038279313770680 ) ) ;
#48371=CARTESIAN_POINT ( 'NONE',  ( 0.3610902822527150557, -10.49957835860567279, 6.364812822043123930 ) ) ;
#48377=( BOUNDED_SURFACE ( )  B_SPLINE_SURFACE ( 3, 1, ( 
 ( #59951, #48661 ),
 ( #14371, #63937 ),
 ( #38992, #43318 ),
 ( #43648, #64266 ) ),
 .UNSPECIFIED., .F., .F., .T. ) 
 B_SPLINE_SURFACE_WITH_KNOTS ( ( 4, 4 ),
 ( 2, 2 ),
 ( 0.000000000000000000, 1.000000000000000000 ),
 ( 0.000000000000000000, 1.000000000000000000 ),
 .UNSPECIFIED. ) 
 GEOMETRIC_REPRESENTATION_ITEM ( )  RATIONAL_B_SPLINE_SURFACE ( (
 ( 1.000000000000000000, 1.000000000000000000),
 ( 0.9942764183789327692, 0.8450855930916585379),
 ( 0.9942764183789327692, 0.8450855930916585379),
 ( 1.000000000000000000, 1.000000000000000000) ) ) 
 REPRESENTATION_ITEM ( '' )  SURFACE ( )  );
#48379=DIRECTION ( 'NONE',  ( 0.000000000000000000, 0.000000000000000000, 1.000000000000000000 ) ) ;
#48383=( GEOMETRIC_REPRESENTATION_CONTEXT ( 3 ) GLOBAL_UNCERTAINTY_ASSIGNED_CONTEXT ( ( #27268 ) ) GLOBAL_UNIT_ASSIGNED_CONTEXT ( ( #60094, #40118, #40450 ) ) REPRESENTATION_CONTEXT ( 'NONE', 'WORKASPACE' ) );
#48387=( BOUNDED_SURFACE ( )  B_SPLINE_SURFACE ( 3, 1, ( 
 ( #54910, #29622 ),
 ( #56214, #5707 ),
 ( #24659, #63091 ),
 ( #33493, #6036 ) ),
 .UNSPECIFIED., .F., .F., .F. ) 
 B_SPLINE_SURFACE_WITH_KNOTS ( ( 4, 4 ),
 ( 2, 2 ),
 ( 0.000000000000000000, 1.000000000000000000 ),
 ( 0.000000000000000000, 1.000000000000000000 ),
 .UNSPECIFIED. ) 
 GEOMETRIC_REPRESENTATION_ITEM ( )  RATIONAL_B_SPLINE_SURFACE ( (
 ( 1.000000000000000000, 1.000000000000000000),
 ( 0.6933888150995267674, 0.9895912004443193632),
 ( 0.6933888150995267674, 0.9895912004443193632),
 ( 1.000000000000000000, 1.000000000000000000) ) ) 
 REPRESENTATION_ITEM ( '' )  SURFACE ( )  );
#48389=CARTESIAN_POINT ( 'NONE',  ( 5.536195898058073439, 0.001726268814999830630, -0.008323005098840517008 ) ) ;
#48391=CARTESIAN_POINT ( 'NONE',  ( 0.000000000000000000, 0.000000000000000000, 0.000000000000000000 ) ) ;
#48393=CARTESIAN_POINT ( 'NONE',  ( 5.530133899448235191, -0.01293763278443415231, 0.009387834778845282821 ) ) ;
#48395=CARTESIAN_POINT ( 'NONE',  ( 1.452237505248555660, -6.833827325205244385, -10.65201107290474702 ) ) ;
#48398=CARTESIAN_POINT ( 'NONE',  ( 0.3053067050349199674, 9.241336250185357315, 8.055646999028040156 ) ) ;
#48401=CARTESIAN_POINT ( 'NONE',  ( 1.937114397841932290, 12.33981801388262589, -3.531416430611173052 ) ) ;
#48405=EDGE_CURVE ( 'NONE', #58225, #48073, #43065, .T. ) ;
#48409=CARTESIAN_POINT ( 'NONE',  ( 2.241451721903216399, 7.528807736569466336, -1.265761656830125315 ) ) ;
#48410=CARTESIAN_POINT ( 'NONE',  ( 2.273267844204865273, -7.553702825375860463, -1.178226273333022212 ) ) ;
#48413=CARTESIAN_POINT ( 'NONE',  ( 1.194176325881340262, 0.5141316333311244380, 12.54527478469375801 ) ) ;
#48417=CARTESIAN_POINT ( 'NONE',  ( 0.2650492433740053722, 10.54996000109284005, -6.218175523534182680 ) ) ;
#48419=B_SPLINE_CURVE_WITH_KNOTS ( 'NONE', 3,
 ( #62627, #47048, #61658, #1506, #12103, #26106, #16114 ),
 .UNSPECIFIED., .F., .F.,
 ( 4, 3, 4 ),
 ( 0.000000000000000000, 0.001700533616330536252, 0.005002426799375401731 ),
 .UNSPECIFIED. ) ;
#48421=SHAPE_DEFINITION_REPRESENTATION ( #43959, #39018 ) ;
#48434=CARTESIAN_POINT ( 'NONE',  ( 5.536195898058073439, -0.007230647766619658148, 0.004468797463753859146 ) ) ;
#48440=CARTESIAN_POINT ( 'NONE',  ( 0.2676618633000451553, -10.52491907319757125, -6.262131165853840109 ) ) ;
#48453=CARTESIAN_POINT ( 'NONE',  ( 2.268878695253354838, -3.949362208797108753, 6.544222817598203790 ) ) ;
#48459=CARTESIAN_POINT ( 'NONE',  ( 0.2648978790185602672, 7.769924372105329269, -9.465406350830530613 ) ) ;
#48463=CARTESIAN_POINT ( 'NONE',  ( 2.524535260912887491, -5.135322114975942043, -5.776056274541106816 ) ) ;
#48465=CARTESIAN_POINT ( 'NONE',  ( 0.2651627682582926027, -6.199212018117366441, -10.56115808354089225 ) ) ;
#48468=CARTESIAN_POINT ( 'NONE',  ( 2.889800649504073782, -5.728825117897722308, 2.156828754871448872 ) ) ;
#48469=CARTESIAN_POINT ( 'NONE',  ( 2.589278595513194503, -3.664724287895325006, 6.829211973730497931 ) ) ;
#48474=VERTEX_POINT ( 'NONE', #64497 ) ;
#48476=DIRECTION ( 'NONE',  ( -0.3939253465568943735, -0.7910971609033234930, 0.4679616473074815763 ) ) ;
#48478=CARTESIAN_POINT ( 'NONE',  ( 1.452237505248552996, 11.24427360515650420, -5.807998527925775534 ) ) ;
#48479=CARTESIAN_POINT ( 'NONE',  ( 0.3164563675027611267, -11.43920928915628110, 4.419430877662304802 ) ) ;
#48484=CARTESIAN_POINT ( 'NONE',  ( 1.719304012338199517, 0.000000000000000000, 0.000000000000000000 ) ) ;
#48485=CARTESIAN_POINT ( 'NONE',  ( 2.835339799623984192, 7.466040501142062524, -2.367573116406901601 ) ) ;
#48486=CARTESIAN_POINT ( 'NONE',  ( 2.589278595513869963, -4.794929105510921552, 6.089088204449140562 ) ) ;
#48489=CARTESIAN_POINT ( 'NONE',  ( 2.257661810676420355, 7.546014018371154819, 1.193649218120614641 ) ) ;
#48490=CARTESIAN_POINT ( 'NONE',  ( 5.515539859299206427, -0.006049968793488818240, 0.0001942659352251156096 ) ) ;
#48494=SURFACE_STYLE_FILL_AREA ( #44142 ) ;
#48504=CARTESIAN_POINT ( 'NONE',  ( 2.573738926104376823, -1.575954828885307801, 7.583190312075767103 ) ) ;
#48513=ORIENTED_EDGE ( 'NONE', *, *, #685, .T. ) ;
#48514=FACE_OUTER_BOUND ( 'NONE', #6921, .T. ) ;
#48520=CARTESIAN_POINT ( 'NONE',  ( 2.990245332647836651, 5.049055049623246028, 6.814589384234954750 ) ) ;
#48522=FACE_OUTER_BOUND ( 'NONE', #35015, .T. ) ;
#48525=CARTESIAN_POINT ( 'NONE',  ( 2.280717697724234938, 3.687451363405509941, -6.699799459371864607 ) ) ;
#48531=CARTESIAN_POINT ( 'NONE',  ( 0.3109076770649089605, -11.60048803586496291, -3.971171685427508091 ) ) ;
#48532=CARTESIAN_POINT ( 'NONE',  ( 0.3675815128205894289, -11.62724744438063063, -3.951233083390586209 ) ) ;
#48535=CARTESIAN_POINT ( 'NONE',  ( 5.514624014163232779, -0.003830004412313187633, 0.001574979445069354207 ) ) ;
#48540=CARTESIAN_POINT ( 'NONE',  ( 0.3053067050349194123, -0.2307671807673114528, 12.25734436043223852 ) ) ;
#48541=CARTESIAN_POINT ( 'NONE',  ( 3.152665057736074417, -6.622010822085853121, 4.377619405894153992 ) ) ;
#48542=ADVANCED_FACE ( 'NONE', ( #19295 ), #37665, .F. ) ;
#48544=CARTESIAN_POINT ( 'NONE',  ( 2.653899356899187989, 7.694895988366112327, 1.091629880170703393 ) ) ;
#48552=CONICAL_SURFACE ( 'NONE', #19862, 7.938172270156617749, 1.280189991382167047 ) ;
#48554=CARTESIAN_POINT ( 'NONE',  ( 5.514624014163232779, 0.003668383633201373166, -0.001921576324372464796 ) ) ;
#48556=CARTESIAN_POINT ( 'NONE',  ( 2.269879328256732887, -3.949706986712154588, -6.544400685875864987 ) ) ;
#48557=VECTOR ( 'NONE', #8342, 1000.000000000000227 ) ;
#48564=CARTESIAN_POINT ( 'NONE',  ( 2.305787727787084407, 5.047606869483056258, 5.756228004061473946 ) ) ;
#48565=( BOUNDED_SURFACE ( )  B_SPLINE_SURFACE ( 3, 1, ( 
 ( #53169, #43174 ),
 ( #17605, #43495 ),
 ( #8585, #32859 ),
 ( #12577, #7615 ) ),
 .UNSPECIFIED., .F., .F., .F. ) 
 B_SPLINE_SURFACE_WITH_KNOTS ( ( 4, 4 ),
 ( 2, 2 ),
 ( 0.000000000000000000, 1.000000000000000000 ),
 ( 0.000000000000000000, 1.000000000000000000 ),
 .UNSPECIFIED. ) 
 GEOMETRIC_REPRESENTATION_ITEM ( )  RATIONAL_B_SPLINE_SURFACE ( (
 ( 1.000000000000000000, 1.000000000000000000),
 ( 0.9856612449720755231, 0.9999558406602322425),
 ( 0.9856612449720755231, 0.9999558406602322425),
 ( 1.000000000000000000, 1.000000000000000000) ) ) 
 REPRESENTATION_ITEM ( '' )  SURFACE ( )  );
#48568=FACE_OUTER_BOUND ( 'NONE', #41090, .T. ) ;
#48574=DIRECTION ( 'NONE',  ( 0.000000000000000000, 0.000000000000000000, 1.000000000000000000 ) ) ;
#48576=ORIENTED_EDGE ( 'NONE', *, *, #44950, .F. ) ;
#48578=CARTESIAN_POINT ( 'NONE',  ( 3.152665057734129750, -7.102135024645910732, 3.546019893116286958 ) ) ;
#48585=DIRECTION ( 'NONE',  ( -0.3865475372811021382, -0.1410344188397464060, 0.9114221272958265008 ) ) ;
#48587=ORIENTED_EDGE ( 'NONE', *, *, #58368, .F. ) ;
#48590=CARTESIAN_POINT ( 'NONE',  ( 2.242819959140645469, 3.728423299584983752, 6.662619100654757709 ) ) ;
#48601=CARTESIAN_POINT ( 'NONE',  ( 2.268878695253352618, -2.752970156154534997, 7.130600918714371517 ) ) ;
#48602=CARTESIAN_POINT ( 'NONE',  ( 2.273267844203306520, 6.695181685738918809, 3.690689057642454252 ) ) ;
#48603=EDGE_LOOP ( 'NONE', ( #50701, #19199, #32952, #8332 ) ) ;
#48604=CARTESIAN_POINT ( 'NONE',  ( 0.3665391374699464300, -5.911453292029527518, -10.76665847464318837 ) ) ;
#48605=CARTESIAN_POINT ( 'NONE',  ( 0.3474126878361764592, 12.03947592323250149, -2.385599230261914894 ) ) ;
#48606=CARTESIAN_POINT ( 'NONE',  ( 0.3006302518452102501, -2.350739146140512936, -12.03044280705495872 ) ) ;
#48612=CARTESIAN_POINT ( 'NONE',  ( 2.524535260912908807, -6.801151891677258199, -3.671333852642867601 ) ) ;
#48622=CARTESIAN_POINT ( 'NONE',  ( 0.2648978790185593790, -12.03635331166810651, -2.256510822326266652 ) ) ;
#48624=CARTESIAN_POINT ( 'NONE',  ( 2.994568964204210815, -7.686291764591495657, -1.761139509856907592 ) ) ;
#48627=CARTESIAN_POINT ( 'NONE',  ( 0.2652384529303158933, 7.922180393770671181, 9.338494547402412138 ) ) ;
#48631=ORIENTED_EDGE ( 'NONE', *, *, #57442, .F. ) ;
#48636=CARTESIAN_POINT ( 'NONE',  ( 0.2739690278137261181, 1.946552041163069013, -12.09341522051407480 ) ) ;
#48637=CARTESIAN_POINT ( 'NONE',  ( 1.719304012340734378, -8.755325027794794934, -9.242227816401850760 ) ) ;
#48647=VERTEX_POINT ( 'NONE', #31238 ) ;
#48652=CARTESIAN_POINT ( 'NONE',  ( 1.719304012338199517, 12.70777170743846796, 0.7661785589580254463 ) ) ;
#48655=ORIENTED_EDGE ( 'NONE', *, *, #51435, .F. ) ;
#48659=CARTESIAN_POINT ( 'NONE',  ( 1.937114397841932290, 3.111612666690241724, -12.45230409340478239 ) ) ;
#48661=CARTESIAN_POINT ( 'NONE',  ( 0.3665391374699472626, 3.952034409876453047, -11.62960183138723025 ) ) ;
#48662=EDGE_CURVE ( 'NONE', #44487, #58379, #20116, .T. ) ;
#48665=CARTESIAN_POINT ( 'NONE',  ( 1.719304012338239485, 12.38166659046522788, 2.961219984258211202 ) ) ;
#48669=EDGE_CURVE ( 'NONE', #23832, #39632, #64743, .T. ) ;
#48674=CARTESIAN_POINT ( 'NONE',  ( 2.241509619876138171, -5.872890204493053545, 4.877966158328288060 ) ) ;
#48680=CARTESIAN_POINT ( 'NONE',  ( 5.514624014163232779, -0.002789935220458067931, 0.003060352188290767217 ) ) ;
#48681=FACE_OUTER_BOUND ( 'NONE', #6919, .T. ) ;
#48684=CARTESIAN_POINT ( 'NONE',  ( 1.937114397841935398, -11.53912442307251496, -5.620553190833097013 ) ) ;
#48699=CARTESIAN_POINT ( 'NONE',  ( 2.889800649504073782, 4.645655809191420182, -3.986129653162600928 ) ) ;
#48703=FACE_OUTER_BOUND ( 'NONE', #4011, .T. ) ;
#48705=FACE_OUTER_BOUND ( 'NONE', #31800, .T. ) ;
#48706=B_SPLINE_CURVE_WITH_KNOTS ( 'NONE', 3,
 ( #62404, #46801, #16868, #26516, #62105, #56456, #22181, #1268, #36825, #47153, #16218, #11549, #31817, #11875, #929, #26201, #36502, #61425, #26850 ),
 .UNSPECIFIED., .F., .F.,
 ( 4, 3, 3, 3, 3, 3, 4 ),
 ( 0.000000000000000000, 2.831840207501608918E-05, 4.217266859843136855E-05, 5.602024318398862116E-05, 6.290810167972007863E-05, 9.120440630948104476E-05, 0.0001153103026479716580 ),
 .UNSPECIFIED. ) ;
#48710=EDGE_CURVE ( 'NONE', #38228, #45313, #62147, .T. ) ;
#48712=FACE_OUTER_BOUND ( 'NONE', #55090, .T. ) ;
#48713=CARTESIAN_POINT ( 'NONE',  ( 2.249013661412013310, -4.816366775941638423, -5.926694833810301155 ) ) ;
#48718=ORIENTED_EDGE ( 'NONE', *, *, #19662, .T. ) ;
#48729=LINE ( 'NONE', #8476, #4319 ) ;
#48730=CARTESIAN_POINT ( 'NONE',  ( 5.530133899448235191, 0.01149180883054601483, -0.01111090067015111857 ) ) ;
#48731=CARTESIAN_POINT ( 'NONE',  ( 3.152665057734127974, -4.377619405892426485, 6.622010822086644488 ) ) ;
#48745=CARTESIAN_POINT ( 'NONE',  ( 5.514624014163232779, 0.003830004412313175489, -0.001574979445069380445 ) ) ;
#48749=( BOUNDED_SURFACE ( )  B_SPLINE_SURFACE ( 3, 1, ( 
 ( #16852, #43347 ),
 ( #11221, #2829 ),
 ( #51140, #28083 ),
 ( #61412, #46789 ) ),
 .UNSPECIFIED., .F., .F., .T. ) 
 B_SPLINE_SURFACE_WITH_KNOTS ( ( 4, 4 ),
 ( 2, 2 ),
 ( 0.000000000000000000, 1.000000000000000000 ),
 ( 0.000000000000000000, 1.000000000000000000 ),
 .UNSPECIFIED. ) 
 GEOMETRIC_REPRESENTATION_ITEM ( )  RATIONAL_B_SPLINE_SURFACE ( (
 ( 1.000000000000000000, 1.000000000000000000),
 ( 0.9942764183789327692, 0.8450855930916580938),
 ( 0.9942764183789327692, 0.8450855930916580938),
 ( 1.000000000000000000, 1.000000000000000000) ) ) 
 REPRESENTATION_ITEM ( '' )  SURFACE ( )  );
#48751=CARTESIAN_POINT ( 'NONE',  ( 0.6473888112830240571, -3.920507224439165217, 11.73602097806018918 ) ) ;
#48753=ORIENTED_EDGE ( 'NONE', *, *, #14802, .F. ) ;
#48756=CARTESIAN_POINT ( 'NONE',  ( 2.266490820343226353, -7.500072841116509181, 1.470039317404140622 ) ) ;
#48757=CARTESIAN_POINT ( 'NONE',  ( 0.3537226245948354442, -10.49813096858605377, -6.362463382302378179 ) ) ;
#48774=EDGE_CURVE ( 'NONE', #18751, #12414, #29633, .T. ) ;
#48784=CARTESIAN_POINT ( 'NONE',  ( 2.524535260911649814, -6.060306679218513182, -4.796565674004641622 ) ) ;
#48786=CARTESIAN_POINT ( 'NONE',  ( 0.2652384529303124516, -10.63836770010961885, -6.065769141714316248 ) ) ;
#48790=CARTESIAN_POINT ( 'NONE',  ( 2.524535260912295964, -3.671333852642895579, 6.801151891677007733 ) ) ;
#48791=CARTESIAN_POINT ( 'NONE',  ( 0.6473888112830264996, -4.540486098228903700, -11.51036712212684421 ) ) ;
#48793=VERTEX_POINT ( 'NONE', #42489 ) ;
#48811=CARTESIAN_POINT ( 'NONE',  ( 0.2648978790185619880, -9.465406350830555482, -7.769924372105300847 ) ) ;
#48813=CARTESIAN_POINT ( 'NONE',  ( 2.241311220309555985, 7.533971938435861659, -1.234192392743096223 ) ) ;
#48825=DIRECTION ( 'NONE',  ( 0.3865475372811021382, 0.9114221272958279441, -0.1410344188397373577 ) ) ;
#48830=CARTESIAN_POINT ( 'NONE',  ( 0.3164563675027620149, 5.922187299605785604, -10.73846246126243109 ) ) ;
#48831=CARTESIAN_POINT ( 'NONE',  ( 2.994568964204209038, 1.761139509856933127, -7.686291764591495657 ) ) ;
#48832=CARTESIAN_POINT ( 'NONE',  ( 2.507146904658100084, -1.553587269793110126, 7.565123178000311199 ) ) ;
#48835=DIRECTION ( 'NONE',  ( 0.000000000000000000, 0.000000000000000000, 1.000000000000000000 ) ) ;
#48843=CARTESIAN_POINT ( 'NONE',  ( 0.3109076770649056853, 10.49874397806414272, -6.333869442011672568 ) ) ;
#48845=CARTESIAN_POINT ( 'NONE',  ( 0.2648978790185619880, -10.67083876753487637, -6.008231198269095685 ) ) ;
#48848=CARTESIAN_POINT ( 'NONE',  ( 2.241352910868908310, -5.901537464758487062, 4.843133558968109043 ) ) ;
#48852=CARTESIAN_POINT ( 'NONE',  ( 0.3654063281920749140, -8.093076148785975477, -9.235228056824000831 ) ) ;
#48859=ORIENTED_EDGE ( 'NONE', *, *, #37826, .F. ) ;
#48860=CARTESIAN_POINT ( 'NONE',  ( 0.3006302518452031447, 0.2259616664572240141, 12.25587491745529434 ) ) ;
#48863=CARTESIAN_POINT ( 'NONE',  ( 0.2911222467163561700, -0.2144311696656475141, 12.25291251554514993 ) ) ;
#48874=EDGE_CURVE ( 'NONE', #3473, #43566, #58478, .T. ) ;
#48878=EDGE_CURVE ( 'NONE', #20299, #12988, #32683, .T. ) ;
#48888=EDGE_LOOP ( 'NONE', ( #11133, #52996, #47017, #64116 ) ) ;
#48889=CARTESIAN_POINT ( 'NONE',  ( 2.280717697723672277, 5.034569468898445699, 5.756537207046734217 ) ) ;
#48890=CARTESIAN_POINT ( 'NONE',  ( 2.241506898688419458, -5.873558213059442146, -4.877157973187039808 ) ) ;
#48892=CARTESIAN_POINT ( 'NONE',  ( 0.3665391374699467075, -11.44911061034383692, -4.447929964102962153 ) ) ;
#48906=B_SPLINE_CURVE_WITH_KNOTS ( 'NONE', 3,
 ( #20286, #5330, #19957, #65183, #50568, #60516, #55203, #5676, #4351, #46232, #45896, #34897, #55544, #5009, #45547, #61494, #25604, #30269, #35575 ),
 .UNSPECIFIED., .F., .F.,
 ( 4, 3, 3, 3, 3, 3, 4 ),
 ( 4.336808689942017736E-19, 2.831840207458012471E-05, 4.217266859783568754E-05, 5.602024318339777164E-05, 6.290810167913131619E-05, 9.120440630890396460E-05, 0.0001153103026480246755 ),
 .UNSPECIFIED. ) ;
#48923=CARTESIAN_POINT ( 'NONE',  ( 2.350038591457877413, 8.533611140766113934, -6.324706260080378506 ) ) ;
#48928=DIRECTION ( 'NONE',  ( 0.000000000000000000, 0.000000000000000000, 1.000000000000000000 ) ) ;
#48931=CARTESIAN_POINT ( 'NONE',  ( 2.261269890822071638, -7.131324074141565994, -2.744033622443687204 ) ) ;
#48933=CARTESIAN_POINT ( 'NONE',  ( 2.241352910868908310, -2.689314586382399952, 7.145045428366567641 ) ) ;
#48936=DIRECTION ( 'NONE',  ( -0.3939253465568943180, 0.9034404741085576562, -0.1691689424289672949 ) ) ;
#48937=CARTESIAN_POINT ( 'NONE',  ( 0.3665391374699472626, -12.13918562134717760, -1.872534962004924086 ) ) ;
#48938=CARTESIAN_POINT ( 'NONE',  ( 0.2872850955227762570, -2.333231805482910204, -12.02931961709053610 ) ) ;
#48942=CARTESIAN_POINT ( 'NONE',  ( 3.031336079629770364, -7.038432939676141586, -3.582646412484407072 ) ) ;
#48944=EDGE_LOOP ( 'NONE', ( #35930, #65173, #29594, #30651 ) ) ;
#48949=CIRCLE ( 'NONE', #39330, 7.938172270156617749 ) ;
#48950=CARTESIAN_POINT ( 'NONE',  ( 0.4613984246114883336, -9.246873830555951912, 8.128335150814478993 ) ) ;
#48953=CARTESIAN_POINT ( 'NONE',  ( 0.3675815128205894289, 1.872154644482084684, 12.13672785388550679 ) ) ;
#48958=( BOUNDED_SURFACE ( )  B_SPLINE_SURFACE ( 3, 1, ( 
 ( #50528, #65457 ),
 ( #9948, #40185 ),
 ( #14274, #15575 ),
 ( #44519, #60819 ) ),
 .UNSPECIFIED., .F., .F., .T. ) 
 B_SPLINE_SURFACE_WITH_KNOTS ( ( 4, 4 ),
 ( 2, 2 ),
 ( 0.000000000000000000, 1.000000000000000000 ),
 ( 0.000000000000000000, 1.000000000000000000 ),
 .UNSPECIFIED. ) 
 GEOMETRIC_REPRESENTATION_ITEM ( )  RATIONAL_B_SPLINE_SURFACE ( (
 ( 1.000000000000000000, 1.000000000000000000),
 ( 0.9942764183789327692, 0.8450855930916585379),
 ( 0.9942764183789327692, 0.8450855930916585379),
 ( 1.000000000000000000, 1.000000000000000000) ) ) 
 REPRESENTATION_ITEM ( '' )  SURFACE ( )  );
#48976=CARTESIAN_POINT ( 'NONE',  ( 0.2652384529303136174, 6.180212112237663646, 10.57229402027109977 ) ) ;
#48981=ORIENTED_EDGE ( 'NONE', *, *, #11852, .F. ) ;
#48982=ORIENTED_EDGE ( 'NONE', *, *, #35470, .T. ) ;
#48989=CARTESIAN_POINT ( 'NONE',  ( 2.994568964204211259, -3.069094401380829673, 7.263701055179717869 ) ) ;
#48990=CARTESIAN_POINT ( 'NONE',  ( 0.3401186441510231084, 10.49699112323343542, 6.355596563012347211 ) ) ;
#48992=CARTESIAN_POINT ( 'NONE',  ( 0.2655924914740778187, -11.52280271232873865, 4.147079829127216399 ) ) ;
#49000=CARTESIAN_POINT ( 'NONE',  ( 5.516018279890452902, 0.002527316374434291236, -0.006286471671802449680 ) ) ;
#49001=VECTOR ( 'NONE', #50681, 1000.000000000000000 ) ;
#49004=EDGE_LOOP ( 'NONE', ( #42023, #4164, #34741, #47056 ) ) ;
#49020=CARTESIAN_POINT ( 'NONE',  ( 0.2646305136544065406, 12.08286001766535378, 1.996350543473033978 ) ) ;
#49040=CARTESIAN_POINT ( 'NONE',  ( 2.241506898688418126, -2.648071636522685512, -7.160521809579523556 ) ) ;
#49060=CARTESIAN_POINT ( 'NONE',  ( 0.2653519789438771870, -4.209148152332840453, -11.50012635727059696 ) ) ;
#49065=EDGE_CURVE ( 'NONE', #42272, #21980, #35031, .T. ) ;
#49070=CARTESIAN_POINT ( 'NONE',  ( 0.5572780756284498871, -12.09922454589796281, -2.443667122521545387 ) ) ;
#49071=CARTESIAN_POINT ( 'NONE',  ( 2.241352910868908754, 3.889181972941541776, -6.569501556381402096 ) ) ;
#49097=CARTESIAN_POINT ( 'NONE',  ( 2.241352910868909643, -1.407733736974916772, 7.503490710578227585 ) ) ;
#49103=CARTESIAN_POINT ( 'NONE',  ( 0.3675815128205894289, -12.04510820461660892, 2.391755495700564449 ) ) ;
#49109=ORIENTED_EDGE ( 'NONE', *, *, #26432, .T. ) ;
#49111=CARTESIAN_POINT ( 'NONE',  ( 2.781367136452587818, 4.783057651000514277, -6.179587792204545238 ) ) ;
#49129=CARTESIAN_POINT ( 'NONE',  ( 2.263328370261532108, -0.1420109704215282709, -7.640407877530313030 ) ) ;
#49130=AXIS2_PLACEMENT_3D ( 'NONE', #43500, #62811, #7280 ) ;
#49131=CARTESIAN_POINT ( 'NONE',  ( 2.258463476536644254, -5.939075453322711695, 4.806099079317522005 ) ) ;
#49132=VERTEX_POINT ( 'NONE', #7862 ) ;
#49138=CARTESIAN_POINT ( 'NONE',  ( 0.2648978790185593790, -12.03635331166810651, -2.256510822326266652 ) ) ;
#49142=EDGE_CURVE ( 'NONE', #11247, #21985, #216, .T. ) ;
#49147=CARTESIAN_POINT ( 'NONE',  ( 0.3665391374699467075, -2.392238720110539951, 12.04754782681756886 ) ) ;
#49148=( BOUNDED_SURFACE ( )  B_SPLINE_SURFACE ( 3, 1, ( 
 ( #22905, #7598 ),
 ( #43158, #33832 ),
 ( #8571, #28858 ),
 ( #49169, #3626 ) ),
 .UNSPECIFIED., .F., .F., .F. ) 
 B_SPLINE_SURFACE_WITH_KNOTS ( ( 4, 4 ),
 ( 2, 2 ),
 ( 0.000000000000000000, 1.000000000000000000 ),
 ( 0.000000000000000000, 1.000000000000000000 ),
 .UNSPECIFIED. ) 
 GEOMETRIC_REPRESENTATION_ITEM ( )  RATIONAL_B_SPLINE_SURFACE ( (
 ( 1.000000000000000000, 1.000000000000000000),
 ( 0.6933888150995267674, 0.9895912004443193632),
 ( 0.6933888150995267674, 0.9895912004443193632),
 ( 1.000000000000000000, 1.000000000000000000) ) ) 
 REPRESENTATION_ITEM ( '' )  SURFACE ( )  );
#49149=CARTESIAN_POINT ( 'NONE',  ( 0.3223008802179254118, -9.550960164375549510, -7.695050880595591281 ) ) ;
#49151=CARTESIAN_POINT ( 'NONE',  ( 2.245754705088394587, 7.538396044169889620, -1.216173395688163295 ) ) ;
#49158=ORIENTED_EDGE ( 'NONE', *, *, #52394, .F. ) ;
#49160=LINE ( 'NONE', #38500, #10023 ) ;
#49163=CARTESIAN_POINT ( 'NONE',  ( 2.034671305879991010, -11.19279775165753854, 3.325478336154509940 ) ) ;
#49169=CARTESIAN_POINT ( 'NONE',  ( 5.516018279890452902, 0.001397286410094419331, 0.006629829924290476899 ) ) ;
#49170=CARTESIAN_POINT ( 'NONE',  ( 2.241317068080773023, -4.977030124433802882, -5.789053609344378515 ) ) ;
#49175=CARTESIAN_POINT ( 'NONE',  ( 1.452237505248552996, 9.303501428256026884, 8.579708443906778115 ) ) ;
#49178=CARTESIAN_POINT ( 'NONE',  ( 0.2655924914740778187, -6.084990060696436665, -10.62761259256423330 ) ) ;
#49185=ORIENTED_EDGE ( 'NONE', *, *, #42048, .T. ) ;
#49186=DIRECTION ( 'NONE',  ( -1.000000000000000000, 0.000000000000000000, 0.000000000000000000 ) ) ;
#49187=CARTESIAN_POINT ( 'NONE',  ( 0.2650492594609233366, 7.955687020697175704, -9.309909082761068433 ) ) ;
#49191=AXIS2_PLACEMENT_3D ( 'NONE', #20245, #11578, #10932 ) ;
#49193=CARTESIAN_POINT ( 'NONE',  ( 0.3675815128205894289, 0.2638082659430137644, -12.27743992903065973 ) ) ;
#49204=CARTESIAN_POINT ( 'NONE',  ( 1.719304012338199517, 0.000000000000000000, 0.000000000000000000 ) ) ;
#49209=CARTESIAN_POINT ( 'NONE',  ( 2.430348790457652619, 5.095533593440028319, 5.769383131055089819 ) ) ;
#49210=ORIENTED_EDGE ( 'NONE', *, *, #24219, .T. ) ;
#49212=CARTESIAN_POINT ( 'NONE',  ( 0.3040950598368152291, 7.687624643091557353, -9.552450779732032160 ) ) ;
#49217=ADVANCED_FACE ( 'NONE', ( #28780 ), #33395, .F. ) ;
#49230=CARTESIAN_POINT ( 'NONE',  ( 2.273267844204674315, 5.029122824445567908, 5.758000272829374211 ) ) ;
#49231=LINE ( 'NONE', #64173, #13061 ) ;
#49232=DIRECTION ( 'NONE',  ( -0.3865475372811021382, 0.4778122177792039071, 0.7888450329201760480 ) ) ;
#49240=CARTESIAN_POINT ( 'NONE',  ( 0.3665391374699472626, 11.44911061034392574, -4.447929964102733003 ) ) ;
#49244=VECTOR ( 'NONE', #64721, 1000.000000000000114 ) ;
#49249=DIRECTION ( 'NONE',  ( 0.3939253465568944290, 0.4511294145502710018, 0.8008152550167613182 ) ) ;
#49250=CARTESIAN_POINT ( 'NONE',  ( 2.273267844204864829, -2.756477528575253633, -7.130811676080301531 ) ) ;
#49252=VERTEX_POINT ( 'NONE', #65565 ) ;
#49256=VERTEX_POINT ( 'NONE', #45622 ) ;
#49268=VERTEX_POINT ( 'NONE', #40639 ) ;
#49269=CARTESIAN_POINT ( 'NONE',  ( 2.251139882113958990, -7.133642337268841338, -2.728563091335224122 ) ) ;
#49278=CARTESIAN_POINT ( 'NONE',  ( 0.3160775863651097417, 3.967735865794352002, 11.60348481172936808 ) ) ;
#49279=CARTESIAN_POINT ( 'NONE',  ( 0.2650492433740082587, -9.451472485870498375, -7.786978278830065214 ) ) ;
#49282=ORIENTED_EDGE ( 'NONE', *, *, #15204, .F. ) ;
#49284=CARTESIAN_POINT ( 'NONE',  ( 0.6473888112830208375, 6.470260187014720721, 10.54705164520780691 ) ) ;
#49288=CARTESIAN_POINT ( 'NONE',  ( 0.4613984246114898879, 9.610550265395851000, 7.694922453052171818 ) ) ;
#49289=CARTESIAN_POINT ( 'NONE',  ( 0.2655924914740778187, -9.352877839710547647, -7.905499957109333842 ) ) ;
#49290=CARTESIAN_POINT ( 'NONE',  ( 3.152665057735260845, 4.377619405893435456, 6.622010822086191517 ) ) ;
#49296=CARTESIAN_POINT ( 'NONE',  ( 1.375507693218337213, 1.606074886185604678, 12.51366828189644664 ) ) ;
#49306=CARTESIAN_POINT ( 'NONE',  ( 0.2653519991613838003, 7.854838327448966595, 9.395283368383198663 ) ) ;
#49314=CARTESIAN_POINT ( 'NONE',  ( 0.3006302518451998140, 1.905681544119403270, -12.10891847026071488 ) ) ;
#49319=EDGE_LOOP ( 'NONE', ( #54664, #28666, #57198, #3227 ) ) ;
#49321=VERTEX_POINT ( 'NONE', #739 ) ;
#49322=B_SPLINE_CURVE_WITH_KNOTS ( 'NONE', 3,
 ( #44917, #39925, #61199, #15627, #60209, #34910, #5022, #60873, #15314, #55220, #29946, #50253, #24976, #52220, #42871, #37887, #6331, #58179, #36901, #61846, #2330, #62179 ),
 .UNSPECIFIED., .F., .F.,
 ( 4, 3, 3, 3, 3, 3, 3, 4 ),
 ( 5.421010862427522170E-20, 4.449119708436901857E-05, 6.626296329540710202E-05, 8.803456484962969336E-05, 0.0001098060367612836182, 0.0001315774408628541618, 0.0001760698110411196781, 0.0001829697163287832395 ),
 .UNSPECIFIED. ) ;
#49330=CARTESIAN_POINT ( 'NONE',  ( 0.3160775863651095752, 10.49803827792122668, 6.338373607799229426 ) ) ;
#49333=DIRECTION ( 'NONE',  ( 1.000000000000000000, -0.000000000000000000, -0.000000000000000000 ) ) ;
#49335=CARTESIAN_POINT ( 'NONE',  ( 2.263328370261531663, -1.466596409249111055, -7.499672967744989371 ) ) ;
#49342=EDGE_CURVE ( 'NONE', #39489, #42516, #46974, .T. ) ;
#49344=ORIENTED_EDGE ( 'NONE', *, *, #32074, .T. ) ;
#49347=CARTESIAN_POINT ( 'NONE',  ( 2.241352910868908754, 2.532612177304442991, 7.202080440908749992 ) ) ;
#49349=CARTESIAN_POINT ( 'NONE',  ( 0.3632410797595283514, 9.572936598843634570, 7.689504457927688996 ) ) ;
#49360=CARTESIAN_POINT ( 'NONE',  ( 0.2655924914740778742, 6.084990060696657821, -10.62761259256410540 ) ) ;
#49362=CARTESIAN_POINT ( 'NONE',  ( 5.520433897694421610, -0.01432141647227066876, 0.004666464468077991673 ) ) ;
#49365=CARTESIAN_POINT ( 'NONE',  ( 2.241537034860907163, -7.517665055735995416, -1.330359961362363119 ) ) ;
#49370=EDGE_CURVE ( 'NONE', #1207, #26844, #46775, .T. ) ;
#49378=B_SPLINE_CURVE_WITH_KNOTS ( 'NONE', 3,
 ( #3953, #50158, #35497, #55795, #29217, #34518, #40143, #60121, #4614, #9236 ),
 .UNSPECIFIED., .F., .F.,
 ( 4, 3, 3, 4 ),
 ( 8.673617379884035472E-19, 6.607638129004469909E-05, 9.911389841680505995E-05, 0.0001667630577588622841 ),
 .UNSPECIFIED. ) ;
#49379=EDGE_CURVE ( 'NONE', #60603, #20926, #43586, .T. ) ;
#49381=B_SPLINE_CURVE_WITH_KNOTS ( 'NONE', 3,
 ( #44945, #33975, #24668, #49620, #59269, #60235, #54919, #59927, #53949, #48976, #3764, #3433, #23701 ),
 .UNSPECIFIED., .F., .F.,
 ( 4, 3, 3, 3, 4 ),
 ( 1.734723475976807094E-18, 6.607593386745509354E-05, 0.0001321518677373535993, 0.0001982171734706209411, 0.0002642860854759494760 ),
 .UNSPECIFIED. ) ;
#49389=CARTESIAN_POINT ( 'NONE',  ( 0.3675815128205894289, 0.2638082659430137644, -12.27743992903065973 ) ) ;
#49393=CARTESIAN_POINT ( 'NONE',  ( 0.2759803524722203583, -12.09509972435083114, 1.940323823244621160 ) ) ;
#49400=VERTEX_POINT ( 'NONE', #18983 ) ;
#49406=FACE_OUTER_BOUND ( 'NONE', #63747, .T. ) ;
#49408=CARTESIAN_POINT ( 'NONE',  ( 2.241317068080775687, -7.533758201955906841, -1.235499051333850185 ) ) ;
#49415=ORIENTED_EDGE ( 'NONE', *, *, #14302, .T. ) ;
#49417=VERTEX_POINT ( 'NONE', #13646 ) ;
#49427=CARTESIAN_POINT ( 'NONE',  ( 5.516018279890452902, -0.006286471671802459221, -0.002527316374434270853 ) ) ;
#49428=EDGE_CURVE ( 'NONE', #36377, #56447, #53592, .T. ) ;
#49430=CARTESIAN_POINT ( 'NONE',  ( 2.241352910868908310, -7.503490710578242684, 1.407733736974842165 ) ) ;
#49431=CARTESIAN_POINT ( 'NONE',  ( 0.2956976708475464455, 0.2200030809427307998, -12.25433786972504890 ) ) ;
#49439=ORIENTED_EDGE ( 'NONE', *, *, #16076, .T. ) ;
#49445=CARTESIAN_POINT ( 'NONE',  ( 1.719304012341272836, -1.452142814148833949, -12.64775761152634281 ) ) ;
#49446=CARTESIAN_POINT ( 'NONE',  ( 2.305787727787084407, 2.461236246751170142, -7.249469779319884566 ) ) ;
#49456=B_SPLINE_CURVE_WITH_KNOTS ( 'NONE', 3,
 ( #19453, #61305, #40357, #9438, #14751, #55340, #64978, #55681, #5478, #30708, #60656, #49705, #9129 ),
 .UNSPECIFIED., .F., .F.,
 ( 4, 3, 3, 3, 4 ),
 ( 1.734723475976807094E-18, 6.607593386745476828E-05, 0.0001321518677373514309, 0.0001982171734706212663, 0.0002642860854759490966 ),
 .UNSPECIFIED. ) ;
#49458=CARTESIAN_POINT ( 'NONE',  ( 2.491965175173986413, -3.673871285745626825, 6.787433375639312594 ) ) ;
#49459=CARTESIAN_POINT ( 'NONE',  ( 2.262775599886256206, -5.943524836196959704, 4.802882839669045723 ) ) ;
#49460=ORIENTED_EDGE ( 'NONE', *, *, #40818, .T. ) ;
#49461=CARTESIAN_POINT ( 'NONE',  ( 2.242418902651940105, -2.517330194228340812, 7.207816731001393862 ) ) ;
#49462=CARTESIAN_POINT ( 'NONE',  ( 5.530133899448235191, 0.008946569461392158557, -0.01324661008606532915 ) ) ;
#49464=ORIENTED_EDGE ( 'NONE', *, *, #32416, .F. ) ;
#49468=CARTESIAN_POINT ( 'NONE',  ( 0.6511581176954489569, 12.37037447926092781, 0.3309006379874227521 ) ) ;
#49470=CARTESIAN_POINT ( 'NONE',  ( 0.6473888112830230579, 12.12394591856681991, -2.472751636945246467 ) ) ;
#49472=CARTESIAN_POINT ( 'NONE',  ( 2.284126774967658147, -7.240052432235668967, 2.466502196988942242 ) ) ;
#49481=VERTEX_POINT ( 'NONE', #13973 ) ;
#49482=ORIENTED_EDGE ( 'NONE', *, *, #5097, .F. ) ;
#49485=VECTOR ( 'NONE', #22395, 1000.000000000000114 ) ;
#49487=B_SPLINE_CURVE_WITH_KNOTS ( 'NONE', 3,
 ( #4090, #7776, #24359, #8104, #17754, #53979, #64581, #59626, #8423, #58316, #3795, #28062, #2809, #23070, #18424, #43327, #29041, #63604, #18078, #49349, #19055, #58992 ),
 .UNSPECIFIED., .F., .F.,
 ( 4, 3, 3, 3, 3, 3, 3, 4 ),
 ( 1.951563910473907981E-18, 4.449119708436932350E-05, 6.626296329540588229E-05, 8.803456484962986954E-05, 0.0001098060367612875891, 0.0001315774408628584986, 0.0001760698110411265628, 0.0001829697163287840526 ),
 .UNSPECIFIED. ) ;
#49495=CARTESIAN_POINT ( 'NONE',  ( 2.288423627607476085, -7.242304196986135700, -2.464337058688830684 ) ) ;
#49502=EDGE_CURVE ( 'NONE', #7744, #10208, #1751, .T. ) ;
#49505=CARTESIAN_POINT ( 'NONE',  ( 5.516018279890452902, 0.006771744149385265123, -0.0002248006052448750405 ) ) ;
#49506=CARTESIAN_POINT ( 'NONE',  ( 0.2671309869109469437, 11.56263543972758967, 4.036029264453025789 ) ) ;
#49508=CARTESIAN_POINT ( 'NONE',  ( 3.152665057734126197, -1.848755561852092333, 7.719888720907804647 ) ) ;
#49516=DIRECTION ( 'NONE',  ( 0.3939253465568944290, -0.4511294145502765529, -0.8008152550167580985 ) ) ;
#49519=CARTESIAN_POINT ( 'NONE',  ( 0.2958664285830424068, 0.2205161970874386923, 12.25438626999990177 ) ) ;
#49523=CARTESIAN_POINT ( 'NONE',  ( 1.452237505248555660, 8.579708443906746140, 9.303501428256057082 ) ) ;
#49524=CARTESIAN_POINT ( 'NONE',  ( 2.247206125382828379, -7.499376972323885227, -1.439877054338178475 ) ) ;
#49525=CARTESIAN_POINT ( 'NONE',  ( 2.241352910868908754, -4.843133558968167662, 5.901537464758438212 ) ) ;
#49527=FACE_OUTER_BOUND ( 'NONE', #7985, .T. ) ;
#49529=CARTESIAN_POINT ( 'NONE',  ( 2.034671305879538039, 0.7032348381694819572, -11.65517003034116605 ) ) ;
#49530=CARTESIAN_POINT ( 'NONE',  ( 0.2648978790185602672, 1.996248716311790128, -12.08224454301446826 ) ) ;
#49535=( BOUNDED_SURFACE ( )  B_SPLINE_SURFACE ( 3, 1, ( 
 ( #1643, #17583 ),
 ( #57828, #31859 ),
 ( #52515, #32191 ),
 ( #42159, #6627 ) ),
 .UNSPECIFIED., .F., .F., .F. ) 
 B_SPLINE_SURFACE_WITH_KNOTS ( ( 4, 4 ),
 ( 2, 2 ),
 ( 0.000000000000000000, 1.000000000000000000 ),
 ( 0.000000000000000000, 1.000000000000000000 ),
 .UNSPECIFIED. ) 
 GEOMETRIC_REPRESENTATION_ITEM ( )  RATIONAL_B_SPLINE_SURFACE ( (
 ( 1.000000000000000000, 1.000000000000000000),
 ( 0.6933888150995267674, 0.9895912004443193632),
 ( 0.6933888150995267674, 0.9895912004443193632),
 ( 1.000000000000000000, 1.000000000000000000) ) ) 
 REPRESENTATION_ITEM ( '' )  SURFACE ( )  );
#49544=ORIENTED_EDGE ( 'NONE', *, *, #26051, .F. ) ;
#49547=CARTESIAN_POINT ( 'NONE',  ( 2.241352910868908310, 4.970878533273761946, 5.794346703933863196 ) ) ;
#49548=CARTESIAN_POINT ( 'NONE',  ( 2.241449424704146320, -5.887589908049611687, -4.860179885671861655 ) ) ;
#49552=CARTESIAN_POINT ( 'NONE',  ( 1.462291587749891209, -12.62932306616585798, -0.6330131614654728178 ) ) ;
#49556=ORIENTED_EDGE ( 'NONE', *, *, #64607, .F. ) ;
#49559=CARTESIAN_POINT ( 'NONE',  ( 2.406456491627778860, 10.41426194694948038, -0.6290357040717751147 ) ) ;
#49561=ORIENTED_EDGE ( 'NONE', *, *, #35566, .T. ) ;
#49581=CARTESIAN_POINT ( 'NONE',  ( 1.549075743845464759, -0.6747257554049737038, 12.65619669351041487 ) ) ;
#49589=CARTESIAN_POINT ( 'NONE',  ( 0.3002738374340838678, 3.979745968261205302, 11.59380198135583484 ) ) ;
#49597=CARTESIAN_POINT ( 'NONE',  ( 2.994568964204211259, 7.020079750321941425, -3.591541975631893369 ) ) ;
#49598=CARTESIAN_POINT ( 'NONE',  ( 0.3053067050349172473, -9.241336250185305801, -8.055646999028104105 ) ) ;
#49600=ORIENTED_EDGE ( 'NONE', *, *, #53045, .T. ) ;
#49604=CARTESIAN_POINT ( 'NONE',  ( 0.8375941296797054791, 1.780036797758661526, 12.30893872205235340 ) ) ;
#49607=DIRECTION ( 'NONE',  ( 0.000000000000000000, 0.000000000000000000, 1.000000000000000000 ) ) ;
#49609=CARTESIAN_POINT ( 'NONE',  ( 1.937114397841935398, 11.72279974487470788, -5.226660192101475033 ) ) ;
#49617=CARTESIAN_POINT ( 'NONE',  ( 0.3632410797595244656, 1.872837903657359027, -12.13515851238021703 ) ) ;
#49620=CARTESIAN_POINT ( 'NONE',  ( 0.2652384770603652409, 6.065775245581168207, 10.63836422907226975 ) ) ;
#49623=ORIENTED_EDGE ( 'NONE', *, *, #55311, .T. ) ;
#49632=CARTESIAN_POINT ( 'NONE',  ( 0.3223008802179253007, -9.236652594547187789, 8.069628056118085979 ) ) ;
#49638=CARTESIAN_POINT ( 'NONE',  ( 2.257661810676422132, -1.459225434025932300, -7.499185766072603343 ) ) ;
#49641=CARTESIAN_POINT ( 'NONE',  ( 0.3040950598368152291, 5.912066680610761793, -10.74226959800785153 ) ) ;
#49643=CARTESIAN_POINT ( 'NONE',  ( 1.287602823386838402, -9.987902848013685997, 7.659913635101823104 ) ) ;
#49658=CARTESIAN_POINT ( 'NONE',  ( 5.516018279890452902, 0.002527316374434291236, -0.006286471671802449680 ) ) ;
#49664=CARTESIAN_POINT ( 'NONE',  ( 0.2638984909335720941, -8.023974293733116880, -9.252728947331158693 ) ) ;
#49668=ORIENTED_EDGE ( 'NONE', *, *, #10804, .F. ) ;
#49671=CARTESIAN_POINT ( 'NONE',  ( 0.2653141334712564303, -7.905403790036909406, -9.352759824582582482 ) ) ;
#49677=B_SPLINE_CURVE_WITH_KNOTS ( 'NONE', 3,
 ( #48564, #8006, #54537, #48889, #64172, #49230, #23616, #3686, #33251, #44518, #29553, #38223, #58544, #38570, #28924, #59194, #8969, #29251, #49547 ),
 .UNSPECIFIED., .F., .F.,
 ( 4, 3, 3, 3, 3, 3, 4 ),
 ( 6.992893892674702526E-18, 2.825908398850998936E-05, 4.208813692510701612E-05, 5.591713746977713896E-05, 6.279584083269157033E-05, 9.105792820349262943E-05, 0.0001153131102488628534 ),
 .UNSPECIFIED. ) ;
#49679=ORIENTED_EDGE ( 'NONE', *, *, #52551, .F. ) ;
#49680=CARTESIAN_POINT ( 'NONE',  ( 2.941278708680199916, 3.185832147968520545, -5.248410529370191924 ) ) ;
#49693=ORIENTED_EDGE ( 'NONE', *, *, #11145, .T. ) ;
#49696=EDGE_CURVE ( 'NONE', #63445, #37474, #47736, .T. ) ;
#49697=ORIENTED_EDGE ( 'NONE', *, *, #26032, .F. ) ;
#49705=CARTESIAN_POINT ( 'NONE',  ( 0.2650492433740053722, 4.084772052580754043, -11.54478237753287573 ) ) ;
#49706=ADVANCED_FACE ( 'NONE', ( #62467 ), #40171, .F. ) ;
#49709=CARTESIAN_POINT ( 'NONE',  ( 1.198791140417495571, 7.669598593075251713, 9.943044756147862984 ) ) ;
#49714=CARTESIAN_POINT ( 'NONE',  ( 0.2653519890518161728, 10.60551359205158661, -6.123106317427046363 ) ) ;
#49718=ADVANCED_FACE ( 'NONE', ( #26260 ), #29815, .T. ) ;
#49722=CARTESIAN_POINT ( 'NONE',  ( 1.937114397841932290, -12.45230409340479660, -3.111612666690204421 ) ) ;
#49727=( BOUNDED_SURFACE ( )  B_SPLINE_SURFACE ( 3, 1, ( 
 ( #9730, #5094 ),
 ( #60279, #9087 ),
 ( #25358, #54668 ),
 ( #34985, #55951 ) ),
 .UNSPECIFIED., .F., .F., .F. ) 
 B_SPLINE_SURFACE_WITH_KNOTS ( ( 4, 4 ),
 ( 2, 2 ),
 ( 0.000000000000000000, 1.000000000000000000 ),
 ( 0.000000000000000000, 1.000000000000000000 ),
 .UNSPECIFIED. ) 
 GEOMETRIC_REPRESENTATION_ITEM ( )  RATIONAL_B_SPLINE_SURFACE ( (
 ( 1.000000000000000000, 1.000000000000000000),
 ( 0.9942764183789327692, 0.8450855930916580938),
 ( 0.9942764183789327692, 0.8450855930916580938),
 ( 1.000000000000000000, 1.000000000000000000) ) ) 
 REPRESENTATION_ITEM ( '' )  SURFACE ( )  );
#49735=CARTESIAN_POINT ( 'NONE',  ( 0.3160775863651064110, -10.49803827792118405, -6.338373607799300480 ) ) ;
#49737=CARTESIAN_POINT ( 'NONE',  ( 2.262775599886257538, 7.640237753423675393, 0.1412024122916144542 ) ) ;
#49739=CARTESIAN_POINT ( 'NONE',  ( 1.948354844646296158, 1.364409644999653226, -11.88693049004315583 ) ) ;
#49742=CARTESIAN_POINT ( 'NONE',  ( 0.4626703367443965598, 3.943760108616825022, 11.66326339726735561 ) ) ;
#49747=FACE_OUTER_BOUND ( 'NONE', #30896, .T. ) ;
#49751=CARTESIAN_POINT ( 'NONE',  ( 2.907497136250300596, 6.243048412628660060, 4.769582063554193674 ) ) ;
#49752=CARTESIAN_POINT ( 'NONE',  ( 2.844750968616321263, -5.286885609674953024, -5.783165144077072384 ) ) ;
#49760=CARTESIAN_POINT ( 'NONE',  ( 1.283627346226862809, -4.817767733507260175, -11.62704807385642169 ) ) ;
#49770=CARTESIAN_POINT ( 'NONE',  ( 0.2646305136544072623, -12.24595685781654453, -0.1321451301299099712 ) ) ;
#49773=CARTESIAN_POINT ( 'NONE',  ( 0.9296196016816532515, 12.46069139398388081, 0.4155906739593158705 ) ) ;
#49787=VERTEX_POINT ( 'NONE', #42851 ) ;
#49788=CARTESIAN_POINT ( 'NONE',  ( 3.152665057736252940, 7.609997527622067715, 2.258875078500286016 ) ) ;
#49793=VECTOR ( 'NONE', #22607, 1000.000000000000000 ) ;
#49794=ADVANCED_FACE ( 'NONE', ( #33542 ), #52152, .T. ) ;
#49801=ORIENTED_EDGE ( 'NONE', *, *, #49826, .T. ) ;
#49804=CARTESIAN_POINT ( 'NONE',  ( 2.963017218115625351, 0.3847317984106394251, -7.865565884553431530 ) ) ;
#49807=CARTESIAN_POINT ( 'NONE',  ( 2.941278708680199916, 5.814102272488588241, 1.972702289976022483 ) ) ;
#49811=VECTOR ( 'NONE', #51477, 1000.000000000000114 ) ;
#49817=CARTESIAN_POINT ( 'NONE',  ( 2.298277635560276533, -1.491234112749247220, 7.506689984432345142 ) ) ;
#49818=CARTESIAN_POINT ( 'NONE',  ( 2.827825597296804272, 2.100863646776170768, -8.776379025186153982 ) ) ;
#49825=CARTESIAN_POINT ( 'NONE',  ( 0.3675815128205912052, 9.235491948680007113, 8.093875121226108860 ) ) ;
#49826=EDGE_CURVE ( 'NONE', #38510, #38095, #30307, .T. ) ;
#49828=CARTESIAN_POINT ( 'NONE',  ( 0.3474126878361805670, 0.2587235634078023927, 12.27082419038177541 ) ) ;
#49832=CARTESIAN_POINT ( 'NONE',  ( 2.268878695253351285, -7.500319319173561539, -1.472930498387347242 ) ) ;
#49835=CARTESIAN_POINT ( 'NONE',  ( 2.653899356900503825, 5.192946150929651061, 5.782420802795840586 ) ) ;
#49836=ORIENTED_EDGE ( 'NONE', *, *, #56369, .T. ) ;
#49844=ORIENTED_EDGE ( 'NONE', *, *, #45821, .F. ) ;
#49848=CARTESIAN_POINT ( 'NONE',  ( 0.2653141617321011503, 12.24612535104216526, 0.04404194803635243238 ) ) ;
#49864=CARTESIAN_POINT ( 'NONE',  ( 0.2657645697724693723, 12.24540328300722081, 0.1513403555225990293 ) ) ;
#49865=CARTESIAN_POINT ( 'NONE',  ( 2.589278595513858860, 6.588350318048553866, -4.081908913132052064 ) ) ;
#49871=ORIENTED_EDGE ( 'NONE', *, *, #18530, .F. ) ;
#49873=CARTESIAN_POINT ( 'NONE',  ( 1.372161826076855995, -2.769012792636821541, -12.30755118281459914 ) ) ;
#49882=CARTESIAN_POINT ( 'NONE',  ( 5.514624014163232779, 0.0001700579043838694037, 0.004137701579365772944 ) ) ;
#49886=CARTESIAN_POINT ( 'NONE',  ( 2.305787727787083519, -6.711944854845849129, 3.682701754025489826 ) ) ;
#49889=ORIENTED_EDGE ( 'NONE', *, *, #42882, .F. ) ;
#49890=VERTEX_POINT ( 'NONE', #19563 ) ;
#49892=LINE ( 'NONE', #33615, #19204 ) ;
#49898=ORIENTED_EDGE ( 'NONE', *, *, #53163, .F. ) ;
#49905=CARTESIAN_POINT ( 'NONE',  ( 1.020182472824526121, 9.854645283131009847, -7.686484208904769133 ) ) ;
#49910=VERTEX_POINT ( 'NONE', #40470 ) ;
#49911=CARTESIAN_POINT ( 'NONE',  ( 1.194176325881331380, 6.717888447700822496, 10.60746084433557535 ) ) ;
#49924=DIRECTION ( 'NONE',  ( -1.000000000000000000, -0.000000000000000000, -0.000000000000000000 ) ) ;
#49926=CARTESIAN_POINT ( 'NONE',  ( 0.2958664285830446272, -12.10650684287252687, -1.910785783655700509 ) ) ;
#49928=CARTESIAN_POINT ( 'NONE',  ( 5.530133899448235191, -0.004396748047611123179, -0.01536822665454899879 ) ) ;
#49937=CARTESIAN_POINT ( 'NONE',  ( 5.515188684475870851, -0.002983184900675359651, -0.004442604682416606034 ) ) ;
#49944=CARTESIAN_POINT ( 'NONE',  ( 3.152665057734129750, 3.161213418913565221, -7.281573230474259972 ) ) ;
#49949=DIRECTION ( 'NONE',  ( 0.000000000000000000, 0.000000000000000000, 1.000000000000000000 ) ) ;
#49953=CARTESIAN_POINT ( 'NONE',  ( 2.907497136250675407, -2.346692756478266251, 7.497839665536838893 ) ) ;
#49962=CARTESIAN_POINT ( 'NONE',  ( 0.7446945582519360896, -9.728576129010020779, 7.698291984229315155 ) ) ;
#49968=CARTESIAN_POINT ( 'NONE',  ( 1.104777566491150997, -6.672212870706140109, -10.60111489796741857 ) ) ;
#49978=ORIENTED_EDGE ( 'NONE', *, *, #28629, .T. ) ;
#49981=CARTESIAN_POINT ( 'NONE',  ( 0.2671309869109481094, 7.995521393275818234, 9.276621593297539548 ) ) ;
#49989=AXIS2_PLACEMENT_3D ( 'NONE', #3837, #10106, #25394 ) ;
#50001=EDGE_CURVE ( 'NONE', #44289, #26844, #54854, .T. ) ;
#50008=CARTESIAN_POINT ( 'NONE',  ( 2.284126774967662588, 6.701756155761997569, -3.686252397487058019 ) ) ;
#50011=AXIS2_PLACEMENT_3D ( 'NONE', #21610, #46535, #992 ) ;
#50029=AXIS2_PLACEMENT_3D ( 'NONE', #48484, #8887, #64716 ) ;
#50030=ORIENTED_EDGE ( 'NONE', *, *, #57949, .T. ) ;
#50040=ORIENTED_EDGE ( 'NONE', *, *, #61940, .T. ) ;
#50050=CARTESIAN_POINT ( 'NONE',  ( 2.835339799623983303, 7.763739326985127143, -1.035140033449970520 ) ) ;
#50056=ORIENTED_EDGE ( 'NONE', *, *, #9814, .F. ) ;
#50063=CARTESIAN_POINT ( 'NONE',  ( 2.241352910868908310, 1.407733736974867034, 7.503490710578237355 ) ) ;
#50068=CARTESIAN_POINT ( 'NONE',  ( 2.655192694323565750, 1.093661162900110284, -9.539062147543583947 ) ) ;
#50089=CARTESIAN_POINT ( 'NONE',  ( 2.491965175173335378, -6.046355957630531464, -4.796682362486714979 ) ) ;
#50098=( BOUNDED_SURFACE ( )  B_SPLINE_SURFACE ( 3, 1, ( 
 ( #18780, #59028 ),
 ( #53031, #3507 ),
 ( #8462, #53376 ),
 ( #59334, #7466 ) ),
 .UNSPECIFIED., .F., .F., .F. ) 
 B_SPLINE_SURFACE_WITH_KNOTS ( ( 4, 4 ),
 ( 2, 2 ),
 ( 0.000000000000000000, 1.000000000000000000 ),
 ( 0.000000000000000000, 1.000000000000000000 ),
 .UNSPECIFIED. ) 
 GEOMETRIC_REPRESENTATION_ITEM ( )  RATIONAL_B_SPLINE_SURFACE ( (
 ( 1.000000000000000000, 1.000000000000000000),
 ( 0.9942764183789327692, 0.8450855930916580938),
 ( 0.9942764183789327692, 0.8450855930916580938),
 ( 1.000000000000000000, 1.000000000000000000) ) ) 
 REPRESENTATION_ITEM ( '' )  SURFACE ( )  );
#50104=CARTESIAN_POINT ( 'NONE',  ( 1.462291587748817623, -6.862867011841285780, 10.62080802716765682 ) ) ;
#50114=CARTESIAN_POINT ( 'NONE',  ( 1.719304012338199517, 0.000000000000000000, 0.000000000000000000 ) ) ;
#50117=( BOUNDED_SURFACE ( )  B_SPLINE_SURFACE ( 3, 1, ( 
 ( #25046, #14066 ),
 ( #65578, #15385 ),
 ( #41955, #6082 ),
 ( #60947, #31001 ) ),
 .UNSPECIFIED., .F., .F., .F. ) 
 B_SPLINE_SURFACE_WITH_KNOTS ( ( 4, 4 ),
 ( 2, 2 ),
 ( 0.000000000000000000, 1.000000000000000000 ),
 ( 0.000000000000000000, 1.000000000000000000 ),
 .UNSPECIFIED. ) 
 GEOMETRIC_REPRESENTATION_ITEM ( )  RATIONAL_B_SPLINE_SURFACE ( (
 ( 1.000000000000000000, 1.000000000000000000),
 ( 0.9942764183789327692, 0.8450855930916585379),
 ( 0.9942764183789327692, 0.8450855930916585379),
 ( 1.000000000000000000, 1.000000000000000000) ) ) 
 REPRESENTATION_ITEM ( '' )  SURFACE ( )  );
#50123=CARTESIAN_POINT ( 'NONE',  ( 2.241311220309554653, -4.978033760028411692, 5.788190037953256706 ) ) ;
#50126=CIRCLE ( 'NONE', #10808, 4.000000000000000000 ) ;
#50147=CARTESIAN_POINT ( 'NONE',  ( 2.899286259009678179, -4.231523595108526159, 6.616268644969679258 ) ) ;
#50150=CARTESIAN_POINT ( 'NONE',  ( 1.719304012338199517, 0.000000000000000000, 0.000000000000000000 ) ) ;
#50155=CARTESIAN_POINT ( 'NONE',  ( 0.2648978790185593790, -0.1321385342563263510, 12.24533305150758089 ) ) ;
#50158=CARTESIAN_POINT ( 'NONE',  ( 2.241449424704146320, -7.507583637787357489, 1.386092121067182159 ) ) ;
#50174=ORIENTED_EDGE ( 'NONE', *, *, #57846, .F. ) ;
#50175=CARTESIAN_POINT ( 'NONE',  ( 2.665405856346786173, 0.5773576323839043622, -9.549966053095394258 ) ) ;
#50176=CARTESIAN_POINT ( 'NONE',  ( 2.241317068080780128, -3.737686401540277537, 6.656851426547345518 ) ) ;
#50182=ADVANCED_FACE ( 'NONE', ( #17519 ), #1569, .F. ) ;
#50208=CARTESIAN_POINT ( 'NONE',  ( 0.3053067050349180800, -12.03105545708855395, -2.355726819985549891 ) ) ;
#50211=CARTESIAN_POINT ( 'NONE',  ( 0.4613984246114871679, -2.415907815801322300, -12.07219521825822817 ) ) ;
#50224=ORIENTED_EDGE ( 'NONE', *, *, #21930, .F. ) ;
#50227=CARTESIAN_POINT ( 'NONE',  ( 0.3401186441510247183, 11.61600526280576595, -3.955862996551386512 ) ) ;
#50231=VECTOR ( 'NONE', #19200, 1000.000000000000114 ) ;
#50245=CARTESIAN_POINT ( 'NONE',  ( 5.530133899448235191, 0.01437126147332072092, 0.006998616117864119544 ) ) ;
#50247=CARTESIAN_POINT ( 'NONE',  ( 0.3218525148189836371, 3.964374483810649163, 11.60666749448225232 ) ) ;
#50248=CARTESIAN_POINT ( 'NONE',  ( 2.263328370261521894, -6.687792802426766769, -3.697218830764027686 ) ) ;
#50251=CARTESIAN_POINT ( 'NONE',  ( 1.547277799337855475, 6.911346840319977147, 10.62321481610070784 ) ) ;
#50253=CARTESIAN_POINT ( 'NONE',  ( 0.3006302518452059758, 10.72687985734942373, 5.932248915294198177 ) ) ;
#50260=CARTESIAN_POINT ( 'NONE',  ( 2.257661810676424796, -4.806737555285489627, 5.938215228162603054 ) ) ;
#50263=CARTESIAN_POINT ( 'NONE',  ( 0.4626703367444975346, 1.858541096401209902, 12.17089897506927620 ) ) ;
#50265=CIRCLE ( 'NONE', #44928, 7.938172270156617749 ) ;
#50270=CARTESIAN_POINT ( 'NONE',  ( 2.257661810676416803, -5.938215228162571968, -4.806737555285515384 ) ) ;
#50275=VECTOR ( 'NONE', #14411, 1000.000000000000227 ) ;
#50276=B_SPLINE_CURVE_WITH_KNOTS ( 'NONE', 3,
 ( #41094, #20169, #25825, #35112, #4573, #25482, #56066, #36095, #14504, #24841, #9861, #15500, #30781, #10847, #5893, #30151 ),
 .UNSPECIFIED., .F., .F.,
 ( 4, 3, 3, 3, 3, 4 ),
 ( 0.000000000000000000, 0.0002999043160757426532, 0.0005998071753051172636, 0.0008997092107374794973, 0.001204458948196454778, 0.001510329163478115952 ),
 .UNSPECIFIED. ) ;
#50282=CARTESIAN_POINT ( 'NONE',  ( 5.516018279890452902, -0.0009545156522404840260, 0.006707902355168859562 ) ) ;
#50283=CARTESIAN_POINT ( 'NONE',  ( 2.994568964204212147, -7.537093683963806967, 2.317954327151198868 ) ) ;
#50286=FACE_OUTER_BOUND ( 'NONE', #36206, .T. ) ;
#50292=CONICAL_SURFACE ( 'NONE', #1405, 7.938172270156617749, 1.280189991382167047 ) ;
#50293=CARTESIAN_POINT ( 'NONE',  ( 2.524535260912702306, 3.671333852642910678, -6.801151891677163164 ) ) ;
#50297=CARTESIAN_POINT ( 'NONE',  ( 3.092491956585575963, -2.283527081234287603, 7.581757403488253111 ) ) ;
#50317=CARTESIAN_POINT ( 'NONE',  ( 2.247112776671469359, 5.774169979601987635, -4.997244136394421332 ) ) ;
#50318=CARTESIAN_POINT ( 'NONE',  ( -14.47334165536099881, 5.400000000000000355, 1.000000000000000000 ) ) ;
#50322=CARTESIAN_POINT ( 'NONE',  ( 2.406456491627198879, 10.00134798414537229, 2.970787154400166941 ) ) ;
#50330=CARTESIAN_POINT ( 'NONE',  ( 0.3109076770649021881, 8.060731492642796425, 9.239379580302124140 ) ) ;
#50334=B_SPLINE_CURVE_WITH_KNOTS ( 'NONE', 3,
 ( #59096, #59400, #33788, #54089, #53774, #19162, #55059, #64376, #45096, #9489, #9175, #44748, #54755 ),
 .UNSPECIFIED., .F., .F.,
 ( 4, 3, 3, 3, 4 ),
 ( 2.168404344971008868E-18, 6.607593386745438881E-05, 0.0001321518677373501841, 0.0001982171734706190437, 0.0002642860854759493676 ),
 .UNSPECIFIED. ) ;
#50344=CARTESIAN_POINT ( 'NONE',  ( 1.109979610369347114, 12.24510427445464522, 2.646302643131894783 ) ) ;
#50345=ORIENTED_EDGE ( 'NONE', *, *, #55307, .T. ) ;
#50350=CIRCLE ( 'NONE', #3662, 12.73084802173761787 ) ;
#50354=CARTESIAN_POINT ( 'NONE',  ( 2.242819959140646358, 6.662619100654793236, -3.728423299584912254 ) ) ;
#50360=CARTESIAN_POINT ( 'NONE',  ( 5.516018279890452902, 0.0002248006052448508899, 0.006771744149385265123 ) ) ;
#50361=ORIENTED_EDGE ( 'NONE', *, *, #12758, .F. ) ;
#50362=CARTESIAN_POINT ( 'NONE',  ( 2.288423627607478306, 0.1612945702821758642, 7.648392725410191773 ) ) ;
#50363=CARTESIAN_POINT ( 'NONE',  ( 0.3537226245948360548, -12.13174752084887587, 1.874138792912971807 ) ) ;
#50365=VERTEX_POINT ( 'NONE', #49103 ) ;
#50372=ORIENTED_EDGE ( 'NONE', *, *, #10327, .F. ) ;
#50383=FACE_OUTER_BOUND ( 'NONE', #25488, .T. ) ;
#50385=CARTESIAN_POINT ( 'NONE',  ( 0.2646305136544065406, -11.55263159009955842, -4.064188116014664232 ) ) ;
#50392=CARTESIAN_POINT ( 'NONE',  ( 1.719304012338249921, 10.22720798541395837, 7.581471372740089976 ) ) ;
#50393=EDGE_CURVE ( 'NONE', #22233, #17330, #18446, .T. ) ;
#50394=CARTESIAN_POINT ( 'NONE',  ( 2.899286259009685285, 7.788326766693364434, -1.011320371384261341 ) ) ;
#50396=CARTESIAN_POINT ( 'NONE',  ( 2.266490820341525048, 5.947069344278602898, 4.800466063946337236 ) ) ;
#50398=ORIENTED_EDGE ( 'NONE', *, *, #3739, .F. ) ;
#50404=CARTESIAN_POINT ( 'NONE',  ( 0.3164563675027661227, 10.49799587805939183, -6.338687639235927485 ) ) ;
#50411=EDGE_LOOP ( 'NONE', ( #61822, #41327, #45865, #42251 ) ) ;
#50415=CARTESIAN_POINT ( 'NONE',  ( 2.244591118396555451, 7.500068934084588967, -1.431619869711765469 ) ) ;
#50418=LINE ( 'NONE', #60708, #10920 ) ;
#50421=DIRECTION ( 'NONE',  ( 0.000000000000000000, 0.000000000000000000, 1.000000000000000000 ) ) ;
#50422=CARTESIAN_POINT ( 'NONE',  ( 0.3665391374699465965, -12.13918562134717760, -1.872534962004925196 ) ) ;
#50429=EDGE_CURVE ( 'NONE', #62374, #17087, #11230, .T. ) ;
#50433=CARTESIAN_POINT ( 'NONE',  ( 2.241506898688419458, 7.634383346098567280, -0.03933068055393580675 ) ) ;
#50434=FACE_OUTER_BOUND ( 'NONE', #15764, .T. ) ;
#50438=B_SPLINE_CURVE_WITH_KNOTS ( 'NONE', 3,
 ( #21856, #52105, #12185, #7190, #52764, #62084, #594, #46452, #21175, #16537, #11524, #15844, #6561, #22160, #62713, #26829 ),
 .UNSPECIFIED., .F., .F.,
 ( 4, 3, 3, 3, 3, 4 ),
 ( 0.000000000000000000, 0.0002176109881720253523, 0.0004352086762394627266, 0.0006528017811446922784, 0.0007615147961451759632, 0.0009453342004947127772 ),
 .UNSPECIFIED. ) ;
#50441=CARTESIAN_POINT ( 'NONE',  ( 0.3675815128205894289, 12.27743992903066150, 0.2638082659428850896 ) ) ;
#50446=CARTESIAN_POINT ( 'NONE',  ( 5.514624014163232779, -0.003668383633201386610, 0.001921576324372439642 ) ) ;
#50455=CARTESIAN_POINT ( 'NONE',  ( 2.257661810674664871, 1.193649218122989852, -7.546014018370192034 ) ) ;
#50462=CARTESIAN_POINT ( 'NONE',  ( 0.2706063244538003398, 11.44820198696415936, 4.353289770698253847 ) ) ;
#50473=CARTESIAN_POINT ( 'NONE',  ( 2.931247277082682068, 0.3703309885897901887, -7.855653518374113631 ) ) ;
#50475=CARTESIAN_POINT ( 'NONE',  ( 5.514970785353741078, 0.001897634820904481583, -0.004324946436530190987 ) ) ;
#50479=CARTESIAN_POINT ( 'NONE',  ( 2.259025283528087513, 7.131631878998428320, -2.741148848567693808 ) ) ;
#50485=CARTESIAN_POINT ( 'NONE',  ( 2.827825597296801607, -2.100863646776117033, 8.776379025186180627 ) ) ;
#50487=CARTESIAN_POINT ( 'NONE',  ( 2.899286259009691502, 4.231523595108580338, -6.616268644969650836 ) ) ;
#50497=( BOUNDED_SURFACE ( )  B_SPLINE_SURFACE ( 3, 1, ( 
 ( #61764, #35814 ),
 ( #65748, #46802 ),
 ( #51157, #25881 ),
 ( #46474, #930 ) ),
 .UNSPECIFIED., .F., .F., .F. ) 
 B_SPLINE_SURFACE_WITH_KNOTS ( ( 4, 4 ),
 ( 2, 2 ),
 ( 0.000000000000000000, 1.000000000000000000 ),
 ( 0.000000000000000000, 1.000000000000000000 ),
 .UNSPECIFIED. ) 
 GEOMETRIC_REPRESENTATION_ITEM ( )  RATIONAL_B_SPLINE_SURFACE ( (
 ( 1.000000000000000000, 1.000000000000000000),
 ( 0.6933888150995267674, 0.9895912004443193632),
 ( 0.6933888150995267674, 0.9895912004443193632),
 ( 1.000000000000000000, 1.000000000000000000) ) ) 
 REPRESENTATION_ITEM ( '' )  SURFACE ( )  );
#50502=CARTESIAN_POINT ( 'NONE',  ( 0.2650492433740064824, -12.04046084639674596, 2.234874822562856966 ) ) ;
#50506=CARTESIAN_POINT ( 'NONE',  ( 2.259025283528085737, -3.701170455111014501, 6.683966451873017967 ) ) ;
#50519=CARTESIAN_POINT ( 'NONE',  ( 0.2648978790185619880, 11.46165506714233828, -4.312320170909121231 ) ) ;
#50520=CARTESIAN_POINT ( 'NONE',  ( 0.3675815128205894289, 6.367184624550164429, 10.50067073900654080 ) ) ;
#50527=CARTESIAN_POINT ( 'NONE',  ( 2.242819959140643693, -6.560218843829757951, -3.905785747113998063 ) ) ;
#50528=CARTESIAN_POINT ( 'NONE',  ( 5.516018279890452902, -0.005752102158673865970, 0.003580555109620777322 ) ) ;
#50533=B_SPLINE_CURVE_WITH_KNOTS ( 'NONE', 3,
 ( #21384, #57295, #37663, #31999, #32334, #11399, #41661, #52322, #2434, #42621, #21733, #36675, #52953, #36991, #57961, #11717, #6762, #42971, #31672 ),
 .UNSPECIFIED., .F., .F.,
 ( 4, 3, 3, 3, 3, 3, 4 ),
 ( 7.884170296961029399E-18, 4.457896483014795814E-05, 6.639290541542046452E-05, 8.820687556478797845E-05, 0.0001100173248778924787, 0.0001545671401658121294, 0.0001830328308068605012 ),
 .UNSPECIFIED. ) ;
#50534=CARTESIAN_POINT ( 'NONE',  ( 1.719304012339893051, -12.70777170743897422, -0.7661785589590540679 ) ) ;
#50539=CARTESIAN_POINT ( 'NONE',  ( 1.459561108994059442, -2.815016945601032106, -12.32692860927485334 ) ) ;
#50548=CARTESIAN_POINT ( 'NONE',  ( 2.969415267404470260, 7.260393470501825597, -3.055358878717542748 ) ) ;
#50551=CARTESIAN_POINT ( 'NONE',  ( 2.903928887688318916, 2.496183838365873431, -8.407112942776702624 ) ) ;
#50556=ORIENTED_EDGE ( 'NONE', *, *, #25110, .F. ) ;
#50559=CARTESIAN_POINT ( 'NONE',  ( 2.717984159219029472, -5.783767685176845141, 5.223388265379668383 ) ) ;
#50568=CARTESIAN_POINT ( 'NONE',  ( 2.247206125382658293, -2.502718378779159814, -7.214589497757414094 ) ) ;
#50570=ORIENTED_EDGE ( 'NONE', *, *, #17127, .F. ) ;
#50574=ORIENTED_EDGE ( 'NONE', *, *, #24260, .F. ) ;
#50580=CARTESIAN_POINT ( 'NONE',  ( 1.633930747250945670, 6.963441708413322218, 10.62371422070954274 ) ) ;
#50586=CARTESIAN_POINT ( 'NONE',  ( 2.241451721903216399, 7.507681056655377105, 1.385577012535781138 ) ) ;
#50587=ORIENTED_EDGE ( 'NONE', *, *, #28819, .F. ) ;
#50589=CARTESIAN_POINT ( 'NONE',  ( 0.9232167919969084258, 5.871274944231854143, -10.99620217063209893 ) ) ;
#50591=CARTESIAN_POINT ( 'NONE',  ( 2.994568964204204153, 3.591541975631971528, 7.020079750321906786 ) ) ;
#50597=CARTESIAN_POINT ( 'NONE',  ( 2.258463476536644698, 0.1358786215989210844, -7.638896687393369689 ) ) ;
#50606=CARTESIAN_POINT ( 'NONE',  ( 2.241352910868909643, 5.794346703933845433, 4.970878533273779709 ) ) ;
#50623=ORIENTED_EDGE ( 'NONE', *, *, #64261, .F. ) ;
#50638=CARTESIAN_POINT ( 'NONE',  ( 0.2956976708475448357, -3.984495122852500959, -11.59055635407405482 ) ) ;
#50649=CARTESIAN_POINT ( 'NONE',  ( 0.2958664285830411300, 8.045892866065361915, 9.245659426743914722 ) ) ;
#50653=DIRECTION ( 'NONE',  ( 1.000000000000000000, -0.000000000000000000, -0.000000000000000000 ) ) ;
#50655=CIRCLE ( 'NONE', #14533, 7.938172270156617749 ) ;
#50658=CARTESIAN_POINT ( 'NONE',  ( 2.844750968615211484, 0.3326424433129591685, 7.828506085988378160 ) ) ;
#50660=CARTESIAN_POINT ( 'NONE',  ( 1.719304012338239485, 12.38166659046522788, 2.961219984258211202 ) ) ;
#50662=CARTESIAN_POINT ( 'NONE',  ( 0.3057689695767506488, -4.409323295154131905, -11.43929056598610217 ) ) ;
#50663=ADVANCED_FACE ( 'NONE', ( #53006 ), #3726, .F. ) ;
#50674=DIRECTION ( 'NONE',  ( -0.3939253465568944290, -0.9190910618577645685, 0.009718094113430031031 ) ) ;
#50681=DIRECTION ( 'NONE',  ( 0.000000000000000000, 1.000000000000000000, 0.000000000000000000 ) ) ;
#50693=DIRECTION ( 'NONE',  ( -1.000000000000000000, -0.000000000000000000, -0.000000000000000000 ) ) ;
#50698=CARTESIAN_POINT ( 'NONE',  ( 0.2652384770603659070, -12.04846497255941173, -2.191555293694098516 ) ) ;
#50701=ORIENTED_EDGE ( 'NONE', *, *, #37692, .T. ) ;
#50705=CARTESIAN_POINT ( 'NONE',  ( 0.2833330754217478487, 9.514385791198202824, -7.719627479384551627 ) ) ;
#50709=DIRECTION ( 'NONE',  ( 0.000000000000000000, 0.000000000000000000, -1.000000000000000000 ) ) ;
#50711=CARTESIAN_POINT ( 'NONE',  ( 5.516018279890452902, 0.001397286410094317416, -0.006629829924290979969 ) ) ;
#50712=ORIENTED_EDGE ( 'NONE', *, *, #2939, .F. ) ;
#50713=EDGE_CURVE ( 'NONE', #38649, #26297, #17609, .T. ) ;
#50716=ORIENTED_EDGE ( 'NONE', *, *, #44767, .T. ) ;
#50721=CARTESIAN_POINT ( 'NONE',  ( 0.5547464869798217624, -12.09851097165511291, 2.442933571354931388 ) ) ;
#50729=DIRECTION ( 'NONE',  ( -1.000000000000000000, -0.000000000000000000, -0.000000000000000000 ) ) ;
#50730=CARTESIAN_POINT ( 'NONE',  ( 2.269879328256729778, 7.500604381673476873, -1.473193649116055992 ) ) ;
#50732=DIRECTION ( 'NONE',  ( 0.3865475372811021937, -0.3335716741247308215, 0.8598319252293086246 ) ) ;
#50737=CARTESIAN_POINT ( 'NONE',  ( 0.2646305136544065406, -9.296005949277169833, -7.972778379581646924 ) ) ;
#50738=CARTESIAN_POINT ( 'NONE',  ( 1.287602823388301010, 2.727479899221430859, -12.28793447239746506 ) ) ;
#50741=CARTESIAN_POINT ( 'NONE',  ( 3.152665057734121756, -0.4801242025592447060, 7.923639299008720549 ) ) ;
#50745=CARTESIAN_POINT ( 'NONE',  ( 5.514624014163232779, 0.003830004412313247914, 0.001574979445068904913 ) ) ;
#50746=CARTESIAN_POINT ( 'NONE',  ( 3.152665057736111720, -7.281573230473792790, 3.161213418915395312 ) ) ;
#50748=CARTESIAN_POINT ( 'NONE',  ( 2.241536586108912488, -3.822683724643419545, -6.608496983003830927 ) ) ;
#50751=EDGE_LOOP ( 'NONE', ( #53606, #21922, #3772, #32117 ) ) ;
#50753=CARTESIAN_POINT ( 'NONE',  ( 0.2646305136544065406, -12.24595685781654275, -0.1321451301299126913 ) ) ;
#50770=ORIENTED_EDGE ( 'NONE', *, *, #5097, .T. ) ;
#50771=CARTESIAN_POINT ( 'NONE',  ( 2.242819959140645913, -4.985618132689713988, 5.782321801516522086 ) ) ;
#50773=AXIS2_PLACEMENT_3D ( 'NONE', #30357, #50653, #90 ) ;
#50777=CARTESIAN_POINT ( 'NONE',  ( 5.536195898058073439, -0.006344799443923986905, 0.005656495196971059354 ) ) ;
#50786=CARTESIAN_POINT ( 'NONE',  ( 0.2646305136544065406, 2.256625640822316647, 12.03696649559615217 ) ) ;
#50794=ORIENTED_EDGE ( 'NONE', *, *, #30635, .T. ) ;
#50795=CARTESIAN_POINT ( 'NONE',  ( 2.258463476536646031, -1.460294809170993968, 7.499249607179734767 ) ) ;
#50811=ORIENTED_EDGE ( 'NONE', *, *, #38722, .T. ) ;
#50812=EDGE_CURVE ( 'NONE', #59321, #35137, #46915, .T. ) ;
#50815=CARTESIAN_POINT ( 'NONE',  ( 5.515188684475870851, -0.004893136156457983908, 0.002166413411657847846 ) ) ;
#50817=CARTESIAN_POINT ( 'NONE',  ( 2.430348790457138364, -7.611893186157356439, -1.144258029164478385 ) ) ;
#50819=CARTESIAN_POINT ( 'NONE',  ( 2.266490820343019408, 2.476945027124536125, -7.230273269342557541 ) ) ;
#50823=CARTESIAN_POINT ( 'NONE',  ( 0.9296196016833884190, -12.34355205587689319, 1.754499435240041150 ) ) ;
#50826=B_SPLINE_CURVE_WITH_KNOTS ( 'NONE', 3,
 ( #5611, #40161, #31194, #20562, #35168, #35513, #30515, #50819, #51499, #60453, #14877, #56116, #9919, #614, #41144, #61426, #30206, #20220, #5946 ),
 .UNSPECIFIED., .F., .F.,
 ( 4, 3, 3, 3, 3, 3, 4 ),
 ( 6.829613154537258970E-18, 2.825908398850651652E-05, 4.208813692510337049E-05, 5.591713746977225327E-05, 6.279584083268735550E-05, 9.105792820348497226E-05, 0.0001153131102488632871 ),
 .UNSPECIFIED. ) ;
#50827=EDGE_CURVE ( 'NONE', #42070, #49910, #31812, .T. ) ;
#50829=CARTESIAN_POINT ( 'NONE',  ( 2.305787727787084407, 2.774453000917148415, 7.135468203929992370 ) ) ;
#50834=CARTESIAN_POINT ( 'NONE',  ( 0.3654063281920733042, -0.2633658439602484802, -12.27672420655578911 ) ) ;
#50837=CARTESIAN_POINT ( 'NONE',  ( 0.3160775863651118511, -11.60348481172938406, 3.967735865794311145 ) ) ;
#50847=CARTESIAN_POINT ( 'NONE',  ( 0.8375941296786644230, 9.275620596396400686, 8.285008510334364473 ) ) ;
#50849=CARTESIAN_POINT ( 'NONE',  ( 3.152665057734127974, -4.377619405892426485, 6.622010822086644488 ) ) ;
#50850=CARTESIAN_POINT ( 'NONE',  ( 0.3040950598368144520, -7.687624643091368171, -9.552450779732186703 ) ) ;
#50852=ORIENTED_EDGE ( 'NONE', *, *, #14547, .F. ) ;
#50853=CARTESIAN_POINT ( 'NONE',  ( 1.375507693218758432, -11.20969178069603700, 5.789143338282145557 ) ) ;
#50864=CARTESIAN_POINT ( 'NONE',  ( 0.000000000000000000, 0.000000000000000000, 0.000000000000000000 ) ) ;
#50875=ORIENTED_EDGE ( 'NONE', *, *, #59857, .T. ) ;
#50876=CARTESIAN_POINT ( 'NONE',  ( 3.031336079628848879, -5.773872239512904514, 5.388626255826518552 ) ) ;
#50879=CARTESIAN_POINT ( 'NONE',  ( 1.719304012338439325, 7.017415949612858306, 10.62216384465677521 ) ) ;
#50897=ADVANCED_FACE ( 'NONE', ( #30359 ), #44438, .F. ) ;
#50901=CARTESIAN_POINT ( 'NONE',  ( 2.305787727787084407, 3.971363876083963351, 6.545285700970541853 ) ) ;
#50906=CARTESIAN_POINT ( 'NONE',  ( 1.014383007554943594, 5.859361736620487981, -11.03701226956410508 ) ) ;
#50913=CARTESIAN_POINT ( 'NONE',  ( 0.3610902822527198297, 12.27530799859938959, -0.2623004149195046208 ) ) ;
#50916=EDGE_CURVE ( 'NONE', #33895, #23378, #34188, .T. ) ;
#50917=CARTESIAN_POINT ( 'NONE',  ( 0.2651627923886311078, -2.213220384814353903, 12.04449855907067501 ) ) ;
#50919=CARTESIAN_POINT ( 'NONE',  ( 1.937114397841935398, 7.538912286488483439, -10.38782037574609163 ) ) ;
#50929=CARTESIAN_POINT ( 'NONE',  ( 2.241537034860904942, 3.813147095850985213, 6.614004440763060266 ) ) ;
#50935=CARTESIAN_POINT ( 'NONE',  ( 2.941278708680199916, -5.721889327162137384, -2.226055275041848525 ) ) ;
#50939=CARTESIAN_POINT ( 'NONE',  ( 3.152665057735716037, -2.258875078500806044, 7.609997527621833235 ) ) ;
#50940=VERTEX_POINT ( 'NONE', #53529 ) ;
#50941=CARTESIAN_POINT ( 'NONE',  ( 2.241352910868908754, 4.843133558968205854, -5.901537464758406237 ) ) ;
#50955=EDGE_CURVE ( 'NONE', #21432, #31007, #53279, .T. ) ;
#50957=CARTESIAN_POINT ( 'NONE',  ( 2.257661810676422576, 5.764872664104583322, -5.013319178751116212 ) ) ;
#50967=CARTESIAN_POINT ( 'NONE',  ( 3.152665057734040488, 0.000000000000000000, 0.000000000000000000 ) ) ;
#50970=CARTESIAN_POINT ( 'NONE',  ( 0.3610902822527199407, 8.091349661862622611, 9.234828023175118972 ) ) ;
#50975=CARTESIAN_POINT ( 'NONE',  ( 2.257661810674664871, 7.224098098129182688, 2.485866587323505961 ) ) ;
#50980=CARTESIAN_POINT ( 'NONE',  ( 2.507146904658095643, -6.052884339496452881, 4.796593924427959621 ) ) ;
#50983=ORIENTED_EDGE ( 'NONE', *, *, #59989, .F. ) ;
#50984=CARTESIAN_POINT ( 'NONE',  ( 0.3632410797595253538, -4.445654054452453430, -11.44577450250091566 ) ) ;
#50987=DIRECTION ( 'NONE',  ( -1.000000000000000000, -0.000000000000000000, -0.000000000000000000 ) ) ;
#50990=CARTESIAN_POINT ( 'NONE',  ( 2.241352910868908310, 6.652881166698564108, -3.744764251556923274 ) ) ;
#50995=B_SPLINE_CURVE_WITH_KNOTS ( 'NONE', 3,
 ( #45982, #41292, #49981, #30354, #15688, #35967, #9389, #14699, #20371, #40311, #50649, #55286, #55949, #50330, #5092, #44991, #5761, #30658, #50970, #5420, #65577, #25356 ),
 .UNSPECIFIED., .F., .F.,
 ( 4, 3, 3, 3, 3, 3, 3, 4 ),
 ( 1.626303258728256651E-19, 4.449119708436531195E-05, 6.626296329540292784E-05, 8.803456484962480090E-05, 0.0001098060367612777635, 0.0001315774408628478192, 0.0001760698110411119260, 0.0001829697163287825890 ),
 .UNSPECIFIED. ) ;
#51006=CARTESIAN_POINT ( 'NONE',  ( 5.515188684475870851, -0.005194992164431762316, 0.001283816547385177240 ) ) ;
#51015=CARTESIAN_POINT ( 'NONE',  ( 2.889800649504073782, -3.118861721612529170, -5.267262008933701445 ) ) ;
#51021=CARTESIAN_POINT ( 'NONE',  ( 5.515188684475870851, 0.0003622115669623291682, -0.005339000964281804575 ) ) ;
#51026=CARTESIAN_POINT ( 'NONE',  ( 5.514970785353741078, 0.002796696073589870733, 0.003805873180274323229 ) ) ;
#51029=CARTESIAN_POINT ( 'NONE',  ( 0.3537226245948408843, 9.569332148897569112, -7.688925565304919552 ) ) ;
#51036=CARTESIAN_POINT ( 'NONE',  ( 1.719304012340749033, -5.066286238787660601, -11.67935079956571087 ) ) ;
#51045=ORIENTED_EDGE ( 'NONE', *, *, #4620, .T. ) ;
#51050=CARTESIAN_POINT ( 'NONE',  ( 1.194176325881333600, -12.26540585042610410, 2.684784923266246626 ) ) ;
#51061=CARTESIAN_POINT ( 'NONE',  ( 2.280717697723836146, 7.502592193582066749, -1.481796453660239044 ) ) ;
#51069=CARTESIAN_POINT ( 'NONE',  ( 3.092491956585259327, 6.343509225034840604, 4.738927301402335424 ) ) ;
#51072=CARTESIAN_POINT ( 'NONE',  ( 0.2652384770603641306, 10.57229757085623056, 6.180206054297643803 ) ) ;
#51084=CARTESIAN_POINT ( 'NONE',  ( 2.241506898688418126, -3.851253041557060719, -6.591904579673272480 ) ) ;
#51086=CARTESIAN_POINT ( 'NONE',  ( 2.253265082352434501, 1.199885753716626091, 7.543541742286975271 ) ) ;
#51088=CARTESIAN_POINT ( 'NONE',  ( 2.406456491625667660, -7.573451137023450741, 7.176027849161565442 ) ) ;
#51093=CYLINDRICAL_SURFACE ( 'NONE', #42634, 6.000000000000000888 ) ;
#51099=CIRCLE ( 'NONE', #19245, 7.938172270156617749 ) ;
#51101=CARTESIAN_POINT ( 'NONE',  ( 0.2650492594609232255, -7.955687020697113532, 9.309909082761121724 ) ) ;
#51116=CARTESIAN_POINT ( 'NONE',  ( 5.515188684475870851, 0.005194992164431771857, -0.001283816547385141027 ) ) ;
#51119=VERTEX_POINT ( 'NONE', #35805 ) ;
#51127=DIRECTION ( 'NONE',  ( 0.3939253465568943180, 0.4679616473074897920, -0.7910971609033186080 ) ) ;
#51131=EDGE_CURVE ( 'NONE', #18651, #8885, #56515, .T. ) ;
#51136=CARTESIAN_POINT ( 'NONE',  ( 0.4613984246114877785, 12.30830943644279962, -0.2828900474740810300 ) ) ;
#51139=CARTESIAN_POINT ( 'NONE',  ( 5.520433897694421610, 0.009283255140285620599, -0.01186170453199863681 ) ) ;
#51140=CARTESIAN_POINT ( 'NONE',  ( 5.515539859299206427, 0.004037661319611307587, 0.004509673239148500115 ) ) ;
#51142=CARTESIAN_POINT ( 'NONE',  ( 0.9232058338315048962, 7.723624854284715902, 9.791640253608173694 ) ) ;
#51144=B_SPLINE_CURVE_WITH_KNOTS ( 'NONE', 3,
 ( #62988, #17450, #37725, #12430, #48038, #2500, #22774, #19980, #28398, #23089, #65206, #50260, #30291, #7801, #43352, #3150, #13426, #4723, #63626 ),
 .UNSPECIFIED., .F., .F.,
 ( 4, 3, 3, 3, 3, 3, 4 ),
 ( 6.269651592512720910E-18, 2.825908398830553593E-05, 4.208813692483162199E-05, 5.591713746942991644E-05, 6.279584083230896894E-05, 9.105792820295216820E-05, 0.0001153131102488888472 ),
 .UNSPECIFIED. ) ;
#51152=VERTEX_POINT ( 'NONE', #19235 ) ;
#51153=CARTESIAN_POINT ( 'NONE',  ( 0.2638984909335716500, 12.24571285024409129, 0.1991813963114414388 ) ) ;
#51154=FACE_OUTER_BOUND ( 'NONE', #63188, .T. ) ;
#51156=DIRECTION ( 'NONE',  ( 0.000000000000000000, 0.000000000000000000, 1.000000000000000000 ) ) ;
#51157=CARTESIAN_POINT ( 'NONE',  ( 5.530133899448235191, 0.01324661008606589467, -0.008946569461392295600 ) ) ;
#51162=CARTESIAN_POINT ( 'NONE',  ( 3.152665057736256493, -0.9030954876717440793, 7.886634106564762270 ) ) ;
#51173=CARTESIAN_POINT ( 'NONE',  ( 0.2650492433740075926, 12.24562113162318688, -0.1101179680249403520 ) ) ;
#51180=CIRCLE ( 'NONE', #56478, 4.000000000000000000 ) ;
#51185=CARTESIAN_POINT ( 'NONE',  ( 2.241352910868909643, -6.569501556381414531, -3.889181972941518683 ) ) ;
#51188=CARTESIAN_POINT ( 'NONE',  ( 1.948354844647008477, -10.97658859989599378, 4.761851831283274272 ) ) ;
#51192=CARTESIAN_POINT ( 'NONE',  ( 2.305787727787084407, -2.461236246751023593, -7.249469779319933416 ) ) ;
#51196=CARTESIAN_POINT ( 'NONE',  ( 0.3278977287071219715, 10.49733767381182759, 6.347150352417348707 ) ) ;
#51200=B_SPLINE_CURVE_WITH_KNOTS ( 'NONE', 3,
 ( #52748, #5652, #22479, #27453, #5307, #25578, #45873 ),
 .UNSPECIFIED., .F., .F.,
 ( 4, 3, 4 ),
 ( 0.000000000000000000, 0.001700533616330527362, 0.005002426799371310386 ),
 .UNSPECIFIED. ) ;
#51206=DIRECTION ( 'NONE',  ( -1.000000000000000000, -0.000000000000000000, -0.000000000000000000 ) ) ;
#51207=CARTESIAN_POINT ( 'NONE',  ( 2.556980015513900639, 2.862731173723978451, 7.190718924764532005 ) ) ;
#51212=CARTESIAN_POINT ( 'NONE',  ( 2.573738926104374158, -6.822065037112458263, 3.667129335223178632 ) ) ;
#51215=CARTESIAN_POINT ( 'NONE',  ( 1.372161826076674362, -12.04315837901297925, -3.755740169579745658 ) ) ;
#51219=VERTEX_POINT ( 'NONE', #40482 ) ;
#51220=CARTESIAN_POINT ( 'NONE',  ( 3.092491956585110113, -5.768471164323004885, 5.424230976134056803 ) ) ;
#51223=CARTESIAN_POINT ( 'NONE',  ( 2.241352910868908754, 2.689314586382447914, -7.145045428366549878 ) ) ;
#51226=ORIENTED_EDGE ( 'NONE', *, *, #37285, .T. ) ;
#51235=CARTESIAN_POINT ( 'NONE',  ( 2.963017218115624019, -7.865565884553436860, -0.3847317984106120581 ) ) ;
#51244=CARTESIAN_POINT ( 'NONE',  ( 2.963017218115621354, 6.272673870919160954, -4.761166637500448218 ) ) ;
#51245=CARTESIAN_POINT ( 'NONE',  ( 2.717984159219280826, 4.139692542159186139, 6.602931111513647089 ) ) ;
#51251=CARTESIAN_POINT ( 'NONE',  ( 2.373367633546869637, 3.681545031436654458, 6.738274194514227489 ) ) ;
#51254=CARTESIAN_POINT ( 'NONE',  ( 0.2671309869109501078, 12.24572650704445032, -0.1620273132356114532 ) ) ;
#51257=CARTESIAN_POINT ( 'NONE',  ( 0.3665391374699465965, -11.44911061034389732, 4.447929964102806721 ) ) ;
#51258=CARTESIAN_POINT ( 'NONE',  ( 1.719304012338836563, -1.452142814150213734, 12.64775761152536759 ) ) ;
#51260=ADVANCED_FACE ( 'NONE', ( #15853 ), #18661, .F. ) ;
#51262=ORIENTED_EDGE ( 'NONE', *, *, #12088, .F. ) ;
#51268=B_SPLINE_CURVE_WITH_KNOTS ( 'NONE', 3,
 ( #58029, #12441, #47402, #47072, #2513, #17123, #26774, #37397, #1530, #32712, #57707, #47713, #21805, #22434, #53025, #42361 ),
 .UNSPECIFIED., .F., .F.,
 ( 4, 3, 3, 3, 3, 4 ),
 ( 2.788974592819220452E-15, 0.0002126834539179592873, 0.0004253519300366052653, 0.0006380165497223855980, 0.0007442707582427891952, 0.0009453531351420179241 ),
 .UNSPECIFIED. ) ;
#51278=ORIENTED_EDGE ( 'NONE', *, *, #39165, .T. ) ;
#51283=CARTESIAN_POINT ( 'NONE',  ( 2.251152103364163271, 4.812779263774475957, -5.930529991878751517 ) ) ;
#51286=CARTESIAN_POINT ( 'NONE',  ( 0.2638984909335720941, -10.50550771760524249, 6.295352574288949121 ) ) ;
#51307=CARTESIAN_POINT ( 'NONE',  ( 0.3278977287071205282, -4.427879319182963513, 11.44003061923229225 ) ) ;
#51312=CARTESIAN_POINT ( 'NONE',  ( 0.4613984246114876120, -12.30830943644279962, 0.2828900474739950432 ) ) ;
#51313=CARTESIAN_POINT ( 'NONE',  ( 1.198791140420743639, 11.96656299555157688, -3.806343609710548304 ) ) ;
#51321=CARTESIAN_POINT ( 'NONE',  ( 2.907497136249980407, 0.3592423305251248866, 7.848280798452631046 ) ) ;
#51334=CARTESIAN_POINT ( 'NONE',  ( 0.2653141617321005952, 2.169890202573355520, -12.05243138604823905 ) ) ;
#51338=EDGE_CURVE ( 'NONE', #24646, #54088, #32511, .T. ) ;
#51345=CARTESIAN_POINT ( 'NONE',  ( 1.719304012338210619, 10.62216384465585328, 7.017415949611872428 ) ) ;
#51361=CARTESIAN_POINT ( 'NONE',  ( 0.5572780756287500914, -11.49107179558554748, -4.507550621618535480 ) ) ;
#51365=LINE ( 'NONE', #16431, #21540 ) ;
#51367=CARTESIAN_POINT ( 'NONE',  ( 3.152665057736217413, -7.923639299008909731, 0.4801242025612903475 ) ) ;
#51371=EDGE_CURVE ( 'NONE', #14741, #16694, #38988, .T. ) ;
#51384=CARTESIAN_POINT ( 'NONE',  ( 0.3610902822527207734, -12.04327049858141763, 2.389900346488049721 ) ) ;
#51387=CARTESIAN_POINT ( 'NONE',  ( 0.3002738374340830352, 12.03040002643111706, 2.350339881554986743 ) ) ;
#51395=CARTESIAN_POINT ( 'NONE',  ( 1.633930747251797211, -10.62371422070957117, 6.963441708413805387 ) ) ;
#51408=CARTESIAN_POINT ( 'NONE',  ( 2.241352910868909643, 7.503490710578251566, -1.407733736974789762 ) ) ;
#51415=FACE_OUTER_BOUND ( 'NONE', #32145, .T. ) ;
#51419=CARTESIAN_POINT ( 'NONE',  ( 3.031336079629849412, 0.9593005538805465804, -7.839300734793278380 ) ) ;
#51424=CARTESIAN_POINT ( 'NONE',  ( 5.514970785353741078, 0.004324946436530305478, -0.001897634820904966005 ) ) ;
#51429=CARTESIAN_POINT ( 'NONE',  ( 0.2648978790185593790, -4.312320170909161199, -11.46165506714232762 ) ) ;
#51430=CARTESIAN_POINT ( 'NONE',  ( 2.262775599886258426, 1.187656132455270352, 7.548684916004837042 ) ) ;
#51435=EDGE_CURVE ( 'NONE', #9266, #14210, #29359, .T. ) ;
#51448=CARTESIAN_POINT ( 'NONE',  ( 2.241352910868908310, 2.532612177304540246, -7.202080440908716241 ) ) ;
#51449=CARTESIAN_POINT ( 'NONE',  ( 0.6473888112830248343, 0.3298838684458830772, 12.36914475328377883 ) ) ;
#51451=ADVANCED_FACE ( 'NONE', ( #13619 ), #64837, .F. ) ;
#51471=B_SPLINE_CURVE_WITH_KNOTS ( 'NONE', 3,
 ( #36706, #6454, #41693, #12083, #7098, #46363, #57003 ),
 .UNSPECIFIED., .F., .F.,
 ( 4, 3, 4 ),
 ( 0.000000000000000000, 0.001700533616330566176, 0.005002426799371234925 ),
 .UNSPECIFIED. ) ;
#51474=EDGE_CURVE ( 'NONE', #49268, #46959, #3320, .T. ) ;
#51477=DIRECTION ( 'NONE',  ( 0.3865475372811021382, -0.5778504531711042835, -0.7187975063895702954 ) ) ;
#51479=CARTESIAN_POINT ( 'NONE',  ( 2.259830038564999644, 7.499347412930722712, 1.462175769136871750 ) ) ;
#51481=CARTESIAN_POINT ( 'NONE',  ( 1.633930747250413207, 12.68212725188695877, -0.7186603069030271795 ) ) ;
#51489=CARTESIAN_POINT ( 'NONE',  ( 5.515539859299206427, 0.003193223631738807775, -0.005142293699651648287 ) ) ;
#51498=CARTESIAN_POINT ( 'NONE',  ( 0.3675815128205894289, -9.574637318041910206, -7.689697408877373519 ) ) ;
#51499=CARTESIAN_POINT ( 'NONE',  ( 2.263328370261319389, 2.479726736363932371, -7.228205514767005901 ) ) ;
#51500=ORIENTED_EDGE ( 'NONE', *, *, #51586, .F. ) ;
#51503=CARTESIAN_POINT ( 'NONE',  ( 2.969415267404973413, -0.9841783286029112121, 7.815364626284227789 ) ) ;
#51507=LINE ( 'NONE', #10567, #54207 ) ;
#51513=CARTESIAN_POINT ( 'NONE',  ( 1.948354844647012696, -11.63671644762473179, 2.783443994771382712 ) ) ;
#51519=CARTESIAN_POINT ( 'NONE',  ( 5.514970785353741078, 0.003262412238248714284, 0.003415090918276149530 ) ) ;
#51520=B_SPLINE_CURVE_WITH_KNOTS ( 'NONE', 3,
 ( #31313, #61895, #6061, #27618, #36286, #51615, #37271, #56592, #26319, #21679, #32282, #57914, #22657, #26645, #6376, #1721, #1057, #63202, #1399 ),
 .UNSPECIFIED., .F., .F.,
 ( 4, 3, 3, 3, 3, 3, 4 ),
 ( 8.396094104928349784E-18, 4.457896483014532217E-05, 6.639290541541883822E-05, 8.820687556478810042E-05, 0.0001100173248778926955, 0.0001545671401658162494, 0.0001830328308068598778 ),
 .UNSPECIFIED. ) ;
#51528=CARTESIAN_POINT ( 'NONE',  ( 1.634816307077890052, 11.34285134320936805, -5.718391684265558439 ) ) ;
#51535=EDGE_CURVE ( 'NONE', #23349, #33895, #10259, .T. ) ;
#51543=CARTESIAN_POINT ( 'NONE',  ( 5.516018279890452902, -0.005976902763918694010, -0.003191189039764501679 ) ) ;
#51544=CARTESIAN_POINT ( 'NONE',  ( 2.907497136250803749, 3.021847490615692688, 7.252103438786950740 ) ) ;
#51554=CARTESIAN_POINT ( 'NONE',  ( 0.2648978790185602672, 4.312320170909236694, 11.46165506714229565 ) ) ;
#51556=CARTESIAN_POINT ( 'NONE',  ( 0.6511581176954477357, 11.51117493088880650, 4.541862140119159008 ) ) ;
#51558=CARTESIAN_POINT ( 'NONE',  ( 2.705197763288548440, -1.076142490489816694, -7.714317563576067016 ) ) ;
#51560=ORIENTED_EDGE ( 'NONE', *, *, #32545, .F. ) ;
#51568=CARTESIAN_POINT ( 'NONE',  ( 3.047904605210430162, -7.891858004695963658, -0.4249306449416186959 ) ) ;
#51570=ORIENTED_EDGE ( 'NONE', *, *, #57846, .T. ) ;
#51573=CARTESIAN_POINT ( 'NONE',  ( 5.514970785353741078, -0.001117786416802588273, -0.004588761610585022875 ) ) ;
#51581=CARTESIAN_POINT ( 'NONE',  ( 1.719304012338834786, 2.961219984257995819, 12.38166659046419227 ) ) ;
#51585=CARTESIAN_POINT ( 'NONE',  ( 0.3341166715381295171, 12.26652061402056049, -0.2526177176100498634 ) ) ;
#51586=EDGE_CURVE ( 'NONE', #19660, #41809, #23010, .T. ) ;
#51594=CARTESIAN_POINT ( 'NONE',  ( 3.152665057736074417, -6.622010822085853121, 4.377619405894153992 ) ) ;
#51598=CARTESIAN_POINT ( 'NONE',  ( 0.3632410797595259644, -1.872837903657279535, 12.13515851238022947 ) ) ;
#51603=B_SPLINE_CURVE_WITH_KNOTS ( 'NONE', 3,
 ( #46701, #42340, #57683, #12418, #11766, #1158, #47377, #41712, #32689, #62006 ),
 .UNSPECIFIED., .F., .F.,
 ( 4, 3, 3, 4 ),
 ( 4.336808689942017736E-19, 6.607638129004468554E-05, 9.911389841680466693E-05, 0.0001667630577588625823 ),
 .UNSPECIFIED. ) ;
#51615=CARTESIAN_POINT ( 'NONE',  ( 0.3160775863651146267, 12.11619190710941396, -1.892533050396041361 ) ) ;
#51621=CARTESIAN_POINT ( 'NONE',  ( 0.2655924914740778187, -11.49267051747965596, -4.229867354073672203 ) ) ;
#51624=CARTESIAN_POINT ( 'NONE',  ( 2.241451721903215066, -6.641849090084981810, 3.764430789729956928 ) ) ;
#51627=CARTESIAN_POINT ( 'NONE',  ( 0.2651627923886328841, 4.105544202112549002, 11.53745192040743639 ) ) ;
#51635=ORIENTED_EDGE ( 'NONE', *, *, #26688, .F. ) ;
#51638=CARTESIAN_POINT ( 'NONE',  ( 0.2648978790185584908, -9.295532325666394868, -7.972372351883127095 ) ) ;
#51641=CARTESIAN_POINT ( 'NONE',  ( 2.242418902651535539, 7.207816731000297850, 2.517330194231067519 ) ) ;
#51648=ORIENTED_EDGE ( 'NONE', *, *, #1015, .F. ) ;
#51661=CARTESIAN_POINT ( 'NONE',  ( 1.014383007554942484, 4.688516792764612973, 11.58298623339616462 ) ) ;
#51662=CARTESIAN_POINT ( 'NONE',  ( 1.549075743846074271, -3.694639393663741167, -12.12370443967618172 ) ) ;
#51663=EDGE_CURVE ( 'NONE', #9187, #36108, #7086, .T. ) ;
#51676=CARTESIAN_POINT ( 'NONE',  ( 0.2801149460245174749, -5.954809120985783188, 10.70654700624300304 ) ) ;
#51683=LINE ( 'NONE', #64256, #18760 ) ;
#51691=ORIENTED_EDGE ( 'NONE', *, *, #39482, .F. ) ;
#51692=CARTESIAN_POINT ( 'NONE',  ( 2.241506898688419458, -2.574154135948738098, 7.187425579579794999 ) ) ;
#51693=ORIENTED_EDGE ( 'NONE', *, *, #47830, .F. ) ;
#51694=CARTESIAN_POINT ( 'NONE',  ( 5.514970785353741078, -0.004233694591582967161, -0.002093325033903798652 ) ) ;
#51696=ORIENTED_EDGE ( 'NONE', *, *, #11193, .T. ) ;
#51699=CARTESIAN_POINT ( 'NONE',  ( 2.241537034860905386, -4.903726641589485347, -5.851376807350193943 ) ) ;
#51705=CARTESIAN_POINT ( 'NONE',  ( 0.3675815128205894289, -12.04510820461660892, 2.391755495700564449 ) ) ;
#51714=CARTESIAN_POINT ( 'NONE',  ( 5.516018279890452902, 0.003191189039764439229, -0.005976902763918727837 ) ) ;
#51727=ADVANCED_FACE ( 'NONE', ( #64647 ), #11815, .F. ) ;
#51731=ORIENTED_EDGE ( 'NONE', *, *, #47413, .T. ) ;
#51738=CARTESIAN_POINT ( 'NONE',  ( 2.430348790457476760, -7.164221884688256381, 2.814990071338049571 ) ) ;
#51745=CARTESIAN_POINT ( 'NONE',  ( 2.177405672431178552, -8.129711416440740024, 7.702458780351658874 ) ) ;
#51749=CARTESIAN_POINT ( 'NONE',  ( 2.899286259009682620, 1.011320371384342831, 7.788326766693353775 ) ) ;
#51751=CARTESIAN_POINT ( 'NONE',  ( -14.47334165536100059, 0.000000000000000000, 0.000000000000000000 ) ) ;
#51753=CARTESIAN_POINT ( 'NONE',  ( 2.556980015513814486, -7.348538402679465342, -2.429125721802482207 ) ) ;
#51768=SURFACE_SIDE_STYLE ('',( #61717 ) ) ;
#51779=ORIENTED_EDGE ( 'NONE', *, *, #62032, .F. ) ;
#51782=CARTESIAN_POINT ( 'NONE',  ( 5.515539859299206427, -0.005991790098944305316, -0.0008592514567752725574 ) ) ;
#51784=CARTESIAN_POINT ( 'NONE',  ( 0.9232167919969107572, 12.34114433434357139, 1.756271097262108505 ) ) ;
#51792=CARTESIAN_POINT ( 'NONE',  ( 2.705197763288552881, 4.134294772210017399, -6.601241161176638172 ) ) ;
#51796=CARTESIAN_POINT ( 'NONE',  ( 5.530133899448235191, -0.01149180883054594197, 0.01111090067015119663 ) ) ;
#51798=CARTESIAN_POINT ( 'NONE',  ( 5.515188684475870851, 0.002166413411657351282, -0.004893136156457789619 ) ) ;
#51804=CARTESIAN_POINT ( 'NONE',  ( 2.241352910868908310, -2.532612177304491397, 7.202080440908734005 ) ) ;
#51806=CARTESIAN_POINT ( 'NONE',  ( 1.633930747252541504, -10.17701904908771127, -7.601388527387344496 ) ) ;
#51810=DIRECTION ( 'NONE',  ( 0.3939253465568943735, 0.8669868725995579783, -0.3052156353794294175 ) ) ;
#51812=CARTESIAN_POINT ( 'NONE',  ( 1.634816307076136122, -12.61459884932949294, 1.494046826342531054 ) ) ;
#51815=CARTESIAN_POINT ( 'NONE',  ( 0.3675815128205912052, 9.235491948680007113, 8.093875121226108860 ) ) ;
#51816=CARTESIAN_POINT ( 'NONE',  ( 2.256373768223415066, 2.737361830682320640, 7.132139410180973194 ) ) ;
#51832=ORIENTED_EDGE ( 'NONE', *, *, #36148, .F. ) ;
#51836=CARTESIAN_POINT ( 'NONE',  ( 3.152665057736111720, -7.281573230473792790, 3.161213418915395312 ) ) ;
#51839=CARTESIAN_POINT ( 'NONE',  ( 1.109979610372473946, 11.08130463534589261, -5.843815872356196373 ) ) ;
#51840=CARTESIAN_POINT ( 'NONE',  ( 1.109979610374045356, 12.41172293674789096, -1.701361252867769513 ) ) ;
#51843=ORIENTED_EDGE ( 'NONE', *, *, #51474, .T. ) ;
#51848=VERTEX_POINT ( 'NONE', #30715 ) ;
#51849=( BOUNDED_SURFACE ( )  B_SPLINE_SURFACE ( 3, 1, ( 
 ( #9176, #45407 ),
 ( #64692, #25137 ),
 ( #19163, #65671 ),
 ( #19503, #60063 ) ),
 .UNSPECIFIED., .F., .F., .F. ) 
 B_SPLINE_SURFACE_WITH_KNOTS ( ( 4, 4 ),
 ( 2, 2 ),
 ( 0.000000000000000000, 1.000000000000000000 ),
 ( 0.000000000000000000, 1.000000000000000000 ),
 .UNSPECIFIED. ) 
 GEOMETRIC_REPRESENTATION_ITEM ( )  RATIONAL_B_SPLINE_SURFACE ( (
 ( 1.000000000000000000, 1.000000000000000000),
 ( 0.9942764183789327692, 0.8450855930916585379),
 ( 0.9942764183789327692, 0.8450855930916585379),
 ( 1.000000000000000000, 1.000000000000000000) ) ) 
 REPRESENTATION_ITEM ( '' )  SURFACE ( )  );
#51852=CARTESIAN_POINT ( 'NONE',  ( 2.368238019615286127, 2.793778585134709225, 7.150288915654823718 ) ) ;
#51856=EDGE_LOOP ( 'NONE', ( #54674, #21825, #40067, #59949 ) ) ;
#51865=CARTESIAN_POINT ( 'NONE',  ( 3.152665057734131526, -0.9030954876737319337, -7.886634106564212487 ) ) ;
#51866=CARTESIAN_POINT ( 'NONE',  ( 2.247206125382826603, 2.720255231378031713, -7.135412558555523255 ) ) ;
#51870=EDGE_CURVE ( 'NONE', #7543, #47037, #37230, .T. ) ;
#51878=CARTESIAN_POINT ( 'NONE',  ( 0.2653141516239115871, 0.04404488958248177488, -12.24612533180317797 ) ) ;
#51879=CARTESIAN_POINT ( 'NONE',  ( 0.2801149460245143108, -8.024198546827411960, -9.257544930777235948 ) ) ;
#51897=CARTESIAN_POINT ( 'NONE',  ( -14.47334165536099881, 0.000000000000000000, 0.000000000000000000 ) ) ;
#51901=AXIS2_PLACEMENT_3D ( 'NONE', #55561, #4714, #10988 ) ;
#51902=B_SPLINE_CURVE_WITH_KNOTS ( 'NONE', 3,
 ( #35656, #31337, #36960, #46625, #751, #10383, #51313, #5421, #41629, #16378, #439, #21351, #20708, #16021, #5763, #40983 ),
 .UNSPECIFIED., .F., .F.,
 ( 4, 3, 3, 3, 3, 4 ),
 ( 0.000000000000000000, 0.0002999043160757465022, 0.0005998071753051236604, 0.0008997092107374906646, 0.001204458948196612204, 0.001510329163478418878 ),
 .UNSPECIFIED. ) ;
#51914=CARTESIAN_POINT ( 'NONE',  ( 2.717984159219906992, -6.602931111513720808, 4.139692542159457034 ) ) ;
#51924=LINE ( 'NONE', #50935, #11948 ) ;
#51935=ORIENTED_EDGE ( 'NONE', *, *, #62219, .T. ) ;
#51937=ORIENTED_EDGE ( 'NONE', *, *, #29794, .T. ) ;
#51938=CARTESIAN_POINT ( 'NONE',  ( 2.241451721903214178, 4.860585618235972127, 5.887257931662863264 ) ) ;
#51939=LINE ( 'NONE', #41276, #58528 ) ;
#51949=VERTEX_POINT ( 'NONE', #5484 ) ;
#51951=CARTESIAN_POINT ( 'NONE',  ( 2.507146904658100972, -5.774795220010153329, -5.128007631637124142 ) ) ;
#51958=CARTESIAN_POINT ( 'NONE',  ( 2.244591118395374174, 7.211060161905881394, 2.510215291313116381 ) ) ;
#51959=ADVANCED_FACE ( 'NONE', ( #50383 ), #5852, .F. ) ;
#51960=ORIENTED_EDGE ( 'NONE', *, *, #32394, .T. ) ;
#51961=CARTESIAN_POINT ( 'NONE',  ( 0.3665391374699465965, -7.691255657244358446, 9.576575648338991442 ) ) ;
#51964=CARTESIAN_POINT ( 'NONE',  ( 2.994568964204194383, -6.289764245798251885, 4.756002438591050208 ) ) ;
#51970=CARTESIAN_POINT ( 'NONE',  ( 0.3675815128205894289, -4.447030445008105737, -11.44679196252413789 ) ) ;
#51977=CARTESIAN_POINT ( 'NONE',  ( 1.459561108992812439, 4.912799202118954156, 11.65083230253652324 ) ) ;
#51978=CARTESIAN_POINT ( 'NONE',  ( 1.719304012340734822, -3.626341562669572305, -12.20344780066098345 ) ) ;
#51982=DIRECTION ( 'NONE',  ( 1.000000000000000000, -0.000000000000000000, -0.000000000000000000 ) ) ;
#51990=CARTESIAN_POINT ( 'NONE',  ( 0.3632410797595241880, -5.910360611678902032, 10.76277061791638801 ) ) ;
#51998=CARTESIAN_POINT ( 'NONE',  ( 1.198791140419921630, -11.61358959650685208, -4.776130053253331731 ) ) ;
#51999=CARTESIAN_POINT ( 'NONE',  ( 3.152665057734113319, -5.461013642405577073, 5.761241965769066553 ) ) ;
#52002=CARTESIAN_POINT ( 'NONE',  ( 0.2638984909335716500, 4.001111175853742985, 11.57533005135180382 ) ) ;
#52016=CARTESIAN_POINT ( 'NONE',  ( 0.3675815128205894289, 8.093875121226078662, 9.235491948680033758 ) ) ;
#52018=CARTESIAN_POINT ( 'NONE',  ( 0.3632410797595232443, -12.04386719438561570, 2.390576695689066167 ) ) ;
#52022=ORIENTED_EDGE ( 'NONE', *, *, #7127, .T. ) ;
#52036=CARTESIAN_POINT ( 'NONE',  ( 1.719304012342639965, 12.38166659047149487, -2.961219984262613458 ) ) ;
#52042=B_SPLINE_CURVE_WITH_KNOTS ( 'NONE', 3,
 ( #14489, #55069, #50433, #23517, #41743, #20150, #20486, #46410, #16149, #60722 ),
 .UNSPECIFIED., .F., .F.,
 ( 4, 3, 3, 4 ),
 ( 9.215718466126787689E-19, 6.607638129004467199E-05, 9.911389841680512771E-05, 0.0001667630577588622028 ),
 .UNSPECIFIED. ) ;
#52046=CARTESIAN_POINT ( 'NONE',  ( 0.2653519890518179492, 12.06014856238023469, -2.126538543977954721 ) ) ;
#52049=DIRECTION ( 'NONE',  ( 0.3939253465568944290, -0.8603393047164960006, -0.3234796780324333820 ) ) ;
#52050=CARTESIAN_POINT ( 'NONE',  ( 2.941278708680199916, 5.383216837018941270, 2.952340773940127949 ) ) ;
#52055=CARTESIAN_POINT ( 'NONE',  ( 3.152665057733776699, 4.377619405892044568, -6.622010822086680015 ) ) ;
#52063=CARTESIAN_POINT ( 'NONE',  ( 0.2655924914740778742, -10.62761259256412671, -6.084990060696620517 ) ) ;
#52070=CARTESIAN_POINT ( 'NONE',  ( 3.152665057734040488, 0.000000000000000000, 0.000000000000000000 ) ) ;
#52078=CARTESIAN_POINT ( 'NONE',  ( 0.2739690278137280055, 11.44648082006011869, -4.360944092821339879 ) ) ;
#52080=B_SPLINE_CURVE_WITH_KNOTS ( 'NONE', 3,
 ( #740, #32292, #7346, #42934, #37280, #31957, #12338, #1409, #11359, #46612, #16365, #47932, #2044, #22308, #52609, #6385 ),
 .UNSPECIFIED., .F., .F.,
 ( 4, 3, 3, 3, 3, 4 ),
 ( 0.000000000000000000, 0.0002999043160757426532, 0.0005998071753051154205, 0.0008997092107374793889, 0.001204458948196636056, 0.001510329163478481979 ),
 .UNSPECIFIED. ) ;
#52087=FACE_OUTER_BOUND ( 'NONE', #57321, .T. ) ;
#52092=ADVANCED_FACE ( 'NONE', ( #28365 ), #44078, .F. ) ;
#52096=CARTESIAN_POINT ( 'NONE',  ( 2.524535260912411871, 7.569872524928948465, -1.559291270914444638 ) ) ;
#52097=ADVANCED_FACE ( 'NONE', ( #8749 ), #48377, .F. ) ;
#52101=FACE_OUTER_BOUND ( 'NONE', #42408, .T. ) ;
#52105=CARTESIAN_POINT ( 'NONE',  ( 2.373367633546870525, -7.591069096729003540, 1.154895193356608063 ) ) ;
#52110=CARTESIAN_POINT ( 'NONE',  ( 0.3675815128205894289, 12.27743992903066328, -0.2638082659428851451 ) ) ;
#52116=FACE_OUTER_BOUND ( 'NONE', #59864, .T. ) ;
#52117=CARTESIAN_POINT ( 'NONE',  ( 2.259830038564999199, -3.938923657569452619, 6.546987858513363179 ) ) ;
#52127=ADVANCED_FACE ( 'NONE', ( #8096 ), #61937, .F. ) ;
#52132=EDGE_CURVE ( 'NONE', #17330, #65715, #6527, .T. ) ;
#52136=CARTESIAN_POINT ( 'NONE',  ( 0.3632410797595242991, 12.13515851238022591, 1.872837903657238234 ) ) ;
#52138=CARTESIAN_POINT ( 'NONE',  ( 1.459561108992816436, -1.570807238541338524, 12.54631635028845515 ) ) ;
#52143=CARTESIAN_POINT ( 'NONE',  ( 0.2956976708475442805, 6.317697191869785733, -10.50256636126820453 ) ) ;
#52151=CARTESIAN_POINT ( 'NONE',  ( 0.3675815128205912052, 6.367184624550311867, -10.50067073900645198 ) ) ;
#52152=CONICAL_SURFACE ( 'NONE', #60631, 7.938172270156617749, 1.280189991382167047 ) ;
#52164=CARTESIAN_POINT ( 'NONE',  ( 2.430348790455934882, 7.694949746373333177, -0.1949172018036633425 ) ) ;
#52165=B_SPLINE_CURVE_WITH_KNOTS ( 'NONE', 3,
 ( #56251, #37537, #22912, #43165, #40966, #46296, #7263, #7604, #28218, #12916, #10693, #36293, #57841, #5745, #33197, #736, #12259, #20995, #26324 ),
 .UNSPECIFIED., .F., .F.,
 ( 4, 3, 3, 3, 3, 3, 4 ),
 ( 6.662331925613552201E-18, 2.825908398831382330E-05, 4.208813692483990936E-05, 5.591713746943949807E-05, 6.279584083232014977E-05, 9.105792820296881071E-05, 0.0001153131102488856488 ),
 .UNSPECIFIED. ) ;
#52166=CARTESIAN_POINT ( 'NONE',  ( 2.251139882114759239, 5.770207524085092743, 5.003859976904558415 ) ) ;
#52167=CARTESIAN_POINT ( 'NONE',  ( 1.375507693222091099, 12.51366828189792635, -1.606074886183993744 ) ) ;
#52171=CARTESIAN_POINT ( 'NONE',  ( 0.2646305136544072623, -10.67138229758233692, 6.008537389229382519 ) ) ;
#52172=VERTEX_POINT ( 'NONE', #53970 ) ;
#52187=ORIENTED_EDGE ( 'NONE', *, *, #7460, .F. ) ;
#52195=CARTESIAN_POINT ( 'NONE',  ( 2.241449424704146320, -7.152834201978780726, 2.668712484599937707 ) ) ;
#52206=CARTESIAN_POINT ( 'NONE',  ( 2.931247277082547509, 4.765826751677452400, 6.255823895766906340 ) ) ;
#52211=CARTESIAN_POINT ( 'NONE',  ( 0.2646305136544065406, 11.55263159009958684, 4.064188116014585184 ) ) ;
#52220=CARTESIAN_POINT ( 'NONE',  ( 0.3109076770649061849, 10.73466383006821445, 5.925244271826481501 ) ) ;
#52222=CARTESIAN_POINT ( 'NONE',  ( 1.719304012338836563, 0.7661785589583339773, 12.70777170743865980 ) ) ;
#52226=AXIS2_PLACEMENT_3D ( 'NONE', #61451, #10931, #15897 ) ;
#52227=CARTESIAN_POINT ( 'NONE',  ( 2.249013661412227805, -6.673008335691891446, 3.714035584818202285 ) ) ;
#52230=CARTESIAN_POINT ( 'NONE',  ( 0.3106921474978442399, 2.360654586927948717, -12.03191800497306296 ) ) ;
#52235=CARTESIAN_POINT ( 'NONE',  ( 1.937114397841932290, -11.53912442307259134, 5.620553190832935364 ) ) ;
#52237=CARTESIAN_POINT ( 'NONE',  ( 2.653899356899525941, -0.2611590963044880254, -7.767552767344014342 ) ) ;
#52244=( BOUNDED_SURFACE ( )  B_SPLINE_SURFACE ( 3, 1, ( 
 ( #46265, #50919 ),
 ( #41577, #61866 ),
 ( #706, #11326 ),
 ( #41241, #31596 ) ),
 .UNSPECIFIED., .F., .F., .F. ) 
 B_SPLINE_SURFACE_WITH_KNOTS ( ( 4, 4 ),
 ( 2, 2 ),
 ( 0.000000000000000000, 1.000000000000000000 ),
 ( 0.000000000000000000, 1.000000000000000000 ),
 .UNSPECIFIED. ) 
 GEOMETRIC_REPRESENTATION_ITEM ( )  RATIONAL_B_SPLINE_SURFACE ( (
 ( 1.000000000000000000, 1.000000000000000000),
 ( 0.6933888150995267674, 0.9895912004443193632),
 ( 0.6933888150995267674, 0.9895912004443193632),
 ( 1.000000000000000000, 1.000000000000000000) ) ) 
 REPRESENTATION_ITEM ( '' )  SURFACE ( )  );
#52246=CARTESIAN_POINT ( 'NONE',  ( 0.2653519991613825790, 2.104847849998860543, 12.06397323649776787 ) ) ;
#52250=CARTESIAN_POINT ( 'NONE',  ( 0.2647959493198558945, -1.981611532097627970, 12.08462848595694084 ) ) ;
#52251=ORIENTED_EDGE ( 'NONE', *, *, #64607, .T. ) ;
#52254=ORIENTED_EDGE ( 'NONE', *, *, #22030, .T. ) ;
#52263=CARTESIAN_POINT ( 'NONE',  ( 0.2648978790185593790, 11.55204314799269305, -4.063980959784929681 ) ) ;
#52266=CARTESIAN_POINT ( 'NONE',  ( 2.262775599887391298, 7.131180968652119923, 2.745802076337088060 ) ) ;
#52278=AXIS2_PLACEMENT_3D ( 'NONE', #65402, #40465, #30805 ) ;
#52282=CARTESIAN_POINT ( 'NONE',  ( 5.515188684475870851, -0.001283816547385159676, -0.005194992164431768387 ) ) ;
#52288=CARTESIAN_POINT ( 'NONE',  ( 2.305787727787083519, -5.756228004061423320, -5.047606869483115766 ) ) ;
#52291=CARTESIAN_POINT ( 'NONE',  ( 2.305787727787085295, 7.566723232958088019, -1.164987321564654676 ) ) ;
#52301=CIRCLE ( 'NONE', #23620, 12.73084802173761787 ) ;
#52307=CARTESIAN_POINT ( 'NONE',  ( 0.2869720083484340045, -12.02930764912520445, -2.332746648244325982 ) ) ;
#52313=CARTESIAN_POINT ( 'NONE',  ( 0.2833330754217419090, -5.950193237802332114, -10.71034013638385929 ) ) ;
#52319=VECTOR ( 'NONE', #33725, 999.9999999999998863 ) ;
#52322=CARTESIAN_POINT ( 'NONE',  ( 0.3053067050349178579, -12.25734436043224740, -0.2307671807673560560 ) ) ;
#52328=CARTESIAN_POINT ( 'NONE',  ( 2.249013661412875731, 6.552953334857355649, 3.921976945966711092 ) ) ;
#52329=ORIENTED_EDGE ( 'NONE', *, *, #23088, .T. ) ;
#52334=CARTESIAN_POINT ( 'NONE',  ( 2.276905613633649850, -7.130967020394715306, 2.759436818562468030 ) ) ;
#52343=CIRCLE ( 'NONE', #3474, 7.938172270156617749 ) ;
#52351=CARTESIAN_POINT ( 'NONE',  ( 0.2653141617321045920, 9.409385893408607870, -7.837919552760626019 ) ) ;
#52375=VECTOR ( 'NONE', #44282, 1000.000000000000114 ) ;
#52384=CARTESIAN_POINT ( 'NONE',  ( 0.2652384770603659070, 12.07140968216696741, -2.061429379240358628 ) ) ;
#52387=VERTEX_POINT ( 'NONE', #41609 ) ;
#52390=CARTESIAN_POINT ( 'NONE',  ( 0.3665391374699472626, -12.27992639892678461, 0.2638605131386739244 ) ) ;
#52394=EDGE_CURVE ( 'NONE', #28876, #8359, #51520, .T. ) ;
#52402=CARTESIAN_POINT ( 'NONE',  ( 2.305787727787084407, 6.711944854845823372, 3.682701754025536012 ) ) ;
#52405=AXIS2_PLACEMENT_3D ( 'NONE', #44002, #69, #25673 ) ;
#52410=CONICAL_SURFACE ( 'NONE', #62980, 7.938172270156617749, 1.280189991382167047 ) ;
#52414=CARTESIAN_POINT ( 'NONE',  ( 0.3537226245948351666, -9.569332148897514045, 7.688925565304987053 ) ) ;
#52415=CARTESIAN_POINT ( 'NONE',  ( 0.2638984909335720941, -5.950360275955130618, 10.70468911391662381 ) ) ;
#52418=CARTESIAN_POINT ( 'NONE',  ( 0.2911222467163546712, -11.44063169461053064, -4.392242282524980723 ) ) ;
#52420=CARTESIAN_POINT ( 'NONE',  ( 0.3675815128205894289, 11.62724744438065727, 3.951233083390508050 ) ) ;
#52421=CARTESIAN_POINT ( 'NONE',  ( 1.719304012338836563, 0.7661785589583339773, 12.70777170743865980 ) ) ;
#52426=ORIENTED_EDGE ( 'NONE', *, *, #16212, .T. ) ;
#52430=B_SPLINE_CURVE_WITH_KNOTS ( 'NONE', 3,
 ( #34087, #54409, #8841, #29130, #9154, #4177, #33764, #28787, #23478, #49431, #43090, #38097, #23148, #24443, #4522, #10461, #46068, #35724, #60041 ),
 .UNSPECIFIED., .F., .F.,
 ( 4, 3, 3, 3, 3, 3, 4 ),
 ( 7.198522745683553356E-18, 4.457896483014757189E-05, 6.639290541542080333E-05, 8.820687556478888647E-05, 0.0001100173248778924787, 0.0001545671401658117229, 0.0001830328308068602031 ),
 .UNSPECIFIED. ) ;
#52431=CARTESIAN_POINT ( 'NONE',  ( 1.372161826076367719, -11.63973780005248670, 4.864129100816739104 ) ) ;
#52440=AXIS2_PLACEMENT_3D ( 'NONE', #24207, #44472, #7618 ) ;
#52447=CARTESIAN_POINT ( 'NONE',  ( 1.372161826075798174, 12.51237317864360854, 1.607409531431936323 ) ) ;
#52449=CARTESIAN_POINT ( 'NONE',  ( 2.941278708680199916, 3.842273877444562835, 4.788765081995642880 ) ) ;
#52453=( BOUNDED_SURFACE ( )  B_SPLINE_SURFACE ( 3, 1, ( 
 ( #32669, #17417 ),
 ( #47669, #37695 ),
 ( #52980, #31393 ),
 ( #51694, #6136 ) ),
 .UNSPECIFIED., .F., .F., .F. ) 
 B_SPLINE_SURFACE_WITH_KNOTS ( ( 4, 4 ),
 ( 2, 2 ),
 ( 0.000000000000000000, 1.000000000000000000 ),
 ( 0.000000000000000000, 1.000000000000000000 ),
 .UNSPECIFIED. ) 
 GEOMETRIC_REPRESENTATION_ITEM ( )  RATIONAL_B_SPLINE_SURFACE ( (
 ( 1.000000000000000000, 1.000000000000000000),
 ( 0.9856612449720755231, 0.9999558406602322425),
 ( 0.9856612449720755231, 0.9999558406602322425),
 ( 1.000000000000000000, 1.000000000000000000) ) ) 
 REPRESENTATION_ITEM ( '' )  SURFACE ( )  );
#52454=CARTESIAN_POINT ( 'NONE',  ( 0.9232167919969138659, 12.45862789703290296, -0.4134278310083473462 ) ) ;
#52456=CARTESIAN_POINT ( 'NONE',  ( 3.152665057733776699, 4.377619405892044568, -6.622010822086680015 ) ) ;
#52467=CIRCLE ( 'NONE', #42899, 7.580821595991582562 ) ;
#52475=CARTESIAN_POINT ( 'NONE',  ( 0.3223008802179259114, 12.11889957318022581, 1.888629463821725141 ) ) ;
#52477=CARTESIAN_POINT ( 'NONE',  ( 2.305787727787084407, -1.164987321564783684, 7.566723232958066703 ) ) ;
#52481=LINE ( 'NONE', #21204, #46904 ) ;
#52484=ADVANCED_FACE ( 'NONE', ( #27294 ), #57561, .T. ) ;
#52488=EDGE_CURVE ( 'NONE', #12917, #35544, #7804, .T. ) ;
#52491=CARTESIAN_POINT ( 'NONE',  ( 2.305787727787083519, -7.249469779319894336, -2.461236246751144829 ) ) ;
#52493=CARTESIAN_POINT ( 'NONE',  ( 2.080613030138688480, 0.000000000000000000, 0.000000000000000000 ) ) ;
#52498=DIRECTION ( 'NONE',  ( 0.000000000000000000, 0.000000000000000000, 1.000000000000000000 ) ) ;
#52503=CARTESIAN_POINT ( 'NONE',  ( 0.8320506296491597675, 3.891425424503466068, -11.81055997318801154 ) ) ;
#52506=CARTESIAN_POINT ( 'NONE',  ( 2.257661810676415914, -1.193649218120645283, 7.546014018371156595 ) ) ;
#52510=ORIENTED_EDGE ( 'NONE', *, *, #43612, .F. ) ;
#52515=CARTESIAN_POINT ( 'NONE',  ( 5.530133899448235191, 0.01594518557925638305, -0.001124651387254824511 ) ) ;
#52519=FACE_OUTER_BOUND ( 'NONE', #45610, .T. ) ;
#52531=CARTESIAN_POINT ( 'NONE',  ( 0.2767916011545388799, 4.367596755337448400, 11.44495079483525757 ) ) ;
#52534=CARTESIAN_POINT ( 'NONE',  ( 2.258463476536308079, 5.014277205346122201, -5.764393264552794882 ) ) ;
#52536=CARTESIAN_POINT ( 'NONE',  ( 2.255723233588950105, 2.736592204236748760, -7.132203433012263893 ) ) ;
#52537=DIRECTION ( 'NONE',  ( -0.3939253465568943180, -0.9068155327749422012, -0.1500280335741567828 ) ) ;
#52543=CARTESIAN_POINT ( 'NONE',  ( 2.273267844205329791, 3.690689057641470150, -6.695181685740229760 ) ) ;
#52544=CARTESIAN_POINT ( 'NONE',  ( 0.2657645697724682066, -2.275433120353170136, 12.03308811492268582 ) ) ;
#52547=EDGE_CURVE ( 'NONE', #64733, #3364, #33919, .T. ) ;
#52551=EDGE_CURVE ( 'NONE', #40530, #58005, #13324, .T. ) ;
#52554=CARTESIAN_POINT ( 'NONE',  ( 0.2676618633000454328, -0.1607051348608467545, 12.24591287309139176 ) ) ;
#52555=CARTESIAN_POINT ( 'NONE',  ( 2.941278708680199916, -2.226055275041753045, -5.721889327162172911 ) ) ;
#52561=CARTESIAN_POINT ( 'NONE',  ( 0.3675815128205894289, 10.50067073900660652, -6.367184624550055183 ) ) ;
#52562=CARTESIAN_POINT ( 'NONE',  ( 0.3218525148189809726, 2.370084734146373773, -12.03385614540601445 ) ) ;
#52568=EDGE_LOOP ( 'NONE', ( #5021, #41607, #29272, #59734 ) ) ;
#52570=CARTESIAN_POINT ( 'NONE',  ( 5.514970785353741078, -0.004532877335078719372, -0.001326349372336280402 ) ) ;
#52571=EDGE_CURVE ( 'NONE', #27962, #18185, #12611, .T. ) ;
#52573=AXIS2_PLACEMENT_3D ( 'NONE', #8345, #4019, #48928 ) ;
#52574=EDGE_LOOP ( 'NONE', ( #37162, #14240, #26124, #58716 ) ) ;
#52576=CARTESIAN_POINT ( 'NONE',  ( 2.440552418640497212, -3.678171968408280978, -6.765628357760817835 ) ) ;
#52578=CARTESIAN_POINT ( 'NONE',  ( 0.5547464869798254261, -7.697709668896136392, 9.648168635481816580 ) ) ;
#52583=VERTEX_POINT ( 'NONE', #64821 ) ;
#52591=DIRECTION ( 'NONE',  ( -1.000000000000000000, -0.000000000000000000, -0.000000000000000000 ) ) ;
#52594=ORIENTED_EDGE ( 'NONE', *, *, #17301, .F. ) ;
#52595=CARTESIAN_POINT ( 'NONE',  ( 0.2653519991613838558, 11.51519138201636139, -4.167757449530301805 ) ) ;
#52597=CARTESIAN_POINT ( 'NONE',  ( 2.241352910868908754, 7.145045428366577411, 2.689314586382375527 ) ) ;
#52601=ORIENTED_EDGE ( 'NONE', *, *, #46390, .T. ) ;
#52603=CARTESIAN_POINT ( 'NONE',  ( 1.283627346226908550, 7.660435136228973541, -9.985833283678474004 ) ) ;
#52607=CARTESIAN_POINT ( 'NONE',  ( 0.2638984909335720941, 9.252728947331188891, -8.023974293733084906 ) ) ;
#52609=CARTESIAN_POINT ( 'NONE',  ( 0.4626703367448980475, 6.399577980714960646, -10.51809671647423450 ) ) ;
#52615=CARTESIAN_POINT ( 'NONE',  ( 2.305787727787084407, 6.711944854845823372, 3.682701754025536012 ) ) ;
#52617=DIRECTION ( 'NONE',  ( -0.3865475372811021937, -0.9046932595863059756, 0.1791957239473633001 ) ) ;
#52618=CARTESIAN_POINT ( 'NONE',  ( 0.2671309869109507185, 12.03155065772887689, -2.286013846429900465 ) ) ;
#52626=CARTESIAN_POINT ( 'NONE',  ( 2.665405856346783953, 3.808819464940546684, -8.776564688671568248 ) ) ;
#52629=CARTESIAN_POINT ( 'NONE',  ( 1.452237505248555660, 0.5922625322517017787, 12.64182585313126239 ) ) ;
#52635=CARTESIAN_POINT ( 'NONE',  ( 2.835339799623983748, -7.649567297875982774, -1.682641786445519871 ) ) ;
#52637=CARTESIAN_POINT ( 'NONE',  ( 2.889800649504073782, 6.039722463373538908, 0.9965440656173926159 ) ) ;
#52644=B_SPLINE_CURVE_WITH_KNOTS ( 'NONE', 3,
 ( #46907, #62192, #41239, #42213, #7000, #47560, #62504, #26613, #37237, #36255, #11324, #1366, #62841, #11972, #11001, #31286 ),
 .UNSPECIFIED., .F., .F.,
 ( 4, 3, 3, 3, 3, 4 ),
 ( 0.000000000000000000, 0.0002999043160757375033, 0.0005998071753051059879, 0.0008997092107374648606, 0.001204458948196129734, 0.001510329163477479742 ),
 .UNSPECIFIED. ) ;
#52646=LINE ( 'NONE', #1772, #27814 ) ;
#52657=EDGE_CURVE ( 'NONE', #26251, #35019, #43458, .T. ) ;
#52662=CARTESIAN_POINT ( 'NONE',  ( 3.152665057734040488, 0.000000000000000000, 0.000000000000000000 ) ) ;
#52664=CARTESIAN_POINT ( 'NONE',  ( 1.547277799339609405, -0.6737945300328305187, -12.65564732076297361 ) ) ;
#52668=CARTESIAN_POINT ( 'NONE',  ( 0.3665391374699467075, -6.368473106897203806, 10.50279796150434741 ) ) ;
#52673=ORIENTED_EDGE ( 'NONE', *, *, #53336, .T. ) ;
#52674=CARTESIAN_POINT ( 'NONE',  ( 0.2650492594609249464, 9.451471004987441304, -7.786980091309354535 ) ) ;
#52697=ADVANCED_FACE ( 'NONE', ( #1961 ), #16879, .F. ) ;
#52705=CARTESIAN_POINT ( 'NONE',  ( 5.520433897694421610, 0.01120198501134835739, 0.01006947824912426785 ) ) ;
#52712=CARTESIAN_POINT ( 'NONE',  ( 0.3160775863651107964, -1.892533050396085992, -12.11619190710940686 ) ) ;
#52721=CARTESIAN_POINT ( 'NONE',  ( 0.2833330754217431302, 9.254504746325796560, 8.029341648258402131 ) ) ;
#52724=CARTESIAN_POINT ( 'NONE',  ( 0.3632410797595245766, 2.390576695689105247, 12.04386719438560327 ) ) ;
#52738=CARTESIAN_POINT ( 'NONE',  ( 0.2676618633000468206, -11.45242956837284432, -4.339362305359559357 ) ) ;
#52743=EDGE_LOOP ( 'NONE', ( #43896, #47506, #46336, #8924 ) ) ;
#52748=CARTESIAN_POINT ( 'NONE',  ( 3.152665057734130638, -4.725420687650661478, -6.378477742800524375 ) ) ;
#52749=CARTESIAN_POINT ( 'NONE',  ( 2.556980015514155102, 1.570584617272727357, 7.578583798307265695 ) ) ;
#52757=CARTESIAN_POINT ( 'NONE',  ( 1.452237505248552996, -4.880303821311088974, 11.67686475128078172 ) ) ;
#52764=CARTESIAN_POINT ( 'NONE',  ( 2.573738926104375935, -7.664876274722922211, 1.112690714006513204 ) ) ;
#52765=CARTESIAN_POINT ( 'NONE',  ( 2.261269890822072970, 7.499479675451366845, 1.464004156081675889 ) ) ;
#52772=CARTESIAN_POINT ( 'NONE',  ( 2.284126774967659479, -3.960764882115048735, 6.543266298866119435 ) ) ;
#52778=CIRCLE ( 'NONE', #65471, 12.73084802173761787 ) ;
#52780=CARTESIAN_POINT ( 'NONE',  ( 0.2647959493198551173, 7.758440170207294706, -9.474789498086916950 ) ) ;
#52782=CARTESIAN_POINT ( 'NONE',  ( 0.9232167919969127556, -9.809608956680815339, -7.691547553333223597 ) ) ;
#52785=CARTESIAN_POINT ( 'NONE',  ( 2.705197763288538670, 2.399370654839271477, 7.410249563424426533 ) ) ;
#52787=CARTESIAN_POINT ( 'NONE',  ( 2.589278595513820225, -1.107986312493286496, 7.670769623692575756 ) ) ;
#52790=CARTESIAN_POINT ( 'NONE',  ( 2.889800649504073782, 3.986129653162648001, 4.645655809191377550 ) ) ;
#52796=CARTESIAN_POINT ( 'NONE',  ( 0.2655924914740778742, 12.24627751708824341, -0.04405032194307659937 ) ) ;
#52802=CARTESIAN_POINT ( 'NONE',  ( 0.2646305136544072623, 7.972778379581675345, -9.296005949277148517 ) ) ;
#52803=ORIENTED_EDGE ( 'NONE', *, *, #36834, .T. ) ;
#52806=CARTESIAN_POINT ( 'NONE',  ( 2.903928887688015159, 8.528865300113499970, -2.041797854847570370 ) ) ;
#52807=CARTESIAN_POINT ( 'NONE',  ( 0.4613984246114881116, 3.943860067443805129, -11.66278164635730619 ) ) ;
#52809=CARTESIAN_POINT ( 'NONE',  ( 5.515188684475870851, 0.003709313826049746507, -0.003857086913166404493 ) ) ;
#52813=CARTESIAN_POINT ( 'NONE',  ( 1.459561108993326473, -5.767168887069098915, 11.25243317554898859 ) ) ;
#52818=EDGE_CURVE ( 'NONE', #59168, #25513, #52343, .T. ) ;
#52823=CARTESIAN_POINT ( 'NONE',  ( 1.937114397841935398, -0.9020203649530801338, -12.80345148322680160 ) ) ;
#52835=CARTESIAN_POINT ( 'NONE',  ( 2.241509619876137283, -7.187074272457174118, 2.575142053947843124 ) ) ;
#52836=CARTESIAN_POINT ( 'NONE',  ( 2.261269890821711481, 5.017604628138070844, -5.762737836065258357 ) ) ;
#52839=CARTESIAN_POINT ( 'NONE',  ( 0.2648978790185584908, 7.972372351883154629, -9.295532325666371776 ) ) ;
#52847=CARTESIAN_POINT ( 'NONE',  ( 0.2655924914740778187, -0.04405032194311705313, 12.24627751708824341 ) ) ;
#52848=CARTESIAN_POINT ( 'NONE',  ( 0.2648978790185619880, -7.972372351882965447, -9.295532325666529871 ) ) ;
#52850=CARTESIAN_POINT ( 'NONE',  ( 0.3223008802179319621, -11.60682919296348281, -3.964361764750287787 ) ) ;
#52859=CARTESIAN_POINT ( 'NONE',  ( 2.258463476536643366, 5.939075453322746334, -4.806099079317481149 ) ) ;
#52860=DIRECTION ( 'NONE',  ( 0.000000000000000000, 0.000000000000000000, 1.000000000000000000 ) ) ;
#52862=CARTESIAN_POINT ( 'NONE',  ( 2.573738926104374158, -4.796056562246135968, -6.081632213771440476 ) ) ;
#52864=CARTESIAN_POINT ( 'NONE',  ( 1.194176325881332490, 10.60746084433564462, -6.717888447700713250 ) ) ;
#52872=ORIENTED_EDGE ( 'NONE', *, *, #62506, .T. ) ;
#52873=CARTESIAN_POINT ( 'NONE',  ( 2.177405672430317463, -5.005033771133682308, 10.01846874165406476 ) ) ;
#52881=CARTESIAN_POINT ( 'NONE',  ( 1.459561108993324030, -7.633517148169429944, 10.08002506399545517 ) ) ;
#52887=EDGE_CURVE ( 'NONE', #15452, #43301, #52301, .T. ) ;
#52889=ORIENTED_EDGE ( 'NONE', *, *, #3052, .F. ) ;
#52894=CARTESIAN_POINT ( 'NONE',  ( 0.2650492433740066489, 11.46945725111973147, -4.291726136518433599 ) ) ;
#52897=ORIENTED_EDGE ( 'NONE', *, *, #8149, .T. ) ;
#52898=ORIENTED_EDGE ( 'NONE', *, *, #40939, .T. ) ;
#52906=CARTESIAN_POINT ( 'NONE',  ( 2.251139882113958990, 3.710800524304825654, 6.675617500148614880 ) ) ;
#52910=EDGE_CURVE ( 'NONE', #21432, #33447, #60775, .T. ) ;
#52911=CARTESIAN_POINT ( 'NONE',  ( 0.7400311444011714590, 11.53023780418231858, -4.574267895796732653 ) ) ;
#52917=CARTESIAN_POINT ( 'NONE',  ( 0.2648978790185584908, -4.312320170909314854, 11.46165506714226900 ) ) ;
#52918=ADVANCED_FACE ( 'NONE', ( #18245 ), #40595, .T. ) ;
#52923=CARTESIAN_POINT ( 'NONE',  ( 0.3632410797595208574, 12.04386719438563169, -2.390576695688982234 ) ) ;
#52928=CARTESIAN_POINT ( 'NONE',  ( 2.907497136251082193, -6.976431712756687276, -3.613027414876620824 ) ) ;
#52932=CARTESIAN_POINT ( 'NONE',  ( 2.406456491626382199, -10.00134798414796578, -2.970787154401012931 ) ) ;
#52948=CARTESIAN_POINT ( 'NONE',  ( 0.3675815128205894289, 4.447030445008180344, 11.44679196252410946 ) ) ;
#52949=CARTESIAN_POINT ( 'NONE',  ( 3.152665057734128862, 5.461013642405629476, -5.761241965769021256 ) ) ;
#52950=VECTOR ( 'NONE', #19232, 1000.000000000000114 ) ;
#52952=CARTESIAN_POINT ( 'NONE',  ( 2.241311220309555097, -0.09281826062101325436, 7.633829235838275551 ) ) ;
#52953=CARTESIAN_POINT ( 'NONE',  ( 0.2833330754217411318, -12.25052326018167115, -0.2021515668286960610 ) ) ;
#52960=CARTESIAN_POINT ( 'NONE',  ( 0.3610902822527226053, -5.910495176556258556, 10.76187877352511713 ) ) ;
#52974=DIRECTION ( 'NONE',  ( 0.3939253465568944290, -0.1691689424289884447, 0.9034404741085536594 ) ) ;
#52979=VERTEX_POINT ( 'NONE', #15199 ) ;
#52980=CARTESIAN_POINT ( 'NONE',  ( 5.514624014163232779, -0.002789935220458489469, -0.003060352188290538233 ) ) ;
#52989=EDGE_CURVE ( 'NONE', #27385, #16341, #10884, .T. ) ;
#52996=ORIENTED_EDGE ( 'NONE', *, *, #6162, .F. ) ;
#52998=EDGE_CURVE ( 'NONE', #11928, #37322, #27572, .T. ) ;
#53004=CARTESIAN_POINT ( 'NONE',  ( 5.520433897694421610, 0.01186170453199825517, -0.009283255140285221613 ) ) ;
#53006=FACE_OUTER_BOUND ( 'NONE', #52568, .T. ) ;
#53010=LINE ( 'NONE', #62984, #60029 ) ;
#53025=CARTESIAN_POINT ( 'NONE',  ( 2.368238019615422463, -1.509700170844607392, -7.526794520527707810 ) ) ;
#53031=CARTESIAN_POINT ( 'NONE',  ( 5.515188684475870851, 0.001485678338381512956, -0.005140903460551593009 ) ) ;
#53033=CARTESIAN_POINT ( 'NONE',  ( 0.9232167919969141989, -12.34114433434356606, -1.756271097262192660 ) ) ;
#53035=CARTESIAN_POINT ( 'NONE',  ( 0.3164563675027637357, 2.365891945210813141, 12.03284811452138570 ) ) ;
#53042=CARTESIAN_POINT ( 'NONE',  ( 0.2834382757448000167, -4.380429851625252446, -11.44241760114839934 ) ) ;
#53043=ORIENTED_EDGE ( 'NONE', *, *, #43531, .T. ) ;
#53045=EDGE_CURVE ( 'NONE', #5308, #49481, #2987, .T. ) ;
#53053=CARTESIAN_POINT ( 'NONE',  ( 1.462291587751482380, 4.914320681886612974, -11.65117843858603663 ) ) ;
#53058=ORIENTED_EDGE ( 'NONE', *, *, #44714, .T. ) ;
#53065=CARTESIAN_POINT ( 'NONE',  ( 0.2648978790185584908, 4.063980959785046032, 11.55204314799265042 ) ) ;
#53070=CARTESIAN_POINT ( 'NONE',  ( 1.104777566491140561, -11.92547689818820622, -3.832109395972772337 ) ) ;
#53072=EDGE_LOOP ( 'NONE', ( #34368, #58480, #28241, #21093 ) ) ;
#53076=CARTESIAN_POINT ( 'NONE',  ( 2.241352910868908310, 1.407733736974966288, -7.503490710578218703 ) ) ;
#53097=CARTESIAN_POINT ( 'NONE',  ( 0.2646305136544072623, 11.55263159009958862, 4.064188116014587848 ) ) ;
#53100=CARTESIAN_POINT ( 'NONE',  ( 0.3057689695767464300, 7.702054583838595647, -9.538231270095025138 ) ) ;
#53101=CARTESIAN_POINT ( 'NONE',  ( 5.514970785353741078, -0.002796696073589764048, 0.003805873180274775124 ) ) ;
#53105=B_SPLINE_CURVE_WITH_KNOTS ( 'NONE', 3,
 ( #18908, #49187, #33854, #8927, #34182, #24877, #59795, #19229, #18609, #29213, #24538, #54153, #45153 ),
 .UNSPECIFIED., .F., .F.,
 ( 4, 3, 3, 3, 4 ),
 ( 1.734723475976807094E-18, 6.607593386745386026E-05, 0.0001321518677373493709, 0.0001982171734706180679, 0.0002642860854759505602 ),
 .UNSPECIFIED. ) ;
#53109=CARTESIAN_POINT ( 'NONE',  ( 0.2653519991613819129, -10.59450977800977789, -6.142165520908282161 ) ) ;
#53121=CARTESIAN_POINT ( 'NONE',  ( 0.5572780756284226866, -8.165890079445430771, 9.256402261579117052 ) ) ;
#53123=CARTESIAN_POINT ( 'NONE',  ( 0.3665391374699467075, 10.76665847464320969, -5.911453292029491102 ) ) ;
#53128=CARTESIAN_POINT ( 'NONE',  ( 0.3665391374699465965, -12.27992639892678461, 0.2638605131386725922 ) ) ;
#53131=EDGE_CURVE ( 'NONE', #56731, #20463, #40276, .T. ) ;
#53136=CARTESIAN_POINT ( 'NONE',  ( 0.8375941296809088499, -7.696026447556186589, -9.769835228044549069 ) ) ;
#53137=CARTESIAN_POINT ( 'NONE',  ( 2.258463476537679426, 5.764393264551986640, 5.014277205347752009 ) ) ;
#53138=DIRECTION ( 'NONE',  ( 0.000000000000000000, 0.000000000000000000, 1.000000000000000000 ) ) ;
#53139=ORIENTED_EDGE ( 'NONE', *, *, #51131, .F. ) ;
#53145=CARTESIAN_POINT ( 'NONE',  ( 1.719304012338199517, 0.000000000000000000, 0.000000000000000000 ) ) ;
#53152=CARTESIAN_POINT ( 'NONE',  ( 2.770579946183334474, -1.653873933978927901, 7.633739187313470786 ) ) ;
#53157=ADVANCED_FACE ( 'NONE', ( #12827 ), #59810, .F. ) ;
#53163=EDGE_CURVE ( 'NONE', #48281, #60037, #33453, .T. ) ;
#53164=DIRECTION ( 'NONE',  ( 0.000000000000000000, 0.000000000000000000, 1.000000000000000000 ) ) ;
#53168=CARTESIAN_POINT ( 'NONE',  ( 0.3675815128205912052, 8.093875121226199454, -9.235491948679927177 ) ) ;
#53169=CARTESIAN_POINT ( 'NONE',  ( 5.514970785353741078, -0.001897634820904511074, 0.004324946436530178843 ) ) ;
#53181=CARTESIAN_POINT ( 'NONE',  ( 1.287602823385183948, 5.809161206980673064, 11.16629420487727131 ) ) ;
#53186=ORIENTED_EDGE ( 'NONE', *, *, #33501, .T. ) ;
#53212=FACE_OUTER_BOUND ( 'NONE', #2046, .T. ) ;
#53213=( BOUNDED_SURFACE ( )  B_SPLINE_SURFACE ( 3, 1, ( 
 ( #5048, #30313 ),
 ( #55594, #25002 ),
 ( #45276, #14996 ),
 ( #65534, #35282 ) ),
 .UNSPECIFIED., .F., .F., .F. ) 
 B_SPLINE_SURFACE_WITH_KNOTS ( ( 4, 4 ),
 ( 2, 2 ),
 ( 0.000000000000000000, 1.000000000000000000 ),
 ( 0.000000000000000000, 1.000000000000000000 ),
 .UNSPECIFIED. ) 
 GEOMETRIC_REPRESENTATION_ITEM ( )  RATIONAL_B_SPLINE_SURFACE ( (
 ( 1.000000000000000000, 1.000000000000000000),
 ( 0.9942764183789327692, 0.8450855930916580938),
 ( 0.9942764183789327692, 0.8450855930916580938),
 ( 1.000000000000000000, 1.000000000000000000) ) ) 
 REPRESENTATION_ITEM ( '' )  SURFACE ( )  );
#53214=CARTESIAN_POINT ( 'NONE',  ( 2.241528039335008327, -5.838210500619341659, -4.919377664485154789 ) ) ;
#53219=EDGE_CURVE ( 'NONE', #47570, #20105, #33759, .T. ) ;
#53234=CARTESIAN_POINT ( 'NONE',  ( 2.269879328256731110, -2.753278809616064748, -7.130835954829873202 ) ) ;
#53245=CARTESIAN_POINT ( 'NONE',  ( 0.2646305136544065406, 0.1321451301299554348, -12.24595685781654275 ) ) ;
#53250=CARTESIAN_POINT ( 'NONE',  ( 5.515539859299206427, -0.002251761459665968176, -0.005618668168217485354 ) ) ;
#53256=CARTESIAN_POINT ( 'NONE',  ( 2.288423627606494648, 6.704349683465941290, 3.684511167348409888 ) ) ;
#53260=CARTESIAN_POINT ( 'NONE',  ( 0.3164563675027607936, 6.338687639236032290, 10.49799587805932255 ) ) ;
#53261=CARTESIAN_POINT ( 'NONE',  ( 2.589278595512835235, -7.587119248534184734, 1.582391164331409916 ) ) ;
#53274=CARTESIAN_POINT ( 'NONE',  ( 5.515539859299206427, -0.004509673239148459349, 0.004037661319611352689 ) ) ;
#53279=B_SPLINE_CURVE_WITH_KNOTS ( 'NONE', 3,
 ( #63151, #23917, #21704, #23243, #17617, #12937, #46967, #54496, #1423, #7628, #27910, #43504, #43186, #28238, #28553, #37880 ),
 .UNSPECIFIED., .F., .F.,
 ( 4, 3, 3, 3, 3, 4 ),
 ( 2.266899309950898873E-15, 0.0002126834539179782880, 0.0004253519300366448929, 0.0006380165497224444702, 0.0007442707582428578252, 0.0009453531351416036505 ),
 .UNSPECIFIED. ) ;
#53280=CARTESIAN_POINT ( 'NONE',  ( 2.573738926104376823, -7.583190312075752892, -1.575954828885333114 ) ) ;
#53283=CARTESIAN_POINT ( 'NONE',  ( 0.3040950598368152291, -1.881452845810457353, 12.11647736519420171 ) ) ;
#53284=CARTESIAN_POINT ( 'NONE',  ( 0.9232058338315048962, 9.791640253608255406, -7.723624854284617314 ) ) ;
#53296=CARTESIAN_POINT ( 'NONE',  ( 0.8375941296815435644, -9.275620596396473516, -8.285008510335705623 ) ) ;
#53304=ORIENTED_EDGE ( 'NONE', *, *, #47230, .F. ) ;
#53307=CARTESIAN_POINT ( 'NONE',  ( 2.251152103363644574, -7.133254101175206863, 2.729599998984383991 ) ) ;
#53317=CARTESIAN_POINT ( 'NONE',  ( 0.2801149460245112022, -7.723514566794048797, 9.509848747524161539 ) ) ;
#53322=ORIENTED_EDGE ( 'NONE', *, *, #60930, .F. ) ;
#53324=ORIENTED_EDGE ( 'NONE', *, *, #6729, .F. ) ;
#53336=EDGE_CURVE ( 'NONE', #46419, #29012, #18867, .T. ) ;
#53360=CARTESIAN_POINT ( 'NONE',  ( 0.2653519991613843554, 12.06397323649778563, -2.104847849998736642 ) ) ;
#53365=CARTESIAN_POINT ( 'NONE',  ( 0.3665391374699465965, -8.095513416941168217, -9.237363111276849281 ) ) ;
#53376=CARTESIAN_POINT ( 'NONE',  ( 0.3040950598368144520, -10.74226959800795811, 5.912066680610576164 ) ) ;
#53377=CARTESIAN_POINT ( 'NONE',  ( 2.245754705088262249, -4.822435078157992550, -5.920355780194852535 ) ) ;
#53397=EDGE_CURVE ( 'NONE', #25053, #26284, #27933, .T. ) ;
#53411=CARTESIAN_POINT ( 'NONE',  ( 1.719304012338199517, 0.000000000000000000, 0.000000000000000000 ) ) ;
#53415=ORIENTED_EDGE ( 'NONE', *, *, #26785, .T. ) ;
#53416=( BOUNDED_SURFACE ( )  B_SPLINE_SURFACE ( 3, 1, ( 
 ( #51573, #6022 ),
 ( #32236, #26277 ),
 ( #16951, #27255 ),
 ( #46555, #57532 ) ),
 .UNSPECIFIED., .F., .F., .F. ) 
 B_SPLINE_SURFACE_WITH_KNOTS ( ( 4, 4 ),
 ( 2, 2 ),
 ( 0.000000000000000000, 1.000000000000000000 ),
 ( 0.000000000000000000, 1.000000000000000000 ),
 .UNSPECIFIED. ) 
 GEOMETRIC_REPRESENTATION_ITEM ( )  RATIONAL_B_SPLINE_SURFACE ( (
 ( 1.000000000000000000, 1.000000000000000000),
 ( 0.9942764183789327692, 0.8450855930916580938),
 ( 0.9942764183789327692, 0.8450855930916580938),
 ( 1.000000000000000000, 1.000000000000000000) ) ) 
 REPRESENTATION_ITEM ( '' )  SURFACE ( )  );
#53419=CARTESIAN_POINT ( 'NONE',  ( 1.633930747252546167, -12.16309769563645915, -3.662223193115497377 ) ) ;
#53430=VECTOR ( 'NONE', #56142, 1000.000000000000114 ) ;
#53433=CARTESIAN_POINT ( 'NONE',  ( 2.249013661412230025, 3.921976945965425454, -6.552953334857869905 ) ) ;
#53438=DIRECTION ( 'NONE',  ( 0.000000000000000000, 0.000000000000000000, 1.000000000000000000 ) ) ;
#53439=CARTESIAN_POINT ( 'NONE',  ( 2.844750968615672004, -2.990088422897184905, -7.242618984642843039 ) ) ;
#53445=CARTESIAN_POINT ( 'NONE',  ( 0.2915757698887302962, 7.711631695122966867, -9.524403232224781135 ) ) ;
#53447=CARTESIAN_POINT ( 'NONE',  ( 2.266490820343225021, 1.470039317404164603, 7.500072841116502964 ) ) ;
#53448=CARTESIAN_POINT ( 'NONE',  ( 2.247206125382826603, 1.439877054338202900, -7.499376972323885227 ) ) ;
#53451=CARTESIAN_POINT ( 'NONE',  ( 2.639814597422731168, 2.414168779979584567, 7.382549681340915271 ) ) ;
#53458=CARTESIAN_POINT ( 'NONE',  ( 3.031336079629237013, -3.582646412484526532, 7.038432939675882238 ) ) ;
#53462=CARTESIAN_POINT ( 'NONE',  ( 0.2655924914740778742, 2.169924872618063105, 12.05257978623654402 ) ) ;
#53464=CARTESIAN_POINT ( 'NONE',  ( 5.515539859299206427, 0.002251761459665927844, 0.005618668168217501833 ) ) ;
#53465=ORIENTED_EDGE ( 'NONE', *, *, #65797, .F. ) ;
#53468=CARTESIAN_POINT ( 'NONE',  ( -14.47334165536100059, 0.000000000000000000, -6.000000000000000888 ) ) ;
#53473=CARTESIAN_POINT ( 'NONE',  ( 0.2869720083484368911, -11.58405933820304234, 3.994435966590022424 ) ) ;
#53478=CARTESIAN_POINT ( 'NONE',  ( 5.520433897694421610, -0.01432141647227114754, -0.004666464468078277902 ) ) ;
#53483=LINE ( 'NONE', #34481, #32214 ) ;
#53485=CARTESIAN_POINT ( 'NONE',  ( 2.284126774969136076, 5.756079777200249659, 5.036818232553848418 ) ) ;
#53492=CARTESIAN_POINT ( 'NONE',  ( 1.719304012338836563, -3.626341562670527985, 12.20344780066003487 ) ) ;
#53499=CARTESIAN_POINT ( 'NONE',  ( 2.507146904658099196, 1.553587269793159642, -7.565123178000298765 ) ) ;
#53515=CARTESIAN_POINT ( 'NONE',  ( 0.3053067050349185796, 8.055646999028132527, -9.241336250185277379 ) ) ;
#53518=CARTESIAN_POINT ( 'NONE',  ( 2.350038591458112780, 6.324706260080001030, 8.533611140765424707 ) ) ;
#53523=CARTESIAN_POINT ( 'NONE',  ( 3.100650473569697585, 4.737096019059274354, 6.348250400753886247 ) ) ;
#53524=CARTESIAN_POINT ( 'NONE',  ( 2.251152103364156609, 3.709836606812680682, -6.676162264141248137 ) ) ;
#53529=CARTESIAN_POINT ( 'NONE',  ( 2.305787727787084407, -0.1666591538753222634, 7.654065630109506024 ) ) ;
#53534=ADVANCED_FACE ( 'NONE', ( #47604 ), #58764, .T. ) ;
#53537=CARTESIAN_POINT ( 'NONE',  ( 0.3537226245948373315, -0.2609894354290372975, 12.27287980220284602 ) ) ;
#53539=CARTESIAN_POINT ( 'NONE',  ( 3.152665057734036491, 7.923639299009025194, 0.4801242025592407647 ) ) ;
#53541=CARTESIAN_POINT ( 'NONE',  ( 2.931247277082684288, -4.765826751677395556, -6.255823895767015586 ) ) ;
#53551=CARTESIAN_POINT ( 'NONE',  ( 1.014383007554949589, -8.367379244277062256, -9.280879504741022856 ) ) ;
#53556=ORIENTED_EDGE ( 'NONE', *, *, #11035, .F. ) ;
#53560=CARTESIAN_POINT ( 'NONE',  ( 3.100650473569578569, -3.562766772868545484, -7.074394303868158040 ) ) ;
#53562=CARTESIAN_POINT ( 'NONE',  ( 5.536195898058073439, -0.0002547682446684437600, -0.008496323383586771791 ) ) ;
#53567=ORIENTED_EDGE ( 'NONE', *, *, #22612, .T. ) ;
#53568=CARTESIAN_POINT ( 'NONE',  ( 2.258463476536645143, 7.224688073723641857, -2.484972401833173805 ) ) ;
#53574=CARTESIAN_POINT ( 'NONE',  ( 2.262775599886257982, -7.548684916004836154, 1.187656132455246150 ) ) ;
#53578=CARTESIAN_POINT ( 'NONE',  ( 2.280717697723838366, -2.762096098144292800, -7.131299706077053990 ) ) ;
#53579=CARTESIAN_POINT ( 'NONE',  ( 20.00005080000000035, 3.872983346207417021, -1.000000000000000000 ) ) ;
#53587=CARTESIAN_POINT ( 'NONE',  ( 2.827825597296797167, 7.250702617666076932, -5.372687261161209094 ) ) ;
#53592=LINE ( 'NONE', #17996, #27680 ) ;
#53596=CARTESIAN_POINT ( 'NONE',  ( 1.372161826075801505, 11.20801830616751893, 5.789954543171472956 ) ) ;
#53598=CARTESIAN_POINT ( 'NONE',  ( 2.259830038564998311, -2.742210045659230211, 7.131511317046845377 ) ) ;
#53602=CARTESIAN_POINT ( 'NONE',  ( 5.515188684475870851, 0.005140903460551586937, 0.001485678338381530954 ) ) ;
#53604=CARTESIAN_POINT ( 'NONE',  ( 0.3341166715381294616, 12.03629799686217972, -2.378838837788969762 ) ) ;
#53605=CARTESIAN_POINT ( 'NONE',  ( 0.2671309869109482205, -2.286013846429945762, -12.03155065772887689 ) ) ;
#53606=ORIENTED_EDGE ( 'NONE', *, *, #15066, .F. ) ;
#53613=CARTESIAN_POINT ( 'NONE',  ( 2.241536586108914264, -1.331908602351589144, -7.517390684805882906 ) ) ;
#53614=CARTESIAN_POINT ( 'NONE',  ( 0.2648321136542700072, -9.289286523730366341, -7.979621084888208316 ) ) ;
#53616=AXIS2_PLACEMENT_3D ( 'NONE', #29591, #9987, #61181 ) ;
#53621=CARTESIAN_POINT ( 'NONE',  ( 2.705197763288547108, -7.617149697727731095, -1.627208841526538663 ) ) ;
#53622=( BOUNDED_SURFACE ( )  B_SPLINE_SURFACE ( 3, 1, ( 
 ( #36715, #62301 ),
 ( #7107, #47366 ),
 ( #17427, #6464 ),
 ( #57997, #48360 ) ),
 .UNSPECIFIED., .F., .F., .F. ) 
 B_SPLINE_SURFACE_WITH_KNOTS ( ( 4, 4 ),
 ( 2, 2 ),
 ( 0.000000000000000000, 1.000000000000000000 ),
 ( 0.000000000000000000, 1.000000000000000000 ),
 .UNSPECIFIED. ) 
 GEOMETRIC_REPRESENTATION_ITEM ( )  RATIONAL_B_SPLINE_SURFACE ( (
 ( 1.000000000000000000, 1.000000000000000000),
 ( 0.9942764183789327692, 0.8450855930916585379),
 ( 0.9942764183789327692, 0.8450855930916585379),
 ( 1.000000000000000000, 1.000000000000000000) ) ) 
 REPRESENTATION_ITEM ( '' )  SURFACE ( )  );
#53623=CARTESIAN_POINT ( 'NONE',  ( 0.3665391374699467075, 4.447929964103001232, -11.44911061034382094 ) ) ;
#53625=CARTESIAN_POINT ( 'NONE',  ( 0.2653141617321028711, 7.837919552760726383, 9.409385893408531487 ) ) ;
#53630=VERTEX_POINT ( 'NONE', #28624 ) ;
#53633=CARTESIAN_POINT ( 'NONE',  ( 0.3223008802179228027, 1.888629463821845489, -12.11889957318022404 ) ) ;
#53639=ORIENTED_EDGE ( 'NONE', *, *, #26515, .T. ) ;
#53643=CARTESIAN_POINT ( 'NONE',  ( 0.2833330754217395220, -7.719627479384596036, -9.514385791198174402 ) ) ;
#53644=CARTESIAN_POINT ( 'NONE',  ( 0.3401186441510245517, -12.03768714635923764, -2.382124782498485693 ) ) ;
#53645=ORIENTED_EDGE ( 'NONE', *, *, #23658, .F. ) ;
#53647=CARTESIAN_POINT ( 'NONE',  ( 2.665405856346676927, 9.549966053095770846, 0.5773576323838272017 ) ) ;
#53652=CARTESIAN_POINT ( 'NONE',  ( 0.2834382757447978518, -7.719209397492048375, 9.514772331577404429 ) ) ;
#53657=CARTESIAN_POINT ( 'NONE',  ( 0.2646305136544065406, -12.08286001766536621, 1.996350543472954264 ) ) ;
#53675=CARTESIAN_POINT ( 'NONE',  ( 0.6473888112830243902, 1.823007254467119198, -12.23851338376146991 ) ) ;
#53677=CARTESIAN_POINT ( 'NONE',  ( 0.3665391374699465965, -2.392238720110376970, -12.04754782681759728 ) ) ;
#53686=CARTESIAN_POINT ( 'NONE',  ( 2.990245332647680332, -6.155689586375244104, -5.834301250882039547 ) ) ;
#53707=CARTESIAN_POINT ( 'NONE',  ( 2.251139882113691648, -4.813633939919740534, -5.929826121558939178 ) ) ;
#53713=ORIENTED_EDGE ( 'NONE', *, *, #16052, .F. ) ;
#53723=CARTESIAN_POINT ( 'NONE',  ( 0.9232058338315048962, -7.723624854284649288, -9.791640253608225208 ) ) ;
#53725=ORIENTED_EDGE ( 'NONE', *, *, #1642, .F. ) ;
#53734=EDGE_CURVE ( 'NONE', #44729, #60783, #59264, .T. ) ;
#53735=CARTESIAN_POINT ( 'NONE',  ( 2.305787727787083519, -2.774453000917102230, -7.135468203930011910 ) ) ;
#53739=ORIENTED_EDGE ( 'NONE', *, *, #52547, .T. ) ;
#53742=CARTESIAN_POINT ( 'NONE',  ( 1.104777566491145890, -3.832109395972729260, 11.92547689818820800 ) ) ;
#53744=ORIENTED_EDGE ( 'NONE', *, *, #54129, .F. ) ;
#53748=CARTESIAN_POINT ( 'NONE',  ( 0.3278977287071214719, -10.49733767381177607, -6.347150352417415320 ) ) ;
#53749=DIRECTION ( 'NONE',  ( -1.000000000000000000, -0.000000000000000000, -0.000000000000000000 ) ) ;
#53752=CARTESIAN_POINT ( 'NONE',  ( 0.9232058338315058954, 3.908895078357680131, -11.84276737136196900 ) ) ;
#53754=EDGE_CURVE ( 'NONE', #62148, #15452, #22033, .T. ) ;
#53762=CARTESIAN_POINT ( 'NONE',  ( 2.653899356900333739, 4.792827201941057602, -6.118160465319149033 ) ) ;
#53764=CARTESIAN_POINT ( 'NONE',  ( 2.034671305879536263, -1.331347915349381683, -11.60021725667554193 ) ) ;
#53769=CARTESIAN_POINT ( 'NONE',  ( 5.516018279890452902, -0.001397286410094361001, 0.006629829924290971295 ) ) ;
#53774=CARTESIAN_POINT ( 'NONE',  ( 0.2653141617321010393, 12.05243138604825859, 2.169890202573236060 ) ) ;
#53780=EDGE_CURVE ( 'NONE', #807, #43133, #48906, .T. ) ;
#53781=CARTESIAN_POINT ( 'NONE',  ( 3.092491956585452506, -3.565393530441456349, 7.070043156103451132 ) ) ;
#53789=CARTESIAN_POINT ( 'NONE',  ( 5.514970785353741078, -0.003415090918276209378, -0.003262412238248218153 ) ) ;
#53793=CARTESIAN_POINT ( 'NONE',  ( 0.2676618633000466541, -11.56235835488943131, 4.037335446657195348 ) ) ;
#53795=CARTESIAN_POINT ( 'NONE',  ( 5.536195898058073439, -0.003145317580921205142, 0.007896796515810326073 ) ) ;
#53797=CARTESIAN_POINT ( 'NONE',  ( 2.241311220309555541, -7.205198716057802599, 2.523702734785320700 ) ) ;
#53800=CARTESIAN_POINT ( 'NONE',  ( 2.034671305879990566, -9.380408876023713205, 6.953089744304931763 ) ) ;
#53808=ORIENTED_EDGE ( 'NONE', *, *, #58503, .T. ) ;
#53815=CARTESIAN_POINT ( 'NONE',  ( 0.3057689695767493721, 5.928746590069732036, -10.73077184758785663 ) ) ;
#53816=CARTESIAN_POINT ( 'NONE',  ( 2.241317068080793451, 6.565357088387198559, -3.896159243838468900 ) ) ;
#53827=CARTESIAN_POINT ( 'NONE',  ( 5.514624014163232779, 0.002789935220458468652, 0.003060352188290557749 ) ) ;
#53847=CARTESIAN_POINT ( 'NONE',  ( 2.440552418640495880, -7.166505277347703817, -2.818488640081646679 ) ) ;
#53848=ORIENTED_EDGE ( 'NONE', *, *, #35444, .T. ) ;
#53850=CARTESIAN_POINT ( 'NONE',  ( 0.3401186441510243297, -0.2556125181570694238, 12.26845925752606981 ) ) ;
#53852=CARTESIAN_POINT ( 'NONE',  ( 0.2653519991613832452, 9.366979519113348474, 7.888569541500555893 ) ) ;
#53853=CARTESIAN_POINT ( 'NONE',  ( 3.092491956585984525, 5.424230976134757576, 5.768471164322518163 ) ) ;
#53858=CARTESIAN_POINT ( 'NONE',  ( 0.3675815128205894289, 2.391755495700603973, 12.04510820461660003 ) ) ;
#53864=CARTESIAN_POINT ( 'NONE',  ( 0.2646305136544072623, -6.008537389229492653, 10.67138229758227652 ) ) ;
#53866=CARTESIAN_POINT ( 'NONE',  ( 0.7400311444011713480, -8.241979373543594889, -9.270387619166411852 ) ) ;
#53877=CARTESIAN_POINT ( 'NONE',  ( 0.2671309869109512181, 9.276621593297619484, -7.995521393275721422 ) ) ;
#53878=FACE_OUTER_BOUND ( 'NONE', #30055, .T. ) ;
#53882=B_SPLINE_CURVE_WITH_KNOTS ( 'NONE', 3,
 ( #24315, #5036, #28, #44580, #4727, #64866, #14334, #24006, #9331, #29618, #49926, #24655, #45579, #13678, #24988, #45261, #65518, #10016, #54270, #8710, #30296, #28989 ),
 .UNSPECIFIED., .F., .F.,
 ( 4, 3, 3, 3, 3, 3, 3, 4 ),
 ( 1.318988870012550679E-18, 4.449119708436909988E-05, 6.626296329540551637E-05, 8.803456484962757917E-05, 0.0001098060367612809348, 0.0001315774408628539991, 0.0001760698110411219549, 0.0001829697163287831582 ),
 .UNSPECIFIED. ) ;
#53883=CARTESIAN_POINT ( 'NONE',  ( 2.247206125382828379, 7.214589497757620151, -2.502718378778734376 ) ) ;
#53886=ORIENTED_EDGE ( 'NONE', *, *, #24188, .F. ) ;
#53890=VERTEX_POINT ( 'NONE', #26263 ) ;
#53891=CARTESIAN_POINT ( 'NONE',  ( 2.994568964204213035, 7.263701055179730304, 3.069094401380807025 ) ) ;
#53897=VERTEX_POINT ( 'NONE', #31884 ) ;
#53901=CARTESIAN_POINT ( 'NONE',  ( 5.514970785353741078, 0.002619824551223704900, 0.003929719953530115030 ) ) ;
#53902=DIRECTION ( 'NONE',  ( 0.3939253465568943735, 0.9034404741085543256, 0.1691689424289857246 ) ) ;
#53906=CARTESIAN_POINT ( 'NONE',  ( 0.4613984246114872789, 11.46927345719242552, -4.475519447653872440 ) ) ;
#53912=CARTESIAN_POINT ( 'NONE',  ( 0.9232058338315058954, -12.21058493388775013, 2.536181247095325109 ) ) ;
#53916=CARTESIAN_POINT ( 'NONE',  ( 0.2739690278137266732, 12.02985305092653334, -2.307031017960325503 ) ) ;
#53917=B_SPLINE_CURVE_WITH_KNOTS ( 'NONE', 3,
 ( #48244, #2695, #42212, #58878, #47252, #22624, #12960, #33243, #52237, #57550, #63174, #17955, #13292, #23267, #1696, #27269 ),
 .UNSPECIFIED., .F., .F.,
 ( 4, 3, 3, 3, 3, 4 ),
 ( 1.908037674429563007E-15, 0.0002126834539180016254, 0.0004253519300366894536, 0.0006380165497225117992, 0.0007442707582429362130, 0.0009453531351410612241 ),
 .UNSPECIFIED. ) ;
#53918=CARTESIAN_POINT ( 'NONE',  ( 0.3474126878361887827, -2.385599230261960635, -12.03947592323248905 ) ) ;
#53919=VECTOR ( 'NONE', #56091, 1000.000000000000000 ) ;
#53928=FACE_OUTER_BOUND ( 'NONE', #38819, .T. ) ;
#53935=CARTESIAN_POINT ( 'NONE',  ( 2.440552418640498544, -7.547055375260043775, -1.531218882877369847 ) ) ;
#53936=B_SPLINE_CURVE_WITH_KNOTS ( 'NONE', 3,
 ( #8981, #60168, #29262, #49559, #3998, #19289, #15909 ),
 .UNSPECIFIED., .F., .F.,
 ( 4, 3, 4 ),
 ( 3.582791971490861909E-18, 0.002398160485434292465, 0.005002426799376466851 ),
 .UNSPECIFIED. ) ;
#53947=CARTESIAN_POINT ( 'NONE',  ( 0.3654063281920728601, 1.872466061177246344, -12.13594617907220652 ) ) ;
#53948=DIRECTION ( 'NONE',  ( -0.3865475372811021382, 0.9046932595863073079, -0.1791957239473569996 ) ) ;
#53949=CARTESIAN_POINT ( 'NONE',  ( 0.2653141334712570965, 6.161213243425262220, 10.58342934917114420 ) ) ;
#53953=VERTEX_POINT ( 'NONE', #16618 ) ;
#53962=CARTESIAN_POINT ( 'NONE',  ( 0.2655924914740778742, -11.49267051747971280, 4.229867354073519436 ) ) ;
#53967=CARTESIAN_POINT ( 'NONE',  ( 2.280717697723837922, -1.481796453660269464, -7.502592193582068525 ) ) ;
#53970=CARTESIAN_POINT ( 'NONE',  ( 2.241352910868908310, 0.08337961031704246850, 7.633946224498473931 ) ) ;
#53977=CARTESIAN_POINT ( 'NONE',  ( 3.152665057734120868, 6.378477742800529704, -4.725420687650643714 ) ) ;
#53979=CARTESIAN_POINT ( 'NONE',  ( 0.2767916011545393240, 9.504925141026355107, 7.727819755721503370 ) ) ;
#53985=ORIENTED_EDGE ( 'NONE', *, *, #37196, .F. ) ;
#53991=CARTESIAN_POINT ( 'NONE',  ( 0.2767916011545364374, -10.51265105824867696, 6.288637995698077354 ) ) ;
#53992=CARTESIAN_POINT ( 'NONE',  ( 5.516018279890452902, 0.0002248006052448508899, 0.006771744149385265123 ) ) ;
#54000=ORIENTED_EDGE ( 'NONE', *, *, #9742, .F. ) ;
#54004=CARTESIAN_POINT ( 'NONE',  ( 0.2653519890538380555, 6.776488011961817416E-18, -12.24619734961521722 ) ) ;
#54008=CARTESIAN_POINT ( 'NONE',  ( 1.372161826076962576, 5.789954543171331736, -11.20801830616803940 ) ) ;
#54013=FACE_OUTER_BOUND ( 'NONE', #20129, .T. ) ;
#54025=CARTESIAN_POINT ( 'NONE',  ( 0.3223008802179250232, 2.370176598416333213, 12.03398982086834934 ) ) ;
#54026=CARTESIAN_POINT ( 'NONE',  ( 0.2652384770603657405, -4.126289928142327312, -11.53005438969048413 ) ) ;
#54035=CARTESIAN_POINT ( 'NONE',  ( 2.241536586108912044, 7.517390684805887346, -1.331908602351562942 ) ) ;
#54037=CARTESIAN_POINT ( 'NONE',  ( 2.247112776671466694, -7.539676020705987192, -1.211104213045449018 ) ) ;
#54038=EDGE_CURVE ( 'NONE', #2298, #28421, #12928, .T. ) ;
#54043=PRODUCT ( 'straight bevel gear_iso_ISO - Straight bevel gear 0.7M 36GT 12PT 20PA 5FW ---36O12H20MD8.0S1', 'straight bevel gear_iso_ISO - Straight bevel gear 0.7M 36GT 12PT 20PA 5FW ---36O12H20MD8.0S1', '', ( #37099 ) ) ;
#54044=EDGE_CURVE ( 'NONE', #24896, #3865, #16309, .T. ) ;
#54048=ORIENTED_EDGE ( 'NONE', *, *, #46062, .F. ) ;
#54058=ORIENTED_EDGE ( 'NONE', *, *, #28208, .F. ) ;
#54060=CARTESIAN_POINT ( 'NONE',  ( 2.260457164927188511, 5.763213574030923603, -5.016645293558149810 ) ) ;
#54064=EDGE_CURVE ( 'NONE', #21980, #11179, #1457, .T. ) ;
#54068=CARTESIAN_POINT ( 'NONE',  ( 0.2646305136544065406, 12.24595685781654453, -0.1321451301298282588 ) ) ;
#54077=CARTESIAN_POINT ( 'NONE',  ( 1.719304012338831678, -5.066286238785654206, 11.67935079956403044 ) ) ;
#54081=CARTESIAN_POINT ( 'NONE',  ( 2.827825597296801163, -1.027532345921625678, -8.965636292765733373 ) ) ;
#54083=VECTOR ( 'NONE', #42535, 1000.000000000000000 ) ;
#54086=CARTESIAN_POINT ( 'NONE',  ( 2.257661810676419023, 1.459225434025981594, 7.499185766072595349 ) ) ;
#54088=VERTEX_POINT ( 'NONE', #13565 ) ;
#54089=CARTESIAN_POINT ( 'NONE',  ( 0.2652384770603652409, 12.04846497255942772, 2.191555293694015916 ) ) ;
#54096=VERTEX_POINT ( 'NONE', #43843 ) ;
#54104=CARTESIAN_POINT ( 'NONE',  ( 1.109979610368937442, 12.51859925746076208, 0.4797593171722376870 ) ) ;
#54110=CARTESIAN_POINT ( 'NONE',  ( 2.249013661412228249, -7.216565855998267942, 2.498855301843061483 ) ) ;
#54111=CARTESIAN_POINT ( 'NONE',  ( 0.3164563675027645129, -9.546944054903041987, -7.696930404785138791 ) ) ;
#54113=CARTESIAN_POINT ( 'NONE',  ( 2.305787727787085295, 7.566723232958088019, -1.164987321564654676 ) ) ;
#54115=CARTESIAN_POINT ( 'NONE',  ( 2.241526690369557429, -3.802233103835215733, 6.620271521148420213 ) ) ;
#54124=B_SPLINE_CURVE_WITH_KNOTS ( 'NONE', 3,
 ( #60957, #40991, #40004, #10723, #51321, #50658, #9739, #35664, #5772, #761, #26038, #46320, #40661, #20382, #21022, #30027 ),
 .UNSPECIFIED., .F., .F.,
 ( 4, 3, 3, 3, 3, 4 ),
 ( 2.285843118747037940E-15, 0.0002126834539180153677, 0.0004253519300367159623, 0.0006380165497225516978, 0.0007442707582429830505, 0.0009453531351407891978 ),
 .UNSPECIFIED. ) ;
#54129=EDGE_CURVE ( 'NONE', #6208, #64016, #36142, .T. ) ;
#54134=CARTESIAN_POINT ( 'NONE',  ( 2.573738926104375047, 1.575954828885357095, -7.583190312075753781 ) ) ;
#54135=CARTESIAN_POINT ( 'NONE',  ( 2.259025283528624417, -5.014999102876465997, -5.764013728791902658 ) ) ;
#54136=EDGE_CURVE ( 'NONE', #9776, #19326, #7675, .T. ) ;
#54141=ORIENTED_EDGE ( 'NONE', *, *, #18085, .T. ) ;
#54143=ORIENTED_EDGE ( 'NONE', *, *, #33394, .F. ) ;
#54148=FACE_OUTER_BOUND ( 'NONE', #62211, .T. ) ;
#54153=CARTESIAN_POINT ( 'NONE',  ( 0.2650492433740053166, 7.786978278830098077, -9.451472485870480611 ) ) ;
#54169=CARTESIAN_POINT ( 'NONE',  ( 0.2648978790185593790, -0.1321385342563263510, 12.24533305150758089 ) ) ;
#54170=CARTESIAN_POINT ( 'NONE',  ( 3.152665057735747567, 7.886634106564638813, 0.9030954876722160352 ) ) ;
#54171=CARTESIAN_POINT ( 'NONE',  ( 0.2648978790185593790, 9.295532325666449935, 7.972372351883061370 ) ) ;
#54172=CARTESIAN_POINT ( 'NONE',  ( 2.717984159220115714, 5.223388265380211948, 5.783767685176838036 ) ) ;
#54177=CARTESIAN_POINT ( 'NONE',  ( 1.719304012338834786, 2.961219984257995819, 12.38166659046419227 ) ) ;
#54182=( BOUNDED_SURFACE ( )  B_SPLINE_SURFACE ( 3, 1, ( 
 ( #27128, #11492 ),
 ( #22462, #37420 ),
 ( #57731, #52415 ),
 ( #41414, #11181 ) ),
 .UNSPECIFIED., .F., .F., .F. ) 
 B_SPLINE_SURFACE_WITH_KNOTS ( ( 4, 4 ),
 ( 2, 2 ),
 ( 0.000000000000000000, 1.000000000000000000 ),
 ( 0.000000000000000000, 1.000000000000000000 ),
 .UNSPECIFIED. ) 
 GEOMETRIC_REPRESENTATION_ITEM ( )  RATIONAL_B_SPLINE_SURFACE ( (
 ( 1.000000000000000000, 1.000000000000000000),
 ( 0.9942764183789327692, 0.8450855930916585379),
 ( 0.9942764183789327692, 0.8450855930916585379),
 ( 1.000000000000000000, 1.000000000000000000) ) ) 
 REPRESENTATION_ITEM ( '' )  SURFACE ( )  );
#54197=CARTESIAN_POINT ( 'NONE',  ( 0.3665391374699464300, 4.447929964103003009, -11.44911061034381916 ) ) ;
#54198=CARTESIAN_POINT ( 'NONE',  ( 2.241509619876138171, -5.823675573301041908, -4.936617871859563245 ) ) ;
#54199=CARTESIAN_POINT ( 'NONE',  ( 0.2648321136542701182, 12.24520788540325711, 0.1417061099915184474 ) ) ;
#54200=CARTESIAN_POINT ( 'NONE',  ( 0.2648978790185610999, 9.295532325666560070, -7.972372351882934360 ) ) ;
#54207=VECTOR ( 'NONE', #5621, 1000.000000000000000 ) ;
#54214=CARTESIAN_POINT ( 'NONE',  ( 2.241311220309555097, -7.533971938435851001, 1.234192392743148847 ) ) ;
#54221=ORIENTED_EDGE ( 'NONE', *, *, #24878, .F. ) ;
#54222=CARTESIAN_POINT ( 'NONE',  ( 2.305787727787083519, 2.461236246751071555, 7.249469779319919205 ) ) ;
#54236=EDGE_CURVE ( 'NONE', #21790, #28847, #50350, .T. ) ;
#54238=CARTESIAN_POINT ( 'NONE',  ( 2.242819959140643693, -7.138786956204143053, -2.707278038035143553 ) ) ;
#54246=B_SPLINE_CURVE_WITH_KNOTS ( 'NONE', 3,
 ( #17865, #53781, #53458, #43119, #38129, #14169, #2605, #33148, #28179, #48469, #29162, #48790, #49458, #64068, #3896, #3243 ),
 .UNSPECIFIED., .F., .F.,
 ( 4, 3, 3, 3, 3, 4 ),
 ( 2.486702240418149477E-15, 0.0002126834539179916508, 0.0004253519300366688538, 0.0006380165497224804657, 0.0007442707582428997838, 0.0009453531351413591629 ),
 .UNSPECIFIED. ) ;
#54248=CARTESIAN_POINT ( 'NONE',  ( 0.3537226245948359438, 3.952322262392388375, 11.62199823003435384 ) ) ;
#54250=CARTESIAN_POINT ( 'NONE',  ( 2.524535260911930923, -7.569872524928807245, 1.559291270914333394 ) ) ;
#54253=LINE ( 'NONE', #45246, #27968 ) ;
#54257=CARTESIAN_POINT ( 'NONE',  ( 0.8320506296491635423, 9.767350172724423629, 7.696193170530645666 ) ) ;
#54259=CARTESIAN_POINT ( 'NONE',  ( 3.152665057735899001, -7.886634106564667235, -0.9030954876721221103 ) ) ;
#54263=CARTESIAN_POINT ( 'NONE',  ( 2.241352910868909643, 3.744764251557084922, -6.652881166698471738 ) ) ;
#54266=EDGE_CURVE ( 'NONE', #47209, #12414, #54581, .T. ) ;
#54268=AXIS2_PLACEMENT_3D ( 'NONE', #50114, #56063, #4571 ) ;
#54270=CARTESIAN_POINT ( 'NONE',  ( 0.3610902822527252698, -12.13436647668549462, -1.873269382026117924 ) ) ;
#54289=CARTESIAN_POINT ( 'NONE',  ( 0.2653519789438759657, -12.24619733037255997, 0.02203059356484748585 ) ) ;
#54293=ORIENTED_EDGE ( 'NONE', *, *, #56996, .T. ) ;
#54295=CARTESIAN_POINT ( 'NONE',  ( 0.2648321136542706178, -7.762514728658031160, -9.471460387169347683 ) ) ;
#54296=EDGE_CURVE ( 'NONE', #42715, #58005, #44877, .T. ) ;
#54300=CARTESIAN_POINT ( 'NONE',  ( 5.516018279890452902, 0.0009545156522407046611, 0.006707902355169304519 ) ) ;
#54304=DIRECTION ( 'NONE',  ( 0.000000000000000000, 0.000000000000000000, 1.000000000000000000 ) ) ;
#54308=VERTEX_POINT ( 'NONE', #31489 ) ;
#54309=CARTESIAN_POINT ( 'NONE',  ( 0.2638984909335720941, 5.950360275955205225, -10.70468911391657940 ) ) ;
#54312=CARTESIAN_POINT ( 'NONE',  ( 0.2739690278137258961, -6.282352088166191173, -10.51531306167493085 ) ) ;
#54315=CARTESIAN_POINT ( 'NONE',  ( 0.2671309869109484980, 4.036029264453140364, -11.56263543972754704 ) ) ;
#54319=AXIS2_PLACEMENT_3D ( 'NONE', #14572, #64791, #44856 ) ;
#54321=CARTESIAN_POINT ( 'NONE',  ( 0.2651627682582921586, -11.47719223137562850, 4.271106202749230363 ) ) ;
#54328=B_SPLINE_CURVE_WITH_KNOTS ( 'NONE', 3,
 ( #42612, #12046, #32324, #3417, #23686, #47629, #62571 ),
 .UNSPECIFIED., .F., .F.,
 ( 4, 3, 4 ),
 ( 4.934630583344367301E-15, 0.002398160485434615557, 0.005002426799381651940 ),
 .UNSPECIFIED. ) ;
#54332=CARTESIAN_POINT ( 'NONE',  ( 1.719304012338199517, 1.559079228025238604E-15, 12.73084802173761787 ) ) ;
#54338=CARTESIAN_POINT ( 'NONE',  ( 0.2911222467163553929, 10.71854909364326325, -5.940753417478811471 ) ) ;
#54379=CARTESIAN_POINT ( 'NONE',  ( 0.2653141617321040924, 6.161204121352837682, -10.58343467791289072 ) ) ;
#54382=CARTESIAN_POINT ( 'NONE',  ( 2.263328370261528555, -7.548992860189814635, -1.186889399881268181 ) ) ;
#54390=EDGE_LOOP ( 'NONE', ( #24800, #37707, #35095, #48576 ) ) ;
#54396=DIRECTION ( 'NONE',  ( 0.000000000000000000, 0.000000000000000000, 1.000000000000000000 ) ) ;
#54398=CARTESIAN_POINT ( 'NONE',  ( 2.242418902651536428, 5.912154560269232917, 4.830735119002372180 ) ) ;
#54401=( BOUNDED_SURFACE ( )  B_SPLINE_SURFACE ( 3, 1, ( 
 ( #40751, #50737 ),
 ( #46717, #21456 ),
 ( #9825, #21109 ),
 ( #41727, #46083 ) ),
 .UNSPECIFIED., .F., .F., .F. ) 
 B_SPLINE_SURFACE_WITH_KNOTS ( ( 4, 4 ),
 ( 2, 2 ),
 ( 0.000000000000000000, 1.000000000000000000 ),
 ( 0.000000000000000000, 1.000000000000000000 ),
 .UNSPECIFIED. ) 
 GEOMETRIC_REPRESENTATION_ITEM ( )  RATIONAL_B_SPLINE_SURFACE ( (
 ( 1.000000000000000000, 1.000000000000000000),
 ( 0.9942764183789327692, 0.8450855930916580938),
 ( 0.9942764183789327692, 0.8450855930916580938),
 ( 1.000000000000000000, 1.000000000000000000) ) ) 
 REPRESENTATION_ITEM ( '' )  SURFACE ( )  );
#54403=B_SPLINE_CURVE_WITH_KNOTS ( 'NONE', 3,
 ( #24161, #10175, #29787, #50104, #35096, #59748, #30456, #14811, #14493, #14177, #60388, #35753, #24828, #54770, #3904, #15487 ),
 .UNSPECIFIED., .F., .F.,
 ( 4, 3, 3, 3, 3, 4 ),
 ( 0.000000000000000000, 0.0002999043160757219450, 0.0005998071753050750882, 0.0008997092107374163967, 0.001204458948194988069, 0.001510329163475231757 ),
 .UNSPECIFIED. ) ;
#54409=CARTESIAN_POINT ( 'NONE',  ( 0.3537226245948383863, 0.2609894354291231178, -12.27287980220284425 ) ) ;
#54416=CARTESIAN_POINT ( 'NONE',  ( 2.255723233588950105, 3.933511348457526591, -6.548644987607518786 ) ) ;
#54420=CARTESIAN_POINT ( 'NONE',  ( 3.092491956585849522, 4.738927301402013903, -6.343509225035191434 ) ) ;
#54421=CARTESIAN_POINT ( 'NONE',  ( -14.47334165536100059, 5.400000000000000355, 0.000000000000000000 ) ) ;
#54441=CARTESIAN_POINT ( 'NONE',  ( 2.288423627607476973, -2.464337058688807147, 7.242304196986142806 ) ) ;
#54442=CARTESIAN_POINT ( 'NONE',  ( 1.452237505248552996, -0.5922625322517893753, 12.64182585313125884 ) ) ;
#54451=CARTESIAN_POINT ( 'NONE',  ( 0.2676618633000448777, -7.994628339664874517, 9.277614237849251211 ) ) ;
#54455=CARTESIAN_POINT ( 'NONE',  ( 0.4613984246114871679, 12.07219521825823527, -2.415907815801280556 ) ) ;
#54465=ORIENTED_EDGE ( 'NONE', *, *, #59118, .T. ) ;
#54467=VERTEX_POINT ( 'NONE', #8845 ) ;
#54470=CARTESIAN_POINT ( 'NONE',  ( 1.937114397841932290, 3.531416430611295620, 12.33981801388259036 ) ) ;
#54475=ORIENTED_EDGE ( 'NONE', *, *, #20480, .F. ) ;
#54478=CARTESIAN_POINT ( 'NONE',  ( 3.152665057734040488, 0.000000000000000000, 0.000000000000000000 ) ) ;
#54481=ORIENTED_EDGE ( 'NONE', *, *, #45906, .F. ) ;
#54482=ORIENTED_EDGE ( 'NONE', *, *, #58278, .T. ) ;
#54485=CARTESIAN_POINT ( 'NONE',  ( 0.2958664285830415741, 10.50235171906349585, -6.318165763623519560 ) ) ;
#54490=CARTESIAN_POINT ( 'NONE',  ( 2.034671305879988346, -2.716450156984129283, 11.35598636043403609 ) ) ;
#54492=CARTESIAN_POINT ( 'NONE',  ( 0.2653519991613819684, -9.395283368383228861, 7.854838327448937285 ) ) ;
#54493=CARTESIAN_POINT ( 'NONE',  ( 2.941278708680199916, -2.952340773940147045, 5.383216837018931500 ) ) ;
#54495=CARTESIAN_POINT ( 'NONE',  ( 0.4626703367448398718, 0.2831487465615306620, -12.30872794628584188 ) ) ;
#54496=CARTESIAN_POINT ( 'NONE',  ( 2.717984159219702267, -4.139692542159338018, -6.602931111513714590 ) ) ;
#54498=CARTESIAN_POINT ( 'NONE',  ( 1.948354844646999817, -11.94326855455517489, 0.7204626209692002181 ) ) ;
#54500=EDGE_CURVE ( 'NONE', #43254, #20748, #17085, .T. ) ;
#54506=CARTESIAN_POINT ( 'NONE',  ( 2.990245332647743393, 7.075286609974440033, 4.676740826320128441 ) ) ;
#54507=CARTESIAN_POINT ( 'NONE',  ( 2.242819959140646802, -7.500446639314762187, -1.426511055719384302 ) ) ;
#54508=CARTESIAN_POINT ( 'NONE',  ( 0.3665391374699465965, 1.872534962004961834, -12.13918562134716694 ) ) ;
#54515=CARTESIAN_POINT ( 'NONE',  ( 5.514970785353741078, -0.004532877335078326457, 0.001326349372336564462 ) ) ;
#54528=CARTESIAN_POINT ( 'NONE',  ( 2.430348790456849262, 5.769383131055064950, -5.095533593439648179 ) ) ;
#54531=CARTESIAN_POINT ( 'NONE',  ( 2.889800649504073782, -3.882893708502015429, -4.732281052280351119 ) ) ;
#54537=CARTESIAN_POINT ( 'NONE',  ( 2.288423627607356625, 5.039850887180204353, 5.755330594804989097 ) ) ;
#54540=CARTESIAN_POINT ( 'NONE',  ( 1.937114397841932290, -11.72279974487460130, -5.226660192101706848 ) ) ;
#54542=CARTESIAN_POINT ( 'NONE',  ( 0.3675815128205912052, -12.27743992903065973, -0.2638082659429707988 ) ) ;
#54547=ORIENTED_EDGE ( 'NONE', *, *, #63485, .T. ) ;
#54548=CARTESIAN_POINT ( 'NONE',  ( 0.8320506296491578802, -2.535206712041371713, -12.17395768195219397 ) ) ;
#54556=LINE ( 'NONE', #23965, #26946 ) ;
#54576=ORIENTED_EDGE ( 'NONE', *, *, #63549, .T. ) ;
#54577=CARTESIAN_POINT ( 'NONE',  ( 2.305787727787083519, -7.135468203929965725, -2.774453000917220802 ) ) ;
#54581=CIRCLE ( 'NONE', #56718, 7.938172270156617749 ) ;
#54586=CARTESIAN_POINT ( 'NONE',  ( 5.514970785353741078, 0.003415090918276187260, 0.003262412238248241138 ) ) ;
#54593=( BOUNDED_SURFACE ( )  B_SPLINE_SURFACE ( 3, 1, ( 
 ( #46570, #40932 ),
 ( #61212, #15640 ),
 ( #20960, #61863 ),
 ( #1027, #21293 ) ),
 .UNSPECIFIED., .F., .F., .F. ) 
 B_SPLINE_SURFACE_WITH_KNOTS ( ( 4, 4 ),
 ( 2, 2 ),
 ( 0.000000000000000000, 1.000000000000000000 ),
 ( 0.000000000000000000, 1.000000000000000000 ),
 .UNSPECIFIED. ) 
 GEOMETRIC_REPRESENTATION_ITEM ( )  RATIONAL_B_SPLINE_SURFACE ( (
 ( 1.000000000000000000, 1.000000000000000000),
 ( 0.6933888150995267674, 0.9895912004443193632),
 ( 0.6933888150995267674, 0.9895912004443193632),
 ( 1.000000000000000000, 1.000000000000000000) ) ) 
 REPRESENTATION_ITEM ( '' )  SURFACE ( )  );
#54598=CARTESIAN_POINT ( 'NONE',  ( 0.2869720083484378348, -9.251312689958709257, -8.034871682535190018 ) ) ;
#54604=CARTESIAN_POINT ( 'NONE',  ( 2.903928887688894012, -2.041797854846922000, -8.528865300110647141 ) ) ;
#54608=CONICAL_SURFACE ( 'NONE', #39723, 7.938172270156617749, 1.280189991382167047 ) ;
#54609=EDGE_CURVE ( 'NONE', #46591, #35774, #25801, .T. ) ;
#54611=CARTESIAN_POINT ( 'NONE',  ( 2.639814597422736497, -5.186391178752170816, 5.782006333156054723 ) ) ;
#54629=CARTESIAN_POINT ( 'NONE',  ( 2.262775599887389966, -1.187656132454015578, -7.548684916005413470 ) ) ;
#54633=CARTESIAN_POINT ( 'NONE',  ( 0.3218525148189841922, -7.695007528464951285, -9.550803867331140395 ) ) ;
#54636=CARTESIAN_POINT ( 'NONE',  ( 2.507146904658096975, 5.774795220010187968, 5.128007631637082397 ) ) ;
#54638=CARTESIAN_POINT ( 'NONE',  ( 0.2706063244538052248, 10.51833723927421538, 6.275112929891649927 ) ) ;
#54652=CARTESIAN_POINT ( 'NONE',  ( 0.3610902822527226053, 3.951920836718878505, -11.62472836966319178 ) ) ;
#54656=CARTESIAN_POINT ( 'NONE',  ( 0.2651627923886342164, -11.53745192040745238, 4.105544202112507257 ) ) ;
#54658=CARTESIAN_POINT ( 'NONE',  ( 0.3675815128205912052, -3.951233083390393030, -11.62724744438069635 ) ) ;
#54664=ORIENTED_EDGE ( 'NONE', *, *, #64171, .F. ) ;
#54668=CARTESIAN_POINT ( 'NONE',  ( 0.3040950598368144520, -11.43390362554250395, -4.428852722102847750 ) ) ;
#54672=CARTESIAN_POINT ( 'NONE',  ( 0.3053067050349155820, 10.73055518945195352, -5.928821939311815115 ) ) ;
#54674=ORIENTED_EDGE ( 'NONE', *, *, #14415, .F. ) ;
#54675=CARTESIAN_POINT ( 'NONE',  ( 2.665405856346786173, -6.944580094494293476, -6.580881457836790460 ) ) ;
#54683=DIRECTION ( 'NONE',  ( 0.000000000000000000, 0.000000000000000000, -1.000000000000000000 ) ) ;
#54684=CARTESIAN_POINT ( 'NONE',  ( 0.3675815128205894289, -12.27743992903066328, 0.2638082659427993804 ) ) ;
#54686=EDGE_CURVE ( 'NONE', #52583, #49787, #38523, .T. ) ;
#54689=LINE ( 'NONE', #61288, #1185 ) ;
#54690=AXIS2_PLACEMENT_3D ( 'NONE', #59012, #38034, #38372 ) ;
#54693=CARTESIAN_POINT ( 'NONE',  ( 2.941278708680199916, -3.185832147968484573, 5.248410529370215016 ) ) ;
#54701=ORIENTED_EDGE ( 'NONE', *, *, #47530, .T. ) ;
#54709=CARTESIAN_POINT ( 'NONE',  ( 2.241352910868908310, 0.08337961031704246850, 7.633946224498473931 ) ) ;
#54710=CARTESIAN_POINT ( 'NONE',  ( 2.241526690369556540, -7.634439869182789273, 0.01730530154274034782 ) ) ;
#54723=CARTESIAN_POINT ( 'NONE',  ( 0.3665391374699467075, -12.04754782681756176, -2.392238720110582584 ) ) ;
#54728=CARTESIAN_POINT ( 'NONE',  ( 0.2648978790185602672, -12.03635331166813494, 2.256510822326103671 ) ) ;
#54733=CARTESIAN_POINT ( 'NONE',  ( 0.3218525148189821938, -10.49750909897047713, -6.342972338926902154 ) ) ;
#54736=CARTESIAN_POINT ( 'NONE',  ( 2.034671305879936831, -11.35598636043418885, -2.716450156984207442 ) ) ;
#54751=CARTESIAN_POINT ( 'NONE',  ( 2.241537034860906275, 5.851376807350209042, -4.903726641589465807 ) ) ;
#54755=CARTESIAN_POINT ( 'NONE',  ( 0.2648978790185593790, 12.08224454301448958, 1.996248716311670446 ) ) ;
#54756=CARTESIAN_POINT ( 'NONE',  ( 0.3040950598368144520, -12.02925914197703605, -2.376091969481339827 ) ) ;
#54759=VECTOR ( 'NONE', #61848, 1000.000000000000000 ) ;
#54761=CARTESIAN_POINT ( 'NONE',  ( 2.835339799623983748, -6.612744557053408023, -4.197472173747776480 ) ) ;
#54763=( BOUNDED_SURFACE ( )  B_SPLINE_SURFACE ( 3, 1, ( 
 ( #34758, #3891 ),
 ( #35431, #30443 ),
 ( #34455, #54756 ),
 ( #24470, #30124 ) ),
 .UNSPECIFIED., .F., .F., .F. ) 
 B_SPLINE_SURFACE_WITH_KNOTS ( ( 4, 4 ),
 ( 2, 2 ),
 ( 0.000000000000000000, 1.000000000000000000 ),
 ( 0.000000000000000000, 1.000000000000000000 ),
 .UNSPECIFIED. ) 
 GEOMETRIC_REPRESENTATION_ITEM ( )  RATIONAL_B_SPLINE_SURFACE ( (
 ( 1.000000000000000000, 1.000000000000000000),
 ( 0.9942764183789327692, 0.8450855930916580938),
 ( 0.9942764183789327692, 0.8450855930916580938),
 ( 1.000000000000000000, 1.000000000000000000) ) ) 
 REPRESENTATION_ITEM ( '' )  SURFACE ( )  );
#54765=CARTESIAN_POINT ( 'NONE',  ( 2.273267844204864385, -2.472013099045079709, 7.234348261136797298 ) ) ;
#54767=B_SPLINE_CURVE_WITH_KNOTS ( 'NONE', 3,
 ( #37512, #47186, #1942, #21904, #11265, #63109, #31533, #7239, #62133, #6285, #53136, #1631, #7580, #958, #17572, #46506 ),
 .UNSPECIFIED., .F., .F.,
 ( 4, 3, 3, 3, 3, 4 ),
 ( 0.000000000000000000, 0.0002999043160757369070, 0.0005998071753051058795, 0.0008997092107374633427, 0.001204458948196129951, 0.001510329163477479742 ),
 .UNSPECIFIED. ) ;
#54770=CARTESIAN_POINT ( 'NONE',  ( 0.5572780756280709680, -6.434474476007936872, 10.53376864352695996 ) ) ;
#54773=CARTESIAN_POINT ( 'NONE',  ( 0.2657645697724698164, -7.987126944299682840, 9.283243433323047356 ) ) ;
#54781=CARTESIAN_POINT ( 'NONE',  ( 3.152665057734040488, 0.000000000000000000, 0.000000000000000000 ) ) ;
#54783=CARTESIAN_POINT ( 'NONE',  ( 2.258463476536646031, 7.546439757228825762, -1.192666169132556186 ) ) ;
#54784=CARTESIAN_POINT ( 'NONE',  ( 2.241449424704146764, -3.763973574060585747, 6.642105568284094375 ) ) ;
#54786=CARTESIAN_POINT ( 'NONE',  ( 2.241352910868908310, 1.243507963608194045, -7.532448145350496560 ) ) ;
#54789=CARTESIAN_POINT ( 'NONE',  ( 1.719304012339819332, -8.755325027794356174, 9.242227816401850760 ) ) ;
#54796=EDGE_CURVE ( 'NONE', #37474, #25513, #62302, .T. ) ;
#54809=ADVANCED_FACE ( 'NONE', ( #15654 ), #7556, .F. ) ;
#54827=CARTESIAN_POINT ( 'NONE',  ( 2.251139882113958546, -7.499076289418093566, -1.448366094935489734 ) ) ;
#54829=CARTESIAN_POINT ( 'NONE',  ( 0.2651627923886298865, -12.07509237025072757, 2.039714259676136177 ) ) ;
#54830=CARTESIAN_POINT ( 'NONE',  ( 2.298277635560276533, -6.709004959608396490, 3.682855706290112163 ) ) ;
#54835=CARTESIAN_POINT ( 'NONE',  ( 1.014383007554948701, 2.605923236272134069, 12.22116704270659326 ) ) ;
#54845=EDGE_CURVE ( 'NONE', #14040, #61553, #20673, .T. ) ;
#54852=CARTESIAN_POINT ( 'NONE',  ( 0.3053067050349166922, 12.25734436043224918, 0.2307671807672694586 ) ) ;
#54854=B_SPLINE_CURVE_WITH_KNOTS ( 'NONE', 3,
 ( #59790, #14530, #34810, #55114, #9543, #19874, #3942, #29834, #4602, #50147, #40134, #60432, #14853, #35142, #4923, #55452 ),
 .UNSPECIFIED., .F., .F.,
 ( 4, 3, 3, 3, 3, 4 ),
 ( 1.563658610346375187E-18, 0.0002176109881720206360, 0.0004352086762394547577, 0.0006528017811446803521, 0.0007615147961451621938, 0.0009453342004947411833 ),
 .UNSPECIFIED. ) ;
#54859=VERTEX_POINT ( 'NONE', #35620 ) ;
#54864=ORIENTED_EDGE ( 'NONE', *, *, #5525, .T. ) ;
#54867=CARTESIAN_POINT ( 'NONE',  ( 5.514970785353741078, -0.003262412238248251547, 0.003415090918276177286 ) ) ;
#54881=ADVANCED_FACE ( 'NONE', ( #6362 ), #35509, .T. ) ;
#54884=CARTESIAN_POINT ( 'NONE',  ( 2.262775599886256206, -7.131180968652209629, -2.745802076335803310 ) ) ;
#54889=CARTESIAN_POINT ( 'NONE',  ( 0.2956976708475431703, -10.72256944221091146, 5.936640677855330672 ) ) ;
#54891=CARTESIAN_POINT ( 'NONE',  ( 2.288423627607474753, -6.704349683466392484, -3.684511167348268668 ) ) ;
#54893=VERTEX_POINT ( 'NONE', #56577 ) ;
#54894=CARTESIAN_POINT ( 'NONE',  ( 2.288423627607479194, -7.648392725410194437, 0.1612945702821492744 ) ) ;
#54898=CARTESIAN_POINT ( 'NONE',  ( 1.194176325881342704, 9.940715479868448057, 7.670099510969100365 ) ) ;
#54899=LINE ( 'NONE', #9653, #61109 ) ;
#54900=CARTESIAN_POINT ( 'NONE',  ( 0.3278977287071226931, -9.235688435081675252, -8.073566434006671955 ) ) ;
#54910=CARTESIAN_POINT ( 'NONE',  ( 5.536195898058073439, 0.004468797463753786288, -0.007230647766619106506 ) ) ;
#54913=B_SPLINE_CURVE_WITH_KNOTS ( 'NONE', 3,
 ( #50534, #4977, #44212, #49552, #55170, #9953, #30548, #15264, #59510, #19281, #19619, #34233, #40529, #39217, #39880, #54542 ),
 .UNSPECIFIED., .F., .F.,
 ( 4, 3, 3, 3, 3, 4 ),
 ( 0.000000000000000000, 0.0002999043160757325702, 0.0005998071753050972059, 0.0008997092107374515249, 0.001204458948195627748, 0.001510329163476482276 ),
 .UNSPECIFIED. ) ;
#54919=CARTESIAN_POINT ( 'NONE',  ( 0.2653519890518172830, 6.123106317427155609, 10.60551359205152089 ) ) ;
#54926=EDGE_CURVE ( 'NONE', #19720, #24646, #56918, .T. ) ;
#54927=B_SPLINE_CURVE_WITH_KNOTS ( 'NONE', 3,
 ( #31495, #46790, #60440, #1902, #57110, #53439, #43102, #22511, #62094, #47781, #22850, #2581, #62722, #37467, #16853, #27480 ),
 .UNSPECIFIED., .F., .F.,
 ( 4, 3, 3, 3, 3, 4 ),
 ( 3.247553071957733784E-15, 0.0002126834539179960960, 0.0004253519300366789910, 0.0006380165497224953193, 0.0007442707582429170226, 0.0009453531351412618015 ),
 .UNSPECIFIED. ) ;
#54930=CARTESIAN_POINT ( 'NONE',  ( 0.3057689695767478177, -9.241339546505145108, 8.055876362038318916 ) ) ;
#54941=VERTEX_POINT ( 'NONE', #32580 ) ;
#54942=CARTESIAN_POINT ( 'NONE',  ( 0.9296196016835478471, -9.812579935705070255, 7.691217109781775640 ) ) ;
#54946=CARTESIAN_POINT ( 'NONE',  ( 1.937114397841932290, -8.920887662793532513, 9.228205347192421470 ) ) ;
#54959=EDGE_CURVE ( 'NONE', #20105, #11073, #55956, .T. ) ;
#54964=CARTESIAN_POINT ( 'NONE',  ( 0.2653519890538380555, 6.776488011961817416E-18, -12.24619734961521722 ) ) ;
#54967=CARTESIAN_POINT ( 'NONE',  ( 2.276905613632199454, 7.236369456722091087, 2.469846004796125261 ) ) ;
#54982=CARTESIAN_POINT ( 'NONE',  ( 2.259830038565000976, 6.684701880279376063, -3.700395974956069090 ) ) ;
#54983=CARTESIAN_POINT ( 'NONE',  ( 0.2646305136544065406, -11.46223899740603258, 4.312539723326095142 ) ) ;
#54991=VERTEX_POINT ( 'NONE', #51036 ) ;
#54994=FACE_OUTER_BOUND ( 'NONE', #18323, .T. ) ;
#54997=DIRECTION ( 'NONE',  ( -1.000000000000000000, -0.000000000000000000, -0.000000000000000000 ) ) ;
#54999=EDGE_CURVE ( 'NONE', #6075, #22574, #46404, .T. ) ;
#55005=CARTESIAN_POINT ( 'NONE',  ( 1.198791140419046553, -12.26651935498936119, -2.686891236233052371 ) ) ;
#55006=CARTESIAN_POINT ( 'NONE',  ( 0.2653519789438752996, 6.104019611498720188, -10.61653328464220891 ) ) ;
#55011=CARTESIAN_POINT ( 'NONE',  ( 2.241528039335007438, -7.634443721858079179, -0.01573255094249829955 ) ) ;
#55022=CARTESIAN_POINT ( 'NONE',  ( 2.177405672432191963, 8.997150696567555173, 6.668684901897946382 ) ) ;
#55026=ORIENTED_EDGE ( 'NONE', *, *, #7460, .T. ) ;
#55030=ORIENTED_EDGE ( 'NONE', *, *, #41402, .F. ) ;
#55035=CARTESIAN_POINT ( 'NONE',  ( 2.263328370261531663, -7.499672967744978713, 1.466596409249135036 ) ) ;
#55039=ADVANCED_FACE ( 'NONE', ( #812 ), #15343, .F. ) ;
#55048=CARTESIAN_POINT ( 'NONE',  ( 2.556980015514111582, 4.795979673457668291, -6.074557383032923141 ) ) ;
#55057=CARTESIAN_POINT ( 'NONE',  ( 1.719304012338833676, 5.066286238785588480, 11.67935079956406597 ) ) ;
#55059=CARTESIAN_POINT ( 'NONE',  ( 0.2653519890518182822, 12.06015162724940737, 2.126521162241097329 ) ) ;
#55060=FACE_OUTER_BOUND ( 'NONE', #43715, .T. ) ;
#55065=CARTESIAN_POINT ( 'NONE',  ( 1.194176325881345591, -4.773862381874661054, -11.61285876598811129 ) ) ;
#55069=CARTESIAN_POINT ( 'NONE',  ( 2.241449424704146320, 7.634218943782391520, -0.06135604983230691367 ) ) ;
#55070=CARTESIAN_POINT ( 'NONE',  ( 2.705197763288466728, 6.601241161176674588, 4.134294772209909929 ) ) ;
#55077=EDGE_CURVE ( 'NONE', #13985, #22233, #9892, .T. ) ;
#55079=CARTESIAN_POINT ( 'NONE',  ( 1.198791140417290624, 12.54673713002838120, 0.5160125886320254818 ) ) ;
#55080=CARTESIAN_POINT ( 'NONE',  ( 0.3632410797595219121, -11.44577450250090145, 4.445654054452488069 ) ) ;
#55081=CARTESIAN_POINT ( 'NONE',  ( 1.547277799341818305, 12.34637640861389940, -2.861188171560576698 ) ) ;
#55082=VERTEX_POINT ( 'NONE', #57330 ) ;
#55088=CARTESIAN_POINT ( 'NONE',  ( 2.244591118396556340, 7.537402265771630638, 1.219892024449276802 ) ) ;
#55090=EDGE_LOOP ( 'NONE', ( #33971, #32163, #28581, #42720 ) ) ;
#55096=CARTESIAN_POINT ( 'NONE',  ( 2.080613030138687147, 0.000000000000000000, -7.580821595991582562 ) ) ;
#55098=CARTESIAN_POINT ( 'NONE',  ( 5.516018279890452902, -0.006629829924290984305, -0.001397286410094293998 ) ) ;
#55107=ORIENTED_EDGE ( 'NONE', *, *, #18318, .T. ) ;
#55110=CARTESIAN_POINT ( 'NONE',  ( 0.2638984909335716500, -8.023974293733243002, 9.252728947331050335 ) ) ;
#55114=CARTESIAN_POINT ( 'NONE',  ( 2.507146904658096087, -4.047319006787518880, 6.577532285019752401 ) ) ;
#55120=CARTESIAN_POINT ( 'NONE',  ( 2.665405856346783509, -2.226920474533445216, 9.304623509366210854 ) ) ;
#55132=CARTESIAN_POINT ( 'NONE',  ( 0.2801149460245120348, 0.1962575296605416630, 12.24954625471156788 ) ) ;
#55138=CARTESIAN_POINT ( 'NONE',  ( 2.241526690369556540, -4.894066724724294382, 5.859443871527027170 ) ) ;
#55143=CARTESIAN_POINT ( 'NONE',  ( 2.781367136451822653, 2.381060477055604530, -7.442815111163104014 ) ) ;
#55145=CARTESIAN_POINT ( 'NONE',  ( 1.459561108992817546, 2.815016945600459675, 12.32692860927455492 ) ) ;
#55154=CARTESIAN_POINT ( 'NONE',  ( 0.3006302518452033667, -0.2259616664571391098, -12.25587491745529967 ) ) ;
#55164=CARTESIAN_POINT ( 'NONE',  ( 2.241352910868908754, 7.503490710578232914, 1.407733736974891681 ) ) ;
#55166=CARTESIAN_POINT ( 'NONE',  ( 5.520433897694421610, -0.009283255140285535598, 0.01186170453199870446 ) ) ;
#55167=LINE ( 'NONE', #39215, #61932 ) ;
#55168=CARTESIAN_POINT ( 'NONE',  ( 2.034671305879985237, -6.436604249850708115, 9.742055912616539359 ) ) ;
#55170=CARTESIAN_POINT ( 'NONE',  ( 1.375507693218805505, -12.60244951981748507, -0.5913006932462674392 ) ) ;
#55176=ORIENTED_EDGE ( 'NONE', *, *, #50916, .F. ) ;
#55177=CARTESIAN_POINT ( 'NONE',  ( 1.283627346226853927, -2.725559306499029777, -12.28700367512553804 ) ) ;
#55180=ORIENTED_EDGE ( 'NONE', *, *, #29881, .T. ) ;
#55203=CARTESIAN_POINT ( 'NONE',  ( 2.251139882113693425, -2.495216312515288415, -7.218573619021111831 ) ) ;
#55211=CARTESIAN_POINT ( 'NONE',  ( 0.2638984909335720941, -12.09426044257623012, -1.930290337334179984 ) ) ;
#55212=CARTESIAN_POINT ( 'NONE',  ( 2.242418902651939661, -6.661183998167568454, -3.730710532463432649 ) ) ;
#55213=VECTOR ( 'NONE', #63746, 1000.000000000000000 ) ;
#55220=CARTESIAN_POINT ( 'NONE',  ( 0.2915757698887297411, 10.71881693660621870, 5.940579417090813941 ) ) ;
#55223=CARTESIAN_POINT ( 'NONE',  ( 2.245754705088263137, -3.721112460997302751, -6.667819336165746513 ) ) ;
#55227=CARTESIAN_POINT ( 'NONE',  ( 0.3675815128205894289, 5.910255304480596550, -10.76447900494934196 ) ) ;
#55233=CARTESIAN_POINT ( 'NONE',  ( 3.047904605210424833, -5.398304302092578055, 5.772373816836799953 ) ) ;
#55234=EDGE_CURVE ( 'NONE', #1325, #23499, #16131, .T. ) ;
#55235=CARTESIAN_POINT ( 'NONE',  ( 0.9232058338315058954, 11.58467545991560144, -4.617996777200457537 ) ) ;
#55241=AXIS2_PLACEMENT_3D ( 'NONE', #16063, #1114, #41328 ) ;
#55246=DIRECTION ( 'NONE',  ( -1.000000000000000000, 0.000000000000000000, 0.000000000000000000 ) ) ;
#55249=ORIENTED_EDGE ( 'NONE', *, *, #17818, .F. ) ;
#55253=CARTESIAN_POINT ( 'NONE',  ( 2.994568964204215700, 3.069094401380881187, -7.263701055179695665 ) ) ;
#55255=CARTESIAN_POINT ( 'NONE',  ( 2.907497136250889902, 3.613027414876690546, -6.976431712756583359 ) ) ;
#55258=LINE ( 'NONE', #40621, #13451 ) ;
#55265=ORIENTED_EDGE ( 'NONE', *, *, #29215, .T. ) ;
#55273=CARTESIAN_POINT ( 'NONE',  ( 0.4613984246114886112, -6.399144685811640976, -10.51786362586221024 ) ) ;
#55276=CARTESIAN_POINT ( 'NONE',  ( 2.244591118396559004, 5.779440292195835660, -4.989853642775266884 ) ) ;
#55284=ORIENTED_EDGE ( 'NONE', *, *, #36174, .T. ) ;
#55286=CARTESIAN_POINT ( 'NONE',  ( 0.3006302518452025341, 8.051021221755775059, 9.243299516615051559 ) ) ;
#55290=CARTESIAN_POINT ( 'NONE',  ( 2.263328370259788169, 7.228205514765998707, 2.479726736365276185 ) ) ;
#55298=CARTESIAN_POINT ( 'NONE',  ( 1.375507693217489891, 12.30831170622553650, 2.770709900325457831 ) ) ;
#55307=EDGE_CURVE ( 'NONE', #35243, #21572, #27185, .T. ) ;
#55311=EDGE_CURVE ( 'NONE', #5064, #35179, #49487, .T. ) ;
#55313=CARTESIAN_POINT ( 'NONE',  ( 2.247206125382829267, 6.670391186503692893, -3.717496781928021132 ) ) ;
#55319=LINE ( 'NONE', #9761, #34059 ) ;
#55322=CARTESIAN_POINT ( 'NONE',  ( 2.941278708680199916, -6.068329152486370504, -0.9331242451665616722 ) ) ;
#55325=CARTESIAN_POINT ( 'NONE',  ( 0.9232058338315058954, 5.905985151448303938, -10.98407661738922592 ) ) ;
#55338=CARTESIAN_POINT ( 'NONE',  ( 0.2648978790185619880, 6.008231198269132989, -10.67083876753485328 ) ) ;
#55340=CARTESIAN_POINT ( 'NONE',  ( 0.2653519991613827456, 4.209134909048904305, -11.50013121838203745 ) ) ;
#55346=CARTESIAN_POINT ( 'NONE',  ( 2.241449424704146764, -7.634218943782393296, 0.06135604983225357439 ) ) ;
#55349=ORIENTED_EDGE ( 'NONE', *, *, #53131, .F. ) ;
#55357=DIRECTION ( 'NONE',  ( 1.000000000000000000, 0.000000000000000000, 0.000000000000000000 ) ) ;
#55358=CARTESIAN_POINT ( 'NONE',  ( 1.462291587748811850, -2.816455204775985433, 12.32753368892814905 ) ) ;
#55359=CARTESIAN_POINT ( 'NONE',  ( 2.269879328255102635, 5.949827370242536162, 4.798845682294834880 ) ) ;
#55361=ORIENTED_EDGE ( 'NONE', *, *, #54845, .T. ) ;
#55380=CARTESIAN_POINT ( 'NONE',  ( 2.263328370261526779, 7.499672967744992036, -1.466596409249078636 ) ) ;
#55392=CARTESIAN_POINT ( 'NONE',  ( 2.440552418640498100, -0.1974238147509794761, 7.698292014589399379 ) ) ;
#55393=FACE_OUTER_BOUND ( 'NONE', #6552, .T. ) ;
#55394=CARTESIAN_POINT ( 'NONE',  ( 2.406456491625670324, -7.176027849161538796, -7.573451137023475610 ) ) ;
#55411=CARTESIAN_POINT ( 'NONE',  ( 0.3160775863651050233, -8.065044686487370384, 9.237902461149218425 ) ) ;
#55416=EDGE_CURVE ( 'NONE', #7383, #1422, #40750, .T. ) ;
#55419=CARTESIAN_POINT ( 'NONE',  ( 0.3218525148189815277, 7.695007528465018787, 9.550803867331095987 ) ) ;
#55428=VERTEX_POINT ( 'NONE', #738 ) ;
#55429=CARTESIAN_POINT ( 'NONE',  ( 2.305787727787084407, -5.047606869483094449, 5.756228004061441084 ) ) ;
#55442=ORIENTED_EDGE ( 'NONE', *, *, #65634, .F. ) ;
#55443=CARTESIAN_POINT ( 'NONE',  ( 2.899286259009685285, 0.3564726075924497528, -7.845618522360449099 ) ) ;
#55448=CARTESIAN_POINT ( 'NONE',  ( 2.080613030138688480, 3.872983346207417021, -1.000000000000000000 ) ) ;
#55449=CARTESIAN_POINT ( 'NONE',  ( 2.241352910868908754, -4.843133558968088614, -5.901537464758503937 ) ) ;
#55452=CARTESIAN_POINT ( 'NONE',  ( 3.152665057734127974, -4.377619405892426485, 6.622010822086644488 ) ) ;
#55453=CARTESIAN_POINT ( 'NONE',  ( 0.2653141617321027046, -10.62747662594935072, 6.084921229689382649 ) ) ;
#55456=CARTESIAN_POINT ( 'NONE',  ( 1.109979610370754655, -11.92772269523372231, 3.830786822172774109 ) ) ;
#55458=CARTESIAN_POINT ( 'NONE',  ( 2.440552418640497656, 4.020120046181139273, -6.568204543009788843 ) ) ;
#55464=ADVANCED_FACE ( 'NONE', ( #6383 ), #14346, .F. ) ;
#55477=CARTESIAN_POINT ( 'NONE',  ( 0.2646305136544065406, 7.770320294339299494, -9.465888453932885582 ) ) ;
#55478=CARTESIAN_POINT ( 'NONE',  ( 2.491965175173692426, 2.439431489055845503, -7.322278065135876091 ) ) ;
#55484=CIRCLE ( 'NONE', #21506, 12.15774668701806149 ) ;
#55485=CARTESIAN_POINT ( 'NONE',  ( 5.530133899448235191, 0.01536822665454940992, 0.004396748047611668750 ) ) ;
#55490=CARTESIAN_POINT ( 'NONE',  ( 0.2671309869109503299, -0.1620273132354846657, -12.24572650704445032 ) ) ;
#55507=CARTESIAN_POINT ( 'NONE',  ( 1.104777566491139673, 9.281442536087595840, -8.411711248088998616 ) ) ;
#55513=FACE_OUTER_BOUND ( 'NONE', #41526, .T. ) ;
#55515=CARTESIAN_POINT ( 'NONE',  ( 1.719304012340731269, -10.22720798541492826, -7.581471372739399861 ) ) ;
#55516=CARTESIAN_POINT ( 'NONE',  ( 1.719304012341585253, 11.38834240361577521, -5.690355757825364513 ) ) ;
#55518=VECTOR ( 'NONE', #35374, 1000.000000000000227 ) ;
#55529=CARTESIAN_POINT ( 'NONE',  ( 0.3002738374340854777, 11.59380198135587925, -3.979745968261089839 ) ) ;
#55540=CARTESIAN_POINT ( 'NONE',  ( 2.994568964204213923, -0.9739368093814204652, -7.825096839971888762 ) ) ;
#55544=CARTESIAN_POINT ( 'NONE',  ( 2.262775599885880951, -2.480428346600847433, -7.227769107231806878 ) ) ;
#55545=EDGE_CURVE ( 'NONE', #19299, #35691, #39210, .T. ) ;
#55547=VERTEX_POINT ( 'NONE', #47598 ) ;
#55554=CARTESIAN_POINT ( 'NONE',  ( 0.3040950598368152291, -12.11647736519419993, -1.881452845810500207 ) ) ;
#55559=CARTESIAN_POINT ( 'NONE',  ( 2.241352910868908310, -7.633946224498474820, 0.08337961031701579540 ) ) ;
#55561=CARTESIAN_POINT ( 'NONE',  ( 1.719304012338199517, 0.000000000000000000, 0.000000000000000000 ) ) ;
#55562=CARTESIAN_POINT ( 'NONE',  ( 1.104777566491148777, 9.895624035730071100, 7.679758239385173546 ) ) ;
#55565=CARTESIAN_POINT ( 'NONE',  ( 2.259830038564642596, -3.700395974956430578, -6.684701880279044772 ) ) ;
#55566=CARTESIAN_POINT ( 'NONE',  ( 0.3675815128205894289, -9.235491948680062180, 8.093875121226046687 ) ) ;
#55578=CARTESIAN_POINT ( 'NONE',  ( 2.266490820343222357, -5.947069344280059511, -4.800466063945444617 ) ) ;
#55594=CARTESIAN_POINT ( 'NONE',  ( 5.515188684475870851, -0.003709313826050263888, -0.003857086913166431381 ) ) ;
#55596=B_SPLINE_CURVE_WITH_KNOTS ( 'NONE', 3,
 ( #9392, #36574, #19408, #26586, #51878, #36225, #54964 ),
 .UNSPECIFIED., .F., .F.,
 ( 4, 3, 4 ),
 ( 2.737610485525898696E-18, 6.607593386745468696E-05, 0.0001321430428585257952 ),
 .UNSPECIFIED. ) ;
#55605=CARTESIAN_POINT ( 'NONE',  ( 2.665405856346786173, -9.505137710817301411, 1.089747929268660931 ) ) ;
#55608=CARTESIAN_POINT ( 'NONE',  ( 2.273267844205335120, 4.797225296800435856, -5.952585402747609500 ) ) ;
#55624=CARTESIAN_POINT ( 'NONE',  ( 0.3632410797595229113, -12.27601307605977965, 0.2628628737173034358 ) ) ;
#55647=VECTOR ( 'NONE', #21871, 1000.000000000000114 ) ;
#55651=ORIENTED_EDGE ( 'NONE', *, *, #6326, .F. ) ;
#55658=CARTESIAN_POINT ( 'NONE',  ( 2.261269890822072970, 6.685978463722182852, -3.699080366006626708 ) ) ;
#55679=DIRECTION ( 'NONE',  ( 0.3939253465568944290, 0.8008152550167598749, -0.4511294145502736663 ) ) ;
#55681=CARTESIAN_POINT ( 'NONE',  ( 0.2653519789438757992, 4.167744179924070203, -11.51519617080776925 ) ) ;
#55682=FACE_OUTER_BOUND ( 'NONE', #12405, .T. ) ;
#55688=ORIENTED_EDGE ( 'NONE', *, *, #22722, .T. ) ;
#55693=CARTESIAN_POINT ( 'NONE',  ( 0.2911222467163634420, 9.524109243548085857, -7.711756541611588744 ) ) ;
#55697=EDGE_CURVE ( 'NONE', #9459, #6270, #38936, .T. ) ;
#55708=ADVANCED_FACE ( 'NONE', ( #56425 ), #30085, .F. ) ;
#55719=ORIENTED_EDGE ( 'NONE', *, *, #64979, .T. ) ;
#55731=CARTESIAN_POINT ( 'NONE',  ( 2.524535260912044610, 6.060306679218721904, 4.796565674004597213 ) ) ;
#55734=CARTESIAN_POINT ( 'NONE',  ( 2.373367633546870969, -0.1808255748566004184, 7.676289145832772221 ) ) ;
#55738=CARTESIAN_POINT ( 'NONE',  ( 0.9232058338315048962, 12.21058493388773591, 2.536181247095406377 ) ) ;
#55739=( BOUNDED_SURFACE ( )  B_SPLINE_SURFACE ( 3, 1, ( 
 ( #27745, #11157 ),
 ( #12893, #43143 ),
 ( #52809, #38153 ),
 ( #31851, #37173 ) ),
 .UNSPECIFIED., .F., .F., .F. ) 
 B_SPLINE_SURFACE_WITH_KNOTS ( ( 4, 4 ),
 ( 2, 2 ),
 ( 0.000000000000000000, 1.000000000000000000 ),
 ( 0.000000000000000000, 1.000000000000000000 ),
 .UNSPECIFIED. ) 
 GEOMETRIC_REPRESENTATION_ITEM ( )  RATIONAL_B_SPLINE_SURFACE ( (
 ( 1.000000000000000000, 1.000000000000000000),
 ( 0.9942764183789327692, 0.8450855930916585379),
 ( 0.9942764183789327692, 0.8450855930916585379),
 ( 1.000000000000000000, 1.000000000000000000) ) ) 
 REPRESENTATION_ITEM ( '' )  SURFACE ( )  );
#55758=DIRECTION ( 'NONE',  ( 0.000000000000000000, 1.000000000000000000, -0.000000000000000000 ) ) ;
#55760=CARTESIAN_POINT ( 'NONE',  ( 0.3164563675027644019, 11.43920928915630952, -4.419430877662233748 ) ) ;
#55775=ORIENTED_EDGE ( 'NONE', *, *, #35866, .F. ) ;
#55776=ORIENTED_EDGE ( 'NONE', *, *, #28967, .F. ) ;
#55779=ORIENTED_EDGE ( 'NONE', *, *, #39331, .T. ) ;
#55790=CARTESIAN_POINT ( 'NONE',  ( 2.241352910868908310, 7.633946224498473931, -0.08337961031706911386 ) ) ;
#55794=CARTESIAN_POINT ( 'NONE',  ( 2.241528039335008327, 5.838210500619377186, 4.919377664485117485 ) ) ;
#55795=CARTESIAN_POINT ( 'NONE',  ( 2.241526690369555208, -7.515450538999844277, 1.342748965918859616 ) ) ;
#55798=CARTESIAN_POINT ( 'NONE',  ( 2.990245332647871290, 7.779904630197308713, 3.377079998295634766 ) ) ;
#55802=B_SPLINE_CURVE_WITH_KNOTS ( 'NONE', 3,
 ( #14111, #7839, #12799, #63340, #23448, #48410, #17806, #33428, #54382, #34405, #22807, #38071, #58375, #43725, #54037, #2537, #2860, #49408, #24104 ),
 .UNSPECIFIED., .F., .F.,
 ( 4, 3, 3, 3, 3, 3, 4 ),
 ( 6.508826038821075435E-18, 2.825908398831318295E-05, 4.208813692484010587E-05, 5.591713746943977590E-05, 6.279584083232033951E-05, 9.105792820296882426E-05, 0.0001153131102488863535 ),
 .UNSPECIFIED. ) ;
#55806=ORIENTED_EDGE ( 'NONE', *, *, #58765, .F. ) ;
#55808=CARTESIAN_POINT ( 'NONE',  ( 0.2653519890538381665, 0.02202471025205905014, 12.24619734961521544 ) ) ;
#55811=CARTESIAN_POINT ( 'NONE',  ( 2.589278595513128778, -7.670769623692313743, -1.107986312493487890 ) ) ;
#55815=CARTESIAN_POINT ( 'NONE',  ( 2.430348790456984265, 2.448665558939242537, -7.297553103283330067 ) ) ;
#55816=LINE ( 'NONE', #57128, #2498 ) ;
#55817=CARTESIAN_POINT ( 'NONE',  ( 2.241509619876138171, -6.592435552901097395, -3.850348903238783649 ) ) ;
#55825=CARTESIAN_POINT ( 'NONE',  ( 0.2648978790185584908, 12.24533305150758089, 0.1321385342562836074 ) ) ;
#55831=EDGE_LOOP ( 'NONE', ( #44506, #3851, #15632, #37308 ) ) ;
#55833=CARTESIAN_POINT ( 'NONE',  ( 0.3665391374699464300, -1.872534962004717141, -12.13918562134720425 ) ) ;
#55840=CARTESIAN_POINT ( 'NONE',  ( 0.8375941296816615811, 10.95781044612504473, -5.882592429484091667 ) ) ;
#55856=CARTESIAN_POINT ( 'NONE',  ( 2.931247277082679403, -6.988361004535458498, 3.607110715259723932 ) ) ;
#55860=ORIENTED_EDGE ( 'NONE', *, *, #20887, .F. ) ;
#55863=CARTESIAN_POINT ( 'NONE',  ( 2.889800649504073782, -3.882893708502079377, 4.732281052280299605 ) ) ;
#55876=CARTESIAN_POINT ( 'NONE',  ( 0.2759803524722206913, -10.70204612651779819, 5.960075719898805247 ) ) ;
#55877=CARTESIAN_POINT ( 'NONE',  ( 5.530133899448235191, 0.009387834778845855280, -0.01293763278443441425 ) ) ;
#55879=EDGE_CURVE ( 'NONE', #14040, #16694, #17786, .T. ) ;
#55891=CARTESIAN_POINT ( 'NONE',  ( 2.655192694323545766, 4.290256727312732110, -8.589732161580133862 ) ) ;
#55897=CARTESIAN_POINT ( 'NONE',  ( 1.452237505248555660, 11.67686475128086343, -4.880303821310893575 ) ) ;
#55898=CARTESIAN_POINT ( 'NONE',  ( 0.3665391374699465965, 9.237363111276877703, -8.095513416941136242 ) ) ;
#55899=CARTESIAN_POINT ( 'NONE',  ( 2.276198483117257254, 0.1540629821339370153, -7.644465698238555262 ) ) ;
#55909=CARTESIAN_POINT ( 'NONE',  ( 2.290907136834313906, -1.168459104840546825, -7.561169784528830817 ) ) ;
#55911=EDGE_CURVE ( 'NONE', #47398, #49321, #35194, .T. ) ;
#55915=B_SPLINE_CURVE_WITH_KNOTS ( 'NONE', 3,
 ( #18476, #58364, #8467, #54026, #3838, #8805, #28109, #49060, #28416, #42714, #3514, #39050, #23436 ),
 .UNSPECIFIED., .F., .F.,
 ( 4, 3, 3, 3, 4 ),
 ( 3.127317220692750759E-18, 6.607593386745410421E-05, 0.0001321518677373518646, 0.0001982171734706181221, 0.0002642860854759469282 ),
 .UNSPECIFIED. ) ;
#55918=CARTESIAN_POINT ( 'NONE',  ( 1.948354844646291939, -0.7204626209691626926, -11.94326855455706848 ) ) ;
#55927=B_SPLINE_CURVE_WITH_KNOTS ( 'NONE', 3,
 ( #50660, #19418, #40324, #10084, #55298, #5103, #9743, #50344, #44650, #55962, #60618, #15056, #19747, #35336, #30366, #25370 ),
 .UNSPECIFIED., .F., .F.,
 ( 4, 3, 3, 3, 3, 4 ),
 ( 0.000000000000000000, 0.0002999043160757478032, 0.0005998071753051258288, 0.0008997092107374931582, 0.001204458948194910874, 0.001510329163474998003 ),
 .UNSPECIFIED. ) ;
#55930=CARTESIAN_POINT ( 'NONE',  ( 1.198791140419160683, -9.943044756148728069, 7.669598593075038551 ) ) ;
#55937=CARTESIAN_POINT ( 'NONE',  ( 0.3654063281920715833, -12.27672420655579444, 0.2633658439602916124 ) ) ;
#55949=CARTESIAN_POINT ( 'NONE',  ( 0.3057689695767479843, 8.055876362038343785, 9.241339546505109581 ) ) ;
#55951=CARTESIAN_POINT ( 'NONE',  ( 0.3665391374699464300, -11.44911061034383515, -4.447929964102962153 ) ) ;
#55956=B_SPLINE_CURVE_WITH_KNOTS ( 'NONE', 3,
 ( #42553, #37255, #20975, #11988, #57902, #41259, #46926, #62859, #57567, #46277, #22286, #47573, #11020, #41920, #2023, #25994 ),
 .UNSPECIFIED., .F., .F.,
 ( 4, 3, 3, 3, 3, 4 ),
 ( 0.000000000000000000, 0.0002176109881720306378, 0.0004352086762394722676, 0.0006528017811447081077, 0.0007615147961451940693, 0.0009453342004947466043 ),
 .UNSPECIFIED. ) ;
#55957=CARTESIAN_POINT ( 'NONE',  ( 1.719304012340734378, -11.38834240361519612, -5.690355757825884986 ) ) ;
#55958=EDGE_CURVE ( 'NONE', #28659, #41303, #20838, .T. ) ;
#55962=CARTESIAN_POINT ( 'NONE',  ( 0.9296196016820552632, 12.19921892949952280, 2.573053270830167438 ) ) ;
#55967=CARTESIAN_POINT ( 'NONE',  ( 3.152665057734040488, 0.000000000000000000, 0.000000000000000000 ) ) ;
#55972=CARTESIAN_POINT ( 'NONE',  ( 1.287602823387597351, -3.781900355161777583, -12.00540336274513820 ) ) ;
#55991=CARTESIAN_POINT ( 'NONE',  ( 2.889800649504073782, -5.334644486274216391, 3.002151847318898170 ) ) ;
#55999=CARTESIAN_POINT ( 'NONE',  ( 2.241528039335009215, -2.625917297988434651, 7.168649579907117264 ) ) ;
#56002=CARTESIAN_POINT ( 'NONE',  ( 0.3040950598368152291, -11.60568999039892191, -3.956873563689648154 ) ) ;
#56011=CARTESIAN_POINT ( 'NONE',  ( 0.2872850955227740921, -12.02931961709053077, 2.333231805482948840 ) ) ;
#56014=CARTESIAN_POINT ( 'NONE',  ( 0.3675815128205894289, 12.04510820461659293, 2.391755495700645273 ) ) ;
#56015=ORIENTED_EDGE ( 'NONE', *, *, #1523, .T. ) ;
#56019=CARTESIAN_POINT ( 'NONE',  ( 2.241536586108911155, 1.331908602351639770, 7.517390684805875800 ) ) ;
#56038=ORIENTED_EDGE ( 'NONE', *, *, #17299, .F. ) ;
#56039=CARTESIAN_POINT ( 'NONE',  ( 2.770579946183334030, -0.3031629740256286953, 7.804957730865693222 ) ) ;
#56043=CARTESIAN_POINT ( 'NONE',  ( 2.368238019615328316, -7.150288915654845034, 2.793778585134697678 ) ) ;
#56046=CARTESIAN_POINT ( 'NONE',  ( 2.241449424704146320, -3.870245369721776019, -6.580749518451838753 ) ) ;
#56047=CARTESIAN_POINT ( 'NONE',  ( 2.639814597422670328, 6.594772041715931898, 4.103563379978007575 ) ) ;
#56052=CARTESIAN_POINT ( 'NONE',  ( 0.2638984909335716500, -12.24571285024408951, -0.1991813963115269814 ) ) ;
#56062=CARTESIAN_POINT ( 'NONE',  ( 0.2911222467163546157, 7.711756541611694438, 9.524109243547997039 ) ) ;
#56063=DIRECTION ( 'NONE',  ( -1.000000000000000000, -0.000000000000000000, -0.000000000000000000 ) ) ;
#56066=CARTESIAN_POINT ( 'NONE',  ( 1.198791140420482959, -1.670544840357492955, -12.44572864632847953 ) ) ;
#56069=CARTESIAN_POINT ( 'NONE',  ( 0.2655924914740778187, 10.58356227062109411, 6.161287456391719708 ) ) ;
#56077=CARTESIAN_POINT ( 'NONE',  ( 2.717984159219991369, 1.631703089060316136, 7.620583877640733306 ) ) ;
#56079=CARTESIAN_POINT ( 'NONE',  ( 0.2646305136544072623, 4.064188116014705976, -11.55263159009954421 ) ) ;
#56081=FACE_OUTER_BOUND ( 'NONE', #28186, .T. ) ;
#56091=DIRECTION ( 'NONE',  ( 0.3865475372811021382, 0.3335716741247249928, -0.8598319252293108450 ) ) ;
#56093=CARTESIAN_POINT ( 'NONE',  ( 0.2652384529303147276, -10.57229402027111931, 6.180212112237623678 ) ) ;
#56096=CARTESIAN_POINT ( 'NONE',  ( 3.152665057734040488, 0.000000000000000000, 0.000000000000000000 ) ) ;
#56102=CARTESIAN_POINT ( 'NONE',  ( 0.2801149460245125344, -10.70654700624298883, -5.954809120985829374 ) ) ;
#56104=CARTESIAN_POINT ( 'NONE',  ( 0.3537226245948383307, 9.233810598191778851, 8.088784578751326393 ) ) ;
#56113=CARTESIAN_POINT ( 'NONE',  ( 0.2650492433740069820, 0.1101179680248975945, 12.24562113162318866 ) ) ;
#56115=CARTESIAN_POINT ( 'NONE',  ( 0.2653519890518167834, -12.06014856238022226, 2.126538543978039542 ) ) ;
#56116=CARTESIAN_POINT ( 'NONE',  ( 2.257661810676208081, 2.485866587321733601, -7.224098098130338208 ) ) ;
#56119=CARTESIAN_POINT ( 'NONE',  ( 2.263328370261528555, -3.697218830763996600, 6.687792802426776539 ) ) ;
#56120=CARTESIAN_POINT ( 'NONE',  ( 0.5572780756284287929, -12.20533540249709148, 1.841882550626854131 ) ) ;
#56132=CARTESIAN_POINT ( 'NONE',  ( 2.241451721903215066, 7.153019588493075176, 2.668222118333474224 ) ) ;
#56141=CARTESIAN_POINT ( 'NONE',  ( 1.719304012338439325, 7.017415949612858306, 10.62216384465677521 ) ) ;
#56142=DIRECTION ( 'NONE',  ( 0.3939253465568944290, -0.9034404741085553248, -0.1691689424289794796 ) ) ;
#56145=CARTESIAN_POINT ( 'NONE',  ( 2.350038591458111892, -5.855794476068393983, 8.861946706685715824 ) ) ;
#56153=CARTESIAN_POINT ( 'NONE',  ( 0.2671309869109484425, -9.276621593297562640, 7.995521393275787148 ) ) ;
#56157=ADVANCED_FACE ( 'NONE', ( #21094 ), #35110, .F. ) ;
#56160=ORIENTED_EDGE ( 'NONE', *, *, #54038, .F. ) ;
#56164=CARTESIAN_POINT ( 'NONE',  ( 2.907497136250587033, 7.252103438786942746, -3.021847490615504839 ) ) ;
#56183=ORIENTED_EDGE ( 'NONE', *, *, #64329, .T. ) ;
#56187=CARTESIAN_POINT ( 'NONE',  ( 0.3665391374699467075, 6.368473106897276637, -10.50279796150430123 ) ) ;
#56188=CARTESIAN_POINT ( 'NONE',  ( 3.152665057734104437, -3.546019893116280741, -7.102135024645891193 ) ) ;
#56189=CARTESIAN_POINT ( 'NONE',  ( 2.835339799623983748, -7.825540862019406241, -0.3287452556171494011 ) ) ;
#56199=CARTESIAN_POINT ( 'NONE',  ( 2.430348790457064201, 4.016278121583625627, 6.566563360302290597 ) ) ;
#56204=CARTESIAN_POINT ( 'NONE',  ( 1.547277799339724202, 5.744300480442041668, -11.29700934613367558 ) ) ;
#56210=CARTESIAN_POINT ( 'NONE',  ( 0.3632410797595229113, 12.27601307605977610, -0.2628628737173892005 ) ) ;
#56213=CARTESIAN_POINT ( 'NONE',  ( 5.536195898058073439, 0.0002547682446687991073, -0.008496323383586253108 ) ) ;
#56214=CARTESIAN_POINT ( 'NONE',  ( 5.530133899448235191, 0.003876417824003443660, -0.01550764871776217670 ) ) ;
#56219=ORIENTED_EDGE ( 'NONE', *, *, #26485, .T. ) ;
#56233=ORIENTED_EDGE ( 'NONE', *, *, #58368, .T. ) ;
#56235=CARTESIAN_POINT ( 'NONE',  ( 2.305787727787083519, -2.461236246751120849, 7.249469779319902329 ) ) ;
#56237=ORIENTED_EDGE ( 'NONE', *, *, #5145, .T. ) ;
#56238=CARTESIAN_POINT ( 'NONE',  ( 2.305787727787084407, 4.792270232040973355, -5.970480882365174047 ) ) ;
#56245=ORIENTED_EDGE ( 'NONE', *, *, #60288, .T. ) ;
#56251=CARTESIAN_POINT ( 'NONE',  ( 2.305787727787084407, 3.971363876083963351, 6.545285700970541853 ) ) ;
#56260=DIRECTION ( 'NONE',  ( 0.000000000000000000, 0.000000000000000000, 1.000000000000000000 ) ) ;
#56263=CARTESIAN_POINT ( 'NONE',  ( 2.639814597422741382, -5.782006333156036959, -5.186391178752193909 ) ) ;
#56270=CARTESIAN_POINT ( 'NONE',  ( 2.247112776669945244, 7.214825360829727252, 2.501955819910834933 ) ) ;
#56275=B_SPLINE_CURVE_WITH_KNOTS ( 'NONE', 3,
 ( #46845, #16912, #63120, #7593, #63430, #58141, #11275, #62448, #22900, #26894, #62141, #37850, #47197, #26556, #17899, #11914 ),
 .UNSPECIFIED., .F., .F.,
 ( 4, 3, 3, 3, 3, 4 ),
 ( 0.000000000000000000, 0.0002999043160757648252, 0.0005998071753051594391, 0.0008997092107375431400, 0.001204458948196864606, 0.001510329163478875110 ),
 .UNSPECIFIED. ) ;
#56278=CARTESIAN_POINT ( 'NONE',  ( 0.2650492594609233921, -7.786980091309387397, -9.451471004987412883 ) ) ;
#56281=CARTESIAN_POINT ( 'NONE',  ( 0.3164563675027650125, -4.419430877662271051, -11.43920928915629176 ) ) ;
#56287=CARTESIAN_POINT ( 'NONE',  ( 0.3106921474978474040, -5.925601485921598410, -10.73438344699978231 ) ) ;
#56290=CARTESIAN_POINT ( 'NONE',  ( 0.2653519890518143964, 2.126521162241218565, -12.06015162724940026 ) ) ;
#56291=DIRECTION ( 'NONE',  ( 0.000000000000000000, 0.000000000000000000, 1.000000000000000000 ) ) ;
#56292=CARTESIAN_POINT ( 'NONE',  ( 0.7446945582524610030, -3.906659168236780388, -11.77484212699384614 ) ) ;
#56296=( BOUNDED_SURFACE ( )  B_SPLINE_SURFACE ( 3, 1, ( 
 ( #46762, #1874 ),
 ( #21505, #16517 ),
 ( #32754, #11509 ),
 ( #47437, #62066 ) ),
 .UNSPECIFIED., .F., .F., .F. ) 
 B_SPLINE_SURFACE_WITH_KNOTS ( ( 4, 4 ),
 ( 2, 2 ),
 ( 0.000000000000000000, 1.000000000000000000 ),
 ( 0.000000000000000000, 1.000000000000000000 ),
 .UNSPECIFIED. ) 
 GEOMETRIC_REPRESENTATION_ITEM ( )  RATIONAL_B_SPLINE_SURFACE ( (
 ( 1.000000000000000000, 1.000000000000000000),
 ( 0.6933888150995267674, 0.9895912004443193632),
 ( 0.6933888150995267674, 0.9895912004443193632),
 ( 1.000000000000000000, 1.000000000000000000) ) ) 
 REPRESENTATION_ITEM ( '' )  SURFACE ( )  );
#56302=CARTESIAN_POINT ( 'NONE',  ( 2.257661810676420355, -6.547845034191119851, 3.936095962955278527 ) ) ;
#56317=ORIENTED_EDGE ( 'NONE', *, *, #25990, .T. ) ;
#56321=LINE ( 'NONE', #21413, #24490 ) ;
#56322=ORIENTED_EDGE ( 'NONE', *, *, #61455, .F. ) ;
#56327=VERTEX_POINT ( 'NONE', #62004 ) ;
#56340=CARTESIAN_POINT ( 'NONE',  ( 0.2647959493198551728, -12.03358727341676015, 2.271080632828021972 ) ) ;
#56347=CARTESIAN_POINT ( 'NONE',  ( 1.547277799338548920, -10.62321481610073626, 6.911346840320337748 ) ) ;
#56369=EDGE_CURVE ( 'NONE', #39884, #46591, #41428, .T. ) ;
#56372=CARTESIAN_POINT ( 'NONE',  ( 5.516018279890452902, 0.003580555109620797271, 0.005752102158673854694 ) ) ;
#56380=ORIENTED_EDGE ( 'NONE', *, *, #16259, .T. ) ;
#56382=CARTESIAN_POINT ( 'NONE',  ( 2.080613030138687147, 0.000000000000000000, 0.000000000000000000 ) ) ;
#56384=CARTESIAN_POINT ( 'NONE',  ( 2.247206125382827935, 1.211896144126927144, 7.539576157880604868 ) ) ;
#56394=CARTESIAN_POINT ( 'NONE',  ( 2.305787727787083519, -7.249469779319894336, -2.461236246751144829 ) ) ;
#56396=CARTESIAN_POINT ( 'NONE',  ( 2.889800649504073782, 4.645655809191365115, 3.986129653162664432 ) ) ;
#56403=CARTESIAN_POINT ( 'NONE',  ( 0.4613984246114877230, 0.2828900474740380644, 12.30830943644279962 ) ) ;
#56405=B_SPLINE_CURVE_WITH_KNOTS ( 'NONE', 3,
 ( #798, #20755, #61975, #10119, #21063, #61307, #25746 ),
 .UNSPECIFIED., .F., .F.,
 ( 4, 3, 4 ),
 ( 8.760178018519042877E-15, 0.002398160485435057911, 0.005002426799385541190 ),
 .UNSPECIFIED. ) ;
#56413=CARTESIAN_POINT ( 'NONE',  ( 0.2869720083484316731, 11.44147823180130885, 4.386174336869626877 ) ) ;
#56414=CARTESIAN_POINT ( 'NONE',  ( 5.514624014163232779, -0.0005510299962882055525, 0.004104370840204387381 ) ) ;
#56418=FACE_OUTER_BOUND ( 'NONE', #62455, .T. ) ;
#56425=FACE_OUTER_BOUND ( 'NONE', #48603, .T. ) ;
#56427=CARTESIAN_POINT ( 'NONE',  ( 0.3675815128205894289, -0.2638082659427565813, -12.27743992903066328 ) ) ;
#56437=DIRECTION ( 'NONE',  ( 0.000000000000000000, 0.000000000000000000, 1.000000000000000000 ) ) ;
#56447=VERTEX_POINT ( 'NONE', #18753 ) ;
#56456=CARTESIAN_POINT ( 'NONE',  ( 2.249013661412238907, 4.816366775941330225, 5.926694833810642216 ) ) ;
#56463=DIRECTION ( 'NONE',  ( 0.3865475372811021382, -0.9114221272958290543, 0.1410344188397309739 ) ) ;
#56464=DIRECTION ( 'NONE',  ( -1.000000000000000000, -0.000000000000000000, -0.000000000000000000 ) ) ;
#56467=CARTESIAN_POINT ( 'NONE',  ( 2.288423627607476973, 2.767471693622796991, 7.131972212895015595 ) ) ;
#56477=VECTOR ( 'NONE', #40732, 1000.000000000000114 ) ;
#56478=AXIS2_PLACEMENT_3D ( 'NONE', #26699, #51982, #21732 ) ;
#56483=CARTESIAN_POINT ( 'NONE',  ( 2.255723233588949661, -6.548644987607536549, -3.933511348457504830 ) ) ;
#56491=ADVANCED_FACE ( 'NONE', ( #8113 ), #12596, .F. ) ;
#56492=CARTESIAN_POINT ( 'NONE',  ( 1.719304012339844867, -11.38834240361479644, 5.690355757826019989 ) ) ;
#56503=ORIENTED_EDGE ( 'NONE', *, *, #22860, .T. ) ;
#56506=CARTESIAN_POINT ( 'NONE',  ( 3.152665057736177445, 3.161213418915486795, 7.281573230473766145 ) ) ;
#56511=CARTESIAN_POINT ( 'NONE',  ( 5.516018279890452902, -0.005042957932158615743, 0.004525000489649755146 ) ) ;
#56515=CIRCLE ( 'NONE', #22361, 7.938172270156617749 ) ;
#56517=ORIENTED_EDGE ( 'NONE', *, *, #9278, .T. ) ;
#56518=B_SPLINE_CURVE_WITH_KNOTS ( 'NONE', 3,
 ( #63560, #18031, #38295, #33324, #53625, #49306, #8064, #28333, #33962, #48627, #63902, #3753, #24010 ),
 .UNSPECIFIED., .F., .F.,
 ( 4, 3, 3, 3, 4 ),
 ( 3.127317220692750759E-18, 6.607593386745608287E-05, 0.0001321518677373537348, 0.0001982171734706250610, 0.0002642860854759490966 ),
 .UNSPECIFIED. ) ;
#56520=CARTESIAN_POINT ( 'NONE',  ( 1.719304012338199295, 11.67935079956398958, 5.066286238785226992 ) ) ;
#56521=EDGE_CURVE ( 'NONE', #62520, #13985, #50995, .T. ) ;
#56522=CARTESIAN_POINT ( 'NONE',  ( 2.440552418640497212, -1.142369876085273184, -7.615619946579185395 ) ) ;
#56523=CARTESIAN_POINT ( 'NONE',  ( 2.298277635560276533, 2.772101951899060612, -7.133696409974365160 ) ) ;
#56530=( BOUNDED_SURFACE ( )  B_SPLINE_SURFACE ( 3, 1, ( 
 ( #2838, #13750 ),
 ( #28403, #3158 ),
 ( #33716, #24079 ),
 ( #34039, #29385 ) ),
 .UNSPECIFIED., .F., .F., .F. ) 
 B_SPLINE_SURFACE_WITH_KNOTS ( ( 4, 4 ),
 ( 2, 2 ),
 ( 0.000000000000000000, 1.000000000000000000 ),
 ( 0.000000000000000000, 1.000000000000000000 ),
 .UNSPECIFIED. ) 
 GEOMETRIC_REPRESENTATION_ITEM ( )  RATIONAL_B_SPLINE_SURFACE ( (
 ( 1.000000000000000000, 1.000000000000000000),
 ( 0.6933888150995267674, 0.9895912004443193632),
 ( 0.6933888150995267674, 0.9895912004443193632),
 ( 1.000000000000000000, 1.000000000000000000) ) ) 
 REPRESENTATION_ITEM ( '' )  SURFACE ( )  );
#56536=CARTESIAN_POINT ( 'NONE',  ( 0.2717059086739026519, -8.007130974639977694, -9.268607328094613962 ) ) ;
#56538=CARTESIAN_POINT ( 'NONE',  ( 2.899286259009685729, -7.845618522360447322, -0.3564726075924216087 ) ) ;
#56549=CARTESIAN_POINT ( 'NONE',  ( 2.639814597422736941, 6.111633106000494919, -4.793557287999567151 ) ) ;
#56550=CARTESIAN_POINT ( 'NONE',  ( 2.589278595513019088, 4.081908913131758965, 6.588350318048411758 ) ) ;
#56554=CARTESIAN_POINT ( 'NONE',  ( 0.3160775863651064110, 2.365582350580221593, -12.03278055228168775 ) ) ;
#56561=CARTESIAN_POINT ( 'NONE',  ( 2.241509619876138171, 2.575142053947867105, 7.187074272457164348 ) ) ;
#56562=FACE_OUTER_BOUND ( 'NONE', #42013, .T. ) ;
#56564=FACE_OUTER_BOUND ( 'NONE', #39970, .T. ) ;
#56568=CARTESIAN_POINT ( 'NONE',  ( 0.3665391374699464300, -2.392238720110541284, 12.04754782681756708 ) ) ;
#56577=CARTESIAN_POINT ( 'NONE',  ( 1.719304012341272836, -1.452142814148833949, -12.64775761152634281 ) ) ;
#56587=CARTESIAN_POINT ( 'NONE',  ( 2.244591118396916940, 4.825158615932057415, -5.917635828476827342 ) ) ;
#56592=CARTESIAN_POINT ( 'NONE',  ( 0.3053067050349213551, 12.11120005789973852, -1.901204202464545912 ) ) ;
#56598=FACE_OUTER_BOUND ( 'NONE', #61289, .T. ) ;
#56603=EDGE_CURVE ( 'NONE', #1422, #31754, #33575, .T. ) ;
#56604=CARTESIAN_POINT ( 'NONE',  ( 2.665405856346787949, -8.776564688671564696, -3.808819464940508936 ) ) ;
#56606=CARTESIAN_POINT ( 'NONE',  ( 0.2646305136544065406, 1.996350543472993566, 12.08286001766535911 ) ) ;
#56609=B_SPLINE_CURVE_WITH_KNOTS ( 'NONE', 3,
 ( #47943, #32305, #52618, #7043, #53916, #27313, #2401, #2055, #37950, #58244, #22319, #33300, #18354, #62891, #42590, #32613, #53604, #48605, #22007, #52923, #23322, #38617 ),
 .UNSPECIFIED., .F., .F.,
 ( 4, 3, 3, 3, 3, 3, 3, 4 ),
 ( 1.311167604876506724E-18, 4.449119708436685016E-05, 6.626296329540322600E-05, 8.803456484962410972E-05, 0.0001098060367612766793, 0.0001315774408628458134, 0.0001760698110411108961, 0.0001829697163287834563 ),
 .UNSPECIFIED. ) ;
#56613=CARTESIAN_POINT ( 'NONE',  ( 0.3002738374340787608, -4.403689978763143387, 11.43949898053769587 ) ) ;
#56617=EDGE_CURVE ( 'NONE', #29012, #42070, #28724, .T. ) ;
#56618=ORIENTED_EDGE ( 'NONE', *, *, #44968, .T. ) ;
#56621=DIRECTION ( 'NONE',  ( 0.000000000000000000, 0.000000000000000000, 1.000000000000000000 ) ) ;
#56622=CARTESIAN_POINT ( 'NONE',  ( 2.241352910868909643, 7.145045428366612050, -2.689314586382279604 ) ) ;
#56624=VERTEX_POINT ( 'NONE', #31970 ) ;
#56631=EDGE_CURVE ( 'NONE', #47398, #50365, #22006, .T. ) ;
#56650=B_SPLINE_CURVE_WITH_KNOTS ( 'NONE', 3,
 ( #33502, #6926, #27196, #42457, #62757, #45113, #55079, #54104, #64710, #49773, #44430, #34771, #49468, #65374, #43801, #50441 ),
 .UNSPECIFIED., .F., .F.,
 ( 4, 3, 3, 3, 3, 4 ),
 ( 0.000000000000000000, 0.0002999043160757219992, 0.0005998071753050768229, 0.0008997092107374199746, 0.001204458948194617922, 0.001510329163474479321 ),
 .UNSPECIFIED. ) ;
#56656=VERTEX_POINT ( 'NONE', #62240 ) ;
#56657=CARTESIAN_POINT ( 'NONE',  ( 0.9296196016816719032, 10.58347995892850157, 6.590257778216622953 ) ) ;
#56671=ORIENTED_EDGE ( 'NONE', *, *, #42241, .T. ) ;
#56673=CARTESIAN_POINT ( 'NONE',  ( 0.3675815128205912052, -11.44679196252406506, -4.447030445008294919 ) ) ;
#56676=ORIENTED_EDGE ( 'NONE', *, *, #10949, .T. ) ;
#56677=DIRECTION ( 'NONE',  ( -0.3939253465568943180, -0.5982248387291149161, -0.6978179301705819126 ) ) ;
#56681=DIRECTION ( 'NONE',  ( -0.3865475372811021937, -0.6075346789811115755, -0.6938894834606104123 ) ) ;
#56686=FACE_OUTER_BOUND ( 'NONE', #5576, .T. ) ;
#56709=CARTESIAN_POINT ( 'NONE',  ( 5.530133899448235191, 0.01459891979722818985, 0.006510401266731672201 ) ) ;
#56714=AXIS2_PLACEMENT_3D ( 'NONE', #30064, #50693, #39056 ) ;
#56718=AXIS2_PLACEMENT_3D ( 'NONE', #35491, #25860, #59792 ) ;
#56725=EDGE_CURVE ( 'NONE', #29440, #64295, #58243, .T. ) ;
#56726=( BOUNDED_SURFACE ( )  B_SPLINE_SURFACE ( 3, 1, ( 
 ( #51519, #15254 ),
 ( #35535, #40863 ),
 ( #5968, #61143 ),
 ( #46500, #55833 ) ),
 .UNSPECIFIED., .F., .F., .F. ) 
 B_SPLINE_SURFACE_WITH_KNOTS ( ( 4, 4 ),
 ( 2, 2 ),
 ( 0.000000000000000000, 1.000000000000000000 ),
 ( 0.000000000000000000, 1.000000000000000000 ),
 .UNSPECIFIED. ) 
 GEOMETRIC_REPRESENTATION_ITEM ( )  RATIONAL_B_SPLINE_SURFACE ( (
 ( 1.000000000000000000, 1.000000000000000000),
 ( 0.9942764183789327692, 0.8450855930916580938),
 ( 0.9942764183789327692, 0.8450855930916580938),
 ( 1.000000000000000000, 1.000000000000000000) ) ) 
 REPRESENTATION_ITEM ( '' )  SURFACE ( )  );
#56728=CARTESIAN_POINT ( 'NONE',  ( 1.198791140420632173, 2.686891236233812208, -12.26651935498972357 ) ) ;
#56731=VERTEX_POINT ( 'NONE', #33299 ) ;
#56738=VECTOR ( 'NONE', #9114, 1000.000000000000114 ) ;
#56740=CARTESIAN_POINT ( 'NONE',  ( 3.031336079629613600, -7.268683861177229311, 3.088871717871501943 ) ) ;
#56746=CARTESIAN_POINT ( 'NONE',  ( 3.152665057735509979, 7.102135024646700323, 3.546019893115181620 ) ) ;
#56755=CARTESIAN_POINT ( 'NONE',  ( 1.719304012338701115, -5.690355757827699534, 11.38834240361771677 ) ) ;
#56758=ADVANCED_FACE ( 'NONE', ( #8686 ), #37265, .F. ) ;
#56761=DIRECTION ( 'NONE',  ( -0.3865475372811021382, -0.2971585806051909029, 0.8730852074079729075 ) ) ;
#56765=CARTESIAN_POINT ( 'NONE',  ( 0.3341166715381319041, 11.44035855572981752, -4.432780143632383485 ) ) ;
#56777=CARTESIAN_POINT ( 'NONE',  ( 5.514970785353741078, -0.003262412238248251547, 0.003415090918276177286 ) ) ;
#56786=CARTESIAN_POINT ( 'NONE',  ( 0.3665391374699472626, 2.392238720110459571, 12.04754782681758130 ) ) ;
#56787=CARTESIAN_POINT ( 'NONE',  ( 2.941278708680199916, -5.814102272488574918, -1.972702289976061563 ) ) ;
#56789=EDGE_CURVE ( 'NONE', #26248, #20510, #4119, .T. ) ;
#56790=CARTESIAN_POINT ( 'NONE',  ( 1.014383007554946481, 12.37541872618881200, 1.731118468093957974 ) ) ;
#56793=CARTESIAN_POINT ( 'NONE',  ( 2.284126774967665252, 7.503320429541878944, 1.483972655035240562 ) ) ;
#56808=ADVANCED_FACE ( 'NONE', ( #25611 ), #34727, .F. ) ;
#56810=FACE_OUTER_BOUND ( 'NONE', #50751, .T. ) ;
#56812=CARTESIAN_POINT ( 'NONE',  ( 0.6473888112830256114, -9.687359867659742108, -7.698027285532567099 ) ) ;
#56815=CARTESIAN_POINT ( 'NONE',  ( 0.2646305136544065406, 9.465888453932961966, 7.770320294339206235 ) ) ;
#56831=ORIENTED_EDGE ( 'NONE', *, *, #19154, .T. ) ;
#56833=CARTESIAN_POINT ( 'NONE',  ( 0.2655924914740778742, 7.838010948425171875, -9.409507842005947253 ) ) ;
#56846=ORIENTED_EDGE ( 'NONE', *, *, #6098, .F. ) ;
#56849=CARTESIAN_POINT ( 'NONE',  ( 2.665405856346782620, 8.559192023451593911, -4.274976649834382414 ) ) ;
#56850=EDGE_CURVE ( 'NONE', #28847, #19799, #21556, .T. ) ;
#56858=VERTEX_POINT ( 'NONE', #36576 ) ;
#56859=ORIENTED_EDGE ( 'NONE', *, *, #55077, .T. ) ;
#56862=CARTESIAN_POINT ( 'NONE',  ( 1.459561108993787437, -12.08294179906958554, -3.725588117663319210 ) ) ;
#56866=CARTESIAN_POINT ( 'NONE',  ( 3.152665057735396736, -5.761241965768377327, 5.461013642406604696 ) ) ;
#56879=CARTESIAN_POINT ( 'NONE',  ( 0.2759803524722184154, -2.313459762622620097, 12.02930579076649131 ) ) ;
#56882=EDGE_CURVE ( 'NONE', #13729, #16301, #24732, .T. ) ;
#56887=CARTESIAN_POINT ( 'NONE',  ( 5.536195898058073439, 0.008071068258923183927, -0.002666509901869637631 ) ) ;
#56894=CARTESIAN_POINT ( 'NONE',  ( 0.2869720083484334494, 2.332746648244354404, -12.02930764912518313 ) ) ;
#56896=CARTESIAN_POINT ( 'NONE',  ( 2.573738926104373714, 3.667129335223202613, 6.822065037112445829 ) ) ;
#56899=B_SPLINE_CURVE_WITH_KNOTS ( 'NONE', 3,
 ( #12049, #46647, #36985, #7378, #27030, #12368, #21726, #16403, #57630, #42616, #22703, #1101, #36670, #62260, #2077, #57956, #63244, #58273, #57290 ),
 .UNSPECIFIED., .F., .F.,
 ( 4, 3, 3, 3, 3, 3, 4 ),
 ( 8.930035652772277260E-18, 2.825908398831343367E-05, 4.208813692484080383E-05, 5.591713746944121247E-05, 6.279584083232122042E-05, 9.105792820296874294E-05, 0.0001153131102488825452 ),
 .UNSPECIFIED. ) ;
#56904=CARTESIAN_POINT ( 'NONE',  ( 2.305787727787084407, 0.1666591538753756929, -7.654065630109506024 ) ) ;
#56907=( BOUNDED_SURFACE ( )  B_SPLINE_SURFACE ( 3, 1, ( 
 ( #13440, #44043 ),
 ( #33410, #12450 ),
 ( #38052, #2165 ),
 ( #22791, #23104 ) ),
 .UNSPECIFIED., .F., .F., .F. ) 
 B_SPLINE_SURFACE_WITH_KNOTS ( ( 4, 4 ),
 ( 2, 2 ),
 ( 0.000000000000000000, 1.000000000000000000 ),
 ( 0.000000000000000000, 1.000000000000000000 ),
 .UNSPECIFIED. ) 
 GEOMETRIC_REPRESENTATION_ITEM ( )  RATIONAL_B_SPLINE_SURFACE ( (
 ( 1.000000000000000000, 1.000000000000000000),
 ( 0.6933888150995267674, 0.9895912004443193632),
 ( 0.6933888150995267674, 0.9895912004443193632),
 ( 1.000000000000000000, 1.000000000000000000) ) ) 
 REPRESENTATION_ITEM ( '' )  SURFACE ( )  );
#56910=CARTESIAN_POINT ( 'NONE',  ( 2.491965175174466474, -6.575382551509648899, 4.041154086925387467 ) ) ;
#56912=CARTESIAN_POINT ( 'NONE',  ( 1.283627346226613009, -7.660435136228935349, 9.985833283678374528 ) ) ;
#56913=CARTESIAN_POINT ( 'NONE',  ( 0.3006302518452044215, -1.905681544119320892, 12.10891847026071844 ) ) ;
#56918=LINE ( 'NONE', #6696, #34427 ) ;
#56920=EDGE_CURVE ( 'NONE', #21262, #5276, #27154, .T. ) ;
#56928=( BOUNDED_SURFACE ( )  B_SPLINE_SURFACE ( 3, 1, ( 
 ( #36321, #36655 ),
 ( #56956, #62555 ),
 ( #17017, #31646 ),
 ( #61270, #51961 ) ),
 .UNSPECIFIED., .F., .F., .F. ) 
 B_SPLINE_SURFACE_WITH_KNOTS ( ( 4, 4 ),
 ( 2, 2 ),
 ( 0.000000000000000000, 1.000000000000000000 ),
 ( 0.000000000000000000, 1.000000000000000000 ),
 .UNSPECIFIED. ) 
 GEOMETRIC_REPRESENTATION_ITEM ( )  RATIONAL_B_SPLINE_SURFACE ( (
 ( 1.000000000000000000, 1.000000000000000000),
 ( 0.6933888150995267674, 0.9895912004443193632),
 ( 0.6933888150995267674, 0.9895912004443193632),
 ( 1.000000000000000000, 1.000000000000000000) ) ) 
 REPRESENTATION_ITEM ( '' )  SURFACE ( )  );
#56935=CARTESIAN_POINT ( 'NONE',  ( 3.152665057735980714, 1.848755561853925533, 7.719888720907654545 ) ) ;
#56943=VERTEX_POINT ( 'NONE', #28882 ) ;
#56956=CARTESIAN_POINT ( 'NONE',  ( 5.530133899448235191, 0.01149180883054544931, 0.01111090067015091734 ) ) ;
#56969=CARTESIAN_POINT ( 'NONE',  ( 0.6473888112830220587, 4.540486098228977419, 11.51036712212681401 ) ) ;
#56970=CARTESIAN_POINT ( 'NONE',  ( 3.152665057734129306, -7.923639299008720549, -0.4801242025592799556 ) ) ;
#56973=CARTESIAN_POINT ( 'NONE',  ( 5.514624014163232779, -0.002529391395135328728, -0.003278974416024598489 ) ) ;
#56980=ORIENTED_EDGE ( 'NONE', *, *, #37229, .F. ) ;
#56983=VERTEX_POINT ( 'NONE', #13572 ) ;
#56984=CARTESIAN_POINT ( 'NONE',  ( 0.2958664285830420737, -5.936220506376309380, 10.72286791615087154 ) ) ;
#56987=LINE ( 'NONE', #11412, #36935 ) ;
#56996=EDGE_CURVE ( 'NONE', #44680, #46784, #48217, .T. ) ;
#57003=CARTESIAN_POINT ( 'NONE',  ( 1.719304012338401133, 5.690355757826538685, 11.38834240361399885 ) ) ;
#57004=B_SPLINE_CURVE_WITH_KNOTS ( 'NONE', 3,
 ( #58336, #13741, #44027, #18765, #23757, #64605, #44330, #38709, #13423, #58688, #3487, #39023, #8443, #59010, #17772, #63623, #3819, #39346, #29065 ),
 .UNSPECIFIED., .F., .F.,
 ( 4, 3, 3, 3, 3, 3, 4 ),
 ( 1.987375409620156722E-18, 2.831840207499653289E-05, 4.217266859840511053E-05, 5.602024318396140769E-05, 6.290810167969449146E-05, 9.120440630945766665E-05, 0.0001153103026479744905 ),
 .UNSPECIFIED. ) ;
#57009=CARTESIAN_POINT ( 'NONE',  ( 2.241536586108913820, -4.912162027558446553, -5.844297002038589817 ) ) ;
#57010=CARTESIAN_POINT ( 'NONE',  ( 2.268878695253351729, -7.642144312464380640, -0.1481365927654333114 ) ) ;
#57014=CARTESIAN_POINT ( 'NONE',  ( 1.719304012338199517, 0.000000000000000000, -12.73084802173761787 ) ) ;
#57033=EDGE_CURVE ( 'NONE', #49321, #45757, #49378, .T. ) ;
#57037=CARTESIAN_POINT ( 'NONE',  ( 0.2651627682582937684, 12.04449770099953732, -2.213224986694458885 ) ) ;
#57042=CARTESIAN_POINT ( 'NONE',  ( 0.2657645697724732581, -1.977350809428451983, -12.08564806881062736 ) ) ;
#57050=CARTESIAN_POINT ( 'NONE',  ( 5.516018279890452902, -0.003191189039764480428, 0.005976902763918706153 ) ) ;
#57051=ORIENTED_EDGE ( 'NONE', *, *, #38212, .T. ) ;
#57054=CARTESIAN_POINT ( 'NONE',  ( 0.3675815128205912052, -12.13672785388549080, -1.872154644482208585 ) ) ;
#57056=CARTESIAN_POINT ( 'NONE',  ( 2.368238019615304779, 6.736275681109179736, 3.681632831800409900 ) ) ;
#57057=CARTESIAN_POINT ( 'NONE',  ( 5.514624014163232779, 0.003946330869975252925, 0.001255375129357681665 ) ) ;
#57059=CARTESIAN_POINT ( 'NONE',  ( 2.963017218115621798, 0.9869543242668126215, 7.812878240621073722 ) ) ;
#57062=CARTESIAN_POINT ( 'NONE',  ( 0.2647959493198541181, -4.326188315749660340, -11.45640103018463130 ) ) ;
#57068=CARTESIAN_POINT ( 'NONE',  ( 0.2869720083484367246, -11.44147823180128043, -4.386174336869709478 ) ) ;
#57076=ORIENTED_EDGE ( 'NONE', *, *, #48405, .F. ) ;
#57078=CARTESIAN_POINT ( 'NONE',  ( 0.5547464869798240938, -11.49049644196206899, 4.506704303875415540 ) ) ;
#57079=ADVANCED_FACE ( 'NONE', ( #52116 ), #48749, .F. ) ;
#57081=CARTESIAN_POINT ( 'NONE',  ( 2.305787727787084407, 1.493241775258423720, 7.508843116234161563 ) ) ;
#57083=DIRECTION ( 'NONE',  ( -1.000000000000000000, 0.000000000000000000, 0.000000000000000000 ) ) ;
#57094=CARTESIAN_POINT ( 'NONE',  ( 2.241449424704146320, 1.265244293929188579, -7.528892370271778489 ) ) ;
#57096=CARTESIAN_POINT ( 'NONE',  ( 0.2646305136544065406, -4.064188116014626040, 11.55263159009957263 ) ) ;
#57097=CARTESIAN_POINT ( 'NONE',  ( 0.2648978790185584908, 6.237101853238694815, -10.53870023327857197 ) ) ;
#57102=CARTESIAN_POINT ( 'NONE',  ( 2.290907136833257418, 7.504812001538602395, 1.488079974904968683 ) ) ;
#57104=( BOUNDED_SURFACE ( )  B_SPLINE_SURFACE ( 3, 1, ( 
 ( #17204, #41813 ),
 ( #57122, #36147 ),
 ( #42438, #7208 ),
 ( #6253, #21545 ) ),
 .UNSPECIFIED., .F., .F., .F. ) 
 B_SPLINE_SURFACE_WITH_KNOTS ( ( 4, 4 ),
 ( 2, 2 ),
 ( 0.000000000000000000, 1.000000000000000000 ),
 ( 0.000000000000000000, 1.000000000000000000 ),
 .UNSPECIFIED. ) 
 GEOMETRIC_REPRESENTATION_ITEM ( )  RATIONAL_B_SPLINE_SURFACE ( (
 ( 1.000000000000000000, 1.000000000000000000),
 ( 0.9942764183789327692, 0.8450855930916580938),
 ( 0.9942764183789327692, 0.8450855930916580938),
 ( 1.000000000000000000, 1.000000000000000000) ) ) 
 REPRESENTATION_ITEM ( '' )  SURFACE ( )  );
#57107=CARTESIAN_POINT ( 'NONE',  ( 2.963017218115632012, 4.265970453344018587, -6.619413971958168830 ) ) ;
#57110=CARTESIAN_POINT ( 'NONE',  ( 2.907497136250430714, -3.021847490615451992, -7.252103438786913436 ) ) ;
#57112=B_SPLINE_CURVE_WITH_KNOTS ( 'NONE', 3,
 ( #60148, #64790, #14571, #24244, #59837, #25225, #28916 ),
 .UNSPECIFIED., .F., .F.,
 ( 4, 3, 4 ),
 ( 0.000000000000000000, 0.001700533616330529530, 0.005002426799372189890 ),
 .UNSPECIFIED. ) ;
#57119=ORIENTED_EDGE ( 'NONE', *, *, #16212, .F. ) ;
#57122=CARTESIAN_POINT ( 'NONE',  ( 5.515188684475870851, 0.004804816249379309685, 0.002355816063606825262 ) ) ;
#57123=CARTESIAN_POINT ( 'NONE',  ( 2.276198483117258142, 1.479169956994163870, -7.501576331167719047 ) ) ;
#57126=CARTESIAN_POINT ( 'NONE',  ( 2.889800649504073782, -3.986129653162679087, 4.645655809191351793 ) ) ;
#57128=CARTESIAN_POINT ( 'NONE',  ( 2.941278708680199916, -4.788765081995603801, -3.842273877444612129 ) ) ;
#57131=CARTESIAN_POINT ( 'NONE',  ( 0.3537226245948368875, 6.362463382302413706, -10.49813096858602890 ) ) ;
#57150=CARTESIAN_POINT ( 'NONE',  ( 3.152665057734040488, 0.000000000000000000, 0.000000000000000000 ) ) ;
#57155=CARTESIAN_POINT ( 'NONE',  ( 0.5572780756296079607, 12.20533540249751248, -1.841882550626559922 ) ) ;
#57157=CARTESIAN_POINT ( 'NONE',  ( 1.547277799338534710, -5.744300480442291246, 11.29700934613309293 ) ) ;
#57160=ADVANCED_FACE ( 'NONE', ( #5597 ), #29548, .T. ) ;
#57169=CARTESIAN_POINT ( 'NONE',  ( 2.969415267404682091, 3.055358878717733706, 7.260393470501830038 ) ) ;
#57174=ORIENTED_EDGE ( 'NONE', *, *, #55958, .F. ) ;
#57178=CARTESIAN_POINT ( 'NONE',  ( 0.2834382757448007384, 4.380429851625326165, 11.44241760114836914 ) ) ;
#57193=CARTESIAN_POINT ( 'NONE',  ( 0.2646305136544072623, 0.1321451301297840164, 12.24595685781654630 ) ) ;
#57194=CARTESIAN_POINT ( 'NONE',  ( 0.2671309869109488311, -7.995521393275754285, -9.276621593297592838 ) ) ;
#57195=CARTESIAN_POINT ( 'NONE',  ( 5.515188684475870851, -0.002355816063606962739, -0.004804816249378818759 ) ) ;
#57198=ORIENTED_EDGE ( 'NONE', *, *, #38849, .T. ) ;
#57205=CARTESIAN_POINT ( 'NONE',  ( 2.406456491625719618, 6.212289237905720185, -8.382123850279317168 ) ) ;
#57211=CARTESIAN_POINT ( 'NONE',  ( 0.2651627923886310523, -2.039714259676093544, -12.07509237025072935 ) ) ;
#57213=CARTESIAN_POINT ( 'NONE',  ( 5.520433897694421610, -0.005630909886753050243, -0.01397038704729912546 ) ) ;
#57216=CARTESIAN_POINT ( 'NONE',  ( 1.937114397841935398, -11.72279974487467236, 5.226660192101551416 ) ) ;
#57217=EDGE_CURVE ( 'NONE', #16200, #34346, #39683, .T. ) ;
#57218=EDGE_CURVE ( 'NONE', #27530, #7920, #12901, .T. ) ;
#57233=DIRECTION ( 'NONE',  ( 0.000000000000000000, 0.000000000000000000, 1.000000000000000000 ) ) ;
#57247=CARTESIAN_POINT ( 'NONE',  ( 2.241536586108912488, 4.912162027558490074, 5.844297002038559619 ) ) ;
#57264=FACE_OUTER_BOUND ( 'NONE', #4480, .T. ) ;
#57270=ORIENTED_EDGE ( 'NONE', *, *, #1033, .F. ) ;
#57275=CARTESIAN_POINT ( 'NONE',  ( 3.152665057734045373, -6.378477742800418682, 4.725420687650736085 ) ) ;
#57279=ORIENTED_EDGE ( 'NONE', *, *, #5860, .F. ) ;
#57290=CARTESIAN_POINT ( 'NONE',  ( 2.241352910868908310, -5.794346703933879184, 4.970878533273742406 ) ) ;
#57293=ORIENTED_EDGE ( 'NONE', *, *, #40818, .F. ) ;
#57295=CARTESIAN_POINT ( 'NONE',  ( 0.3537226245948391079, -12.27287980220284425, -0.2609894354290803187 ) ) ;
#57304=CARTESIAN_POINT ( 'NONE',  ( 0.3006302518452070860, -5.932248915294235481, 10.72687985734940064 ) ) ;
#57310=CARTESIAN_POINT ( 'NONE',  ( 1.020182472823633058, -11.58401323226483370, -4.691131056023109203 ) ) ;
#57313=CARTESIAN_POINT ( 'NONE',  ( 1.283627346226880794, -0.5505361391623975198, -12.57362488724982086 ) ) ;
#57315=CARTESIAN_POINT ( 'NONE',  ( 0.3654063281920739148, -7.689576266239727786, 9.573804659448637011 ) ) ;
#57317=CARTESIAN_POINT ( 'NONE',  ( 2.368238019615417134, -7.674602282636111994, 0.1797502808085719161 ) ) ;
#57321=EDGE_LOOP ( 'NONE', ( #37517, #24278, #11024, #60990 ) ) ;
#57327=CARTESIAN_POINT ( 'NONE',  ( 1.287602823385623152, -4.819820779359250018, 11.62763122279965522 ) ) ;
#57330=CARTESIAN_POINT ( 'NONE',  ( 2.305787727787084407, 6.545285700970527643, 3.971363876083986888 ) ) ;
#57336=ORIENTED_EDGE ( 'NONE', *, *, #19776, .F. ) ;
#57355=CARTESIAN_POINT ( 'NONE',  ( 0.2657645697724715927, 4.330388001246573637, -11.45515365350257042 ) ) ;
#57362=VERTEX_POINT ( 'NONE', #6092 ) ;
#57365=CARTESIAN_POINT ( 'NONE',  ( 3.152665057735448251, 0.9030954876725900693, -7.886634106564547331 ) ) ;
#57370=ORIENTED_EDGE ( 'NONE', *, *, #42690, .T. ) ;
#57371=CARTESIAN_POINT ( 'NONE',  ( 3.152665057736253829, 5.761241965767907480, -5.461013642407265500 ) ) ;
#57373=CARTESIAN_POINT ( 'NONE',  ( 2.259830038564642596, -4.804964945109423624, -5.940579220576854169 ) ) ;
#57375=EDGE_CURVE ( 'NONE', #34835, #61726, #54124, .T. ) ;
#57377=CARTESIAN_POINT ( 'NONE',  ( 2.589278595513552883, 6.829211973730671126, 3.664724287895261945 ) ) ;
#57382=AXIS2_PLACEMENT_3D ( 'NONE', #12870, #38130, #12524 ) ;
#57385=DIRECTION ( 'NONE',  ( 0.000000000000000000, 0.000000000000000000, 1.000000000000000000 ) ) ;
#57391=CARTESIAN_POINT ( 'NONE',  ( 3.152665057734040488, 0.000000000000000000, 0.000000000000000000 ) ) ;
#57406=CARTESIAN_POINT ( 'NONE',  ( 5.514624014163232779, -0.003498325728817824280, 0.002216125254993654876 ) ) ;
#57409=ORIENTED_EDGE ( 'NONE', *, *, #57218, .F. ) ;
#57410=CARTESIAN_POINT ( 'NONE',  ( 2.251152103363643686, -7.218942724308478276, -2.494172441821568498 ) ) ;
#57414=CARTESIAN_POINT ( 'NONE',  ( 2.241352910868908310, 1.243507963608194045, -7.532448145350496560 ) ) ;
#57430=CARTESIAN_POINT ( 'NONE',  ( 2.253265082352433168, -3.929729351083036448, 6.549959928643428242 ) ) ;
#57431=CARTESIAN_POINT ( 'NONE',  ( 0.2872850955227733705, -10.71476594226529855, -5.944938343726364316 ) ) ;
#57440=VECTOR ( 'NONE', #27393, 1000.000000000000114 ) ;
#57441=CARTESIAN_POINT ( 'NONE',  ( 0.3006302518452004802, 7.704827863860923109, -9.533790235540664071 ) ) ;
#57442=EDGE_CURVE ( 'NONE', #16864, #27117, #6555, .T. ) ;
#57445=CARTESIAN_POINT ( 'NONE',  ( 0.2653519890538380555, 6.776488011961817416E-18, -12.24619734961521722 ) ) ;
#57447=ORIENTED_EDGE ( 'NONE', *, *, #52394, .T. ) ;
#57448=CARTESIAN_POINT ( 'NONE',  ( 0.2834382757448011825, 12.09963924911735234, 1.927645269570926523 ) ) ;
#57450=CARTESIAN_POINT ( 'NONE',  ( 0.2650492433740058718, -10.66007796911765126, -6.027445608088962459 ) ) ;
#57464=ORIENTED_EDGE ( 'NONE', *, *, #50393, .T. ) ;
#57473=CARTESIAN_POINT ( 'NONE',  ( 0.2869720083484354478, 1.922200714744161099, 12.10169797402141967 ) ) ;
#57479=CARTESIAN_POINT ( 'NONE',  ( 1.104777566491150997, 3.832109395972810084, -11.92547689818819201 ) ) ;
#57481=CARTESIAN_POINT ( 'NONE',  ( 2.259830038566069899, 5.763537486834052537, 5.015955067337202422 ) ) ;
#57482=CARTESIAN_POINT ( 'NONE',  ( 1.549075743848461251, 12.58108552526874213, -1.533250336941020864 ) ) ;
#57495=CARTESIAN_POINT ( 'NONE',  ( 5.536195898058073439, -0.007896796515810315664, -0.003145317580921232464 ) ) ;
#57500=B_SPLINE_CURVE_WITH_KNOTS ( 'NONE', 3,
 ( #6593, #57131, #21884, #46485, #32159, #7217, #37816, #12523, #36833, #52143, #41824, #12213, #31513, #16230, #22533, #17549, #62413, #937, #41476 ),
 .UNSPECIFIED., .F., .F.,
 ( 4, 3, 3, 3, 3, 3, 4 ),
 ( 9.311523146975038413E-18, 4.457896483014980806E-05, 6.639290541542299884E-05, 8.820687556479185447E-05, 0.0001100173248778954196, 0.0001545671401658161410, 0.0001830328308068609891 ),
 .UNSPECIFIED. ) ;
#57506=EDGE_CURVE ( 'NONE', #58835, #37505, #15941, .T. ) ;
#57510=CARTESIAN_POINT ( 'NONE',  ( 0.3675815128205894289, 4.447030445008180344, 11.44679196252410946 ) ) ;
#57524=CARTESIAN_POINT ( 'NONE',  ( 0.3223008802179246901, -8.069628056118055781, -9.236652594547214434 ) ) ;
#57528=VERTEX_POINT ( 'NONE', #12677 ) ;
#57532=CARTESIAN_POINT ( 'NONE',  ( 0.3665391374699464300, -4.447929964102923961, 11.44911061034385114 ) ) ;
#57533=CARTESIAN_POINT ( 'NONE',  ( 0.3675815128205894289, -0.2638082659429279997, 12.27743992903066150 ) ) ;
#57537=CARTESIAN_POINT ( 'NONE',  ( 2.262775599886257538, -6.687241191563680687, 3.697834000591617709 ) ) ;
#57540=CARTESIAN_POINT ( 'NONE',  ( 0.2911222467163533945, 2.338869407811021706, -12.02952766044173494 ) ) ;
#57541=CARTESIAN_POINT ( 'NONE',  ( 2.177405672432017880, 2.605669267166041969, 10.89176600224714697 ) ) ;
#57542=CARTESIAN_POINT ( 'NONE',  ( 0.2650492433740059828, -2.234874822562814778, -12.04046084639675662 ) ) ;
#57550=CARTESIAN_POINT ( 'NONE',  ( 2.589278595512887193, -0.2408616556819203613, -7.746633201027049331 ) ) ;
#57551=EDGE_CURVE ( 'NONE', #25513, #9187, #46940, .T. ) ;
#57558=CARTESIAN_POINT ( 'NONE',  ( 2.305787727787084407, -6.545285700970554288, 3.971363876083942035 ) ) ;
#57561=CONICAL_SURFACE ( 'NONE', #46972, 7.938172270156617749, 1.280189991382167047 ) ;
#57565=ORIENTED_EDGE ( 'NONE', *, *, #13417, .T. ) ;
#57567=CARTESIAN_POINT ( 'NONE',  ( 2.835339799623983748, 7.825540862019418675, 0.3287452556170962770 ) ) ;
#57577=CARTESIAN_POINT ( 'NONE',  ( 0.2651627923886335503, 11.53745192040748258, -4.105544202112433538 ) ) ;
#57585=CONICAL_SURFACE ( 'NONE', #45904, 7.938172270156617749, 1.280189991382167047 ) ;
#57590=CARTESIAN_POINT ( 'NONE',  ( 2.241526690369556984, -6.602966219605664655, 3.832206765347563326 ) ) ;
#57594=CARTESIAN_POINT ( 'NONE',  ( 0.3040950598368144520, 1.881452845810376528, 12.11647736519422125 ) ) ;
#57595=VERTEX_POINT ( 'NONE', #8364 ) ;
#57598=CARTESIAN_POINT ( 'NONE',  ( 0.3665391374699465965, -1.872534962004882786, 12.13918562134718115 ) ) ;
#57608=ORIENTED_EDGE ( 'NONE', *, *, #49142, .T. ) ;
#57630=CARTESIAN_POINT ( 'NONE',  ( 2.263328370261525446, -5.761609105518017415, 5.019946231381285706 ) ) ;
#57640=CARTESIAN_POINT ( 'NONE',  ( 1.287602823388407147, -9.277923463524041736, -8.506034117235955705 ) ) ;
#57652=CARTESIAN_POINT ( 'NONE',  ( 5.515188684475870851, 0.005320786921497270942, -0.0005703990286343011730 ) ) ;
#57657=CARTESIAN_POINT ( 'NONE',  ( 0.3341166715381265195, -7.691251065848407897, 9.559079491641842452 ) ) ;
#57660=CARTESIAN_POINT ( 'NONE',  ( 2.781367136452750355, -7.808329083463750209, 0.3081277311327201285 ) ) ;
#57662=ORIENTED_EDGE ( 'NONE', *, *, #33573, .T. ) ;
#57665=ORIENTED_EDGE ( 'NONE', *, *, #29869, .F. ) ;
#57668=CARTESIAN_POINT ( 'NONE',  ( 0.5572780756280620862, -4.507550621618262809, 11.49107179558539649 ) ) ;
#57669=ORIENTED_EDGE ( 'NONE', *, *, #29128, .T. ) ;
#57671=CARTESIAN_POINT ( 'NONE',  ( 0.8320506296491581022, 8.282532257448822932, 9.275353261146570105 ) ) ;
#57672=CARTESIAN_POINT ( 'NONE',  ( 2.903928887688507210, -8.712847781149033466, -0.9983813550131417358 ) ) ;
#57673=CARTESIAN_POINT ( 'NONE',  ( 2.241352910868908310, -5.794346703933879184, 4.970878533273742406 ) ) ;
#57681=VECTOR ( 'NONE', #48825, 1000.000000000000227 ) ;
#57683=CARTESIAN_POINT ( 'NONE',  ( 2.241506898688420790, -7.187425579579784340, -2.574154135948760302 ) ) ;
#57700=CARTESIAN_POINT ( 'NONE',  ( 0.2648978790185593790, 12.08224454301451445, -1.996248716311504801 ) ) ;
#57707=CARTESIAN_POINT ( 'NONE',  ( 2.556980015514294102, -1.570584617272726913, -7.578583798307318986 ) ) ;
#57716=CARTESIAN_POINT ( 'NONE',  ( 0.8320506296491604337, -12.30686996250299714, -1.781423711749702044 ) ) ;
#57730=CARTESIAN_POINT ( 'NONE',  ( 0.2833330754217384118, -9.514385791198149533, 7.719627479384628899 ) ) ;
#57731=CARTESIAN_POINT ( 'NONE',  ( 5.515188684475870851, 0.005140903460551137644, -0.001485678338381731097 ) ) ;
#57738=CARTESIAN_POINT ( 'NONE',  ( 0.9232167919969146430, 11.84868134597557265, 3.872606616958310877 ) ) ;
#57739=CARTESIAN_POINT ( 'NONE',  ( 1.547277799337862136, 0.6737945300320472564, 12.65564732076243182 ) ) ;
#57740=ORIENTED_EDGE ( 'NONE', *, *, #9171, .F. ) ;
#57745=ORIENTED_EDGE ( 'NONE', *, *, #27332, .F. ) ;
#57747=CARTESIAN_POINT ( 'NONE',  ( 1.719304012339844867, -11.67935079956417610, 5.066286238786176455 ) ) ;
#57754=CARTESIAN_POINT ( 'NONE',  ( 5.514970785353741078, -0.002796696073589764915, 0.003805873180274771655 ) ) ;
#57755=CARTESIAN_POINT ( 'NONE',  ( 1.547277799337861692, -3.695326562729266850, 12.12286970032301880 ) ) ;
#57757=ORIENTED_EDGE ( 'NONE', *, *, #9007, .T. ) ;
#57764=CARTESIAN_POINT ( 'NONE',  ( 0.3675815128205894289, 12.13672785388550324, 1.872154644482125763 ) ) ;
#57768=EDGE_CURVE ( 'NONE', #49400, #18739, #30643, .T. ) ;
#57776=CARTESIAN_POINT ( 'NONE',  ( 2.245754705088395475, -3.913944702466310765, 6.556487589645220382 ) ) ;
#57781=CARTESIAN_POINT ( 'NONE',  ( 5.514970785353741078, -0.004588761610585017671, 0.001117786416802601067 ) ) ;
#57783=ORIENTED_EDGE ( 'NONE', *, *, #39920, .T. ) ;
#57788=ORIENTED_EDGE ( 'NONE', *, *, #4625, .T. ) ;
#57790=CARTESIAN_POINT ( 'NONE',  ( 0.3109076770649027432, 12.11383728282219430, 1.896437056876507876 ) ) ;
#57802=CARTESIAN_POINT ( 'NONE',  ( 1.462291587749818600, -8.602888600421563225, 9.267729738232196368 ) ) ;
#57808=EDGE_CURVE ( 'NONE', #46784, #62148, #49322, .T. ) ;
#57811=CARTESIAN_POINT ( 'NONE',  ( 0.2676618633000465430, 1.968216791520492892, 12.08777609394270414 ) ) ;
#57819=CARTESIAN_POINT ( 'NONE',  ( 2.244591118396556784, -1.219892024449305223, 7.537402265771622645 ) ) ;
#57828=CARTESIAN_POINT ( 'NONE',  ( 5.520433897694421610, 0.01491416502703863355, 0.002108682515300534625 ) ) ;
#57834=CARTESIAN_POINT ( 'NONE',  ( 2.280717697724244264, -5.034569468898799194, -5.756537207046680926 ) ) ;
#57838=CARTESIAN_POINT ( 'NONE',  ( 0.3665391374699472626, -2.392238720110378303, -12.04754782681759728 ) ) ;
#57840=ORIENTED_EDGE ( 'NONE', *, *, #48669, .F. ) ;
#57841=CARTESIAN_POINT ( 'NONE',  ( 2.256373768223413290, 3.934258165100065874, 6.548448293197146164 ) ) ;
#57844=B_SPLINE_CURVE_WITH_KNOTS ( 'NONE', 3,
 ( #43187, #22598, #58170, #42864, #13575, #33863, #63460, #12275, #32539, #23244, #48221, #37881, #6975, #48531, #7971, #52850, #42514, #2323, #2982, #43505, #17618, #12591 ),
 .UNSPECIFIED., .F., .F.,
 ( 4, 3, 3, 3, 3, 3, 3, 4 ),
 ( 8.690541527449942710E-19, 4.449119708436876107E-05, 6.626296329540655992E-05, 8.803456484962991020E-05, 0.0001098060367612845804, 0.0001315774408628562759, 0.0001760698110411223073, 0.0001829697163287816132 ),
 .UNSPECIFIED. ) ;
#57846=EDGE_CURVE ( 'NONE', #53953, #14946, #26935, .T. ) ;
#57866=FACE_OUTER_BOUND ( 'NONE', #35504, .T. ) ;
#57867=CARTESIAN_POINT ( 'NONE',  ( 2.261269890822071194, 5.942064862945676040, -4.803890999604265133 ) ) ;
#57870=CARTESIAN_POINT ( 'NONE',  ( 2.717984159218819862, 7.719081760283970084, 1.073093837952745933 ) ) ;
#57871=EDGE_LOOP ( 'NONE', ( #35717, #11016, #47044, #51635 ) ) ;
#57877=ADVANCED_FACE ( 'NONE', ( #62486 ), #53416, .F. ) ;
#57883=LINE ( 'NONE', #47559, #14749 ) ;
#57887=EDGE_CURVE ( 'NONE', #58982, #44487, #14412, .T. ) ;
#57889=ADVANCED_FACE ( 'NONE', ( #57866 ), #64450, .F. ) ;
#57890=ORIENTED_EDGE ( 'NONE', *, *, #47413, .F. ) ;
#57894=CARTESIAN_POINT ( 'NONE',  ( 0.2651627682582926582, 2.213224986694582341, 12.04449770099951422 ) ) ;
#57896=CARTESIAN_POINT ( 'NONE',  ( 1.194176325881349587, -7.670099510969132339, 9.940715479868426740 ) ) ;
#57898=VERTEX_POINT ( 'NONE', #3961 ) ;
#57902=CARTESIAN_POINT ( 'NONE',  ( 2.573738926104377267, 7.741646296020607387, 0.2352053552897726552 ) ) ;
#57910=CARTESIAN_POINT ( 'NONE',  ( 2.276905613633651182, -2.759436818562446270, -7.130967020394719746 ) ) ;
#57911=CARTESIAN_POINT ( 'NONE',  ( 2.249013661412873510, 7.134443398813564485, 2.724484898588741100 ) ) ;
#57913=ORIENTED_EDGE ( 'NONE', *, *, #8650, .T. ) ;
#57914=CARTESIAN_POINT ( 'NONE',  ( 0.2869720083484405548, 12.10169797402142677, -1.922200714744033645 ) ) ;
#57916=CARTESIAN_POINT ( 'NONE',  ( 3.152665057734120868, 6.378477742800529704, -4.725420687650643714 ) ) ;
#57920=CARTESIAN_POINT ( 'NONE',  ( 2.241509619876137727, -6.630717740088877932, 3.784042210004685103 ) ) ;
#57930=CARTESIAN_POINT ( 'NONE',  ( 2.247112776669942580, 6.670755883243522533, 3.716786765235448708 ) ) ;
#57933=CARTESIAN_POINT ( 'NONE',  ( 2.556980015514017435, 7.348538402679566595, 2.429125721802398719 ) ) ;
#57935=CARTESIAN_POINT ( 'NONE',  ( 2.305787727787084407, -7.508843116234166004, 1.493241775258399073 ) ) ;
#57949=EDGE_CURVE ( 'NONE', #8885, #62664, #31839, .T. ) ;
#57954=B_SPLINE_CURVE_WITH_KNOTS ( 'NONE', 3,
 ( #50155, #58851, #23577, #24211, #33549, #18610, #3648 ),
 .UNSPECIFIED., .F., .F.,
 ( 4, 3, 4 ),
 ( 2.764715539838036307E-18, 6.607593386745461920E-05, 0.0001321430428584417424 ),
 .UNSPECIFIED. ) ;
#57955=CARTESIAN_POINT ( 'NONE',  ( 5.514970785353741078, -0.003805873180274799410, -0.002796696073589726318 ) ) ;
#57956=CARTESIAN_POINT ( 'NONE',  ( 2.244591118396555895, -5.779440292195805462, 4.989853642775300635 ) ) ;
#57960=CARTESIAN_POINT ( 'NONE',  ( 2.242819959140646358, -0.1024002568249904599, 7.634209046698944512 ) ) ;
#57961=CARTESIAN_POINT ( 'NONE',  ( 0.2706063244538045032, -12.24670371972917948, -0.1752385892653291755 ) ) ;
#57967=CARTESIAN_POINT ( 'NONE',  ( 2.241526690369557429, 4.894066724724331685, -5.859443871526991643 ) ) ;
#57975=CARTESIAN_POINT ( 'NONE',  ( 2.263328370261528111, -7.131064289852361071, 2.746620058315270896 ) ) ;
#57981=ORIENTED_EDGE ( 'NONE', *, *, #323, .F. ) ;
#57987=CARTESIAN_POINT ( 'NONE',  ( 1.452237505248552996, -12.08199618361515526, 3.767214359061084927 ) ) ;
#57990=VERTEX_POINT ( 'NONE', #29226 ) ;
#57992=CARTESIAN_POINT ( 'NONE',  ( 2.241451721903216843, -4.860585618235927718, -5.887257931662889909 ) ) ;
#57993=EDGE_CURVE ( 'NONE', #22233, #10582, #33827, .T. ) ;
#57997=CARTESIAN_POINT ( 'NONE',  ( 5.514970785353741078, -0.004324946436530173639, -0.001897634820904526036 ) ) ;
#58005=VERTEX_POINT ( 'NONE', #43861 ) ;
#58009=CARTESIAN_POINT ( 'NONE',  ( 5.530133899448235191, 0.01437126147332034622, -0.006998616117863649434 ) ) ;
#58019=CARTESIAN_POINT ( 'NONE',  ( 0.2706063244538070012, 4.353289770698386185, -11.44820198696410962 ) ) ;
#58023=CARTESIAN_POINT ( 'NONE',  ( 0.2653141334712594834, 12.05242949860146595, -2.169900597054395863 ) ) ;
#58024=DIRECTION ( 'NONE',  ( -0.000000000000000000, 0.000000000000000000, 1.000000000000000000 ) ) ;
#58027=CARTESIAN_POINT ( 'NONE',  ( 0.3278977287071224711, -1.885359334311883961, -12.12129679591848763 ) ) ;
#58029=CARTESIAN_POINT ( 'NONE',  ( 3.152665057736135701, -1.848755561854027452, -7.719888720907647439 ) ) ;
#58034=CARTESIAN_POINT ( 'NONE',  ( 3.152665057734040488, 0.000000000000000000, 0.000000000000000000 ) ) ;
#58038=CARTESIAN_POINT ( 'NONE',  ( 0.3006302518452041439, 2.350739146140591984, 12.03044280705495161 ) ) ;
#58046=CARTESIAN_POINT ( 'NONE',  ( 0.2801149460245132006, -4.374013318106476866, -11.44368419510490575 ) ) ;
#58050=CARTESIAN_POINT ( 'NONE',  ( 2.241528039335009215, 7.521191296022435857, -1.310213701658512697 ) ) ;
#58052=CARTESIAN_POINT ( 'NONE',  ( 2.305787727787084407, 3.682701754025606178, -6.711944854845784292 ) ) ;
#58053=CARTESIAN_POINT ( 'NONE',  ( 0.2648978790185584908, 6.008231198268983775, 10.67083876753494032 ) ) ;
#58054=CARTESIAN_POINT ( 'NONE',  ( 1.633930747250947890, 0.7186603069032649893, 12.68212725188713286 ) ) ;
#58058=CARTESIAN_POINT ( 'NONE',  ( 2.241509619876138171, -0.03828218718775380086, 7.634391113243450988 ) ) ;
#58059=VERTEX_POINT ( 'NONE', #65110 ) ;
#58060=B_SPLINE_CURVE_WITH_KNOTS ( 'NONE', 3,
 ( #40375, #59368, #3542, #60340, #34079, #3864, #55359, #50396, #59702, #29427, #4171, #60033, #30083, #35050, #28774, #64998, #54398, #4842, #14449 ),
 .UNSPECIFIED., .F., .F.,
 ( 4, 3, 3, 3, 3, 3, 4 ),
 ( 5.131381242747340533E-18, 2.825908398991825956E-05, 4.208813692703089221E-05, 5.591713747221501498E-05, 6.279584083538142171E-05, 9.105792820727961210E-05, 0.0001153131102486980953 ),
 .UNSPECIFIED. ) ;
#58072=CARTESIAN_POINT ( 'NONE',  ( 0.3675815128205894289, -3.951233083390547129, 11.62724744438064306 ) ) ;
#58073=CARTESIAN_POINT ( 'NONE',  ( 0.2648978790185593790, 11.55204314799269305, -4.063980959784929681 ) ) ;
#58086=ORIENTED_EDGE ( 'NONE', *, *, #32199, .F. ) ;
#58089=CARTESIAN_POINT ( 'NONE',  ( 0.2651627923886317739, -6.199207987242170148, 10.56116046379971962 ) ) ;
#58093=CARTESIAN_POINT ( 'NONE',  ( 0.2648978790185602672, -11.55204314799261311, -4.063980959785162383 ) ) ;
#58095=VERTEX_POINT ( 'NONE', #65429 ) ;
#58096=CARTESIAN_POINT ( 'NONE',  ( 0.2655924914740778742, 11.52280271232870845, 4.147079829127291006 ) ) ;
#58106=CARTESIAN_POINT ( 'NONE',  ( 0.2717059086739011531, 12.09156413799790464, 1.953280559502737157 ) ) ;
#58107=LINE ( 'NONE', #18545, #59755 ) ;
#58108=CARTESIAN_POINT ( 'NONE',  ( 2.491965175174627678, -1.130870800982672009, 7.634639040875272009 ) ) ;
#58110=ADVANCED_FACE ( 'NONE', ( #9245 ), #62321, .F. ) ;
#58113=ORIENTED_EDGE ( 'NONE', *, *, #36328, .T. ) ;
#58115=FACE_OUTER_BOUND ( 'NONE', #35196, .T. ) ;
#58116=CARTESIAN_POINT ( 'NONE',  ( 5.515188684475870851, 0.001283816547385122813, 0.005194992164431777061 ) ) ;
#58119=CARTESIAN_POINT ( 'NONE',  ( 0.7446945582518111895, -8.243982823409156779, 9.270687147117351756 ) ) ;
#58120=CARTESIAN_POINT ( 'NONE',  ( 2.406456491626289385, -10.14681500356121013, 2.427896847126302049 ) ) ;
#58130=CARTESIAN_POINT ( 'NONE',  ( 1.948354844646196460, 11.63671644762978197, -2.783443994772825114 ) ) ;
#58131=CARTESIAN_POINT ( 'NONE',  ( 2.241509619876137283, 0.03828218718780714014, -7.634391113243452764 ) ) ;
#58132=CARTESIAN_POINT ( 'NONE',  ( 2.844750968614003117, 7.828506085987995355, -0.3326424433124895996 ) ) ;
#58133=CARTESIAN_POINT ( 'NONE',  ( 2.249013661412875287, 5.772355099775897891, 5.000301708457582706 ) ) ;
#58141=CARTESIAN_POINT ( 'NONE',  ( 1.287602823388787066, 8.506034117236191960, -9.277923463523999104 ) ) ;
#58151=DIRECTION ( 'NONE',  ( 0.000000000000000000, 0.000000000000000000, 1.000000000000000000 ) ) ;
#58158=CARTESIAN_POINT ( 'NONE',  ( 0.3675815128205894289, 11.44679196252409348, 4.447030445008218535 ) ) ;
#58159=EDGE_CURVE ( 'NONE', #60104, #35544, #44074, .T. ) ;
#58166=CARTESIAN_POINT ( 'NONE',  ( 5.514624014163232779, 0.0008859786816842089114, -0.004045310349816142945 ) ) ;
#58170=CARTESIAN_POINT ( 'NONE',  ( 0.2671309869109498303, -11.56263543972755592, -4.036029264453098619 ) ) ;
#58173=EDGE_CURVE ( 'NONE', #46419, #29718, #58342, .T. ) ;
#58177=ORIENTED_EDGE ( 'NONE', *, *, #40300, .F. ) ;
#58179=CARTESIAN_POINT ( 'NONE',  ( 0.3474126878361830650, 10.75620725594716021, 5.911350916722074800 ) ) ;
#58180=CARTESIAN_POINT ( 'NONE',  ( 2.241311220309555097, 5.907514893712990656, -4.835827934490959379 ) ) ;
#58184=CARTESIAN_POINT ( 'NONE',  ( 3.031336079628654367, 7.839300734792826297, 0.9593005538809813437 ) ) ;
#58190=CARTESIAN_POINT ( 'NONE',  ( 0.2648978790185584908, -1.996248716311547433, -12.08224454301450734 ) ) ;
#58193=CARTESIAN_POINT ( 'NONE',  ( 0.3675815128205894289, 10.76447900494948584, -5.910255304480332761 ) ) ;
#58194=ORIENTED_EDGE ( 'NONE', *, *, #49065, .F. ) ;
#58196=CARTESIAN_POINT ( 'NONE',  ( 2.406456491624854976, -4.662370073865575115, 9.333533259768456603 ) ) ;
#58202=CARTESIAN_POINT ( 'NONE',  ( 0.2638984909335716500, 10.50550771760519986, 6.295352574289022840 ) ) ;
#58213=CARTESIAN_POINT ( 'NONE',  ( 0.2655924914740778742, -2.083162675473693604, 12.06787830249864513 ) ) ;
#58219=CARTESIAN_POINT ( 'NONE',  ( 2.305787727787083519, -2.774453000917102230, -7.135468203930011910 ) ) ;
#58220=DIRECTION ( 'NONE',  ( -1.000000000000000000, 0.000000000000000000, 0.000000000000000000 ) ) ;
#58224=CARTESIAN_POINT ( 'NONE',  ( 2.290907136833251201, 2.463690939638674582, 7.243397831411258814 ) ) ;
#58225=VERTEX_POINT ( 'NONE', #53735 ) ;
#58228=CARTESIAN_POINT ( 'NONE',  ( 2.258463476536646475, 3.701774005560860115, 6.683417898966894199 ) ) ;
#58231=EDGE_CURVE ( 'NONE', #31007, #23822, #64021, .T. ) ;
#58241=ORIENTED_EDGE ( 'NONE', *, *, #40930, .F. ) ;
#58243=LINE ( 'NONE', #64520, #34954 ) ;
#58244=CARTESIAN_POINT ( 'NONE',  ( 0.2915757698887306848, 12.02962099476165569, -2.339174865979159357 ) ) ;
#58251=CARTESIAN_POINT ( 'NONE',  ( 2.305787727787084407, -6.711944854845797614, -3.682701754025583085 ) ) ;
#58252=B_SPLINE_CURVE_WITH_KNOTS ( 'NONE', 3,
 ( #15768, #37373, #21782, #31084, #1157, #21439, #41051, #42032, #42339, #62626, #62312, #46067, #5507, #56347, #51395, #61657 ),
 .UNSPECIFIED., .F., .F.,
 ( 4, 3, 3, 3, 3, 4 ),
 ( 2.710505431213761085E-19, 0.0003017745587525266565, 0.0006035491769808777520, 0.0009053241094668224281, 0.001207275924539992148, 0.001510325902532976602 ),
 .UNSPECIFIED. ) ;
#58256=CARTESIAN_POINT ( 'NONE',  ( 2.241526690369557873, -1.342748965918832971, -7.515450538999847829 ) ) ;
#58263=AXIS2_PLACEMENT_3D ( 'NONE', #14974, #31589, #20654 ) ;
#58273=CARTESIAN_POINT ( 'NONE',  ( 2.241317068080791230, -5.789053609344619211, 4.977030124433455605 ) ) ;
#58278=EDGE_CURVE ( 'NONE', #24195, #46588, #30212, .T. ) ;
#58293=CARTESIAN_POINT ( 'NONE',  ( 2.273267844204865273, -7.130811676080292649, 2.756477528575274061 ) ) ;
#58296=CARTESIAN_POINT ( 'NONE',  ( 3.152665057734128862, 5.761241965769081652, 5.461013642405580626 ) ) ;
#58303=LINE ( 'NONE', #11739, #29205 ) ;
#58307=ORIENTED_EDGE ( 'NONE', *, *, #1033, .T. ) ;
#58313=DIRECTION ( 'NONE',  ( 0.000000000000000000, 0.000000000000000000, 1.000000000000000000 ) ) ;
#58314=CARTESIAN_POINT ( 'NONE',  ( 0.3610902822527289335, -3.951920836718799457, 11.62472836966322731 ) ) ;
#58315=EDGE_CURVE ( 'NONE', #28659, #25549, #10007, .T. ) ;
#58316=CARTESIAN_POINT ( 'NONE',  ( 0.2915757698887286864, 9.524403232224875282, 7.711631695122881602 ) ) ;
#58330=FACE_OUTER_BOUND ( 'NONE', #43650, .T. ) ;
#58333=CARTESIAN_POINT ( 'NONE',  ( 2.241506898688419014, -7.525229609709731093, -1.286963596520069864 ) ) ;
#58334=CARTESIAN_POINT ( 'NONE',  ( 0.9232167919969126446, -10.99620217063211669, -5.871274944231814175 ) ) ;
#58336=CARTESIAN_POINT ( 'NONE',  ( 2.241352910868909643, -5.794346703933810794, -4.970878533273820565 ) ) ;
#58342=CIRCLE ( 'NONE', #12651, 12.73084802173761787 ) ;
#58345=CARTESIAN_POINT ( 'NONE',  ( 5.520433897694421610, -0.004666464468077943101, -0.01432141647227068090 ) ) ;
#58348=CARTESIAN_POINT ( 'NONE',  ( 0.3053067050349179690, -1.901204202464590542, -12.11120005789973142 ) ) ;
#58349=CARTESIAN_POINT ( 'NONE',  ( 1.452237505248555660, -8.579708443906683968, -9.303501428256112149 ) ) ;
#58354=CARTESIAN_POINT ( 'NONE',  ( 5.536195898058073439, -0.008411485181668792652, 0.001224473329857563367 ) ) ;
#58360=CARTESIAN_POINT ( 'NONE',  ( 1.104777566491147001, -12.40974092093471093, -1.703053712365451222 ) ) ;
#58364=CARTESIAN_POINT ( 'NONE',  ( 0.2650492594609233921, -4.084774262246008369, -11.54478160586241309 ) ) ;
#58365=ORIENTED_EDGE ( 'NONE', *, *, #2214, .T. ) ;
#58368=EDGE_CURVE ( 'NONE', #18433, #42715, #11140, .T. ) ;
#58369=CARTESIAN_POINT ( 'NONE',  ( 0.2739690278137290047, -4.360944092821376294, -11.44648082006009560 ) ) ;
#58373=CARTESIAN_POINT ( 'NONE',  ( 0.3040950598368144520, -9.552450779732161834, 7.687624643091400145 ) ) ;
#58375=CARTESIAN_POINT ( 'NONE',  ( 2.256373768223414622, -7.545294827890042022, -1.195444820369755412 ) ) ;
#58376=CARTESIAN_POINT ( 'NONE',  ( 2.491965175174396752, 3.673871285745645920, -6.787433375639467137 ) ) ;
#58379=VERTEX_POINT ( 'NONE', #20304 ) ;
#58380=CARTESIAN_POINT ( 'NONE',  ( 1.719304012341432264, 5.066286238787408358, -11.67935079956426847 ) ) ;
#58382=CARTESIAN_POINT ( 'NONE',  ( 0.2648978790185584908, 10.67083876753500427, -6.008231198268870976 ) ) ;
#58398=B_SPLINE_CURVE_WITH_KNOTS ( 'NONE', 3,
 ( #62345, #27118, #37077, #47414, #1850, #18785, #63995, #8466, #38733, #3169, #23108, #58038, #27762, #63327, #53035, #54025, #12782, #17794, #28108, #52724, #43713, #33073 ),
 .UNSPECIFIED., .F., .F.,
 ( 4, 3, 3, 3, 3, 3, 3, 4 ),
 ( 1.318988870012550486E-18, 4.449119708436802246E-05, 6.626296329540413402E-05, 8.803456484962554629E-05, 0.0001098060367612792949, 0.0001315774408628498792, 0.0001760698110411158834, 0.0001829697163287818842 ),
 .UNSPECIFIED. ) ;
#58399=CARTESIAN_POINT ( 'NONE',  ( 1.719304012340733934, -12.20344780066092305, -3.626341562669774365 ) ) ;
#58405=CARTESIAN_POINT ( 'NONE',  ( 1.719304012339844867, -10.62216384465586216, 7.017415949612814785 ) ) ;
#58413=ORIENTED_EDGE ( 'NONE', *, *, #31019, .T. ) ;
#58421=CARTESIAN_POINT ( 'NONE',  ( 2.290907136833251201, -3.965134647955939950, 6.543263131934282661 ) ) ;
#58429=CARTESIAN_POINT ( 'NONE',  ( 0.2646305136544065406, 11.55263159009964191, -4.064188116014433305 ) ) ;
#58431=CARTESIAN_POINT ( 'NONE',  ( 2.284126774967658591, 1.483972655035312505, -7.503320429541866510 ) ) ;
#58433=CARTESIAN_POINT ( 'NONE',  ( 2.770579946183322928, 2.384572752174086041, 7.437949029067695506 ) ) ;
#58435=CARTESIAN_POINT ( 'NONE',  ( 0.2653141334712559307, -10.62748186152493268, -6.084912053827449263 ) ) ;
#58437=EDGE_CURVE ( 'NONE', #11101, #281, #35725, .T. ) ;
#58439=CARTESIAN_POINT ( 'NONE',  ( 2.256373768223416842, -0.1329433694243792041, -7.638251659827605344 ) ) ;
#58445=ORIENTED_EDGE ( 'NONE', *, *, #14917, .T. ) ;
#58450=CARTESIAN_POINT ( 'NONE',  ( 1.937114397841932290, 11.53912442307263042, -5.620553190832856316 ) ) ;
#58451=CARTESIAN_POINT ( 'NONE',  ( 0.2915757698887289640, -11.44067056871811516, 4.392559307431859850 ) ) ;
#58457=CARTESIAN_POINT ( 'NONE',  ( 5.516018279890452902, -0.005042957932159101465, -0.004525000489649917343 ) ) ;
#58460=CARTESIAN_POINT ( 'NONE',  ( 3.152665057734040488, 0.000000000000000000, 0.000000000000000000 ) ) ;
#58461=CARTESIAN_POINT ( 'NONE',  ( 1.719304012341460908, 3.626341562669523011, -12.20344780066162649 ) ) ;
#58463=CARTESIAN_POINT ( 'NONE',  ( 2.251152103363642798, -1.202724109297136135, 7.542379262759451031 ) ) ;
#58467=CARTESIAN_POINT ( 'NONE',  ( 0.2655924914740778187, -10.62761259256421198, 6.084990060696473968 ) ) ;
#58472=CARTESIAN_POINT ( 'NONE',  ( 2.990245332647814891, -8.130497889782889231, 2.413832934171158406 ) ) ;
#58477=CARTESIAN_POINT ( 'NONE',  ( 2.257661810676415470, 6.547845034191149161, -3.936095962955222127 ) ) ;
#58478=LINE ( 'NONE', #32198, #9538 ) ;
#58480=ORIENTED_EDGE ( 'NONE', *, *, #30635, .F. ) ;
#58488=CARTESIAN_POINT ( 'NONE',  ( 0.3632410797595211904, 4.445654054452527149, 11.44577450250088546 ) ) ;
#58496=CARTESIAN_POINT ( 'NONE',  ( 0.2648978790185602672, 11.55204314799263798, 4.063980959785085112 ) ) ;
#58499=CARTESIAN_POINT ( 'NONE',  ( 2.573738926104314650, 4.796056562246174160, 6.081632213771376527 ) ) ;
#58500=FACE_OUTER_BOUND ( 'NONE', #7025, .T. ) ;
#58503=EDGE_CURVE ( 'NONE', #62889, #33447, #23029, .T. ) ;
#58517=CARTESIAN_POINT ( 'NONE',  ( 2.276198483117257254, 5.955030244776342130, -4.795748742147450727 ) ) ;
#58520=CARTESIAN_POINT ( 'NONE',  ( 2.491965175173322944, 7.634639040874793281, 1.130870800982929802 ) ) ;
#58525=B_SPLINE_CURVE_WITH_KNOTS ( 'NONE', 3,
 ( #56014, #10454, #5500, #36043, #25767, #26101, #20775, #31077, #51387, #46376, #819, #32681, #48020, #2476, #42333, #63289, #16452, #12413, #26746 ),
 .UNSPECIFIED., .F., .F.,
 ( 4, 3, 3, 3, 3, 3, 4 ),
 ( 8.475001095641158209E-18, 4.457896483014948957E-05, 6.639290541542329700E-05, 8.820687556479254565E-05, 0.0001100173248778965173, 0.0001545671401658162494, 0.0001830328308068602031 ),
 .UNSPECIFIED. ) ;
#58528=VECTOR ( 'NONE', #735, 1000.000000000000114 ) ;
#58530=VERTEX_POINT ( 'NONE', #22947 ) ;
#58533=CARTESIAN_POINT ( 'NONE',  ( 0.8320506296491612108, -8.282532257448750102, -9.275353261146616290 ) ) ;
#58534=CARTESIAN_POINT ( 'NONE',  ( 2.241317068080778352, -3.896159243838514641, -6.565357088387215434 ) ) ;
#58535=EDGE_CURVE ( 'NONE', #35691, #26251, #13463, .T. ) ;
#58539=B_SPLINE_CURVE_WITH_KNOTS ( 'NONE', 3,
 ( #10163, #55734, #55392, #40083, #40410, #45406, #4870, #56039, #30442, #25136, #45740, #21114, #60372, #65670, #20143, #50741 ),
 .UNSPECIFIED., .F., .F.,
 ( 4, 3, 3, 3, 3, 4 ),
 ( 0.000000000000000000, 0.0002176109881720239428, 0.0004352086762394612087, 0.0006528017811446903268, 0.0007615147961451737947, 0.0009453342004947317507 ),
 .UNSPECIFIED. ) ;
#58544=CARTESIAN_POINT ( 'NONE',  ( 2.256373768223201015, 5.011614056001653772, 5.765785888499388001 ) ) ;
#58553=CARTESIAN_POINT ( 'NONE',  ( 0.3040950598368152291, 11.43390362554258921, -4.428852722102617712 ) ) ;
#58573=ORIENTED_EDGE ( 'NONE', *, *, #38439, .F. ) ;
#58575=CARTESIAN_POINT ( 'NONE',  ( 0.3040950598368144520, 0.2511348647277356072, -12.25911170648142523 ) ) ;
#58579=CARTESIAN_POINT ( 'NONE',  ( 1.194176325881335599, 11.61285876598812017, -4.773862381874613092 ) ) ;
#58584=CARTESIAN_POINT ( 'NONE',  ( 2.258463476536644254, -7.131741622455323615, -2.740340677911303757 ) ) ;
#58587=CARTESIAN_POINT ( 'NONE',  ( 2.253265082352432724, -2.732639326785855971, 7.132841660187154709 ) ) ;
#58588=ADVANCED_FACE ( 'NONE', ( #49527 ), #43678, .F. ) ;
#58595=CARTESIAN_POINT ( 'NONE',  ( 2.430348790456934527, -7.544199152378932460, 1.528169972228280660 ) ) ;
#58599=VECTOR ( 'NONE', #7375, 1000.000000000000114 ) ;
#58605=CARTESIAN_POINT ( 'NONE',  ( 2.241537034860907163, -1.321063441155939433, -7.519304283075094020 ) ) ;
#58606=CARTESIAN_POINT ( 'NONE',  ( 0.2706063244538038370, -9.268878137104346493, -8.006269958070696191 ) ) ;
#58607=CARTESIAN_POINT ( 'NONE',  ( 0.2648978790185593790, 11.55204314799269305, -4.063980959784929681 ) ) ;
#58613=CARTESIAN_POINT ( 'NONE',  ( 0.2648978790185602672, 6.237101853238547378, 10.53870023327865901 ) ) ;
#58623=ORIENTED_EDGE ( 'NONE', *, *, #55311, .F. ) ;
#58624=CARTESIAN_POINT ( 'NONE',  ( 2.249013661412229581, -0.1200550008339695413, 7.636012530783589547 ) ) ;
#58629=CARTESIAN_POINT ( 'NONE',  ( 0.6511581176972002227, -9.263557799003038440, -8.205008037407102606 ) ) ;
#58631=CARTESIAN_POINT ( 'NONE',  ( 2.268878695254624489, 6.544222817597994180, 3.949362208798293583 ) ) ;
#58632=VERTEX_POINT ( 'NONE', #4633 ) ;
#58637=VECTOR ( 'NONE', #12146, 1000.000000000000114 ) ;
#58640=EDGE_CURVE ( 'NONE', #17330, #36274, #32540, .T. ) ;
#58642=CARTESIAN_POINT ( 'NONE',  ( 2.573738926104372382, 5.779258037547013949, 5.156412073069302160 ) ) ;
#58643=CARTESIAN_POINT ( 'NONE',  ( 2.770579946183331810, -2.954332771348870512, 7.230573341413142785 ) ) ;
#58646=ORIENTED_EDGE ( 'NONE', *, *, #9811, .T. ) ;
#58647=CARTESIAN_POINT ( 'NONE',  ( 0.3474126878361793458, -7.689340002166794363, 9.566300984424369602 ) ) ;
#58660=FACE_OUTER_BOUND ( 'NONE', #30261, .T. ) ;
#58667=ORIENTED_EDGE ( 'NONE', *, *, #64698, .T. ) ;
#58673=ORIENTED_EDGE ( 'NONE', *, *, #18530, .T. ) ;
#58678=ADVANCED_FACE ( 'NONE', ( #21196 ), #50497, .F. ) ;
#58680=CARTESIAN_POINT ( 'NONE',  ( 0.3665391374699465965, 11.62960183138726933, 3.952034409876336252 ) ) ;
#58681=CARTESIAN_POINT ( 'NONE',  ( 0.3675815128205894289, -10.76447900494936327, -5.910255304480558358 ) ) ;
#58684=( BOUNDED_SURFACE ( )  B_SPLINE_SURFACE ( 3, 1, ( 
 ( #21621, #41885 ),
 ( #16625, #36895 ),
 ( #57195, #11620 ),
 ( #12589, #52211 ) ),
 .UNSPECIFIED., .F., .F., .F. ) 
 B_SPLINE_SURFACE_WITH_KNOTS ( ( 4, 4 ),
 ( 2, 2 ),
 ( 0.000000000000000000, 1.000000000000000000 ),
 ( 0.000000000000000000, 1.000000000000000000 ),
 .UNSPECIFIED. ) 
 GEOMETRIC_REPRESENTATION_ITEM ( )  RATIONAL_B_SPLINE_SURFACE ( (
 ( 1.000000000000000000, 1.000000000000000000),
 ( 0.9942764183789327692, 0.8450855930916585379),
 ( 0.9942764183789327692, 0.8450855930916585379),
 ( 1.000000000000000000, 1.000000000000000000) ) ) 
 REPRESENTATION_ITEM ( '' )  SURFACE ( )  );
#58686=CARTESIAN_POINT ( 'NONE',  ( 3.152665057733930798, -5.761241965769118067, -5.461013642405381674 ) ) ;
#58688=CARTESIAN_POINT ( 'NONE',  ( 2.258463476536646475, -5.764393264552599483, -5.014277205346519217 ) ) ;
#58698=CARTESIAN_POINT ( 'NONE',  ( 5.516018279890452902, 0.005331956019561467572, 0.004180585980734550546 ) ) ;
#58704=CARTESIAN_POINT ( 'NONE',  ( 2.034671305879989234, -0.7032348381693109829, 11.65517003033966681 ) ) ;
#58708=CARTESIAN_POINT ( 'NONE',  ( 0.3002738374340845895, 9.243462099800829890, 8.050654058169905980 ) ) ;
#58716=ORIENTED_EDGE ( 'NONE', *, *, #54500, .F. ) ;
#58720=CARTESIAN_POINT ( 'NONE',  ( 1.719304012339893939, -12.38166659046436457, -2.961219984258754767 ) ) ;
#58722=CARTESIAN_POINT ( 'NONE',  ( 0.2646305136544065406, -9.465888453933013480, 7.770320294339142286 ) ) ;
#58730=EDGE_CURVE ( 'NONE', #23561, #51119, #15553, .T. ) ;
#58746=CARTESIAN_POINT ( 'NONE',  ( 2.280717697723838810, 5.756537207046756421, -5.034569468898497213 ) ) ;
#58749=CARTESIAN_POINT ( 'NONE',  ( 5.530133899448235191, -0.01536822665454943594, -0.004396748047611565534 ) ) ;
#58753=CARTESIAN_POINT ( 'NONE',  ( 2.903928887688355331, -7.316175791235651538, 4.835706109686327636 ) ) ;
#58764=CONICAL_SURFACE ( 'NONE', #60875, 7.938172270156617749, 1.280189991382167047 ) ;
#58765=EDGE_CURVE ( 'NONE', #16970, #45562, #50826, .T. ) ;
#58767=CARTESIAN_POINT ( 'NONE',  ( 2.717984159219948737, 4.788867404453592158, -6.148373979319133653 ) ) ;
#58771=CARTESIAN_POINT ( 'NONE',  ( 0.3665391374699467075, 11.44911061034386357, 4.447929964102883993 ) ) ;
#58775=CARTESIAN_POINT ( 'NONE',  ( 2.273267844204864385, 1.476347988307471715, 7.501135923490785729 ) ) ;
#58778=VECTOR ( 'NONE', #49232, 1000.000000000000227 ) ;
#58782=CARTESIAN_POINT ( 'NONE',  ( 0.2648978790185619880, -10.67083876753487637, -6.008231198269095685 ) ) ;
#58796=CARTESIAN_POINT ( 'NONE',  ( 2.889800649504073782, -5.267262008933692563, 3.118861721612547377 ) ) ;
#58799=EDGE_CURVE ( 'NONE', #16694, #32172, #23865, .T. ) ;
#58801=CARTESIAN_POINT ( 'NONE',  ( 0.3341166715381274632, -11.44035855572978733, 4.432780143632454539 ) ) ;
#58805=CARTESIAN_POINT ( 'NONE',  ( 2.241352910868909643, -7.202080440908757986, 2.532612177304417678 ) ) ;
#58807=CARTESIAN_POINT ( 'NONE',  ( 2.931247277082684288, 7.508560300462436388, -2.338794445044915626 ) ) ;
#58812=CARTESIAN_POINT ( 'NONE',  ( 2.245754705088792491, 5.777230445737854048, 4.993005209688604396 ) ) ;
#58813=FACE_OUTER_BOUND ( 'NONE', #25037, .T. ) ;
#58814=ORIENTED_EDGE ( 'NONE', *, *, #39099, .F. ) ;
#58816=EDGE_CURVE ( 'NONE', #47920, #28421, #62691, .T. ) ;
#58821=DIRECTION ( 'NONE',  ( -0.3865475372811021382, 0.4442537292684497485, -0.8082200352954570510 ) ) ;
#58827=CARTESIAN_POINT ( 'NONE',  ( 2.247112776671465362, 6.554209700764031865, -3.918650674719026394 ) ) ;
#58834=CARTESIAN_POINT ( 'NONE',  ( 5.516018279890452902, -0.006440244342253398716, 0.002104829434641079973 ) ) ;
#58835=VERTEX_POINT ( 'NONE', #22862 ) ;
#58842=CARTESIAN_POINT ( 'NONE',  ( 0.3002738374340851446, 8.050654058169996574, -9.243462099800746401 ) ) ;
#58845=CARTESIAN_POINT ( 'NONE',  ( 0.2872850955227719272, 11.58431228138438662, 3.994021792079137878 ) ) ;
#58846=ORIENTED_EDGE ( 'NONE', *, *, #21244, .F. ) ;
#58851=CARTESIAN_POINT ( 'NONE',  ( 0.2650492594609232810, -0.1101156276917609755, 12.24562116224018560 ) ) ;
#58852=CARTESIAN_POINT ( 'NONE',  ( 2.889800649504073782, -1.129261637821570075, -6.016320774579819286 ) ) ;
#58858=CARTESIAN_POINT ( 'NONE',  ( 0.5572780756279106518, 5.905274004878355854, 10.83930267798883484 ) ) ;
#58861=CARTESIAN_POINT ( 'NONE',  ( 2.639814597422735609, -7.207158938903925005, -2.896050884406603743 ) ) ;
#58863=DIRECTION ( 'NONE',  ( 0.000000000000000000, 0.000000000000000000, 1.000000000000000000 ) ) ;
#58864=CARTESIAN_POINT ( 'NONE',  ( 2.245754705088394587, 5.920355780195151851, -4.822435078157686128 ) ) ;
#58870=CARTESIAN_POINT ( 'NONE',  ( 1.547277799339725091, 10.62321481610081086, -6.911346840320961249 ) ) ;
#58876=( BOUNDED_SURFACE ( )  B_SPLINE_SURFACE ( 3, 1, ( 
 ( #43380, #58722 ),
 ( #33736, #38067 ),
 ( #24102, #58373 ),
 ( #12797, #33085 ) ),
 .UNSPECIFIED., .F., .F., .F. ) 
 B_SPLINE_SURFACE_WITH_KNOTS ( ( 4, 4 ),
 ( 2, 2 ),
 ( 0.000000000000000000, 1.000000000000000000 ),
 ( 0.000000000000000000, 1.000000000000000000 ),
 .UNSPECIFIED. ) 
 GEOMETRIC_REPRESENTATION_ITEM ( )  RATIONAL_B_SPLINE_SURFACE ( (
 ( 1.000000000000000000, 1.000000000000000000),
 ( 0.9942764183789327692, 0.8450855930916580938),
 ( 0.9942764183789327692, 0.8450855930916580938),
 ( 1.000000000000000000, 1.000000000000000000) ) ) 
 REPRESENTATION_ITEM ( '' )  SURFACE ( )  );
#58877=ORIENTED_EDGE ( 'NONE', *, *, #61672, .F. ) ;
#58878=CARTESIAN_POINT ( 'NONE',  ( 2.969415267404130532, -0.3878973768016590884, -7.867532449842983944 ) ) ;
#58879=CARTESIAN_POINT ( 'NONE',  ( 2.969415267403965331, 5.777543886622456881, -5.354299007565090029 ) ) ;
#58883=EDGE_CURVE ( 'NONE', #18517, #20299, #27722, .T. ) ;
#58887=ORIENTED_EDGE ( 'NONE', *, *, #18599, .T. ) ;
#58889=CARTESIAN_POINT ( 'NONE',  ( 2.941278708680199916, -0.9331242451664579773, -6.068329152486386491 ) ) ;
#58892=CARTESIAN_POINT ( 'NONE',  ( 1.452237505248555660, -10.06489946308196970, -7.672309600508799399 ) ) ;
#58898=CARTESIAN_POINT ( 'NONE',  ( 2.241352910868909643, 7.202080440908774861, -2.532612177304371048 ) ) ;
#58904=CARTESIAN_POINT ( 'NONE',  ( 2.350038591458109227, -9.502240128958682419, 4.746773736939463362 ) ) ;
#58906=CARTESIAN_POINT ( 'NONE',  ( 2.963017218115626239, 7.259628195185936939, 3.051711603120559335 ) ) ;
#58910=ORIENTED_EDGE ( 'NONE', *, *, #45906, .T. ) ;
#58915=CARTESIAN_POINT ( 'NONE',  ( 0.2653519789438754106, -4.167744179923992931, 11.51519617080779945 ) ) ;
#58918=CARTESIAN_POINT ( 'NONE',  ( 2.241352910868908310, -5.901537464758421336, -4.843133558968188979 ) ) ;
#58921=CARTESIAN_POINT ( 'NONE',  ( 1.633930747254533244, 11.67150509329711028, -5.012862767615578363 ) ) ;
#58922=CARTESIAN_POINT ( 'NONE',  ( 1.375507693218991134, -0.5913006932463059639, 12.60244951981753481 ) ) ;
#58923=ORIENTED_EDGE ( 'NONE', *, *, #36311, .T. ) ;
#58924=CARTESIAN_POINT ( 'NONE',  ( 2.241352910868908310, -7.145045428366559648, -2.689314586382423045 ) ) ;
#58926=CARTESIAN_POINT ( 'NONE',  ( 2.290907136833252089, -2.768669624188737632, 7.132394668149376393 ) ) ;
#58927=CARTESIAN_POINT ( 'NONE',  ( 5.520433897694421610, 0.004666464468078041980, 0.01432141647227064968 ) ) ;
#58928=CONICAL_SURFACE ( 'NONE', #27042, 7.938172270156617749, 1.280189991382167047 ) ;
#58931=FACE_OUTER_BOUND ( 'NONE', #42309, .T. ) ;
#58932=CARTESIAN_POINT ( 'NONE',  ( 0.2767916011545376032, -2.313848297676370347, -12.02950149294536430 ) ) ;
#58936=CARTESIAN_POINT ( 'NONE',  ( 2.430348790457596664, -6.761480562106405579, -3.678671624790093464 ) ) ;
#58949=LINE ( 'NONE', #52637, #58599 ) ;
#58952=FACE_OUTER_BOUND ( 'NONE', #34881, .T. ) ;
#58956=VERTEX_POINT ( 'NONE', #38463 ) ;
#58959=CARTESIAN_POINT ( 'NONE',  ( 0.2915757698887304072, 1.916267336493336693, -12.10419100255477076 ) ) ;
#58973=CARTESIAN_POINT ( 'NONE',  ( 2.705197763288547108, -2.925192046931958778, 7.218866228162280407 ) ) ;
#58982=VERTEX_POINT ( 'NONE', #55057 ) ;
#58984=ORIENTED_EDGE ( 'NONE', *, *, #33870, .F. ) ;
#58985=CARTESIAN_POINT ( 'NONE',  ( 0.2647959493198543401, -6.249846955854195585, -10.53111783886897612 ) ) ;
#58986=ORIENTED_EDGE ( 'NONE', *, *, #65525, .T. ) ;
#58988=CARTESIAN_POINT ( 'NONE',  ( 0.2767916011545388244, 4.010899340181579120, -11.57477803659169169 ) ) ;
#58990=CARTESIAN_POINT ( 'NONE',  ( 5.516018279890452902, 0.002104829434641014487, 0.006440244342253419532 ) ) ;
#58992=CARTESIAN_POINT ( 'NONE',  ( 0.3675815128205894289, 9.574637318041965273, 7.689697408877307794 ) ) ;
#59001=CARTESIAN_POINT ( 'NONE',  ( 2.941278708680199916, 0.1348063076486946399, 6.138172921908581436 ) ) ;
#59002=FACE_OUTER_BOUND ( 'NONE', #12003, .T. ) ;
#59010=CARTESIAN_POINT ( 'NONE',  ( 2.268878695253356614, -5.759001817705827975, -5.025754889199108177 ) ) ;
#59012=CARTESIAN_POINT ( 'NONE',  ( 3.152665057734040488, 0.000000000000000000, 0.000000000000000000 ) ) ;
#59013=CARTESIAN_POINT ( 'NONE',  ( 2.080613030138688480, 5.400000000000000355, -1.000000000000000000 ) ) ;
#59021=DIRECTION ( 'NONE',  ( 0.3865475372811021382, -0.4778122177792148983, 0.7888450329201692757 ) ) ;
#59028=CARTESIAN_POINT ( 'NONE',  ( 0.2646305136544065406, -10.67138229758233692, 6.008537389229378967 ) ) ;
#59031=DIRECTION ( 'NONE',  ( -1.000000000000000000, -0.000000000000000000, -0.000000000000000000 ) ) ;
#59034=CARTESIAN_POINT ( 'NONE',  ( 5.536195898058073439, 0.005656495196970996904, 0.006344799443924045018 ) ) ;
#59035=EDGE_LOOP ( 'NONE', ( #7780, #55776, #608, #56980 ) ) ;
#59043=CARTESIAN_POINT ( 'NONE',  ( 0.2651627923886339944, 6.199207987242239426, -10.56116046379966811 ) ) ;
#59048=FACE_OUTER_BOUND ( 'NONE', #48944, .T. ) ;
#59051=CARTESIAN_POINT ( 'NONE',  ( 5.515539859299206427, -0.005924322247675101009, 0.001241880655086994309 ) ) ;
#59053=CARTESIAN_POINT ( 'NONE',  ( 0.2653141334712571520, 10.58342934917120637, -6.161213243425151198 ) ) ;
#59061=CARTESIAN_POINT ( 'NONE',  ( 2.305787727787083519, -7.135468203930003028, 2.774453000917123990 ) ) ;
#59065=( BOUNDED_SURFACE ( )  B_SPLINE_SURFACE ( 3, 1, ( 
 ( #65746, #34529 ),
 ( #4629, #5264 ),
 ( #65431, #25532 ),
 ( #30513, #54508 ) ),
 .UNSPECIFIED., .F., .F., .F. ) 
 B_SPLINE_SURFACE_WITH_KNOTS ( ( 4, 4 ),
 ( 2, 2 ),
 ( 0.000000000000000000, 1.000000000000000000 ),
 ( 0.000000000000000000, 1.000000000000000000 ),
 .UNSPECIFIED. ) 
 GEOMETRIC_REPRESENTATION_ITEM ( )  RATIONAL_B_SPLINE_SURFACE ( (
 ( 1.000000000000000000, 1.000000000000000000),
 ( 0.6933888150995267674, 0.9895912004443193632),
 ( 0.6933888150995267674, 0.9895912004443193632),
 ( 1.000000000000000000, 1.000000000000000000) ) ) 
 REPRESENTATION_ITEM ( '' )  SURFACE ( )  );
#59071=CARTESIAN_POINT ( 'NONE',  ( 2.305787727787084407, -7.508843116234166004, 1.493241775258399073 ) ) ;
#59072=CARTESIAN_POINT ( 'NONE',  ( 0.2706063244538025603, -10.51833723927417807, -6.275112929891721869 ) ) ;
#59080=ORIENTED_EDGE ( 'NONE', *, *, #1062, .T. ) ;
#59082=CARTESIAN_POINT ( 'NONE',  ( 0.8375941296792225321, 3.890418817178149524, 11.81283813871825750 ) ) ;
#59085=CARTESIAN_POINT ( 'NONE',  ( 0.2652384529303135619, -11.53005674806959746, -4.126283314267688240 ) ) ;
#59089=B_SPLINE_CURVE_WITH_KNOTS ( 'NONE', 3,
 ( #29446, #34102, #54081, #23163, #38790, #53764, #49445 ),
 .UNSPECIFIED., .F., .F.,
 ( 4, 3, 4 ),
 ( 0.000000000000000000, 0.001700533616330539939, 0.005002426799371323396 ),
 .UNSPECIFIED. ) ;
#59096=CARTESIAN_POINT ( 'NONE',  ( 0.2648978790185584908, 12.03635331166812250, 2.256510822326184940 ) ) ;
#59105=CARTESIAN_POINT ( 'NONE',  ( 2.266490820343225021, -2.476945027124318521, 7.230273269342697873 ) ) ;
#59106=CARTESIAN_POINT ( 'NONE',  ( 0.3665391374699465965, 10.76665847464312442, 5.911453292029641204 ) ) ;
#59114=CARTESIAN_POINT ( 'NONE',  ( 0.3106921474978429076, -8.060345844326345599, 9.239619355094122355 ) ) ;
#59118=EDGE_CURVE ( 'NONE', #7370, #62374, #65738, .T. ) ;
#59122=CARTESIAN_POINT ( 'NONE',  ( 3.152665057734040488, 0.000000000000000000, 0.000000000000000000 ) ) ;
#59124=CARTESIAN_POINT ( 'NONE',  ( 2.941278708680199916, 2.952340773940109298, 5.383216837018951040 ) ) ;
#59125=CARTESIAN_POINT ( 'NONE',  ( 2.241506898688419458, -3.783130304541474587, 6.631235260227153816 ) ) ;
#59128=FACE_OUTER_BOUND ( 'NONE', #62971, .T. ) ;
#59129=VERTEX_POINT ( 'NONE', #58613 ) ;
#59131=ORIENTED_EDGE ( 'NONE', *, *, #30281, .T. ) ;
#59134=CARTESIAN_POINT ( 'NONE',  ( 2.827825597296806492, -8.650999012440189873, 2.568788224597731595 ) ) ;
#59136=ORIENTED_EDGE ( 'NONE', *, *, #62219, .F. ) ;
#59138=CARTESIAN_POINT ( 'NONE',  ( 2.242418902651939661, 6.561482094363304540, -3.903399295463767515 ) ) ;
#59139=CARTESIAN_POINT ( 'NONE',  ( 2.297017764050237165, -5.044319338147413845, -5.755222757172084869 ) ) ;
#59146=ORIENTED_EDGE ( 'NONE', *, *, #53397, .T. ) ;
#59147=CARTESIAN_POINT ( 'NONE',  ( 5.514970785353741078, 0.004233694591582952416, 0.002093325033903827709 ) ) ;
#59150=CARTESIAN_POINT ( 'NONE',  ( 0.3610902822527243816, 10.49957835860572430, -6.364812822043059981 ) ) ;
#59154=EDGE_CURVE ( 'NONE', #41809, #56943, #28657, .T. ) ;
#59156=CARTESIAN_POINT ( 'NONE',  ( 2.251139882113958102, -1.448366094935465531, 7.499076289418100671 ) ) ;
#59158=CARTESIAN_POINT ( 'NONE',  ( 0.2651627682582933243, -9.324228491541576958, 7.938957913267723931 ) ) ;
#59168=VERTEX_POINT ( 'NONE', #14642 ) ;
#59173=CARTESIAN_POINT ( 'NONE',  ( 2.305787727787083519, -6.711944854845849129, 3.682701754025489826 ) ) ;
#59185=CARTESIAN_POINT ( 'NONE',  ( 0.9232167919969141989, -8.324955738482405110, -9.278116382137454821 ) ) ;
#59189=EDGE_CURVE ( 'NONE', #62456, #14132, #53882, .T. ) ;
#59194=CARTESIAN_POINT ( 'NONE',  ( 2.244591118396413343, 4.989853642774898290, 5.779440292196087015 ) ) ;
#59195=CARTESIAN_POINT ( 'NONE',  ( 2.573738926104375047, -3.667129335223154207, -6.822065037112471586 ) ) ;
#59196=CARTESIAN_POINT ( 'NONE',  ( 0.3278977287071228597, 12.26453627383315848, 0.2481246099268475946 ) ) ;
#59197=CARTESIAN_POINT ( 'NONE',  ( 0.3164563675027631806, 9.237806174449874064, -8.065346584422156795 ) ) ;
#59203=CARTESIAN_POINT ( 'NONE',  ( 2.251139882113958990, 7.218573619021379173, -2.495216312514809687 ) ) ;
#59208=CARTESIAN_POINT ( 'NONE',  ( 2.242819959140645469, -7.536009875295344607, 1.224821922055950418 ) ) ;
#59210=CARTESIAN_POINT ( 'NONE',  ( 2.241509619876138171, 6.630717740088905465, -3.784042210004639806 ) ) ;
#59215=CARTESIAN_POINT ( 'NONE',  ( 2.276198483117258586, 2.469789406312234092, 7.236140649716372941 ) ) ;
#59220=CARTESIAN_POINT ( 'NONE',  ( 5.515188684475870851, 0.003709313826050237434, 0.003857086913166458270 ) ) ;
#59236=B_SPLINE_CURVE_WITH_KNOTS ( 'NONE', 3,
 ( #30119, #24464, #65025, #23844, #65667, #54751, #3573, #59396, #44104, #40406 ),
 .UNSPECIFIED., .F., .F.,
 ( 4, 3, 3, 4 ),
 ( 1.226634733346699349E-18, 6.607638129004494304E-05, 9.911389841680424680E-05, 0.0001667630577588614710 ),
 .UNSPECIFIED. ) ;
#59238=ORIENTED_EDGE ( 'NONE', *, *, #38849, .F. ) ;
#59241=CARTESIAN_POINT ( 'NONE',  ( 2.244591118396559448, -7.634724215899725941, 0.1074970442783885205 ) ) ;
#59248=CARTESIAN_POINT ( 'NONE',  ( 1.459561108993331358, -9.267924853468697322, 8.601340491611225048 ) ) ;
#59249=ADVANCED_FACE ( 'NONE', ( #5704 ), #26211, .F. ) ;
#59251=CARTESIAN_POINT ( 'NONE',  ( 0.3665391374699465965, -9.237363111276819083, 8.095513416941198415 ) ) ;
#59264=B_SPLINE_CURVE_WITH_KNOTS ( 'NONE', 3,
 ( #58924, #38262, #54238, #8347, #8038, #64835, #49269, #19314, #59885, #58584, #39586, #48931, #54884, #3725, #14307, #34585, #44244, #9306, #54577 ),
 .UNSPECIFIED., .F., .F.,
 ( 4, 3, 3, 3, 3, 3, 4 ),
 ( 0.000000000000000000, 2.831840207499539448E-05, 4.217266859840335547E-05, 5.602024318395820929E-05, 6.290810167968980229E-05, 9.120440630945211011E-05, 0.0001153103026479757780 ),
 .UNSPECIFIED. ) ;
#59269=CARTESIAN_POINT ( 'NONE',  ( 0.2653141617321009282, 6.084921229689422617, 10.62747662594933296 ) ) ;
#59271=ORIENTED_EDGE ( 'NONE', *, *, #59189, .F. ) ;
#59274=CARTESIAN_POINT ( 'NONE',  ( 0.3278977287071230817, -7.693417476735460170, -9.554671284920370766 ) ) ;
#59275=EDGE_CURVE ( 'NONE', #34346, #58095, #41968, .T. ) ;
#59278=CARTESIAN_POINT ( 'NONE',  ( 2.305787727787085295, 5.756228004061457959, 5.047606869483074910 ) ) ;
#59279=CARTESIAN_POINT ( 'NONE',  ( 0.3002738374340835348, 10.50101454678644686, 6.323236184341160637 ) ) ;
#59284=CARTESIAN_POINT ( 'NONE',  ( 2.266490820343228574, -1.470039317404115309, -7.500072841116513622 ) ) ;
#59287=CARTESIAN_POINT ( 'NONE',  ( 5.514970785353741078, 0.003415090918276138254, -0.003262412238248725994 ) ) ;
#59291=CARTESIAN_POINT ( 'NONE',  ( 3.152665057734128862, 2.258875078502223133, 7.609997527621164437 ) ) ;
#59292=CARTESIAN_POINT ( 'NONE',  ( 0.3057689695767515925, 3.975296631252121404, -11.59726335252429230 ) ) ;
#59294=CARTESIAN_POINT ( 'NONE',  ( 0.3223008802179286869, -3.964361764750254924, 11.60682919296350946 ) ) ;
#59295=CARTESIAN_POINT ( 'NONE',  ( 0.2648978790185619880, -11.46165506714231341, 4.312320170909196726 ) ) ;
#59312=CARTESIAN_POINT ( 'NONE',  ( 0.6473888112830253894, -10.87693551365366673, -5.898884566269122942 ) ) ;
#59319=CARTESIAN_POINT ( 'NONE',  ( 2.941278708680199916, -1.198640839021267723, -6.021511413163973536 ) ) ;
#59321=VERTEX_POINT ( 'NONE', #58193 ) ;
#59326=FACE_OUTER_BOUND ( 'NONE', #21043, .T. ) ;
#59327=CARTESIAN_POINT ( 'NONE',  ( 5.515539859299206427, 0.005142293699651638746, 0.003193223631738825990 ) ) ;
#59331=CARTESIAN_POINT ( 'NONE',  ( 1.719304012338199517, 0.000000000000000000, 0.000000000000000000 ) ) ;
#59334=CARTESIAN_POINT ( 'NONE',  ( 5.516018279890452902, 0.0002248006052446666569, -0.006771744149385742172 ) ) ;
#59335=B_SPLINE_CURVE_WITH_KNOTS ( 'NONE', 3,
 ( #37701, #47674, #46368, #16444, #6458, #810, #27377, #26092, #26740, #21077, #36710, #5832, #31068, #57010, #11433, #31703, #47032, #1490, #21767 ),
 .UNSPECIFIED., .F., .F.,
 ( 4, 3, 3, 3, 3, 3, 4 ),
 ( 0.000000000000000000, 2.831840207499292453E-05, 4.217266859840086181E-05, 5.602024318395534971E-05, 6.290810167968737638E-05, 9.120440630944575398E-05, 0.0001153103026479753850 ),
 .UNSPECIFIED. ) ;
#59336=CARTESIAN_POINT ( 'NONE',  ( 0.3002738374340856442, -12.10874171309340142, 1.906042098268977636 ) ) ;
#59352=CARTESIAN_POINT ( 'NONE',  ( 3.152665057734087117, 7.886634106564184954, -0.9030954876737516956 ) ) ;
#59359=VERTEX_POINT ( 'NONE', #18293 ) ;
#59367=CARTESIAN_POINT ( 'NONE',  ( 0.2648978790185619880, -11.46165506714231341, 4.312320170909196726 ) ) ;
#59368=CARTESIAN_POINT ( 'NONE',  ( 2.297017764049618993, 5.967068736726843348, 4.791851130936075620 ) ) ;
#59376=CARTESIAN_POINT ( 'NONE',  ( 2.241449424704145876, -1.265244293929138841, 7.528892370271786483 ) ) ;
#59377=CARTESIAN_POINT ( 'NONE',  ( 0.2759803524722184154, -10.51260004517008717, -6.288205958087898395 ) ) ;
#59387=CARTESIAN_POINT ( 'NONE',  ( 2.305787727787084407, 4.792270232040973355, -5.970480882365174047 ) ) ;
#59396=CARTESIAN_POINT ( 'NONE',  ( 2.241509619876138171, 5.872890204493088184, -4.877966158328247204 ) ) ;
#59397=CARTESIAN_POINT ( 'NONE',  ( 2.305787727787084407, 1.493241775258423720, 7.508843116234161563 ) ) ;
#59400=CARTESIAN_POINT ( 'NONE',  ( 0.2650492594609241692, 12.04046128294318052, 2.234872523101219866 ) ) ;
#59402=CARTESIAN_POINT ( 'NONE',  ( 2.177405672431210970, -7.702458780351562062, -8.129711416440695615 ) ) ;
#59405=CARTESIAN_POINT ( 'NONE',  ( 2.259025283528088401, -0.1366755880739185802, -7.639069972920481177 ) ) ;
#59406=CARTESIAN_POINT ( 'NONE',  ( 2.261269890822071638, -5.942064862945643178, 4.803890999604306877 ) ) ;
#59409=CARTESIAN_POINT ( 'NONE',  ( 2.241352910868908754, 7.145045428366577411, 2.689314586382375527 ) ) ;
#59422=CARTESIAN_POINT ( 'NONE',  ( 0.3040950598368144520, 10.74226959800799719, -5.912066680610498892 ) ) ;
#59425=( BOUNDED_SURFACE ( )  B_SPLINE_SURFACE ( 3, 1, ( 
 ( #41485, #63096 ),
 ( #42138, #52796 ),
 ( #37497, #16885 ),
 ( #26217, #12224 ) ),
 .UNSPECIFIED., .F., .F., .F. ) 
 B_SPLINE_SURFACE_WITH_KNOTS ( ( 4, 4 ),
 ( 2, 2 ),
 ( 0.000000000000000000, 1.000000000000000000 ),
 ( 0.000000000000000000, 1.000000000000000000 ),
 .UNSPECIFIED. ) 
 GEOMETRIC_REPRESENTATION_ITEM ( )  RATIONAL_B_SPLINE_SURFACE ( (
 ( 1.000000000000000000, 1.000000000000000000),
 ( 0.9856612449720755231, 0.9999558406602322425),
 ( 0.9856612449720755231, 0.9999558406602322425),
 ( 1.000000000000000000, 1.000000000000000000) ) ) 
 REPRESENTATION_ITEM ( '' )  SURFACE ( )  );
#59430=CARTESIAN_POINT ( 'NONE',  ( 2.251152103361941492, 1.202724109300151500, -7.542379262758394987 ) ) ;
#59444=CARTESIAN_POINT ( 'NONE',  ( 2.266490820343221024, 6.544980046121079198, -3.946561086901401172 ) ) ;
#59446=CARTESIAN_POINT ( 'NONE',  ( 2.257661810676955927, -5.013319178751810767, -5.764872664104216504 ) ) ;
#59451=CARTESIAN_POINT ( 'NONE',  ( 5.520433897694421610, -0.01120198501134877893, 0.01006947824912462000 ) ) ;
#59452=EDGE_LOOP ( 'NONE', ( #10594, #29138, #4308, #47643 ) ) ;
#59456=CARTESIAN_POINT ( 'NONE',  ( 0.2834382757448002943, 10.50792790568177182, -6.300836243950055149 ) ) ;
#59459=CARTESIAN_POINT ( 'NONE',  ( 2.827825597296801163, 5.372687261161280148, 7.250702617666018313 ) ) ;
#59460=ORIENTED_EDGE ( 'NONE', *, *, #11757, .F. ) ;
#59461=CARTESIAN_POINT ( 'NONE',  ( 2.350038591458109227, -2.471682575235262025, 10.33030559206112997 ) ) ;
#59464=CARTESIAN_POINT ( 'NONE',  ( 0.2653141334712589838, -9.352759824582554060, 7.905403790036936940 ) ) ;
#59466=DIRECTION ( 'NONE',  ( -0.3939253465568943735, -0.1691689424289704313, -0.9034404741085569901 ) ) ;
#59467=CARTESIAN_POINT ( 'NONE',  ( 0.3632410797595244656, -8.092233745354578289, -9.235006602299437262 ) ) ;
#59471=CARTESIAN_POINT ( 'NONE',  ( 1.462291587748370647, 5.766456054324373248, 11.25382118863233316 ) ) ;
#59472=EDGE_CURVE ( 'NONE', #64505, #6215, #24235, .T. ) ;
#59474=ORIENTED_EDGE ( 'NONE', *, *, #11007, .T. ) ;
#59481=CARTESIAN_POINT ( 'NONE',  ( 0.3665391374699464300, 11.44911061034386179, 4.447929964102885769 ) ) ;
#59483=CARTESIAN_POINT ( 'NONE',  ( 0.2653519890518169499, 9.381137101569672510, 7.871697161810723209 ) ) ;
#59486=CARTESIAN_POINT ( 'NONE',  ( 0.3665391374699472626, 7.691255657244420618, -9.576575648338943481 ) ) ;
#59494=CARTESIAN_POINT ( 'NONE',  ( 0.2655924914740778187, -6.161287456391757011, 10.58356227062107457 ) ) ;
#59496=CARTESIAN_POINT ( 'NONE',  ( 2.305787727787083519, 5.756228004061526349, -5.047606869482997638 ) ) ;
#59507=DIRECTION ( 'NONE',  ( 0.3939253465568944290, 0.009718094113439539050, -0.9190910618577644575 ) ) ;
#59509=CARTESIAN_POINT ( 'NONE',  ( 2.907497136251136816, 6.617189382231139838, -4.235253383576361053 ) ) ;
#59510=CARTESIAN_POINT ( 'NONE',  ( 1.020182472822753317, -12.48987306958581556, -0.4462553704985335323 ) ) ;
#59522=VERTEX_POINT ( 'NONE', #65124 ) ;
#59526=CARTESIAN_POINT ( 'NONE',  ( 2.770579946183333142, 7.230573341413149002, 2.954332771348846087 ) ) ;
#59531=CARTESIAN_POINT ( 'NONE',  ( 2.941278708680199916, 6.021511413163961990, 1.198640839021329452 ) ) ;
#59539=CARTESIAN_POINT ( 'NONE',  ( 0.2650492433740059273, 11.54478237753292014, 4.084772052580635915 ) ) ;
#59546=CARTESIAN_POINT ( 'NONE',  ( 0.9232167919969114234, 10.99620217063216465, 5.871274944231739568 ) ) ;
#59552=DIRECTION ( 'NONE',  ( 0.3865475372811021382, -0.8598319252293120663, -0.3335716741247219952 ) ) ;
#59571=CARTESIAN_POINT ( 'NONE',  ( 1.287602823386241324, 1.639728374786390663, 12.47973441446148257 ) ) ;
#59576=CARTESIAN_POINT ( 'NONE',  ( 2.440552418640496768, -5.099602138956240260, 5.770332237304425682 ) ) ;
#59583=ORIENTED_EDGE ( 'NONE', *, *, #50001, .T. ) ;
#59589=CARTESIAN_POINT ( 'NONE',  ( 0.2647959493198558945, 1.981611532097707240, -12.08462848595693018 ) ) ;
#59591=CARTESIAN_POINT ( 'NONE',  ( 2.705197763288546664, -7.410249563424439856, 2.399370654839244832 ) ) ;
#59598=B_SPLINE_CURVE_WITH_KNOTS ( 'NONE', 3,
 ( #10145, #23905, #18602, #28538, #65650, #44164, #23231, #59456, #45715, #34175, #54485, #43493, #38857, #48843, #50404, #25118, #3291, #4849, #59150, #45383, #13561, #40385 ),
 .UNSPECIFIED., .F., .F.,
 ( 4, 3, 3, 3, 3, 3, 3, 4 ),
 ( 8.940560153363745023E-19, 4.449119708436977073E-05, 6.626296329540607203E-05, 8.803456484962844653E-05, 0.0001098060367612834013, 0.0001315774408628557881, 0.0001760698110411249636, 0.0001829697163287847303 ),
 .UNSPECIFIED. ) ;
#59599=CARTESIAN_POINT ( 'NONE',  ( 0.3053067050349173583, -7.702091166065946126, -9.538004819224426001 ) ) ;
#59603=CARTESIAN_POINT ( 'NONE',  ( 0.3474126878361814552, -9.233692382639425489, 8.085727498271742419 ) ) ;
#59612=CARTESIAN_POINT ( 'NONE',  ( 0.3665391374699472626, 5.911453292029753115, -10.76665847464306403 ) ) ;
#59615=EDGE_CURVE ( 'NONE', #12134, #36790, #40170, .T. ) ;
#59626=CARTESIAN_POINT ( 'NONE',  ( 0.2834382757448019041, 9.514772331577425746, 7.719209397492011071 ) ) ;
#59631=( BOUNDED_SURFACE ( )  B_SPLINE_SURFACE ( 3, 1, ( 
 ( #33320, #53623 ),
 ( #3081, #23342 ),
 ( #55485, #4953 ),
 ( #30845, #295 ) ),
 .UNSPECIFIED., .F., .F., .F. ) 
 B_SPLINE_SURFACE_WITH_KNOTS ( ( 4, 4 ),
 ( 2, 2 ),
 ( 0.000000000000000000, 1.000000000000000000 ),
 ( 0.000000000000000000, 1.000000000000000000 ),
 .UNSPECIFIED. ) 
 GEOMETRIC_REPRESENTATION_ITEM ( )  RATIONAL_B_SPLINE_SURFACE ( (
 ( 1.000000000000000000, 1.000000000000000000),
 ( 0.6933888150995267674, 0.9895912004443193632),
 ( 0.6933888150995267674, 0.9895912004443193632),
 ( 1.000000000000000000, 1.000000000000000000) ) ) 
 REPRESENTATION_ITEM ( '' )  SURFACE ( )  );
#59635=ORIENTED_EDGE ( 'NONE', *, *, #36975, .F. ) ;
#59636=CARTESIAN_POINT ( 'NONE',  ( 5.514970785353741078, 0.0003039746380528286578, 0.004713149585127535644 ) ) ;
#59638=CARTESIAN_POINT ( 'NONE',  ( 0.2739690278137234536, -10.51531306167491486, 6.282352088166227588 ) ) ;
#59643=CARTESIAN_POINT ( 'NONE',  ( 0.2833330754217378566, 10.71034013638387528, -5.950193237802298363 ) ) ;
#59659=PLANE ( 'NONE',  #19240 ) ;
#59667=EDGE_CURVE ( 'NONE', #6215, #44872, #51507, .T. ) ;
#59674=CARTESIAN_POINT ( 'NONE',  ( 2.241451721903215066, 6.581017239736967284, 3.869794645251144694 ) ) ;
#59679=EDGE_CURVE ( 'NONE', #58379, #58530, #60228, .T. ) ;
#59689=ORIENTED_EDGE ( 'NONE', *, *, #51535, .F. ) ;
#59694=ORIENTED_EDGE ( 'NONE', *, *, #56882, .T. ) ;
#59701=FACE_OUTER_BOUND ( 'NONE', #4321, .T. ) ;
#59702=CARTESIAN_POINT ( 'NONE',  ( 2.263328370259782840, 5.944174889969469078, 4.802372801875639752 ) ) ;
#59722=LINE ( 'NONE', #54421, #42560 ) ;
#59734=ORIENTED_EDGE ( 'NONE', *, *, #56617, .F. ) ;
#59738=CARTESIAN_POINT ( 'NONE',  ( 2.507146904658100084, -6.577532285019736413, -4.047319006787544637 ) ) ;
#59743=CARTESIAN_POINT ( 'NONE',  ( 2.251152103363645018, -2.494172441821545405, 7.218942724308482717 ) ) ;
#59748=CARTESIAN_POINT ( 'NONE',  ( 1.287602823385640693, -6.765713844064606519, 10.61402828236298213 ) ) ;
#59755=VECTOR ( 'NONE', #43438, 1000.000000000000114 ) ;
#59757=CARTESIAN_POINT ( 'NONE',  ( 1.459561108995800272, 12.32692860927524769, -2.815016945601904297 ) ) ;
#59759=CARTESIAN_POINT ( 'NONE',  ( 2.305787727787085295, -7.249469779319927198, 2.461236246751046242 ) ) ;
#59762=CARTESIAN_POINT ( 'NONE',  ( 2.653899356900494055, -4.792827201941008752, 6.118160465319252062 ) ) ;
#59763=CARTESIAN_POINT ( 'NONE',  ( 2.242819959140645025, 7.536009875295354377, -1.224821922055896906 ) ) ;
#59764=CARTESIAN_POINT ( 'NONE',  ( 2.241352910868909643, -3.744764251557037849, 6.652881166698498383 ) ) ;
#59767=CARTESIAN_POINT ( 'NONE',  ( 2.244591118395375062, 1.219892024453471890, -7.537402265770549725 ) ) ;
#59769=ORIENTED_EDGE ( 'NONE', *, *, #55307, .F. ) ;
#59774=CARTESIAN_POINT ( 'NONE',  ( 1.719304012339881282, -12.20344780066076318, 3.626341562669963992 ) ) ;
#59783=CARTESIAN_POINT ( 'NONE',  ( 2.263328370261528555, -7.228205514767154227, -2.479726736363712103 ) ) ;
#59787=ORIENTED_EDGE ( 'NONE', *, *, #4406, .T. ) ;
#59790=CARTESIAN_POINT ( 'NONE',  ( 2.305787727787085295, -3.971363876084009537, 6.545285700970515208 ) ) ;
#59792=DIRECTION ( 'NONE',  ( 0.000000000000000000, 0.000000000000000000, 1.000000000000000000 ) ) ;
#59794=CARTESIAN_POINT ( 'NONE',  ( 2.290907136833255198, -1.488079974904993996, 7.504812001538600619 ) ) ;
#59795=CARTESIAN_POINT ( 'NONE',  ( 0.2653519890518161728, 7.871697161810815579, -9.381137101569592573 ) ) ;
#59796=CARTESIAN_POINT ( 'NONE',  ( 0.2650492594609250574, -9.451471004987384461, 7.786980091309421148 ) ) ;
#59800=CARTESIAN_POINT ( 'NONE',  ( 1.198791140420486290, 0.5160125886334614442, -12.54673713002939195 ) ) ;
#59808=ORIENTED_EDGE ( 'NONE', *, *, #43628, .F. ) ;
#59810=( BOUNDED_SURFACE ( )  B_SPLINE_SURFACE ( 3, 1, ( 
 ( #22831, #43087 ),
 ( #17511, #18163 ),
 ( #58749, #52757 ),
 ( #17829, #37782 ) ),
 .UNSPECIFIED., .F., .F., .F. ) 
 B_SPLINE_SURFACE_WITH_KNOTS ( ( 4, 4 ),
 ( 2, 2 ),
 ( 0.000000000000000000, 1.000000000000000000 ),
 ( 0.000000000000000000, 1.000000000000000000 ),
 .UNSPECIFIED. ) 
 GEOMETRIC_REPRESENTATION_ITEM ( )  RATIONAL_B_SPLINE_SURFACE ( (
 ( 1.000000000000000000, 1.000000000000000000),
 ( 0.6933888150995267674, 0.9895912004443193632),
 ( 0.6933888150995267674, 0.9895912004443193632),
 ( 1.000000000000000000, 1.000000000000000000) ) ) 
 REPRESENTATION_ITEM ( '' )  SURFACE ( )  );
#59813=CARTESIAN_POINT ( 'NONE',  ( 2.241311220309555541, -7.501736494813736833, -1.417008678104561659 ) ) ;
#59814=FACE_OUTER_BOUND ( 'NONE', #24136, .T. ) ;
#59818=CARTESIAN_POINT ( 'NONE',  ( 3.152665057736164123, 5.461013642407259283, 5.761241965767907480 ) ) ;
#59821=CARTESIAN_POINT ( 'NONE',  ( 3.152665057736245391, 2.258875078500370837, -7.609997527622033076 ) ) ;
#59823=CARTESIAN_POINT ( 'NONE',  ( 0.8320506296491596565, 2.535206712041455202, 12.17395768195218331 ) ) ;
#59824=B_SPLINE_CURVE_WITH_KNOTS ( 'NONE', 3,
 ( #34939, #40267, #35616, #24329, #45938, #40944, #29634, #61224, #39955, #64884, #5373, #60236, #54629, #4400, #20325, #19362, #55909, #40609, #59930 ),
 .UNSPECIFIED., .F., .F.,
 ( 4, 3, 3, 3, 3, 3, 4 ),
 ( 0.000000000000000000, 2.831840207624787838E-05, 4.217266860011569017E-05, 5.602024318565227519E-05, 6.290810168137421878E-05, 9.120440631109840335E-05, 0.0001153103026478316740 ),
 .UNSPECIFIED. ) ;
#59826=EDGE_CURVE ( 'NONE', #4955, #29543, #9607, .T. ) ;
#59837=CARTESIAN_POINT ( 'NONE',  ( 2.350038591457886739, 7.305692696276214093, -7.710465783964237652 ) ) ;
#59842=VERTEX_POINT ( 'NONE', #26862 ) ;
#59845=LINE ( 'NONE', #34553, #53430 ) ;
#59846=CARTESIAN_POINT ( 'NONE',  ( 2.258463476537674097, 6.547539277367620869, 3.937122681833869375 ) ) ;
#59847=CARTESIAN_POINT ( 'NONE',  ( 0.3675815128205894289, 12.27743992903066150, 0.2638082659428850896 ) ) ;
#59848=CARTESIAN_POINT ( 'NONE',  ( 2.717984159220097062, 6.602931111513763440, -4.139692542159497890 ) ) ;
#59854=VERTEX_POINT ( 'NONE', #48148 ) ;
#59855=ORIENTED_EDGE ( 'NONE', *, *, #28699, .T. ) ;
#59856=CARTESIAN_POINT ( 'NONE',  ( 1.104777566491140783, -2.644034362100612601, -12.24382064406182735 ) ) ;
#59857=EDGE_CURVE ( 'NONE', #44559, #62520, #16878, .T. ) ;
#59864=EDGE_LOOP ( 'NONE', ( #37441, #42776, #59990, #28352 ) ) ;
#59868=ORIENTED_EDGE ( 'NONE', *, *, #9927, .F. ) ;
#59870=VERTEX_POINT ( 'NONE', #42797 ) ;
#59878=EDGE_LOOP ( 'NONE', ( #31928, #12242, #11202, #40973 ) ) ;
#59879=CARTESIAN_POINT ( 'NONE',  ( 0.2652384770603662401, 11.48486213386625820, 4.250454630553602620 ) ) ;
#59881=LINE ( 'NONE', #13644, #48557 ) ;
#59883=CARTESIAN_POINT ( 'NONE',  ( 1.109979610370801506, -0.4797593171729975792, 12.51859925746135538 ) ) ;
#59884=VERTEX_POINT ( 'NONE', #47166 ) ;
#59885=CARTESIAN_POINT ( 'NONE',  ( 2.255723233588950549, -7.132203433012270999, -2.736592204236721670 ) ) ;
#59891=CARTESIAN_POINT ( 'NONE',  ( 1.198791140420805812, 9.943044756149616248, -7.669598593074792525 ) ) ;
#59902=CARTESIAN_POINT ( 'NONE',  ( 0.3675815128205894289, 9.574637318041965273, 7.689697408877307794 ) ) ;
#59911=CARTESIAN_POINT ( 'NONE',  ( 1.948354844646766448, -10.70340528294945770, -5.347695345041388215 ) ) ;
#59916=CARTESIAN_POINT ( 'NONE',  ( 2.305787727787084407, -5.047606869483094449, 5.756228004061441084 ) ) ;
#59918=FACE_OUTER_BOUND ( 'NONE', #9971, .T. ) ;
#59927=CARTESIAN_POINT ( 'NONE',  ( 0.2653519789438769649, 6.142177718873936598, 10.59450269107735565 ) ) ;
#59930=CARTESIAN_POINT ( 'NONE',  ( 2.305787727787084407, -1.164987321564681100, -7.566723232958083578 ) ) ;
#59934=CARTESIAN_POINT ( 'NONE',  ( 2.705197763288550217, 2.925192046932006740, -7.218866228162253762 ) ) ;
#59940=CARTESIAN_POINT ( 'NONE',  ( 3.152665057736049103, -0.4801242025610908959, -7.923639299008895520 ) ) ;
#59942=CARTESIAN_POINT ( 'NONE',  ( 0.2767916011545360488, -9.260929738915292475, 8.018602152763836699 ) ) ;
#59948=FACE_OUTER_BOUND ( 'NONE', #40475, .T. ) ;
#59949=ORIENTED_EDGE ( 'NONE', *, *, #42375, .T. ) ;
#59951=CARTESIAN_POINT ( 'NONE',  ( 5.516018279890452902, -0.006629829924290480368, 0.001397286410094396563 ) ) ;
#59954=CARTESIAN_POINT ( 'NONE',  ( 1.020182472822861230, -9.854645283130160749, 7.686484208904955651 ) ) ;
#59958=CARTESIAN_POINT ( 'NONE',  ( 5.520433897694421610, -0.01006947824912458184, -0.01120198501134881015 ) ) ;
#59962=CARTESIAN_POINT ( 'NONE',  ( 0.2706063244538032819, -4.023948952279190472, -11.56807224179757121 ) ) ;
#59976=CARTESIAN_POINT ( 'NONE',  ( 0.2956976708475454463, 10.72256944221094699, -5.936640677855251624 ) ) ;
#59977=EDGE_CURVE ( 'NONE', #32302, #54991, #31597, .T. ) ;
#59989=EDGE_CURVE ( 'NONE', #31716, #16864, #28418, .T. ) ;
#59990=ORIENTED_EDGE ( 'NONE', *, *, #31651, .T. ) ;
#59991=CARTESIAN_POINT ( 'NONE',  ( 2.245754705088395919, 6.667819336165991650, -3.721112460996948368 ) ) ;
#59993=CARTESIAN_POINT ( 'NONE',  ( 2.889800649504073782, 4.732281052280313816, 3.882893708502064278 ) ) ;
#59998=CARTESIAN_POINT ( 'NONE',  ( 2.276905613633651182, 0.1540880535620979541, 7.644700064315450128 ) ) ;
#60006=VERTEX_POINT ( 'NONE', #20808 ) ;
#60008=ADVANCED_FACE ( 'NONE', ( #15152 ), #32586, .F. ) ;
#60013=CARTESIAN_POINT ( 'NONE',  ( 0.3218525148189785301, -6.342972338926866627, 10.49750909897050555 ) ) ;
#60015=( BOUNDED_SURFACE ( )  B_SPLINE_SURFACE ( 3, 1, ( 
 ( #56213, #49609 ),
 ( #49928, #55897 ),
 ( #39940, #55235 ),
 ( #19989, #10331 ) ),
 .UNSPECIFIED., .F., .F., .F. ) 
 B_SPLINE_SURFACE_WITH_KNOTS ( ( 4, 4 ),
 ( 2, 2 ),
 ( 0.000000000000000000, 1.000000000000000000 ),
 ( 0.000000000000000000, 1.000000000000000000 ),
 .UNSPECIFIED. ) 
 GEOMETRIC_REPRESENTATION_ITEM ( )  RATIONAL_B_SPLINE_SURFACE ( (
 ( 1.000000000000000000, 1.000000000000000000),
 ( 0.6933888150995267674, 0.9895912004443193632),
 ( 0.6933888150995267674, 0.9895912004443193632),
 ( 1.000000000000000000, 1.000000000000000000) ) ) 
 REPRESENTATION_ITEM ( '' )  SURFACE ( )  );
#60018=CARTESIAN_POINT ( 'NONE',  ( 2.241352910868908310, -7.633946224498474820, 0.08337961031701579540 ) ) ;
#60022=EDGE_LOOP ( 'NONE', ( #44357, #55249, #28038, #42024 ) ) ;
#60029=VECTOR ( 'NONE', #604, 1000.000000000000114 ) ;
#60031=EDGE_CURVE ( 'NONE', #40020, #23561, #1486, .T. ) ;
#60033=CARTESIAN_POINT ( 'NONE',  ( 2.257661810674660874, 5.938215228160625969, 4.806737555286991537 ) ) ;
#60036=CARTESIAN_POINT ( 'NONE',  ( 0.3665391374699467075, 1.872534962004800851, 12.13918562134719359 ) ) ;
#60037=VERTEX_POINT ( 'NONE', #60720 ) ;
#60038=MECHANICAL_DESIGN_GEOMETRIC_PRESENTATION_REPRESENTATION('',(#63205),#17559);
#60041=CARTESIAN_POINT ( 'NONE',  ( 0.2648978790185584908, 0.1321385342564118659, -12.24533305150758089 ) ) ;
#60043=CARTESIAN_POINT ( 'NONE',  ( 2.284126774967663476, 7.647017279602157380, 0.1584898568958162390 ) ) ;
#60049=EDGE_LOOP ( 'NONE', ( #14935, #31874, #46430, #9005 ) ) ;
#60051=CARTESIAN_POINT ( 'NONE',  ( 3.031336079629687319, 4.750429016921711600, -6.309383307296628551 ) ) ;
#60057=CARTESIAN_POINT ( 'NONE',  ( 3.152665057734040488, 0.000000000000000000, 0.000000000000000000 ) ) ;
#60058=CARTESIAN_POINT ( 'NONE',  ( 2.781367136451863509, 6.179587792204241481, 4.783057651000522270 ) ) ;
#60059=CARTESIAN_POINT ( 'NONE',  ( 2.491965175174582381, -5.121563073453708093, -5.773748672882058841 ) ) ;
#60063=CARTESIAN_POINT ( 'NONE',  ( 0.2646305136544065406, 10.53923716745255490, -6.237419468586969273 ) ) ;
#60078=CARTESIAN_POINT ( 'NONE',  ( 0.3610902822527181644, -11.44530431865296016, 4.444884365376562840 ) ) ;
#60086=CARTESIAN_POINT ( 'NONE',  ( 2.249013661412230913, 7.540851674528681770, -1.207748565003158081 ) ) ;
#60094=( LENGTH_UNIT ( ) NAMED_UNIT ( * ) SI_UNIT ( .MILLI., .METRE. ) );
#60104=VERTEX_POINT ( 'NONE', #43043 ) ;
#60105=CARTESIAN_POINT ( 'NONE',  ( 2.639814597422740050, 0.2564041122426181651, -7.763021810282384472 ) ) ;
#60112=CARTESIAN_POINT ( 'NONE',  ( 0.2652384770603669617, -10.63836422907228396, 6.065775245581129127 ) ) ;
#60115=EDGE_LOOP ( 'NONE', ( #37567, #31292, #33632, #24274 ) ) ;
#60117=CARTESIAN_POINT ( 'NONE',  ( 2.034671305879536263, 2.716450156984552944, -11.35598636043548204 ) ) ;
#60118=ADVANCED_FACE ( 'NONE', ( #16791 ), #46596, .F. ) ;
#60121=CARTESIAN_POINT ( 'NONE',  ( 2.241509619876139503, -7.525055189891911134, 1.287997509666546803 ) ) ;
#60125=LINE ( 'NONE', #14866, #5569 ) ;
#60130=ORIENTED_EDGE ( 'NONE', *, *, #59275, .F. ) ;
#60135=CARTESIAN_POINT ( 'NONE',  ( 5.514970785353741078, -0.001117786416802142449, 0.004588761610584822515 ) ) ;
#60137=EDGE_LOOP ( 'NONE', ( #17564, #48086, #42799, #45863 ) ) ;
#60139=CARTESIAN_POINT ( 'NONE',  ( 2.244591118396556784, -3.724266936773029890, 6.665613643996593396 ) ) ;
#60141=CARTESIAN_POINT ( 'NONE',  ( 0.4613984246114880006, 2.415907815801404457, 12.07219521825821040 ) ) ;
#60148=CARTESIAN_POINT ( 'NONE',  ( 3.152665057734128862, 5.461013642405629476, -5.761241965769021256 ) ) ;
#60151=VERTEX_POINT ( 'NONE', #52055 ) ;
#60157=CARTESIAN_POINT ( 'NONE',  ( 1.719304012338398246, 7.581471372739840398, 10.22720798541364395 ) ) ;
#60158=CARTESIAN_POINT ( 'NONE',  ( 1.283627346226907218, 9.278077665801971463, -8.503905436512024352 ) ) ;
#60168=CARTESIAN_POINT ( 'NONE',  ( 1.948354844648341411, 11.94326855455022240, -0.7204626209688785865 ) ) ;
#60172=ORIENTED_EDGE ( 'NONE', *, *, #14239, .T. ) ;
#60180=ORIENTED_EDGE ( 'NONE', *, *, #40771, .F. ) ;
#60199=CARTESIAN_POINT ( 'NONE',  ( 5.516018279890452902, 0.003191189039764837348, 0.005976902763919047894 ) ) ;
#60200=CARTESIAN_POINT ( 'NONE',  ( 0.2759803524722208024, 4.011137970318948476, 11.57441428600633770 ) ) ;
#60201=CARTESIAN_POINT ( 'NONE',  ( 2.256373768223409737, -6.681391662621552818, -3.703993494727584324 ) ) ;
#60205=CARTESIAN_POINT ( 'NONE',  ( 2.241317068080781905, -7.633845645378816158, 0.09149433816013313736 ) ) ;
#60209=CARTESIAN_POINT ( 'NONE',  ( 0.2739690278137231760, 10.69833303470765884, 5.965352196073636648 ) ) ;
#60210=CARTESIAN_POINT ( 'NONE',  ( 1.547277799337567483, 10.12789507952265566, 7.618736734813758460 ) ) ;
#60219=CARTESIAN_POINT ( 'NONE',  ( 2.655192694323885050, -8.589732161579133773, -4.290256727312194762 ) ) ;
#60225=CARTESIAN_POINT ( 'NONE',  ( 2.273267844204862165, -5.952585402747270216, -4.797225296800606387 ) ) ;
#60228=B_SPLINE_CURVE_WITH_KNOTS ( 'NONE', 3,
 ( #50829, #16231, #56467, #31514, #36513, #31202, #5275, #11559, #41825, #61435, #5954, #20572, #51816, #6266, #30847, #26210, #297, #46814, #40852 ),
 .UNSPECIFIED., .F., .F.,
 ( 4, 3, 3, 3, 3, 3, 4 ),
 ( 7.230905111020012517E-18, 2.825908398831274927E-05, 4.208813692483992291E-05, 5.591713746943835966E-05, 6.279584083231888939E-05, 9.105792820296731993E-05, 0.0001153131102488850796 ),
 .UNSPECIFIED. ) ;
#60229=EDGE_LOOP ( 'NONE', ( #43477, #12860, #53848, #37334 ) ) ;
#60233=B_SPLINE_CURVE_WITH_KNOTS ( 'NONE', 3,
 ( #64527, #34600, #54894, #25282, #18997, #34907, #23995, #9319, #38950, #45560, #24639, #5019, #65196, #12, #39922, #59241, #19331, #60205, #55559 ),
 .UNSPECIFIED., .F., .F.,
 ( 4, 3, 3, 3, 3, 3, 4 ),
 ( 6.759600587344757484E-18, 2.825908398830985241E-05, 4.208813692483710399E-05, 5.591713746943576435E-05, 6.279584083231437640E-05, 9.105792820296104511E-05, 0.0001153131102488857436 ),
 .UNSPECIFIED. ) ;
#60235=CARTESIAN_POINT ( 'NONE',  ( 0.2653519991613836893, 6.104031847945017297, 10.61652626436030111 ) ) ;
#60236=CARTESIAN_POINT ( 'NONE',  ( 2.261269890823172091, -1.189259211194653609, -7.547924622048553189 ) ) ;
#60243=CARTESIAN_POINT ( 'NONE',  ( 2.653899356900220941, 3.657605971842848636, -6.857477569908583703 ) ) ;
#60255=LINE ( 'NONE', #14680, #60380 ) ;
#60257=B_SPLINE_CURVE_WITH_KNOTS ( 'NONE', 3,
 ( #34926, #5361, #11323, #11000, #46906, #62191, #16643, #56561, #11645, #30604 ),
 .UNSPECIFIED., .F., .F.,
 ( 4, 3, 3, 4 ),
 ( 4.336808689942017736E-19, 6.607638129004463133E-05, 9.911389841680550718E-05, 0.0001667630577588626365 ),
 .UNSPECIFIED. ) ;
#60274=ORIENTED_EDGE ( 'NONE', *, *, #17938, .T. ) ;
#60277=CARTESIAN_POINT ( 'NONE',  ( 1.283627346226615895, -12.57362488724973915, 0.5505361391623344591 ) ) ;
#60278=DIRECTION ( 'NONE',  ( 0.9486832985018465170, 3.872673197958691324E-17, 0.3162277646628396943 ) ) ;
#60279=CARTESIAN_POINT ( 'NONE',  ( 5.515188684475870851, 0.004893136156457998653, -0.002166413411657814019 ) ) ;
#60281=CARTESIAN_POINT ( 'NONE',  ( 2.260457164925434359, 7.226149053011227785, 2.482766715768787158 ) ) ;
#60285=CARTESIAN_POINT ( 'NONE',  ( 2.305787727787084407, -5.970480882365253983, 4.792270232040873879 ) ) ;
#60288=EDGE_CURVE ( 'NONE', #29095, #11102, #5297, .T. ) ;
#60293=ADVANCED_FACE ( 'NONE', ( #38725 ), #14918, .T. ) ;
#60294=CONICAL_SURFACE ( 'NONE', #20982, 7.938172270156617749, 1.280189991382167047 ) ;
#60300=VERTEX_POINT ( 'NONE', #49389 ) ;
#60308=ORIENTED_EDGE ( 'NONE', *, *, #59615, .T. ) ;
#60309=CARTESIAN_POINT ( 'NONE',  ( 2.241352910868908310, 0.08337961031704246850, 7.633946224498473931 ) ) ;
#60314=CARTESIAN_POINT ( 'NONE',  ( 1.719304012338199517, 0.000000000000000000, 0.000000000000000000 ) ) ;
#60330=CARTESIAN_POINT ( 'NONE',  ( 2.941278708680199916, 4.048809123187934844, 4.615461433467269003 ) ) ;
#60337=CARTESIAN_POINT ( 'NONE',  ( 2.903928887688582705, 7.046356840275206146, 5.221047506680442929 ) ) ;
#60338=CARTESIAN_POINT ( 'NONE',  ( 3.047904605210433271, 7.845751380824992793, -0.9519317672905968086 ) ) ;
#60340=CARTESIAN_POINT ( 'NONE',  ( 2.280717697722505655, 5.957695241724533908, 4.794838658391401331 ) ) ;
#60346=EDGE_CURVE ( 'NONE', #58059, #35179, #54689, .T. ) ;
#60350=CARTESIAN_POINT ( 'NONE',  ( 2.241537034860906275, 1.321063441155988949, 7.519304283075082473 ) ) ;
#60357=ORIENTED_EDGE ( 'NONE', *, *, #21113, .F. ) ;
#60372=CARTESIAN_POINT ( 'NONE',  ( 2.994568964204213035, -0.3996732855055282752, 7.875338388187476113 ) ) ;
#60376=EDGE_CURVE ( 'NONE', #49890, #7383, #55319, .T. ) ;
#60380=VECTOR ( 'NONE', #60925, 1000.000000000000114 ) ;
#60381=( BOUNDED_SURFACE ( )  B_SPLINE_SURFACE ( 3, 1, ( 
 ( #36453, #31769 ),
 ( #11500, #11186 ),
 ( #41763, #56069 ),
 ( #26802, #40796 ) ),
 .UNSPECIFIED., .F., .F., .F. ) 
 B_SPLINE_SURFACE_WITH_KNOTS ( ( 4, 4 ),
 ( 2, 2 ),
 ( 0.000000000000000000, 1.000000000000000000 ),
 ( 0.000000000000000000, 1.000000000000000000 ),
 .UNSPECIFIED. ) 
 GEOMETRIC_REPRESENTATION_ITEM ( )  RATIONAL_B_SPLINE_SURFACE ( (
 ( 1.000000000000000000, 1.000000000000000000),
 ( 0.9856612449720755231, 0.9999558406602322425),
 ( 0.9856612449720755231, 0.9999558406602322425),
 ( 1.000000000000000000, 1.000000000000000000) ) ) 
 REPRESENTATION_ITEM ( '' )  SURFACE ( )  );
#60383=CARTESIAN_POINT ( 'NONE',  ( 2.269879328256730666, -2.474479066008269168, 7.232310762824155859 ) ) ;
#60388=CARTESIAN_POINT ( 'NONE',  ( 0.8375941296792348556, -6.548446001455606513, 10.57337970710551822 ) ) ;
#60390=CARTESIAN_POINT ( 'NONE',  ( 5.514624014163232779, 0.004045310349816153353, -0.0008859786816847026571 ) ) ;
#60391=CARTESIAN_POINT ( 'NONE',  ( 0.2833330754217411318, -8.029341648258412789, 9.254504746325759257 ) ) ;
#60402=B_SPLINE_CURVE_WITH_KNOTS ( 'NONE', 3,
 ( #49825, #56104, #24546, #44825, #12451, #43047, #3166, #48398, #58708, #23431, #27115, #43709, #52721, #12137, #47722, #37406, #38390, #63006, #2166 ),
 .UNSPECIFIED., .F., .F.,
 ( 4, 3, 3, 3, 3, 3, 4 ),
 ( 1.158841720744533638E-17, 4.457896483014492915E-05, 6.639290541541691376E-05, 8.820687556478305888E-05, 0.0001100173248778826531, 0.0001545671401658026156, 0.0001830328308068575197 ),
 .UNSPECIFIED. ) ;
#60407=CARTESIAN_POINT ( 'NONE',  ( 2.290907136833254309, -5.041121061899943356, 5.755317856506266594 ) ) ;
#60413=DIRECTION ( 'NONE',  ( 0.3865475372811021382, 0.2971585806051794676, 0.8730852074079769043 ) ) ;
#60419=EDGE_LOOP ( 'NONE', ( #26143, #45889, #65129, #33209 ) ) ;
#60425=FACE_OUTER_BOUND ( 'NONE', #16019, .T. ) ;
#60429=ADVANCED_FACE ( 'NONE', ( #24745 ), #64070, .F. ) ;
#60432=CARTESIAN_POINT ( 'NONE',  ( 2.963017218115616913, -4.265970453343964408, 6.619413971958201692 ) ) ;
#60436=CARTESIAN_POINT ( 'NONE',  ( 2.242418902651939661, 7.634109827927225922, -0.09970190380435364763 ) ) ;
#60438=CARTESIAN_POINT ( 'NONE',  ( 2.241536586108912932, 5.852386772940070259, 4.902521014023349721 ) ) ;
#60440=CARTESIAN_POINT ( 'NONE',  ( 3.031336079629145530, -3.088871717871215505, -7.268683861177180461 ) ) ;
#60441=CARTESIAN_POINT ( 'NONE',  ( 3.152665057734040488, 0.000000000000000000, 0.000000000000000000 ) ) ;
#60453=CARTESIAN_POINT ( 'NONE',  ( 2.260457164926975349, 2.482766715767231069, -7.226149053012312251 ) ) ;
#60456=CARTESIAN_POINT ( 'NONE',  ( 2.907497136250260628, 2.346692756478441666, -7.497839665536633724 ) ) ;
#60461=CARTESIAN_POINT ( 'NONE',  ( 2.889800649504073782, 0.06738247734058958049, -6.121013568931505944 ) ) ;
#60464=CARTESIAN_POINT ( 'NONE',  ( 5.514970785353741078, 0.004233694591582517000, -0.002093325033904037177 ) ) ;
#60466=CARTESIAN_POINT ( 'NONE',  ( 0.2650492594609233366, 12.24562116224018382, 0.1101156276917182181 ) ) ;
#60476=CARTESIAN_POINT ( 'NONE',  ( 2.655192694323992519, 5.293797899975493770, 8.010337395398677174 ) ) ;
#60478=DIRECTION ( 'NONE',  ( 1.000000000000000000, 0.000000000000000000, 0.000000000000000000 ) ) ;
#60480=CARTESIAN_POINT ( 'NONE',  ( 2.241352910868908754, 3.889181972941450738, 6.569501556381455387 ) ) ;
#60484=CARTESIAN_POINT ( 'NONE',  ( 2.931247277082690061, -2.338794445044939163, -7.508560300462427506 ) ) ;
#60495=CARTESIAN_POINT ( 'NONE',  ( 1.937114397841935398, 10.63710405811943716, -7.182898292393653961 ) ) ;
#60502=EDGE_CURVE ( 'NONE', #52979, #54859, #50533, .T. ) ;
#60508=CARTESIAN_POINT ( 'NONE',  ( 2.430348790456883901, -5.769383131055034752, 5.095533593439705022 ) ) ;
#60509=CARTESIAN_POINT ( 'NONE',  ( 0.8375941296786605372, 11.54987202580242389, 4.612912274495619691 ) ) ;
#60516=CARTESIAN_POINT ( 'NONE',  ( 2.249013661412014642, -2.498855301843467380, -7.216565855998053891 ) ) ;
#60522=CARTESIAN_POINT ( 'NONE',  ( 0.2911222467163514516, -10.71854909364322772, 5.940753417478891407 ) ) ;
#60524=CARTESIAN_POINT ( 'NONE',  ( 2.273267844204860832, -6.695181685739923338, -3.690689057641690418 ) ) ;
#60532=CARTESIAN_POINT ( 'NONE',  ( 2.573738926104375935, 6.822065037112484909, -3.667129335223129782 ) ) ;
#60540=DIRECTION ( 'NONE',  ( 0.3939253465568944290, -0.8008152550167628725, 0.4511294145502680597 ) ) ;
#60541=CARTESIAN_POINT ( 'NONE',  ( 3.100650473569583010, 3.562766772868595222, 7.074394303868141165 ) ) ;
#60546=CARTESIAN_POINT ( 'NONE',  ( 2.241352910868908754, 1.243507963608094347, 7.532448145350512547 ) ) ;
#60556=FACE_OUTER_BOUND ( 'NONE', #24737, .T. ) ;
#60557=CARTESIAN_POINT ( 'NONE',  ( 3.152665057734040488, 0.000000000000000000, 0.000000000000000000 ) ) ;
#60558=CARTESIAN_POINT ( 'NONE',  ( 2.241352910868908754, 3.889181972941450738, 6.569501556381455387 ) ) ;
#60568=CARTESIAN_POINT ( 'NONE',  ( 2.406456491625824867, -0.6290357040720556681, -10.41426194695600671 ) ) ;
#60573=( BOUNDED_SURFACE ( )  B_SPLINE_SURFACE ( 3, 1, ( 
 ( #53789, #8222 ),
 ( #28493, #3250 ),
 ( #23522, #64077 ),
 ( #38811, #33801 ) ),
 .UNSPECIFIED., .F., .F., .F. ) 
 B_SPLINE_SURFACE_WITH_KNOTS ( ( 4, 4 ),
 ( 2, 2 ),
 ( 0.000000000000000000, 1.000000000000000000 ),
 ( 0.000000000000000000, 1.000000000000000000 ),
 .UNSPECIFIED. ) 
 GEOMETRIC_REPRESENTATION_ITEM ( )  RATIONAL_B_SPLINE_SURFACE ( (
 ( 1.000000000000000000, 1.000000000000000000),
 ( 0.9856612449720755231, 0.9999558406602322425),
 ( 0.9856612449720755231, 0.9999558406602322425),
 ( 1.000000000000000000, 1.000000000000000000) ) ) 
 REPRESENTATION_ITEM ( '' )  SURFACE ( )  );
#60575=EDGE_CURVE ( 'NONE', #49787, #46103, #39867, .T. ) ;
#60577=FACE_OUTER_BOUND ( 'NONE', #60817, .T. ) ;
#60584=ORIENTED_EDGE ( 'NONE', *, *, #26258, .F. ) ;
#60588=CARTESIAN_POINT ( 'NONE',  ( 1.194176325881346035, -6.717888447700763876, -10.60746084433563041 ) ) ;
#60603=VERTEX_POINT ( 'NONE', #3681 ) ;
#60618=CARTESIAN_POINT ( 'NONE',  ( 0.8375941296789963797, 12.17542732751272183, 2.537217542321736463 ) ) ;
#60631=AXIS2_PLACEMENT_3D ( 'NONE', #63139, #12925, #12576 ) ;
#60638=CARTESIAN_POINT ( 'NONE',  ( 2.263328370261531219, 0.1420109704215806457, 7.640407877530307701 ) ) ;
#60647=VERTEX_POINT ( 'NONE', #50520 ) ;
#60652=ORIENTED_EDGE ( 'NONE', *, *, #1745, .F. ) ;
#60654=CARTESIAN_POINT ( 'NONE',  ( 1.719304012340733934, -11.67935079956419031, -5.066286238786891438 ) ) ;
#60655=CARTESIAN_POINT ( 'NONE',  ( 0.2911222467163532279, -6.312159098066242535, 10.50411792397755661 ) ) ;
#60656=CARTESIAN_POINT ( 'NONE',  ( 0.2651627682582903267, 4.105539787731869339, -11.53745347823611667 ) ) ;
#60661=LINE ( 'NONE', #800, #48356 ) ;
#60663=ORIENTED_EDGE ( 'NONE', *, *, #64156, .F. ) ;
#60665=ADVANCED_FACE ( 'NONE', ( #19269 ), #24246, .T. ) ;
#60670=CARTESIAN_POINT ( 'NONE',  ( 0.3053067050349255740, 9.538004819224459752, -7.702091166065907935 ) ) ;
#60674=CARTESIAN_POINT ( 'NONE',  ( 3.152665057734040488, 0.000000000000000000, 0.000000000000000000 ) ) ;
#60676=CARTESIAN_POINT ( 'NONE',  ( 2.705197763288549773, 7.714317563576064352, -1.076142490489789605 ) ) ;
#60694=CARTESIAN_POINT ( 'NONE',  ( 2.665405856346778624, -9.304623509366210854, -2.226920474533478078 ) ) ;
#60699=CIRCLE ( 'NONE', #26707, 4.000000000000000000 ) ;
#60708=CARTESIAN_POINT ( 'NONE',  ( 2.941278708680199916, 5.383216837018982126, -2.952340773940052898 ) ) ;
#60714=B_SPLINE_CURVE_WITH_KNOTS ( 'NONE', 3,
 ( #15552, #30835, #54829, #613, #5610, #35813, #56115, #41143, #10555, #34833, #65114, #50502, #34530 ),
 .UNSPECIFIED., .F., .F.,
 ( 4, 3, 3, 3, 4 ),
 ( 3.035766082959412415E-18, 6.607593386745472762E-05, 0.0001321518677373527319, 0.0001982171734706220795, 0.0002642860854759487171 ),
 .UNSPECIFIED. ) ;
#60720=CARTESIAN_POINT ( 'NONE',  ( 0.3675815128205894289, 10.50067073900660652, -6.367184624550055183 ) ) ;
#60722=CARTESIAN_POINT ( 'NONE',  ( 2.241352910868908310, 7.633946224498473931, 0.08337961031706864201 ) ) ;
#60723=FACE_OUTER_BOUND ( 'NONE', #7464, .T. ) ;
#60734=CARTESIAN_POINT ( 'NONE',  ( 0.2646305136544072623, 9.465888453933068547, -7.770320294339081890 ) ) ;
#60740=CARTESIAN_POINT ( 'NONE',  ( 0.3002738374340830907, -11.43949898053768166, -4.403689978763186019 ) ) ;
#60741=CARTESIAN_POINT ( 'NONE',  ( 2.241451721903216843, 2.668222118333546611, -7.153019588493043202 ) ) ;
#60747=( LENGTH_UNIT ( ) NAMED_UNIT ( * ) SI_UNIT ( .MILLI., .METRE. ) );
#60750=CARTESIAN_POINT ( 'NONE',  ( 0.3053067050349130840, 11.43920902168906828, 4.409108891833689370 ) ) ;
#60762=CARTESIAN_POINT ( 'NONE',  ( 2.373367633546870969, 0.1808255748566540144, -7.676289145832772221 ) ) ;
#60764=CARTESIAN_POINT ( 'NONE',  ( 5.515188684475870851, 0.002983184900674853111, -0.004442604682416488940 ) ) ;
#60774=CARTESIAN_POINT ( 'NONE',  ( 2.255723233588951437, -1.456523090672661613, 7.499053486174015681 ) ) ;
#60775=CIRCLE ( 'NONE', #8766, 7.938172270156617749 ) ;
#60783=VERTEX_POINT ( 'NONE', #30857 ) ;
#60787=( BOUNDED_SURFACE ( )  B_SPLINE_SURFACE ( 3, 1, ( 
 ( #21725, #27029 ),
 ( #1768, #17038 ),
 ( #42281, #16402 ),
 ( #57955, #61597 ) ),
 .UNSPECIFIED., .F., .F., .F. ) 
 B_SPLINE_SURFACE_WITH_KNOTS ( ( 4, 4 ),
 ( 2, 2 ),
 ( 0.000000000000000000, 1.000000000000000000 ),
 ( 0.000000000000000000, 1.000000000000000000 ),
 .UNSPECIFIED. ) 
 GEOMETRIC_REPRESENTATION_ITEM ( )  RATIONAL_B_SPLINE_SURFACE ( (
 ( 1.000000000000000000, 1.000000000000000000),
 ( 0.9856612449720755231, 0.9999558406602322425),
 ( 0.9856612449720755231, 0.9999558406602322425),
 ( 1.000000000000000000, 1.000000000000000000) ) ) 
 REPRESENTATION_ITEM ( '' )  SURFACE ( )  );
#60792=CARTESIAN_POINT ( 'NONE',  ( 3.152665057735899001, -7.886634106564667235, -0.9030954876721221103 ) ) ;
#60798=AXIS2_PLACEMENT_3D ( 'NONE', #12314, #31934, #8016 ) ;
#60800=CARTESIAN_POINT ( 'NONE',  ( 0.3675815128205894289, -7.689697408877338880, 9.574637318041938627 ) ) ;
#60805=CARTESIAN_POINT ( 'NONE',  ( 5.536195898058073439, 0.004468797463753785421, 0.007230647766619707588 ) ) ;
#60809=EDGE_CURVE ( 'NONE', #8001, #1325, #26730, .T. ) ;
#60817=EDGE_LOOP ( 'NONE', ( #54864, #10882, #57336, #3605 ) ) ;
#60818=CARTESIAN_POINT ( 'NONE',  ( 2.262775599886255762, -6.546038779272016050, -3.942403752832075892 ) ) ;
#60819=CARTESIAN_POINT ( 'NONE',  ( 0.2646305136544065406, -0.1321451301297000003, -12.24595685781654630 ) ) ;
#60824=CARTESIAN_POINT ( 'NONE',  ( 0.9296196016852261712, 10.99907063288950049, -5.870433615766662783 ) ) ;
#60842=CARTESIAN_POINT ( 'NONE',  ( 2.406456491625819094, 2.970787154401585806, -10.00134798414976345 ) ) ;
#60851=CARTESIAN_POINT ( 'NONE',  ( 2.844750968615358033, -5.783165144077080377, 5.286885609674477848 ) ) ;
#60873=CARTESIAN_POINT ( 'NONE',  ( 0.2834382757447994061, 10.71064820518743055, 5.949714385480675993 ) ) ;
#60875=AXIS2_PLACEMENT_3D ( 'NONE', #2395, #63216, #12016 ) ;
#60877=CARTESIAN_POINT ( 'NONE',  ( 2.298277635560095344, -3.682855706290095732, -6.709004959608344976 ) ) ;
#60882=CARTESIAN_POINT ( 'NONE',  ( 1.948354844648095607, -2.783443994770122387, -11.63671644762040458 ) ) ;
#60887=CARTESIAN_POINT ( 'NONE',  ( 0.3057689695767448201, 12.25749431726083394, -0.2309407641933178545 ) ) ;
#60889=CARTESIAN_POINT ( 'NONE',  ( 2.288423627607476973, -5.962686897379168904, -4.792733268640440691 ) ) ;
#60895=EDGE_CURVE ( 'NONE', #53953, #60970, #50126, .T. ) ;
#60908=CARTESIAN_POINT ( 'NONE',  ( 0.2638984909335716500, 8.023974293733301622, -9.252728947330998821 ) ) ;
#60915=CARTESIAN_POINT ( 'NONE',  ( 2.350038591458109227, -10.55267716396077482, 1.210550722320991701 ) ) ;
#60925=DIRECTION ( 'NONE',  ( -0.3939253465568944290, 0.7910971609033267127, -0.4679616473074760807 ) ) ;
#60928=CARTESIAN_POINT ( 'NONE',  ( 5.514624014163232779, 0.003498325728817963057, 0.002216125254993220762 ) ) ;
#60930=EDGE_CURVE ( 'NONE', #23499, #51119, #63111, .T. ) ;
#60935=CARTESIAN_POINT ( 'NONE',  ( 0.3278977287071186963, -3.961557589215535913, -11.60975784853196657 ) ) ;
#60945=CARTESIAN_POINT ( 'NONE',  ( 1.104777566491143892, -12.51694124543052311, 0.4777483965053294646 ) ) ;
#60947=CARTESIAN_POINT ( 'NONE',  ( 5.514970785353741078, -0.002093325033904051488, -0.004233694591582509194 ) ) ;
#60951=CARTESIAN_POINT ( 'NONE',  ( 3.152665057734040488, 0.000000000000000000, 0.000000000000000000 ) ) ;
#60957=CARTESIAN_POINT ( 'NONE',  ( 3.152665057735546839, 0.4801242025606423658, 7.923639299008859105 ) ) ;
#60969=CARTESIAN_POINT ( 'NONE',  ( 0.2676618633000466541, -5.983781707237532110, -10.68562420805848490 ) ) ;
#60970=VERTEX_POINT ( 'NONE', #44766 ) ;
#60973=CARTESIAN_POINT ( 'NONE',  ( 2.241352910868908754, -3.889181972941404553, -6.569501556381482921 ) ) ;
#60975=EDGE_CURVE ( 'NONE', #10208, #25087, #24238, .T. ) ;
#60977=CARTESIAN_POINT ( 'NONE',  ( 0.2638984909335720941, -10.70468911391660072, -5.950360275955167921 ) ) ;
#60980=CARTESIAN_POINT ( 'NONE',  ( 2.266490820343227242, 0.1453321357832749183, 7.641399530653802508 ) ) ;
#60982=CARTESIAN_POINT ( 'NONE',  ( 5.530133899448235191, -0.01324661008606523721, -0.008946569461392297334 ) ) ;
#60985=CARTESIAN_POINT ( 'NONE',  ( 2.241537034860907163, 6.609284473755334233, 3.821322318518396433 ) ) ;
#60986=ORIENTED_EDGE ( 'NONE', *, *, #43540, .F. ) ;
#60990=ORIENTED_EDGE ( 'NONE', *, *, #22345, .F. ) ;
#60999=FACE_OUTER_BOUND ( 'NONE', #14025, .T. ) ;
#61001=CARTESIAN_POINT ( 'NONE',  ( 2.241526690369557429, -2.594870554108887895, 7.179945570618750494 ) ) ;
#61002=VERTEX_POINT ( 'NONE', #33806 ) ;
#61006=CARTESIAN_POINT ( 'NONE',  ( 3.152665057736177445, 3.161213418915486795, 7.281573230473766145 ) ) ;
#61012=CARTESIAN_POINT ( 'NONE',  ( 0.4626703367443949499, -2.416235258139843634, 12.07256244737114059 ) ) ;
#61013=CARTESIAN_POINT ( 'NONE',  ( 5.514970785353741078, 0.002796696073589738894, -0.003805873180274792905 ) ) ;
#61022=DIRECTION ( 'NONE',  ( 0.3865475372811021937, 0.4442537292684328731, 0.8082200352954663769 ) ) ;
#61030=ORIENTED_EDGE ( 'NONE', *, *, #63977, .F. ) ;
#61050=CARTESIAN_POINT ( 'NONE',  ( 0.2646305136544072623, -12.08286001766534312, -1.996350543473119021 ) ) ;
#61051=CARTESIAN_POINT ( 'NONE',  ( 2.969415267404796221, -7.260393470501854019, 3.055358878717769677 ) ) ;
#61055=CARTESIAN_POINT ( 'NONE',  ( 2.241311220309555097, 1.234192392743173050, 7.533971938435846560 ) ) ;
#61065=CARTESIAN_POINT ( 'NONE',  ( 2.653899356900045081, -7.388433688587411119, -2.411250235128119090 ) ) ;
#61067=CARTESIAN_POINT ( 'NONE',  ( 0.2648321136542688414, 7.762514728658100438, 9.471460387169299722 ) ) ;
#61073=CARTESIAN_POINT ( 'NONE',  ( 0.3109076770649040200, 11.43910935267338580, -4.414555973477709117 ) ) ;
#61078=CARTESIAN_POINT ( 'NONE',  ( 0.3002738374340798710, 11.43949898053770653, 4.403689978763103419 ) ) ;
#61087=CARTESIAN_POINT ( 'NONE',  ( 2.276905613633648073, -7.236369456722863802, -2.469846004795382743 ) ) ;
#61091=CARTESIAN_POINT ( 'NONE',  ( 0.2648978790185593790, 9.295532325666449935, 7.972372351883061370 ) ) ;
#61097=ADVANCED_FACE ( 'NONE', ( #20497 ), #51093, .T. ) ;
#61098=DIRECTION ( 'NONE',  ( -1.000000000000000000, -0.000000000000000000, -0.000000000000000000 ) ) ;
#61103=CARTESIAN_POINT ( 'NONE',  ( 5.536195898058073439, 0.001224473329857981652, -0.008411485181669245415 ) ) ;
#61107=CARTESIAN_POINT ( 'NONE',  ( 2.827825597296800719, 8.278234963587719264, 3.592949031604448340 ) ) ;
#61109=VECTOR ( 'NONE', #39927, 1000.000000000000114 ) ;
#61114=CARTESIAN_POINT ( 'NONE',  ( 0.2652384529303108418, 0.06607367983853688898, 12.24598125395192838 ) ) ;
#61120=ORIENTED_EDGE ( 'NONE', *, *, #11852, .T. ) ;
#61122=CARTESIAN_POINT ( 'NONE',  ( 5.515539859299206427, 0.0001942659352247811874, -0.006049968793488399305 ) ) ;
#61124=CARTESIAN_POINT ( 'NONE',  ( 0.8320506296491587683, -1.781423711749659189, 12.30686996250300069 ) ) ;
#61126=B_SPLINE_CURVE_WITH_KNOTS ( 'NONE', 3,
 ( #16679, #61565, #51627, #36302, #11047, #6073, #26330, #1069, #46951, #21338, #41944, #1731, #21997 ),
 .UNSPECIFIED., .F., .F.,
 ( 4, 3, 3, 3, 4 ),
 ( 2.602085213965210642E-18, 6.607593386745585248E-05, 0.0001321518677373532740, 0.0001982171734706192877, 0.0002642860854759484460 ),
 .UNSPECIFIED. ) ;
#61129=CARTESIAN_POINT ( 'NONE',  ( 1.452237505248552996, 12.64182585313126062, 0.5922625322517451885 ) ) ;
#61136=CARTESIAN_POINT ( 'NONE',  ( 0.2652384529303146166, 12.24598125395190884, -0.06607367983857954929 ) ) ;
#61137=CARTESIAN_POINT ( 'NONE',  ( 2.241528039335006994, 7.168649579907130587, 2.625917297988412002 ) ) ;
#61141=ORIENTED_EDGE ( 'NONE', *, *, #56789, .T. ) ;
#61143=CARTESIAN_POINT ( 'NONE',  ( 0.3040950598368144520, -1.881452845810294594, -12.11647736519423191 ) ) ;
#61148=CARTESIAN_POINT ( 'NONE',  ( 1.375507693217069560, 9.273955665125992454, 8.553661013311447903 ) ) ;
#61149=CARTESIAN_POINT ( 'NONE',  ( 1.372161826076961910, 9.274145586376256745, -8.551811013234910774 ) ) ;
#61155=CARTESIAN_POINT ( 'NONE',  ( 0.3675815128205894289, -2.391755495700522705, -12.04510820461661780 ) ) ;
#61156=CARTESIAN_POINT ( 'NONE',  ( 0.3006302518452019235, -9.243299516615085309, 8.051021221755751966 ) ) ;
#61159=ORIENTED_EDGE ( 'NONE', *, *, #14959, .T. ) ;
#61169=ORIENTED_EDGE ( 'NONE', *, *, #58315, .T. ) ;
#61170=CARTESIAN_POINT ( 'NONE',  ( 3.152665057736245391, 2.258875078500370837, -7.609997527622033076 ) ) ;
#61181=DIRECTION ( 'NONE',  ( 0.000000000000000000, 0.000000000000000000, 1.000000000000000000 ) ) ;
#61182=ORIENTED_EDGE ( 'NONE', *, *, #10420, .F. ) ;
#61187=( BOUNDED_SURFACE ( )  B_SPLINE_SURFACE ( 3, 1, ( 
 ( #17536, #53097 ),
 ( #1599, #58096 ),
 ( #62731, #17197 ),
 ( #57781, #12851 ) ),
 .UNSPECIFIED., .F., .F., .F. ) 
 B_SPLINE_SURFACE_WITH_KNOTS ( ( 4, 4 ),
 ( 2, 2 ),
 ( 0.000000000000000000, 1.000000000000000000 ),
 ( 0.000000000000000000, 1.000000000000000000 ),
 .UNSPECIFIED. ) 
 GEOMETRIC_REPRESENTATION_ITEM ( )  RATIONAL_B_SPLINE_SURFACE ( (
 ( 1.000000000000000000, 1.000000000000000000),
 ( 0.9856612449720755231, 0.9999558406602322425),
 ( 0.9856612449720755231, 0.9999558406602322425),
 ( 1.000000000000000000, 1.000000000000000000) ) ) 
 REPRESENTATION_ITEM ( '' )  SURFACE ( )  );
#61188=CARTESIAN_POINT ( 'NONE',  ( 2.305787727787085295, 5.970480882365287734, -4.792270232040832134 ) ) ;
#61190=CARTESIAN_POINT ( 'NONE',  ( 5.515188684475870851, -0.0003622115669623649468, 0.005339000964281801972 ) ) ;
#61192=CARTESIAN_POINT ( 'NONE',  ( 1.634816307077888498, 10.17753964889907436, -7.601181930720465552 ) ) ;
#61194=CARTESIAN_POINT ( 'NONE',  ( 2.573738926104374158, -7.741646296020614493, -0.2352053552898267230 ) ) ;
#61195=EDGE_CURVE ( 'NONE', #43792, #9473, #22122, .T. ) ;
#61199=CARTESIAN_POINT ( 'NONE',  ( 0.2671309869109465551, 10.68612389951478114, 5.982543484153262980 ) ) ;
#61210=CARTESIAN_POINT ( 'NONE',  ( 5.530133899448235191, -0.008946569461392342437, -0.01324661008606586518 ) ) ;
#61212=CARTESIAN_POINT ( 'NONE',  ( 5.530133899448235191, -0.01536822665454898318, 0.004396748047611176956 ) ) ;
#61214=CARTESIAN_POINT ( 'NONE',  ( 2.242418902651938772, -5.912154560271186021, -4.830735119000208577 ) ) ;
#61216=CARTESIAN_POINT ( 'NONE',  ( 2.253265082352431392, 0.1282654837135756010, -7.637296367516834827 ) ) ;
#61224=CARTESIAN_POINT ( 'NONE',  ( 2.253265082353311577, -1.199885753715151715, -7.543541742287505514 ) ) ;
#61235=CARTESIAN_POINT ( 'NONE',  ( 2.259025283528617756, 4.805599953367311272, -5.939720477913882135 ) ) ;
#61241=CARTESIAN_POINT ( 'NONE',  ( 0.3006302518452045880, -6.323626002161014448, -10.50091819089221978 ) ) ;
#61247=CARTESIAN_POINT ( 'NONE',  ( 0.3164563675027638467, -12.26087493884171487, 0.2404665832030958295 ) ) ;
#61248=CARTESIAN_POINT ( 'NONE',  ( 5.514970785353741078, 0.003805873180274780762, 0.002796696073589751037 ) ) ;
#61255=CARTESIAN_POINT ( 'NONE',  ( 0.3053067050349138056, -4.409108891833727562, 11.43920902168905407 ) ) ;
#61260=ORIENTED_EDGE ( 'NONE', *, *, #43354, .F. ) ;
#61270=CARTESIAN_POINT ( 'NONE',  ( 5.516018279890452902, 0.006707902355168863032, 0.0009545156522404598482 ) ) ;
#61271=ORIENTED_EDGE ( 'NONE', *, *, #32624, .F. ) ;
#61274=CARTESIAN_POINT ( 'NONE',  ( 0.2648978790185619880, -7.972372351882965447, -9.295532325666529871 ) ) ;
#61284=CARTESIAN_POINT ( 'NONE',  ( 1.719304012338199517, 0.000000000000000000, 0.000000000000000000 ) ) ;
#61287=CARTESIAN_POINT ( 'NONE',  ( 0.2655924914740778187, 9.352877839710604491, 7.905499957109269893 ) ) ;
#61288=CARTESIAN_POINT ( 'NONE',  ( 2.941278708680199916, 4.788765081995630446, 3.842273877444578822 ) ) ;
#61289=EDGE_LOOP ( 'NONE', ( #42356, #30320, #12969, #14698 ) ) ;
#61291=CARTESIAN_POINT ( 'NONE',  ( 1.109979610368954095, 10.60154531817190993, 6.674783385103837396 ) ) ;
#61302=CARTESIAN_POINT ( 'NONE',  ( 3.152665057735509979, 7.102135024646700323, 3.546019893115181620 ) ) ;
#61303=FACE_OUTER_BOUND ( 'NONE', #62283, .T. ) ;
#61305=CARTESIAN_POINT ( 'NONE',  ( 0.2650492594609225039, 4.291723947796471705, -11.46945808033129310 ) ) ;
#61307=CARTESIAN_POINT ( 'NONE',  ( 2.903928887688177696, 7.316175791236187997, -4.835706109686608301 ) ) ;
#61316=ORIENTED_EDGE ( 'NONE', *, *, #1361, .F. ) ;
#61317=VERTEX_POINT ( 'NONE', #24412 ) ;
#61322=CARTESIAN_POINT ( 'NONE',  ( 2.931247277082682512, 7.800615791174669411, -0.9994150891045507912 ) ) ;
#61323=CARTESIAN_POINT ( 'NONE',  ( 1.109979610369596470, -2.646302643132046217, 12.24510427445470384 ) ) ;
#61325=ORIENTED_EDGE ( 'NONE', *, *, #5245, .T. ) ;
#61343=( BOUNDED_SURFACE ( )  B_SPLINE_SURFACE ( 3, 1, ( 
 ( #21960, #6681 ),
 ( #17639, #16965 ),
 ( #37235, #11971 ),
 ( #52570, #6999 ) ),
 .UNSPECIFIED., .F., .F., .F. ) 
 B_SPLINE_SURFACE_WITH_KNOTS ( ( 4, 4 ),
 ( 2, 2 ),
 ( 0.000000000000000000, 1.000000000000000000 ),
 ( 0.000000000000000000, 1.000000000000000000 ),
 .UNSPECIFIED. ) 
 GEOMETRIC_REPRESENTATION_ITEM ( )  RATIONAL_B_SPLINE_SURFACE ( (
 ( 1.000000000000000000, 1.000000000000000000),
 ( 0.9856612449720755231, 0.9999558406602322425),
 ( 0.9856612449720755231, 0.9999558406602322425),
 ( 1.000000000000000000, 1.000000000000000000) ) ) 
 REPRESENTATION_ITEM ( '' )  SURFACE ( )  );
#61344=FACE_OUTER_BOUND ( 'NONE', #36285, .T. ) ;
#61347=ORIENTED_EDGE ( 'NONE', *, *, #26688, .T. ) ;
#61349=CARTESIAN_POINT ( 'NONE',  ( 0.2652384529303122851, 10.63836770010965793, 6.065769141714241641 ) ) ;
#61350=CARTESIAN_POINT ( 'NONE',  ( 2.907497136251165681, 1.009055026157950952, -7.791429554169957861 ) ) ;
#61353=CARTESIAN_POINT ( 'NONE',  ( 2.639814597422738718, -6.594772041715911470, -4.103563379978084846 ) ) ;
#61354=CARTESIAN_POINT ( 'NONE',  ( 5.530133899448235191, -0.001661287012794241151, 0.01589823604557754830 ) ) ;
#61356=CARTESIAN_POINT ( 'NONE',  ( 2.241451721903217731, -3.764430789729930726, -6.641849090084989804 ) ) ;
#61368=CARTESIAN_POINT ( 'NONE',  ( 2.430348790457330210, -7.297553103283477505, -2.448665558939176368 ) ) ;
#61389=ORIENTED_EDGE ( 'NONE', *, *, #30011, .F. ) ;
#61394=ORIENTED_EDGE ( 'NONE', *, *, #62630, .T. ) ;
#61395=ORIENTED_EDGE ( 'NONE', *, *, #31265, .T. ) ;
#61397=B_SPLINE_CURVE_WITH_KNOTS ( 'NONE', 3,
 ( #59397, #44105, #3575, #17855, #38119, #58775, #12858, #53447, #29151, #2908, #23168, #54086, #8208, #28474, #18842, #34107, #3230, #43780, #64056 ),
 .UNSPECIFIED., .F., .F.,
 ( 4, 3, 3, 3, 3, 3, 4 ),
 ( 6.829613154537258970E-18, 2.825908398831227493E-05, 4.208813692483927239E-05, 5.591713746943774302E-05, 6.279584083231731729E-05, 9.105792820296498889E-05, 0.0001153131102488858250 ),
 .UNSPECIFIED. ) ;
#61407=VERTEX_POINT ( 'NONE', #13449 ) ;
#61412=CARTESIAN_POINT ( 'NONE',  ( 5.516018279890452902, 0.005042957932159071975, 0.004525000489649949435 ) ) ;
#61416=CARTESIAN_POINT ( 'NONE',  ( 0.3675815128205894289, 9.574637318041965273, 7.689697408877307794 ) ) ;
#61425=CARTESIAN_POINT ( 'NONE',  ( 2.298277635560284526, 4.791911337974176455, 5.967558917212159031 ) ) ;
#61426=CARTESIAN_POINT ( 'NONE',  ( 2.244591118396414675, 2.510215291309781271, -7.211060161907408173 ) ) ;
#61427=VERTEX_POINT ( 'NONE', #58607 ) ;
#61435=CARTESIAN_POINT ( 'NONE',  ( 2.260457164927186291, 2.742969430850518808, 7.131443009846811343 ) ) ;
#61446=ORIENTED_EDGE ( 'NONE', *, *, #2199, .F. ) ;
#61451=CARTESIAN_POINT ( 'NONE',  ( 1.719304012338199517, 0.000000000000000000, 0.000000000000000000 ) ) ;
#61455=EDGE_CURVE ( 'NONE', #8359, #36589, #43600, .T. ) ;
#61456=CARTESIAN_POINT ( 'NONE',  ( 0.7446945582530694052, 10.91757157182845717, -5.891988114923994324 ) ) ;
#61457=CARTESIAN_POINT ( 'NONE',  ( 1.020182472826105746, 12.37761526492893083, -1.729367949133470361 ) ) ;
#61460=CARTESIAN_POINT ( 'NONE',  ( 2.963017218115631568, -2.328652339224295709, -7.522800244854603413 ) ) ;
#61463=CARTESIAN_POINT ( 'NONE',  ( 0.3164563675027640133, -9.237806174449815444, 8.065346584422218967 ) ) ;
#61466=ORIENTED_EDGE ( 'NONE', *, *, #16552, .F. ) ;
#61471=FACE_OUTER_BOUND ( 'NONE', #30924, .T. ) ;
#61481=CARTESIAN_POINT ( 'NONE',  ( 0.3675815128205894289, -11.62724744438063063, -3.951233083390586209 ) ) ;
#61484=CIRCLE ( 'NONE', #32801, 12.73084802173761787 ) ;
#61485=ORIENTED_EDGE ( 'NONE', *, *, #6213, .T. ) ;
#61489=FACE_OUTER_BOUND ( 'NONE', #34073, .T. ) ;
#61491=CARTESIAN_POINT ( 'NONE',  ( 2.305787727787084407, -6.545285700970554288, 3.971363876083942035 ) ) ;
#61494=CARTESIAN_POINT ( 'NONE',  ( 2.284126774967169649, -2.466502196989121654, -7.240052432235436264 ) ) ;
#61500=CARTESIAN_POINT ( 'NONE',  ( 0.2833330754217371905, -2.326361469893312606, 12.02930703389099598 ) ) ;
#61513=ORIENTED_EDGE ( 'NONE', *, *, #48405, .T. ) ;
#61523=CARTESIAN_POINT ( 'NONE',  ( 5.536195898058073439, -0.0002547682446687435961, 0.008496323383586254843 ) ) ;
#61550=CARTESIAN_POINT ( 'NONE',  ( 2.258463476537673653, 7.131741622455168184, 2.740340677912665335 ) ) ;
#61553=VERTEX_POINT ( 'NONE', #49530 ) ;
#61555=ORIENTED_EDGE ( 'NONE', *, *, #39665, .T. ) ;
#61559=CARTESIAN_POINT ( 'NONE',  ( 1.719304012338820131, 1.452142814150020556, 12.64775761152757561 ) ) ;
#61563=CARTESIAN_POINT ( 'NONE',  ( 3.152665057734127529, -7.281573230474269742, -3.161213418913537687 ) ) ;
#61565=CARTESIAN_POINT ( 'NONE',  ( 0.2650492594609232810, 4.084774262246084753, 11.54478160586238644 ) ) ;
#61572=CARTESIAN_POINT ( 'NONE',  ( 2.241352910868908754, 3.744764251556992996, 6.652881166698525028 ) ) ;
#61575=ORIENTED_EDGE ( 'NONE', *, *, #28327, .T. ) ;
#61579=CARTESIAN_POINT ( 'NONE',  ( 0.2653519991613836893, -9.366979519113291630, -7.888569541500616289 ) ) ;
#61596=CARTESIAN_POINT ( 'NONE',  ( 0.3675815128205894289, -5.910255304480370953, -10.76447900494946452 ) ) ;
#61597=CARTESIAN_POINT ( 'NONE',  ( 0.2646305136544072623, 4.064188116014551433, 11.55263159009959928 ) ) ;
#61610=CARTESIAN_POINT ( 'NONE',  ( 5.514970785353741078, -0.004713149585127533042, 0.0003039746380528807537 ) ) ;
#61620=CARTESIAN_POINT ( 'NONE',  ( 2.305787727787083519, 1.493241775258524084, -7.508843116234142911 ) ) ;
#61623=CARTESIAN_POINT ( 'NONE',  ( 5.514970785353741078, 0.004532877335078317783, -0.001326349372336594603 ) ) ;
#61625=AXIS2_PLACEMENT_3D ( 'NONE', #46439, #63602, #13083 ) ;
#61627=ORIENTED_EDGE ( 'NONE', *, *, #17547, .F. ) ;
#61628=CARTESIAN_POINT ( 'NONE',  ( 5.515539859299206427, -0.005751553894235456911, -0.001886660928063758945 ) ) ;
#61630=CARTESIAN_POINT ( 'NONE',  ( 3.031336079629839197, -7.886784934834946803, 0.4165536638494340416 ) ) ;
#61631=CARTESIAN_POINT ( 'NONE',  ( 0.2653141334712562083, -12.06772877558522516, -2.083134085643168820 ) ) ;
#61646=CARTESIAN_POINT ( 'NONE',  ( 2.440552418640498988, 7.615619946579186283, -1.142369876085246316 ) ) ;
#61657=CARTESIAN_POINT ( 'NONE',  ( 1.719304012339844867, -10.62216384465586216, 7.017415949612814785 ) ) ;
#61658=CARTESIAN_POINT ( 'NONE',  ( 2.827825597296803828, -7.528560921609593670, -4.975864478227487453 ) ) ;
#61662=VECTOR ( 'NONE', #59021, 1000.000000000000114 ) ;
#61672=EDGE_CURVE ( 'NONE', #36560, #20729, #28262, .T. ) ;
#61686=CARTESIAN_POINT ( 'NONE',  ( 2.556980015514025872, -7.190718924764563980, 2.862731173724000655 ) ) ;
#61690=CARTESIAN_POINT ( 'NONE',  ( 2.241352910868908754, 1.243507963608094347, 7.532448145350512547 ) ) ;
#61694=FACE_OUTER_BOUND ( 'NONE', #14428, .T. ) ;
#61699=AXIS2_PLACEMENT_3D ( 'NONE', #39146, #19547, #39477 ) ;
#61701=CARTESIAN_POINT ( 'NONE',  ( 5.514624014163232779, -0.002529391395135029055, 0.003278974416024975358 ) ) ;
#61713=ORIENTED_EDGE ( 'NONE', *, *, #58816, .T. ) ;
#61717=SURFACE_STYLE_FILL_AREA ( #35466 ) ;
#61726=VERTEX_POINT ( 'NONE', #34837 ) ;
#61735=EDGE_CURVE ( 'NONE', #18185, #16970, #19508, .T. ) ;
#61743=( BOUNDED_SURFACE ( )  B_SPLINE_SURFACE ( 3, 1, ( 
 ( #17220, #21887 ),
 ( #58116, #62751 ),
 ( #53464, #7909 ),
 ( #2922, #42134 ) ),
 .UNSPECIFIED., .F., .F., .F. ) 
 B_SPLINE_SURFACE_WITH_KNOTS ( ( 4, 4 ),
 ( 2, 2 ),
 ( 0.000000000000000000, 1.000000000000000000 ),
 ( 0.000000000000000000, 1.000000000000000000 ),
 .UNSPECIFIED. ) 
 GEOMETRIC_REPRESENTATION_ITEM ( )  RATIONAL_B_SPLINE_SURFACE ( (
 ( 1.000000000000000000, 1.000000000000000000),
 ( 0.9942764183789327692, 0.8450855930916580938),
 ( 0.9942764183789327692, 0.8450855930916580938),
 ( 1.000000000000000000, 1.000000000000000000) ) ) 
 REPRESENTATION_ITEM ( '' )  SURFACE ( )  );
#61744=CARTESIAN_POINT ( 'NONE',  ( 0.5547464869798262033, 12.33891836761635830, -0.3049355384529440771 ) ) ;
#61745=CARTESIAN_POINT ( 'NONE',  ( 2.507146904658100972, 4.047319006787570395, -6.577532285019726643 ) ) ;
#61755=CIRCLE ( 'NONE', #18259, 7.938172270156617749 ) ;
#61760=CARTESIAN_POINT ( 'NONE',  ( 3.152665057734040488, 0.000000000000000000, 0.000000000000000000 ) ) ;
#61762=CARTESIAN_POINT ( 'NONE',  ( 1.459561108993782996, -10.08002506399567899, -7.633517148169387312 ) ) ;
#61764=CARTESIAN_POINT ( 'NONE',  ( 5.516018279890452902, 0.006771744149385740437, 0.0002248006052446895335 ) ) ;
#61766=CARTESIAN_POINT ( 'NONE',  ( 5.515188684475870851, -0.0005703990286343194960, -0.005320786921497270075 ) ) ;
#61775=EDGE_LOOP ( 'NONE', ( #20703, #47484, #57662, #40347 ) ) ;
#61788=CARTESIAN_POINT ( 'NONE',  ( 5.514970785353741078, -0.0005190732562555385940, 0.004694330894494707501 ) ) ;
#61794=CARTESIAN_POINT ( 'NONE',  ( 2.406456491626151273, -9.571062220821335842, 4.152987573055939130 ) ) ;
#61798=EDGE_LOOP ( 'NONE', ( #5313, #15004, #16269, #61446 ) ) ;
#61799=CARTESIAN_POINT ( 'NONE',  ( 0.6511581176963334716, -10.87850887236078989, 5.898618881004756176 ) ) ;
#61804=ORIENTED_EDGE ( 'NONE', *, *, #13420, .T. ) ;
#61817=B_SPLINE_CURVE_WITH_KNOTS ( 'NONE', 3,
 ( #34514, #13267, #49818, #39831, #33548, #60117, #14538 ),
 .UNSPECIFIED., .F., .F.,
 ( 4, 3, 4 ),
 ( 0.000000000000000000, 0.001700533616330535819, 0.005002426799371335539 ),
 .UNSPECIFIED. ) ;
#61818=ORIENTED_EDGE ( 'NONE', *, *, #13278, .F. ) ;
#61819=CARTESIAN_POINT ( 'NONE',  ( 0.2648321136542730048, 11.55519783395232558, -4.054947570138777380 ) ) ;
#61822=ORIENTED_EDGE ( 'NONE', *, *, #12034, .F. ) ;
#61827=CARTESIAN_POINT ( 'NONE',  ( 2.251139882113959434, 2.728563091335249435, -7.133642337268828015 ) ) ;
#61836=CARTESIAN_POINT ( 'NONE',  ( 0.3160775863651080764, -2.365582350580143878, 12.03278055228170196 ) ) ;
#61837=CARTESIAN_POINT ( 'NONE',  ( 0.3665391374699467075, -9.237363111276712502, -8.095513416941326312 ) ) ;
#61846=CARTESIAN_POINT ( 'NONE',  ( 0.3632410797595246876, 10.76277061791640399, 5.910360611678860288 ) ) ;
#61848=DIRECTION ( 'NONE',  ( -0.3865475372811021382, -0.3335716741247135575, -0.8598319252293152859 ) ) ;
#61853=CARTESIAN_POINT ( 'NONE',  ( 2.406456491625782679, 4.662370073864249953, -9.333533259765646406 ) ) ;
#61854=CARTESIAN_POINT ( 'NONE',  ( 0.2648978790185584908, 2.256510822326303956, -12.03635331166809941 ) ) ;
#61859=EDGE_CURVE ( 'NONE', #2298, #42095, #44111, .T. ) ;
#61860=CARTESIAN_POINT ( 'NONE',  ( 0.3164563675027630696, 12.26087493884171664, -0.2404665832031822048 ) ) ;
#61863=CARTESIAN_POINT ( 'NONE',  ( 0.9232058338315058954, -4.617996777200498393, -11.58467545991558367 ) ) ;
#61864=CARTESIAN_POINT ( 'NONE',  ( 0.9232058338315058954, -11.58467545991557301, 4.617996777200534808 ) ) ;
#61866=CARTESIAN_POINT ( 'NONE',  ( 1.452237505248555660, 7.672309600508830485, -10.06489946308194483 ) ) ;
#61873=CARTESIAN_POINT ( 'NONE',  ( 2.907497136250956515, -6.617189382231103423, 4.235253383576313091 ) ) ;
#61876=EDGE_CURVE ( 'NONE', #18185, #20267, #39580, .T. ) ;
#61882=ORIENTED_EDGE ( 'NONE', *, *, #33383, .F. ) ;
#61895=CARTESIAN_POINT ( 'NONE',  ( 0.3537226245948401626, 12.13174752084888830, -1.874138792912886764 ) ) ;
#61897=CARTESIAN_POINT ( 'NONE',  ( 1.194176325881334932, 7.670099510969203394, -9.940715479868371673 ) ) ;
#61899=CARTESIAN_POINT ( 'NONE',  ( 2.241528039335009659, 4.895273998034002538, 5.858435878248524631 ) ) ;
#61906=CARTESIAN_POINT ( 'NONE',  ( 2.350038591458045723, -9.744161863086636899, -4.227970903880900799 ) ) ;
#61908=CARTESIAN_POINT ( 'NONE',  ( 0.3665391374699464300, 1.872534962004799297, 12.13918562134719181 ) ) ;
#61921=CARTESIAN_POINT ( 'NONE',  ( 5.514970785353741078, -0.004713149585127258956, -0.0003039746380524797073 ) ) ;
#61926=ORIENTED_EDGE ( 'NONE', *, *, #14702, .T. ) ;
#61932=VECTOR ( 'NONE', #19278, 1000.000000000000114 ) ;
#61934=CARTESIAN_POINT ( 'NONE',  ( 3.152665057734129750, -7.102135024645910732, 3.546019893116286958 ) ) ;
#61937=( BOUNDED_SURFACE ( )  B_SPLINE_SURFACE ( 3, 1, ( 
 ( #28049, #59612 ),
 ( #64572, #49641 ),
 ( #38679, #54309 ),
 ( #48350, #38330 ) ),
 .UNSPECIFIED., .F., .F., .F. ) 
 B_SPLINE_SURFACE_WITH_KNOTS ( ( 4, 4 ),
 ( 2, 2 ),
 ( 0.000000000000000000, 1.000000000000000000 ),
 ( 0.000000000000000000, 1.000000000000000000 ),
 .UNSPECIFIED. ) 
 GEOMETRIC_REPRESENTATION_ITEM ( )  RATIONAL_B_SPLINE_SURFACE ( (
 ( 1.000000000000000000, 1.000000000000000000),
 ( 0.9942764183789327692, 0.8450855930916585379),
 ( 0.9942764183789327692, 0.8450855930916585379),
 ( 1.000000000000000000, 1.000000000000000000) ) ) 
 REPRESENTATION_ITEM ( '' )  SURFACE ( )  );
#61939=B_SPLINE_CURVE_WITH_KNOTS ( 'NONE', 3,
 ( #59764, #54784, #59125, #54115, #48174, #2627, #63420, #28199, #13535, #33816 ),
 .UNSPECIFIED., .F., .F.,
 ( 4, 3, 3, 4 ),
 ( 1.226634733346699349E-18, 6.607638129004547159E-05, 9.911389841680564271E-05, 0.0001667630577588624196 ),
 .UNSPECIFIED. ) ;
#61940=EDGE_CURVE ( 'NONE', #56624, #37857, #32478, .T. ) ;
#61956=CARTESIAN_POINT ( 'NONE',  ( 5.520433897694421610, 0.01432141647227063407, -0.004666464468078087950 ) ) ;
#61960=EDGE_LOOP ( 'NONE', ( #22323, #15281, #47231, #34889 ) ) ;
#61966=ORIENTED_EDGE ( 'NONE', *, *, #15464, .F. ) ;
#61972=DIRECTION ( 'NONE',  ( 0.3939253465568944290, 0.9068155327749443106, -0.1500280335741446258 ) ) ;
#61975=CARTESIAN_POINT ( 'NONE',  ( 2.177405672430977379, 9.343720763426027531, -6.173731551724596756 ) ) ;
#61992=CARTESIAN_POINT ( 'NONE',  ( 1.633930747250582849, 8.702439996574263148, 9.253127167384969098 ) ) ;
#61994=CARTESIAN_POINT ( 'NONE',  ( 0.2834382757448007384, -12.02923522794683642, 2.326926314863269951 ) ) ;
#62004=CARTESIAN_POINT ( 'NONE',  ( 2.241352910868908310, 1.407733736974867034, 7.503490710578237355 ) ) ;
#62006=CARTESIAN_POINT ( 'NONE',  ( 2.241352910868908310, -7.145045428366559648, -2.689314586382423045 ) ) ;
#62007=CARTESIAN_POINT ( 'NONE',  ( 5.536195898058073439, 0.008411485181668783978, -0.001224473329857621697 ) ) ;
#62010=B_SPLINE_CURVE_WITH_KNOTS ( 'NONE', 3,
 ( #956, #25237, #641, #20899, #61148, #40869, #5973, #25564, #1300, #30544, #50847, #45509, #45859, #35540, #10264, #21225 ),
 .UNSPECIFIED., .F., .F.,
 ( 4, 3, 3, 3, 3, 4 ),
 ( 0.000000000000000000, 0.0002999043160757210776, 0.0005998071753050730282, 0.0008997092107374146620, 0.001204458948194614670, 0.001510329163474479104 ),
 .UNSPECIFIED. ) ;
#62026=CIRCLE ( 'NONE', #21695, 4.000000000000000000 ) ;
#62032=EDGE_CURVE ( 'NONE', #8001, #65794, #58107, .T. ) ;
#62038=CARTESIAN_POINT ( 'NONE',  ( 1.014383007554949589, -12.37541872618880667, -1.731118468094042351 ) ) ;
#62041=CARTESIAN_POINT ( 'NONE',  ( 2.653899356900181417, 6.857477569908602355, 3.657605971842781134 ) ) ;
#62059=CARTESIAN_POINT ( 'NONE',  ( 0.2915757698887314064, 11.44067056871814714, -4.392559307431786131 ) ) ;
#62063=EDGE_LOOP ( 'NONE', ( #6150, #300, #19486, #4765 ) ) ;
#62066=CARTESIAN_POINT ( 'NONE',  ( 1.937114397841932290, -10.38782037574621597, 7.538912286488311132 ) ) ;
#62069=ORIENTED_EDGE ( 'NONE', *, *, #63306, .T. ) ;
#62072=CARTESIAN_POINT ( 'NONE',  ( 0.2655924914740778742, 11.49267051747974122, -4.229867354073444830 ) ) ;
#62075=B_SPLINE_CURVE_WITH_KNOTS ( 'NONE', 3,
 ( #2778, #32985, #22359, #7389, #6765, #27038, #1776 ),
 .UNSPECIFIED., .F., .F.,
 ( 4, 3, 4 ),
 ( 1.013772664892015885E-14, 0.002398160485434997630, 0.005002426799387000092 ),
 .UNSPECIFIED. ) ;
#62077=CARTESIAN_POINT ( 'NONE',  ( 2.717984159219562379, 7.620583877640641823, -1.631703089060060119 ) ) ;
#62084=CARTESIAN_POINT ( 'NONE',  ( 2.639814597422739606, -7.689608172406200204, 1.095525832903460506 ) ) ;
#62085=CARTESIAN_POINT ( 'NONE',  ( 2.268878695253354394, 7.500319319173578414, 1.472930498387300613 ) ) ;
#62094=CARTESIAN_POINT ( 'NONE',  ( 2.653899356899724893, -2.902068786425232805, -7.209790345489500929 ) ) ;
#62101=CARTESIAN_POINT ( 'NONE',  ( 2.241352910868908310, 1.407733736974966288, -7.503490710578218703 ) ) ;
#62105=CARTESIAN_POINT ( 'NONE',  ( 2.247206125382836817, 4.819320926502623337, 5.923516414428621424 ) ) ;
#62106=CARTESIAN_POINT ( 'NONE',  ( 0.2653519890538383330, -0.02202471025202958066, -12.24619734961521544 ) ) ;
#62108=CARTESIAN_POINT ( 'NONE',  ( 0.3665391374699472626, 9.576575648339021640, 7.691255657244324695 ) ) ;
#62117=ORIENTED_EDGE ( 'NONE', *, *, #38799, .F. ) ;
#62120=CARTESIAN_POINT ( 'NONE',  ( 3.152665057735335452, -7.719888720907720270, 1.848755561853250295 ) ) ;
#62123=ADVANCED_FACE ( 'NONE', ( #55060 ), #54763, .F. ) ;
#62131=LINE ( 'NONE', #27205, #37330 ) ;
#62132=CARTESIAN_POINT ( 'NONE',  ( 2.177405672431695027, -10.27382588316267231, 4.457418613956002140 ) ) ;
#62133=CARTESIAN_POINT ( 'NONE',  ( 1.020182472823639053, -7.686484208904866833, -9.854645283130558653 ) ) ;
#62135=CARTESIAN_POINT ( 'NONE',  ( 0.7446945582541437680, 12.27434006248903664, -1.802628359587088891 ) ) ;
#62141=CARTESIAN_POINT ( 'NONE',  ( 0.8375941296819096049, 8.285008510335908127, -9.275620596396473516 ) ) ;
#62146=( BOUNDED_SURFACE ( )  B_SPLINE_SURFACE ( 3, 1, ( 
 ( #30240, #25242 ),
 ( #21908, #38156 ),
 ( #2634, #58467 ),
 ( #6289, #52171 ) ),
 .UNSPECIFIED., .F., .F., .F. ) 
 B_SPLINE_SURFACE_WITH_KNOTS ( ( 4, 4 ),
 ( 2, 2 ),
 ( 0.000000000000000000, 1.000000000000000000 ),
 ( 0.000000000000000000, 1.000000000000000000 ),
 .UNSPECIFIED. ) 
 GEOMETRIC_REPRESENTATION_ITEM ( )  RATIONAL_B_SPLINE_SURFACE ( (
 ( 1.000000000000000000, 1.000000000000000000),
 ( 0.9856612449720755231, 0.9999558406602322425),
 ( 0.9856612449720755231, 0.9999558406602322425),
 ( 1.000000000000000000, 1.000000000000000000) ) ) 
 REPRESENTATION_ITEM ( '' )  SURFACE ( )  );
#62147=LINE ( 'NONE', #16600, #62610 ) ;
#62148=VERTEX_POINT ( 'NONE', #4203 ) ;
#62158=CARTESIAN_POINT ( 'NONE',  ( 2.290907136832905255, 5.041121061899806577, -5.755317856506234619 ) ) ;
#62162=ADVANCED_FACE ( 'NONE', ( #55393 ), #51849, .F. ) ;
#62174=CARTESIAN_POINT ( 'NONE',  ( 2.440552418640495436, -7.698292014589408261, -0.1974238147510066488 ) ) ;
#62175=ORIENTED_EDGE ( 'NONE', *, *, #23920, .F. ) ;
#62179=CARTESIAN_POINT ( 'NONE',  ( 0.3675815128205894289, 10.76447900494940235, 5.910255304480483751 ) ) ;
#62183=CARTESIAN_POINT ( 'NONE',  ( 3.152665057735747567, 7.886634106564638813, 0.9030954876722160352 ) ) ;
#62186=CARTESIAN_POINT ( 'NONE',  ( 0.3401186441510221092, 2.382124782498519000, -12.03768714635922166 ) ) ;
#62191=CARTESIAN_POINT ( 'NONE',  ( 2.241537034860906275, 2.606707005150542766, 7.175668896091105253 ) ) ;
#62192=CARTESIAN_POINT ( 'NONE',  ( 1.634816307077033404, -5.718391684265862196, -11.34285134320889377 ) ) ;
#62203=EDGE_LOOP ( 'NONE', ( #31759, #19822, #24948, #9620 ) ) ;
#62207=ORIENTED_EDGE ( 'NONE', *, *, #7002, .T. ) ;
#62211=EDGE_LOOP ( 'NONE', ( #40658, #61271, #65787, #49668 ) ) ;
#62213=CARTESIAN_POINT ( 'NONE',  ( 0.2653519890518175051, 11.50765826381083201, -4.188454465438567809 ) ) ;
#62219=EDGE_CURVE ( 'NONE', #35774, #56983, #46466, .T. ) ;
#62221=CARTESIAN_POINT ( 'NONE',  ( 0.8320506296491566589, 7.696193170530746031, -9.767350172724349022 ) ) ;
#62227=CARTESIAN_POINT ( 'NONE',  ( 2.241537034860906275, -6.614004440763070924, 3.813147095850959900 ) ) ;
#62230=FACE_OUTER_BOUND ( 'NONE', #26541, .T. ) ;
#62234=ORIENTED_EDGE ( 'NONE', *, *, #64047, .F. ) ;
#62236=ADVANCED_FACE ( 'NONE', ( #36069 ), #27174, .F. ) ;
#62240=CARTESIAN_POINT ( 'NONE',  ( 0.2648978790185593790, 4.312320170909392125, -11.46165506714223703 ) ) ;
#62254=CARTESIAN_POINT ( 'NONE',  ( 0.2872850955227765346, -4.386654201695071364, -11.44140577127596892 ) ) ;
#62260=CARTESIAN_POINT ( 'NONE',  ( 2.251152103363644574, -5.769488058190768598, 5.004701566805206170 ) ) ;
#62266=ORIENTED_EDGE ( 'NONE', *, *, #4130, .F. ) ;
#62267=CARTESIAN_POINT ( 'NONE',  ( 1.452237505248555660, 2.778494755359055546, 12.34692280296792788 ) ) ;
#62268=CARTESIAN_POINT ( 'NONE',  ( 1.198791140420721657, -9.279671759317723811, -8.460175745279153503 ) ) ;
#62270=CARTESIAN_POINT ( 'NONE',  ( 2.241311220309654129, 6.564680916077612949, 3.897297589552382480 ) ) ;
#62276=CARTESIAN_POINT ( 'NONE',  ( 2.288423627607477862, -7.131972212895026253, 2.767471693622772566 ) ) ;
#62279=DIRECTION ( 'NONE',  ( 0.000000000000000000, 0.000000000000000000, 1.000000000000000000 ) ) ;
#62280=CARTESIAN_POINT ( 'NONE',  ( 0.7446945582524583385, -11.53120448859782599, -4.576048078259130847 ) ) ;
#62282=CARTESIAN_POINT ( 'NONE',  ( 0.8320506296491575471, -0.3827056590415959247, -12.42924193558400603 ) ) ;
#62283=EDGE_LOOP ( 'NONE', ( #26629, #40114, #12358, #57981 ) ) ;
#62287=CARTESIAN_POINT ( 'NONE',  ( 0.2650492433740065934, -12.07870441534855210, -2.017984765249196677 ) ) ;
#62288=EDGE_LOOP ( 'NONE', ( #1824, #55030, #3425, #17703 ) ) ;
#62297=CARTESIAN_POINT ( 'NONE',  ( 1.634816307075114272, -5.013416918607946471, 11.67158647524045811 ) ) ;
#62299=CARTESIAN_POINT ( 'NONE',  ( 1.547277799337564597, 8.651049845883598266, 9.261681528764491134 ) ) ;
#62301=CARTESIAN_POINT ( 'NONE',  ( 0.3665391374699472626, 12.04754782681760794, -2.392238720110336558 ) ) ;
#62302=B_SPLINE_CURVE_WITH_KNOTS ( 'NONE', 3,
 ( #20330, #45945, #10672, #14663, #19700, #10036, #59934, #44598, #39959, #15002, #46, #14357, #55253, #25322, #30959, #49944 ),
 .UNSPECIFIED., .F., .F.,
 ( 4, 3, 3, 3, 3, 4 ),
 ( 0.000000000000000000, 0.0002176109881720252981, 0.0004352086762394631603, 0.0006528017811446922784, 0.0007615147961451762884, 0.0009453342004947409664 ),
 .UNSPECIFIED. ) ;
#62303=CARTESIAN_POINT ( 'NONE',  ( 0.2638984909335716500, -11.57533005135181803, 4.001111175853703017 ) ) ;
#62312=CARTESIAN_POINT ( 'NONE',  ( 1.283627346226612564, -10.61381050043334717, 6.763590725840863627 ) ) ;
#62321=( BOUNDED_SURFACE ( )  B_SPLINE_SURFACE ( 3, 1, ( 
 ( #4280, #24552 ),
 ( #39845, #9913 ),
 ( #48745, #34421 ),
 ( #4168, #34077 ) ),
 .UNSPECIFIED., .F., .F., .F. ) 
 B_SPLINE_SURFACE_WITH_KNOTS ( ( 4, 4 ),
 ( 2, 2 ),
 ( 0.000000000000000000, 1.000000000000000000 ),
 ( 0.000000000000000000, 1.000000000000000000 ),
 .UNSPECIFIED. ) 
 GEOMETRIC_REPRESENTATION_ITEM ( )  RATIONAL_B_SPLINE_SURFACE ( (
 ( 1.000000000000000000, 1.000000000000000000),
 ( 0.9856612449720755231, 0.9999558406602322425),
 ( 0.9856612449720755231, 0.9999558406602322425),
 ( 1.000000000000000000, 1.000000000000000000) ) ) 
 REPRESENTATION_ITEM ( '' )  SURFACE ( )  );
#62324=FACE_OUTER_BOUND ( 'NONE', #32777, .T. ) ;
#62327=CARTESIAN_POINT ( 'NONE',  ( 20.00005080000000035, 5.400000000000000355, 1.000000000000000000 ) ) ;
#62329=PLANE ( 'NONE',  #62846 ) ;
#62333=CARTESIAN_POINT ( 'NONE',  ( 0.2646305136544065406, -12.24595685781654630, 0.1321451301297427439 ) ) ;
#62343=CARTESIAN_POINT ( 'NONE',  ( 1.283627346226765997, -12.47820286973617598, -1.641214790177956351 ) ) ;
#62344=ORIENTED_EDGE ( 'NONE', *, *, #59679, .T. ) ;
#62345=CARTESIAN_POINT ( 'NONE',  ( 0.2648978790185619880, 2.256510822326142751, 12.03635331166812783 ) ) ;
#62349=ORIENTED_EDGE ( 'NONE', *, *, #47230, .T. ) ;
#62358=CARTESIAN_POINT ( 'NONE',  ( 0.3160775863651087980, 5.922381034681598599, 10.73821170199157748 ) ) ;
#62359=FACE_OUTER_BOUND ( 'NONE', #26698, .T. ) ;
#62368=LINE ( 'NONE', #42399, #25814 ) ;
#62370=ORIENTED_EDGE ( 'NONE', *, *, #56521, .T. ) ;
#62372=CARTESIAN_POINT ( 'NONE',  ( 1.633930747250948334, -3.662223193116080466, 12.16309769563573084 ) ) ;
#62374=VERTEX_POINT ( 'NONE', #2840 ) ;
#62386=ADVANCED_FACE ( 'NONE', ( #48705 ), #36497, .F. ) ;
#62396=CARTESIAN_POINT ( 'NONE',  ( 5.536195898058073439, -0.004027525919832901369, 0.007485416011288145710 ) ) ;
#62404=CARTESIAN_POINT ( 'NONE',  ( 2.241352910868908310, 4.843133558968128582, 5.901537464758471074 ) ) ;
#62407=CARTESIAN_POINT ( 'NONE',  ( 2.899286259009674183, 2.348384892629369336, 7.494390643303780131 ) ) ;
#62413=CARTESIAN_POINT ( 'NONE',  ( 0.2657645697724684286, 6.253766234004070945, -10.52916014490824814 ) ) ;
#62423=DIRECTION ( 'NONE',  ( 0.000000000000000000, 0.000000000000000000, 1.000000000000000000 ) ) ;
#62438=CARTESIAN_POINT ( 'NONE',  ( 2.241352910868909643, -1.243507963608144751, 7.532448145350502777 ) ) ;
#62439=CARTESIAN_POINT ( 'NONE',  ( 3.152665057734040488, 0.000000000000000000, 0.000000000000000000 ) ) ;
#62443=CARTESIAN_POINT ( 'NONE',  ( 2.665405856346791502, -6.580881457836760262, 6.944580094494306799 ) ) ;
#62444=ORIENTED_EDGE ( 'NONE', *, *, #1091, .T. ) ;
#62448=CARTESIAN_POINT ( 'NONE',  ( 1.109979610372777925, 8.414317452283274434, -9.281420052101090334 ) ) ;
#62455=EDGE_LOOP ( 'NONE', ( #5591, #5071, #46098, #44449 ) ) ;
#62456=VERTEX_POINT ( 'NONE', #29078 ) ;
#62458=ORIENTED_EDGE ( 'NONE', *, *, #48774, .T. ) ;
#62459=ORIENTED_EDGE ( 'NONE', *, *, #14959, .F. ) ;
#62467=FACE_OUTER_BOUND ( 'NONE', #17815, .T. ) ;
#62478=CARTESIAN_POINT ( 'NONE',  ( 0.3057689695767498161, -8.055876362038281613, -9.241339546505164648 ) ) ;
#62480=CARTESIAN_POINT ( 'NONE',  ( 3.100650473569751320, -7.907988569972081550, -0.4517506188708853010 ) ) ;
#62482=ORIENTED_EDGE ( 'NONE', *, *, #52571, .F. ) ;
#62486=FACE_OUTER_BOUND ( 'NONE', #41407, .T. ) ;
#62488=CARTESIAN_POINT ( 'NONE',  ( 1.719304012341537957, 12.20344780066137602, -3.626341562669237906 ) ) ;
#62489=CARTESIAN_POINT ( 'NONE',  ( 2.655192694323502245, 5.716669423975853093, -7.714239566601391651 ) ) ;
#62490=CARTESIAN_POINT ( 'NONE',  ( 2.258463476536644254, -6.683417898966903969, 3.701774005560837466 ) ) ;
#62501=B_SPLINE_CURVE_WITH_KNOTS ( 'NONE', 3,
 ( #26165, #5568, #14836, #46127, #4908, #41102, #35777, #60750, #61078, #15190, #29817, #56413, #10859, #35122, #50462, #25839, #10199, #576, #9526 ),
 .UNSPECIFIED., .F., .F.,
 ( 4, 3, 3, 3, 3, 3, 4 ),
 ( 7.714043218345438553E-18, 4.457896483015216620E-05, 6.639290541542676644E-05, 8.820687556479619128E-05, 0.0001100173248779016537, 0.0001545671401658254380, 0.0001830328308068593899 ),
 .UNSPECIFIED. ) ;
#62503=CARTESIAN_POINT ( 'NONE',  ( 2.941278708680199916, -5.248410529370202582, -3.185832147968502781 ) ) ;
#62504=CARTESIAN_POINT ( 'NONE',  ( 1.198791140419927403, -5.826488554585672830, -11.12379938352737341 ) ) ;
#62506=EDGE_CURVE ( 'NONE', #52387, #5064, #19091, .T. ) ;
#62511=( BOUNDED_SURFACE ( )  B_SPLINE_SURFACE ( 3, 1, ( 
 ( #5714, #29630 ),
 ( #49937, #1701 ),
 ( #47899, #2013 ),
 ( #42545, #56568 ) ),
 .UNSPECIFIED., .F., .F., .F. ) 
 B_SPLINE_SURFACE_WITH_KNOTS ( ( 4, 4 ),
 ( 2, 2 ),
 ( 0.000000000000000000, 1.000000000000000000 ),
 ( 0.000000000000000000, 1.000000000000000000 ),
 .UNSPECIFIED. ) 
 GEOMETRIC_REPRESENTATION_ITEM ( )  RATIONAL_B_SPLINE_SURFACE ( (
 ( 1.000000000000000000, 1.000000000000000000),
 ( 0.9942764183789327692, 0.8450855930916580938),
 ( 0.9942764183789327692, 0.8450855930916580938),
 ( 1.000000000000000000, 1.000000000000000000) ) ) 
 REPRESENTATION_ITEM ( '' )  SURFACE ( )  );
#62515=CARTESIAN_POINT ( 'NONE',  ( 0.3164563675027642353, -1.892265234253194706, 12.11636128244743205 ) ) ;
#62520=VERTEX_POINT ( 'NONE', #16711 ) ;
#62526=ORIENTED_EDGE ( 'NONE', *, *, #58816, .F. ) ;
#62529=CARTESIAN_POINT ( 'NONE',  ( 2.268878695254623601, 7.130600918714364411, 2.752970156155734038 ) ) ;
#62530=VERTEX_POINT ( 'NONE', #60973 ) ;
#62541=FACE_OUTER_BOUND ( 'NONE', #19284, .T. ) ;
#62546=CARTESIAN_POINT ( 'NONE',  ( 1.452237505248555660, -1.611965288198815127, 12.55261342181974982 ) ) ;
#62551=CARTESIAN_POINT ( 'NONE',  ( 0.2650492594609241137, -9.309909082761093302, -7.955687020697146394 ) ) ;
#62555=CARTESIAN_POINT ( 'NONE',  ( 1.452237505248555660, -7.672309600508763872, 10.06489946308199634 ) ) ;
#62558=CARTESIAN_POINT ( 'NONE',  ( 2.177405672431943273, -10.73538068360496922, -3.189307221897523803 ) ) ;
#62563=ORIENTED_EDGE ( 'NONE', *, *, #64329, .F. ) ;
#62571=CARTESIAN_POINT ( 'NONE',  ( 3.152665057735716037, -2.258875078500806044, 7.609997527621833235 ) ) ;
#62575=CARTESIAN_POINT ( 'NONE',  ( 1.372161826076013780, 4.864129100816595219, 11.63973780005242453 ) ) ;
#62580=CARTESIAN_POINT ( 'NONE',  ( 5.514624014163232779, -0.003668383633201705799, -0.001921576324372078603 ) ) ;
#62584=CARTESIAN_POINT ( 'NONE',  ( 0.9232058338315058954, 2.536181247095365077, 12.21058493388774302 ) ) ;
#62588=CARTESIAN_POINT ( 'NONE',  ( 2.242819959140783137, 6.560218843829382251, 3.905785747114707718 ) ) ;
#62596=EDGE_CURVE ( 'NONE', #7749, #44332, #14641, .T. ) ;
#62602=CARTESIAN_POINT ( 'NONE',  ( 0.3057689695767464300, -7.702054583838531698, 9.538231270095076653 ) ) ;
#62604=CARTESIAN_POINT ( 'NONE',  ( 2.430348790457650399, -7.694949746373904276, 0.1949172018040290222 ) ) ;
#62606=ORIENTED_EDGE ( 'NONE', *, *, #42882, .T. ) ;
#62608=ORIENTED_EDGE ( 'NONE', *, *, #47808, .F. ) ;
#62610=VECTOR ( 'NONE', #36871, 1000.000000000000114 ) ;
#62621=CARTESIAN_POINT ( 'NONE',  ( 2.705197763288545332, 7.617149697727742641, 1.627208841526486038 ) ) ;
#62623=B_SPLINE_CURVE_WITH_KNOTS ( 'NONE', 3,
 ( #65469, #19933, #36542, #56849, #14919, #29906, #55516 ),
 .UNSPECIFIED., .F., .F.,
 ( 4, 3, 4 ),
 ( 0.000000000000000000, 0.001700533616330574633, 0.005002426799371369366 ),
 .UNSPECIFIED. ) ;
#62626=CARTESIAN_POINT ( 'NONE',  ( 1.194176325881343592, -10.60746084433560199, 6.717888447700793186 ) ) ;
#62627=CARTESIAN_POINT ( 'NONE',  ( 3.152665057734125309, -6.622010822086626725, -4.377619405892440696 ) ) ;
#62630=EDGE_CURVE ( 'NONE', #56943, #21481, #23389, .T. ) ;
#62648=EDGE_LOOP ( 'NONE', ( #29196, #44284, #32653, #15067 ) ) ;
#62650=CARTESIAN_POINT ( 'NONE',  ( 0.3537226245948370540, -1.874138792912929619, -12.13174752084888119 ) ) ;
#62654=EDGE_CURVE ( 'NONE', #8110, #5463, #24913, .T. ) ;
#62659=CARTESIAN_POINT ( 'NONE',  ( 2.241352910868908310, -0.08337961031698915004, -7.633946224498474820 ) ) ;
#62664=VERTEX_POINT ( 'NONE', #47971 ) ;
#62665=CARTESIAN_POINT ( 'NONE',  ( 2.903928887688247418, -6.365315087929495519, 6.032681461746848939 ) ) ;
#62676=ORIENTED_EDGE ( 'NONE', *, *, #13121, .F. ) ;
#62681=CARTESIAN_POINT ( 'NONE',  ( 2.889800649504073782, 5.728825117897737407, -2.156828754871411125 ) ) ;
#62688=EDGE_LOOP ( 'NONE', ( #34061, #45287, #30802, #28766 ) ) ;
#62691=B_SPLINE_CURVE_WITH_KNOTS ( 'NONE', 3,
 ( #57445, #62106, #47473, #11550, #1604, #63389, #17205 ),
 .UNSPECIFIED., .F., .F.,
 ( 4, 3, 4 ),
 ( 0.0001321430428585257952, 0.0001982171734706201550, 0.0002642860854759486087 ),
 .UNSPECIFIED. ) ;
#62704=CARTESIAN_POINT ( 'NONE',  ( 2.241352910868908754, -7.202080440908725123, -2.532612177304514933 ) ) ;
#62708=CARTESIAN_POINT ( 'NONE',  ( 5.515188684475870851, 0.004804816249378827432, -0.002355816063606946259 ) ) ;
#62713=CARTESIAN_POINT ( 'NONE',  ( 3.100650473569745547, -7.866294126167263201, 0.9283202922944633340 ) ) ;
#62717=DIRECTION ( 'NONE',  ( 0.000000000000000000, 0.000000000000000000, 1.000000000000000000 ) ) ;
#62718=ORIENTED_EDGE ( 'NONE', *, *, #23367, .F. ) ;
#62722=CARTESIAN_POINT ( 'NONE',  ( 2.491965175173876723, -2.837956678388268816, -7.177226758613644897 ) ) ;
#62724=B_SPLINE_CURVE_WITH_KNOTS ( 'NONE', 3,
 ( #57764, #26826, #7188, #21520, #16841, #37788, #51784, #56790, #17178, #6557, #1580, #52447, #47127, #6885, #1890, #47768 ),
 .UNSPECIFIED., .F., .F.,
 ( 4, 3, 3, 3, 3, 4 ),
 ( 0.000000000000000000, 0.0003017745587525228618, 0.0006035491769808714636, 0.0009053241094668154892, 0.001207275924539020053, 0.001510325902531028941 ),
 .UNSPECIFIED. ) ;
#62731=CARTESIAN_POINT ( 'NONE',  ( 5.514624014163232779, -0.004104370840204392586, -0.0005510299962881638107 ) ) ;
#62734=CARTESIAN_POINT ( 'NONE',  ( 0.2958664285830439056, 7.708042451272294926, -9.529149585189859550 ) ) ;
#62736=CARTESIAN_POINT ( 'NONE',  ( 0.7400311444011723472, -9.726551103566755785, -7.698344902199187878 ) ) ;
#62742=CARTESIAN_POINT ( 'NONE',  ( 2.781367136452695288, -1.052455537429601851, 7.743208838465638344 ) ) ;
#62751=CARTESIAN_POINT ( 'NONE',  ( 0.2638984909335716500, 6.295352574289132974, -10.50550771760513591 ) ) ;
#62757=CARTESIAN_POINT ( 'NONE',  ( 1.375507693217066008, 12.60244951981694150, 0.5913006932453851450 ) ) ;
#62762=CARTESIAN_POINT ( 'NONE',  ( 0.2759803524722201917, 1.940323823244660906, 12.09509972435082403 ) ) ;
#62772=CARTESIAN_POINT ( 'NONE',  ( 2.297017764050092392, 7.563558677601596614, 1.166330442180198768 ) ) ;
#62784=VERTEX_POINT ( 'NONE', #60546 ) ;
#62787=CARTESIAN_POINT ( 'NONE',  ( 2.288423627607777622, -5.039850887180386430, -5.755330594805019295 ) ) ;
#62790=CARTESIAN_POINT ( 'NONE',  ( 0.3040950598368152291, -2.376091969481135546, -12.02925914197707513 ) ) ;
#62797=CARTESIAN_POINT ( 'NONE',  ( 0.2958664285830405749, 4.398464391600323431, 11.43993536884558893 ) ) ;
#62802=CARTESIAN_POINT ( 'NONE',  ( 0.2657645697724685396, 7.987126944299760112, -9.283243433322994065 ) ) ;
#62803=CARTESIAN_POINT ( 'NONE',  ( 2.889800649504073782, -6.039722463373532690, -0.9965440656174344713 ) ) ;
#62807=ORIENTED_EDGE ( 'NONE', *, *, #2863, .T. ) ;
#62809=CARTESIAN_POINT ( 'NONE',  ( 2.835339799623868284, 4.778327228934593052, 6.206025468804318379 ) ) ;
#62811=DIRECTION ( 'NONE',  ( -1.000000000000000000, -0.000000000000000000, -0.000000000000000000 ) ) ;
#62821=CARTESIAN_POINT ( 'NONE',  ( 2.406456491626458583, 4.152987573055560766, 9.571062220820376609 ) ) ;
#62822=CARTESIAN_POINT ( 'NONE',  ( 0.2833330754217383007, -0.2021515668286508749, 12.25052326018167648 ) ) ;
#62823=CARTESIAN_POINT ( 'NONE',  ( 2.373367633546870969, 5.996611082972032492, -4.795703124519829608 ) ) ;
#62827=CARTESIAN_POINT ( 'NONE',  ( 2.284126774967659923, -6.701756155761970923, 3.686252397487106425 ) ) ;
#62831=DIRECTION ( 'NONE',  ( -1.000000000000000000, -0.000000000000000000, -0.000000000000000000 ) ) ;
#62836=CIRCLE ( 'NONE', #18235, 12.73084802173761787 ) ;
#62840=DIRECTION ( 'NONE',  ( -0.3939253465568944290, -0.3052156353794380217, 0.8669868725995547587 ) ) ;
#62841=CARTESIAN_POINT ( 'NONE',  ( 0.6511581176968139761, -5.898618881004688674, -10.87850887236101372 ) ) ;
#62844=VECTOR ( 'NONE', #39204, 1000.000000000000000 ) ;
#62846=AXIS2_PLACEMENT_3D ( 'NONE', #16782, #44032, #58024 ) ;
#62852=CARTESIAN_POINT ( 'NONE',  ( 1.104777566491154550, -7.679758239385205520, 9.895624035730048007 ) ) ;
#62859=CARTESIAN_POINT ( 'NONE',  ( 2.770579946183334474, 7.804957730865694110, 0.3031629740256017724 ) ) ;
#62864=CARTESIAN_POINT ( 'NONE',  ( 2.034671305879989678, -10.44529075078586722, 5.218565780488946260 ) ) ;
#62865=ORIENTED_EDGE ( 'NONE', *, *, #58730, .F. ) ;
#62866=CARTESIAN_POINT ( 'NONE',  ( 0.2652384770603677389, 11.53005438969049834, -4.126289928142288232 ) ) ;
#62887=CARTESIAN_POINT ( 'NONE',  ( 1.719304012340734378, -7.581471372739226666, -10.22720798541506682 ) ) ;
#62888=CARTESIAN_POINT ( 'NONE',  ( 2.257661810674659097, 6.682681612746527833, 3.702552158177466968 ) ) ;
#62889=VERTEX_POINT ( 'NONE', #46909 ) ;
#62891=CARTESIAN_POINT ( 'NONE',  ( 0.3109076770649020771, 12.03190317807027476, -2.361108455562717978 ) ) ;
#62892=CARTESIAN_POINT ( 'NONE',  ( 0.2647959493198558945, -2.271080632827979784, -12.03358727341676726 ) ) ;
#62907=ORIENTED_EDGE ( 'NONE', *, *, #30011, .T. ) ;
#62911=CARTESIAN_POINT ( 'NONE',  ( 2.931247277082682956, -7.672001188570249930, -1.728824746592349193 ) ) ;
#62918=CARTESIAN_POINT ( 'NONE',  ( 2.573738926104379487, 5.156412073069364332, -5.779258037546964211 ) ) ;
#62921=EDGE_CURVE ( 'NONE', #60300, #11928, #25303, .T. ) ;
#62943=CARTESIAN_POINT ( 'NONE',  ( 3.152665057733834431, -3.161213418913157991, 7.281573230474281289 ) ) ;
#62958=CARTESIAN_POINT ( 'NONE',  ( 2.241449424704146320, -4.954182807723299220, -5.808712090826661623 ) ) ;
#62961=CARTESIAN_POINT ( 'NONE',  ( 0.4613984246114876120, 8.128335150814509191, 9.246873830555923490 ) ) ;
#62968=VERTEX_POINT ( 'NONE', #20661 ) ;
#62971=EDGE_LOOP ( 'NONE', ( #62807, #43905, #20349, #16882 ) ) ;
#62977=DIRECTION ( 'NONE',  ( 0.3865475372811021382, -0.1410344188397403553, -0.9114221272958275000 ) ) ;
#62980=AXIS2_PLACEMENT_3D ( 'NONE', #27947, #48259, #2706 ) ;
#62981=EDGE_CURVE ( 'NONE', #36790, #11928, #10646, .T. ) ;
#62984=CARTESIAN_POINT ( 'NONE',  ( 2.941278708680199916, -4.615461433467283214, 4.048809123187920633 ) ) ;
#62988=CARTESIAN_POINT ( 'NONE',  ( 2.305787727787084407, -4.792270232040933386, 5.970480882365206909 ) ) ;
#62991=ADVANCED_FACE ( 'NONE', ( #56564 ), #52244, .F. ) ;
#63006=CARTESIAN_POINT ( 'NONE',  ( 0.2648321136542701182, 9.289286523730419631, 7.979621084888147919 ) ) ;
#63017=ADVANCED_FACE ( 'NONE', ( #58115 ), #22519, .F. ) ;
#63018=CARTESIAN_POINT ( 'NONE',  ( 0.2671309869109527169, -4.340541005679448006, -11.45180222993658248 ) ) ;
#63019=ORIENTED_EDGE ( 'NONE', *, *, #6524, .T. ) ;
#63020=CARTESIAN_POINT ( 'NONE',  ( 0.2869720083484341155, -9.519277517057156857, 7.715523637151736835 ) ) ;
#63029=CARTESIAN_POINT ( 'NONE',  ( 0.6511581176971957818, 4.541862140119915736, -11.51117493088913157 ) ) ;
#63033=EDGE_LOOP ( 'NONE', ( #4738, #59460, #64742, #20848 ) ) ;
#63035=CARTESIAN_POINT ( 'NONE',  ( 0.9232167919969139769, -11.56588005394301177, 4.649596781010366442 ) ) ;
#63037=CARTESIAN_POINT ( 'NONE',  ( 2.524535260912860402, 1.559291270914676231, 7.569872524929055047 ) ) ;
#63038=ADVANCED_FACE ( 'NONE', ( #29166 ), #43277, .F. ) ;
#63044=ADVANCED_FACE ( 'NONE', ( #8536 ), #38636, .F. ) ;
#63045=CARTESIAN_POINT ( 'NONE',  ( 1.283627346226433596, -3.783098238613557207, 12.00363697230081605 ) ) ;
#63048=VERTEX_POINT ( 'NONE', #59409 ) ;
#63051=ORIENTED_EDGE ( 'NONE', *, *, #47973, .F. ) ;
#63053=LINE ( 'NONE', #56787, #12854 ) ;
#63061=ORIENTED_EDGE ( 'NONE', *, *, #65210, .T. ) ;
#63065=CARTESIAN_POINT ( 'NONE',  ( 0.2653519890518140634, -6.123091032184224680, 10.60552241699065590 ) ) ;
#63076=CARTESIAN_POINT ( 'NONE',  ( 0.2717059086739015417, 7.737372654246708947, -9.494961435243615355 ) ) ;
#63084=CARTESIAN_POINT ( 'NONE',  ( 0.3675815128205894289, 12.13672785388550324, 1.872154644482125763 ) ) ;
#63091=CARTESIAN_POINT ( 'NONE',  ( 0.9232058338315058954, 12.34162163148533686, 1.793035206307387330 ) ) ;
#63096=CARTESIAN_POINT ( 'NONE',  ( 0.2646305136544072623, 12.24595685781654630, -0.1321451301298267600 ) ) ;
#63098=CARTESIAN_POINT ( 'NONE',  ( 0.2801149460245134226, -11.44368419510489154, 4.374013318106511505 ) ) ;
#63101=ORIENTED_EDGE ( 'NONE', *, *, #8650, .F. ) ;
#63103=CARTESIAN_POINT ( 'NONE',  ( 1.452237505248555660, -12.64182585313126417, 0.5922625322516575919 ) ) ;
#63107=CARTESIAN_POINT ( 'NONE',  ( 2.305787727787085295, 7.249469779319941409, -2.461236246750998724 ) ) ;
#63109=CARTESIAN_POINT ( 'NONE',  ( 1.287602823387600459, -7.659913635101688989, -9.987902848014105217 ) ) ;
#63110=CARTESIAN_POINT ( 'NONE',  ( 2.259025283528084849, 7.546748801935450501, 1.191911401085038458 ) ) ;
#63111=B_SPLINE_CURVE_WITH_KNOTS ( 'NONE', 3,
 ( #12227, #27857, #8226, #47810, #2268, #22544, #63098, #17882, #38141, #58451, #12882, #33163, #28191, #38482, #48479, #2928, #58801, #13219, #60078, #55080, #23867, #9192 ),
 .UNSPECIFIED., .F., .F.,
 ( 4, 3, 3, 3, 3, 3, 3, 4 ),
 ( 1.755771606739170543E-18, 4.449119708436685694E-05, 6.626296329540286008E-05, 8.803456484962358117E-05, 0.0001098060367612769232, 0.0001315774408628471958, 0.0001760698110411115195, 0.0001829697163287824263 ),
 .UNSPECIFIED. ) ;
#63117=CARTESIAN_POINT ( 'NONE',  ( 0.5547464869798244269, -5.905377260991297561, 10.83828453080463561 ) ) ;
#63118=ORIENTED_EDGE ( 'NONE', *, *, #3500, .F. ) ;
#63120=CARTESIAN_POINT ( 'NONE',  ( 1.549075743847258435, 8.652116335902604760, -9.261503792573503091 ) ) ;
#63121=ADVANCED_FACE ( 'NONE', ( #60723 ), #65788, .F. ) ;
#63124=CARTESIAN_POINT ( 'NONE',  ( 5.516018279890452902, -0.005752102158673865970, 0.003580555109620777322 ) ) ;
#63131=EDGE_LOOP ( 'NONE', ( #42332, #31151, #12100, #22941 ) ) ;
#63139=CARTESIAN_POINT ( 'NONE',  ( 3.152665057734040488, 0.000000000000000000, 0.000000000000000000 ) ) ;
#63145=EDGE_CURVE ( 'NONE', #55082, #8885, #7459, .T. ) ;
#63148=ADVANCED_FACE ( 'NONE', ( #50434 ), #20773, .F. ) ;
#63151=CARTESIAN_POINT ( 'NONE',  ( 3.152665057736204535, -4.377619405894248139, -6.622010822085805160 ) ) ;
#63164=CARTESIAN_POINT ( 'NONE',  ( 3.100650473569755317, -4.737096019059220176, -6.348250400753952860 ) ) ;
#63167=CARTESIAN_POINT ( 'NONE',  ( 1.719304012341585475, 10.62216384465587993, -7.017415949613843296 ) ) ;
#63174=CARTESIAN_POINT ( 'NONE',  ( 2.556980015513285132, -0.2307166419793932888, -7.736177238086551000 ) ) ;
#63175=CARTESIAN_POINT ( 'NONE',  ( 2.297017764050093280, -3.968300849026712651, -6.543724852214719334 ) ) ;
#63182=CARTESIAN_POINT ( 'NONE',  ( 2.280717697723838366, -6.543326285614656790, 3.958470850374288030 ) ) ;
#63183=CARTESIAN_POINT ( 'NONE',  ( 3.047904605210340456, -3.577928268982041526, -7.047014837597050274 ) ) ;
#63188=EDGE_LOOP ( 'NONE', ( #17937, #52673, #9220, #5164 ) ) ;
#63189=EDGE_LOOP ( 'NONE', ( #49679, #63051, #8690, #16554 ) ) ;
#63192=CARTESIAN_POINT ( 'NONE',  ( 5.514624014163232779, 0.001574979445068891036, -0.003830004412313253118 ) ) ;
#63193=ORIENTED_EDGE ( 'NONE', *, *, #3351, .T. ) ;
#63195=CARTESIAN_POINT ( 'NONE',  ( 2.247206125382827935, -7.539576157880608420, 1.211896144126903163 ) ) ;
#63202=CARTESIAN_POINT ( 'NONE',  ( 0.2648321136542692855, 12.08378267055568500, -1.986804758683992755 ) ) ;
#63205=STYLED_ITEM ( 'NONE', ( #35775 ), #28612 ) ;
#63216=DIRECTION ( 'NONE',  ( -1.000000000000000000, -0.000000000000000000, -0.000000000000000000 ) ) ;
#63223=CARTESIAN_POINT ( 'NONE',  ( 0.2801149460245133671, -2.320387321174087969, -12.02936836014265864 ) ) ;
#63226=ORIENTED_EDGE ( 'NONE', *, *, #40597, .T. ) ;
#63230=ORIENTED_EDGE ( 'NONE', *, *, #25721, .T. ) ;
#63231=CARTESIAN_POINT ( 'NONE',  ( 1.948354844646893458, -11.46941405766446920, -3.407825014329160407 ) ) ;
#63240=CARTESIAN_POINT ( 'NONE',  ( 2.639814597422737830, -7.600559958731733623, -1.600543348184890080 ) ) ;
#63244=CARTESIAN_POINT ( 'NONE',  ( 2.242418902651938772, -5.783980263416061085, 4.983487297755536005 ) ) ;
#63245=CARTESIAN_POINT ( 'NONE',  ( 2.305787727787083519, 5.047606869483132641, -5.756228004061408221 ) ) ;
#63247=CARTESIAN_POINT ( 'NONE',  ( 2.262775599886255762, -0.1412024122916401558, 7.640237753423681610 ) ) ;
#63251=CARTESIAN_POINT ( 'NONE',  ( 2.941278708680199916, 6.021511413163979753, -1.198640839021246851 ) ) ;
#63252=LINE ( 'NONE', #18388, #52375 ) ;
#63254=CARTESIAN_POINT ( 'NONE',  ( 2.241506898688419458, 4.877157973187056683, -5.873558213059427047 ) ) ;
#63257=ORIENTED_EDGE ( 'NONE', *, *, #37196, .T. ) ;
#63267=VERTEX_POINT ( 'NONE', #17132 ) ;
#63268=DIRECTION ( 'NONE',  ( -1.000000000000000000, -0.000000000000000000, -0.000000000000000000 ) ) ;
#63279=CARTESIAN_POINT ( 'NONE',  ( 2.241536586108913376, 7.171901127201328663, -2.617055111126378453 ) ) ;
#63280=CARTESIAN_POINT ( 'NONE',  ( 0.3223008802179242460, 3.964361764750334860, -11.60682919296347926 ) ) ;
#63282=CARTESIAN_POINT ( 'NONE',  ( 5.536195898058073439, 0.008071068258923569036, 0.002666509901870094731 ) ) ;
#63286=CARTESIAN_POINT ( 'NONE',  ( 2.241528039335008327, -5.858435878248543283, 4.895273998033984775 ) ) ;
#63287=VERTEX_POINT ( 'NONE', #51429 ) ;
#63289=CARTESIAN_POINT ( 'NONE',  ( 0.2676618633000453218, 12.03196378632210539, 2.284744117040117040 ) ) ;
#63295=CARTESIAN_POINT ( 'NONE',  ( 0.3665391374699472626, -8.095513416941169993, -9.237363111276847505 ) ) ;
#63298=CARTESIAN_POINT ( 'NONE',  ( 2.241352910868909643, -7.532448145350499225, -1.243507963608171174 ) ) ;
#63301=( BOUNDED_SURFACE ( )  B_SPLINE_SURFACE ( 3, 1, ( 
 ( #28002, #12678 ),
 ( #17700, #38282 ),
 ( #33637, #49289 ),
 ( #3744, #13029 ) ),
 .UNSPECIFIED., .F., .F., .F. ) 
 B_SPLINE_SURFACE_WITH_KNOTS ( ( 4, 4 ),
 ( 2, 2 ),
 ( 0.000000000000000000, 1.000000000000000000 ),
 ( 0.000000000000000000, 1.000000000000000000 ),
 .UNSPECIFIED. ) 
 GEOMETRIC_REPRESENTATION_ITEM ( )  RATIONAL_B_SPLINE_SURFACE ( (
 ( 1.000000000000000000, 1.000000000000000000),
 ( 0.9856612449720755231, 0.9999558406602322425),
 ( 0.9856612449720755231, 0.9999558406602322425),
 ( 1.000000000000000000, 1.000000000000000000) ) ) 
 REPRESENTATION_ITEM ( '' )  SURFACE ( )  );
#63306=EDGE_CURVE ( 'NONE', #11115, #27117, #5766, .T. ) ;
#63309=CARTESIAN_POINT ( 'NONE',  ( 5.516018279890452902, 0.006440244342253029219, 0.002104829434640694864 ) ) ;
#63313=LINE ( 'NONE', #37059, #42908 ) ;
#63319=ADVANCED_FACE ( 'NONE', ( #48712 ), #50098, .F. ) ;
#63323=CARTESIAN_POINT ( 'NONE',  ( 2.290907136832898150, -4.792500160339676185, -5.963935563308297994 ) ) ;
#63327=CARTESIAN_POINT ( 'NONE',  ( 0.3109076770649043531, 2.361108455562842767, 12.03190317807024989 ) ) ;
#63340=CARTESIAN_POINT ( 'NONE',  ( 2.280717697723837478, -7.556934756535378384, -1.173604464351679866 ) ) ;
#63342=CARTESIAN_POINT ( 'NONE',  ( 0.4613984246114881116, 11.66278164635734882, 3.943860067443686557 ) ) ;
#63347=ADVANCED_FACE ( 'NONE', ( #48061 ), #56907, .F. ) ;
#63363=DIRECTION ( 'NONE',  ( 0.3865475372811021382, -0.9220659470476461061, -0.01937500237528736249 ) ) ;
#63366=CARTESIAN_POINT ( 'NONE',  ( 0.3053067050349136391, -10.49978800868456652, -6.328522421120378993 ) ) ;
#63374=VECTOR ( 'NONE', #60278, 1000.000000000000227 ) ;
#63379=CARTESIAN_POINT ( 'NONE',  ( 0.2653519789438738563, -11.51519617080779234, -4.167744179924032011 ) ) ;
#63386=CARTESIAN_POINT ( 'NONE',  ( 0.3610902822527232159, 7.689482111308977963, -9.572034936626812041 ) ) ;
#63387=FACE_OUTER_BOUND ( 'NONE', #33943, .T. ) ;
#63389=CARTESIAN_POINT ( 'NONE',  ( 0.2650492433740075371, -0.1101179680248120796, -12.24562113162318866 ) ) ;
#63391=CARTESIAN_POINT ( 'NONE',  ( 0.2739690278137236756, 12.09341522051409790, 1.946552041162949997 ) ) ;
#63396=CARTESIAN_POINT ( 'NONE',  ( 2.241352910868908310, -0.08337961031698915004, -7.633946224498474820 ) ) ;
#63402=CARTESIAN_POINT ( 'NONE',  ( 5.516018279890452902, -0.0002248006052448983238, -0.006771744149385263388 ) ) ;
#63407=CARTESIAN_POINT ( 'NONE',  ( 0.3675815128205894289, -8.093875121226139058, 9.235491948679980467 ) ) ;
#63409=CARTESIAN_POINT ( 'NONE',  ( 5.536195898058073439, 0.006672323185952914494, 0.005266167600748188592 ) ) ;
#63412=EDGE_CURVE ( 'NONE', #3821, #14132, #10102, .T. ) ;
#63414=CARTESIAN_POINT ( 'NONE',  ( 0.2648978790185593790, 1.996248716311628479, 12.08224454301449313 ) ) ;
#63416=FACE_OUTER_BOUND ( 'NONE', #40419, .T. ) ;
#63417=CARTESIAN_POINT ( 'NONE',  ( 0.2739690278137253965, -9.499928778897061221, -7.732471127692689628 ) ) ;
#63418=FACE_OUTER_BOUND ( 'NONE', #32977, .T. ) ;
#63420=CARTESIAN_POINT ( 'NONE',  ( 2.241528039335009215, -3.830846649711559859, 6.603755931420473679 ) ) ;
#63422=CARTESIAN_POINT ( 'NONE',  ( 2.255723233589912446, 5.766109278027927054, 5.010912740809442489 ) ) ;
#63428=VECTOR ( 'NONE', #51127, 1000.000000000000000 ) ;
#63430=CARTESIAN_POINT ( 'NONE',  ( 1.375507693220862970, 8.553661013313627492, -9.273955665125701131 ) ) ;
#63434=ORIENTED_EDGE ( 'NONE', *, *, #63977, .T. ) ;
#63435=CARTESIAN_POINT ( 'NONE',  ( 0.2958664285830411300, 5.936220506376383987, -10.72286791615082358 ) ) ;
#63436=CARTESIAN_POINT ( 'NONE',  ( 2.256373768223410625, 6.548448293197187908, -3.934258165099992155 ) ) ;
#63445=VERTEX_POINT ( 'NONE', #9763 ) ;
#63446=CARTESIAN_POINT ( 'NONE',  ( 0.3474126878361774584, 4.439989671676218386, 11.44231427242451460 ) ) ;
#63447=CARTESIAN_POINT ( 'NONE',  ( 2.241311220309522234, 4.978033760028339749, -5.788190037953302891 ) ) ;
#63449=CARTESIAN_POINT ( 'NONE',  ( 0.2706063244538048362, 8.006269958070731718, -9.268878137104316295 ) ) ;
#63451=CARTESIAN_POINT ( 'NONE',  ( 0.3109076770649005228, 11.60048803586498778, 3.971171685427437037 ) ) ;
#63452=VERTEX_POINT ( 'NONE', #30382 ) ;
#63454=CARTESIAN_POINT ( 'NONE',  ( 2.305787727787083519, 4.792270232040894307, 5.970480882365237996 ) ) ;
#63455=CARTESIAN_POINT ( 'NONE',  ( 2.260457164927710316, 3.699855525212757179, -6.685239696063914216 ) ) ;
#63458=CARTESIAN_POINT ( 'NONE',  ( 1.549075743846619391, 0.6747257554056480533, -12.65619669351077548 ) ) ;
#63460=CARTESIAN_POINT ( 'NONE',  ( 0.2801149460245140332, -11.57793225195134745, -4.005169813315220040 ) ) ;
#63461=CARTESIAN_POINT ( 'NONE',  ( 2.903928887688508098, -8.753847148605458983, 0.5297564406061141540 ) ) ;
#63469=CARTESIAN_POINT ( 'NONE',  ( 2.259830038564997423, 5.940579220577243191, -4.804964945109127861 ) ) ;
#63472=CARTESIAN_POINT ( 'NONE',  ( 2.907497136249922676, 7.791429554169492455, 1.009055026158340862 ) ) ;
#63485=EDGE_CURVE ( 'NONE', #61726, #52172, #34318, .T. ) ;
#63496=CARTESIAN_POINT ( 'NONE',  ( 1.937114397841935398, -10.38782037574611472, -7.538912286488452352 ) ) ;
#63497=ORIENTED_EDGE ( 'NONE', *, *, #10015, .F. ) ;
#63502=EDGE_CURVE ( 'NONE', #48073, #63287, #26061, .T. ) ;
#63514=ORIENTED_EDGE ( 'NONE', *, *, #34823, .F. ) ;
#63525=CARTESIAN_POINT ( 'NONE',  ( 2.241352910868908310, 2.532612177304540246, -7.202080440908716241 ) ) ;
#63539=AXIS2_PLACEMENT_3D ( 'NONE', #49204, #43515, #58863 ) ;
#63546=CARTESIAN_POINT ( 'NONE',  ( 2.241449424704146320, -1.386092121067156180, -7.507583637787362818 ) ) ;
#63547=CARTESIAN_POINT ( 'NONE',  ( 0.3218525148189836926, -9.236582760335920739, -8.069481661595439448 ) ) ;
#63549=EDGE_CURVE ( 'NONE', #62664, #33142, #12183, .T. ) ;
#63552=EDGE_CURVE ( 'NONE', #60603, #1207, #15367, .T. ) ;
#63559=ADVANCED_FACE ( 'NONE', ( #21044 ), #47564, .F. ) ;
#63560=CARTESIAN_POINT ( 'NONE',  ( 0.2648978790185584908, 7.769924372105204036, 9.465406350830633642 ) ) ;
#63569=CARTESIAN_POINT ( 'NONE',  ( 0.7446945582529739260, -9.270687147117394389, -8.243982823409684357 ) ) ;
#63570=ORIENTED_EDGE ( 'NONE', *, *, #58159, .F. ) ;
#63576=B_SPLINE_CURVE_WITH_KNOTS ( 'NONE', 3,
 ( #36214, #36564, #56522, #10967, #25265, #31252, #51558, #6003, #19953, #26259, #5005, #11293, #55540, #45543, #31562, #51865 ),
 .UNSPECIFIED., .F., .F.,
 ( 4, 3, 3, 3, 3, 4 ),
 ( 4.336808689942017736E-19, 0.0002176109881720250270, 0.0004352086762394615340, 0.0006528017811446905436, 0.0007615147961451741200, 0.0009453342004947430264 ),
 .UNSPECIFIED. ) ;
#63577=CARTESIAN_POINT ( 'NONE',  ( 0.2956976708475470006, -7.708404409946589375, -9.528782683728165281 ) ) ;
#63579=CARTESIAN_POINT ( 'NONE',  ( 2.260457164927185847, -7.131443009846823777, 2.742969430850495272 ) ) ;
#63582=CARTESIAN_POINT ( 'NONE',  ( 2.770579946183327369, 5.784075095088785368, 5.249166435139375864 ) ) ;
#63596=CARTESIAN_POINT ( 'NONE',  ( 0.2801149460245161982, -6.294737133725727851, -10.51028947658250345 ) ) ;
#63600=CARTESIAN_POINT ( 'NONE',  ( 0.2958664285830434615, 3.984029505266722726, -11.59077733151251621 ) ) ;
#63602=DIRECTION ( 'NONE',  ( -1.000000000000000000, -0.000000000000000000, -0.000000000000000000 ) ) ;
#63603=CARTESIAN_POINT ( 'NONE',  ( 0.3109076770649074062, -3.971171685427473452, 11.60048803586498245 ) ) ;
#63604=CARTESIAN_POINT ( 'NONE',  ( 0.3474126878361875059, 9.566300984424410458, 7.689340002166765053 ) ) ;
#63620=EDGE_CURVE ( 'NONE', #20463, #10376, #5460, .T. ) ;
#63623=CARTESIAN_POINT ( 'NONE',  ( 2.284126774967663920, -5.756079777200378444, -5.036818232552951358 ) ) ;
#63624=DIRECTION ( 'NONE',  ( -1.000000000000000000, -0.000000000000000000, -0.000000000000000000 ) ) ;
#63626=CARTESIAN_POINT ( 'NONE',  ( 2.241352910868908754, -4.843133558968167662, 5.901537464758438212 ) ) ;
#63642=ORIENTED_EDGE ( 'NONE', *, *, #21484, .T. ) ;
#63671=B_SPLINE_CURVE_WITH_KNOTS ( 'NONE', 3,
 ( #35829, #41484, #41831, #6923, #20579, #47172, #61137, #21890, #56132, #25897 ),
 .UNSPECIFIED., .F., .F.,
 ( 4, 3, 3, 4 ),
 ( 4.336808689942017736E-19, 6.607638129004537672E-05, 9.911389841680465337E-05, 0.0001667630577588625010 ),
 .UNSPECIFIED. ) ;
#63681=( BOUNDED_SURFACE ( )  B_SPLINE_SURFACE ( 3, 1, ( 
 ( #8515, #58771 ),
 ( #14153, #29766 ),
 ( #19153, #24807 ),
 ( #33477, #8855 ) ),
 .UNSPECIFIED., .F., .F., .F. ) 
 B_SPLINE_SURFACE_WITH_KNOTS ( ( 4, 4 ),
 ( 2, 2 ),
 ( 0.000000000000000000, 1.000000000000000000 ),
 ( 0.000000000000000000, 1.000000000000000000 ),
 .UNSPECIFIED. ) 
 GEOMETRIC_REPRESENTATION_ITEM ( )  RATIONAL_B_SPLINE_SURFACE ( (
 ( 1.000000000000000000, 1.000000000000000000),
 ( 0.6933888150995267674, 0.9895912004443193632),
 ( 0.6933888150995267674, 0.9895912004443193632),
 ( 1.000000000000000000, 1.000000000000000000) ) ) 
 REPRESENTATION_ITEM ( '' )  SURFACE ( )  );
#63683=CARTESIAN_POINT ( 'NONE',  ( 2.297017764050092836, 5.755222757172114179, -5.044319338147307263 ) ) ;
#63686=DIRECTION ( 'NONE',  ( -0.3865475372811021937, 0.7888450329201810440, -0.4778122177791956915 ) ) ;
#63695=CARTESIAN_POINT ( 'NONE',  ( 2.247206125382829711, 3.917979829727999075, -6.554642244888417402 ) ) ;
#63698=VERTEX_POINT ( 'NONE', #48637 ) ;
#63701=CARTESIAN_POINT ( 'NONE',  ( 1.719304012338833676, 3.626341562670448493, 12.20344780066006152 ) ) ;
#63709=CARTESIAN_POINT ( 'NONE',  ( 0.3164563675027635137, 7.696930404785163660, -9.546944054903010013 ) ) ;
#63710=CARTESIAN_POINT ( 'NONE',  ( 5.515539859299206427, -0.001886660928063817059, 0.005751553894235436962 ) ) ;
#63717=CARTESIAN_POINT ( 'NONE',  ( 2.653899356900444761, -1.091629880170381428, 7.694895988366584838 ) ) ;
#63730=CARTESIAN_POINT ( 'NONE',  ( 1.287602823386651441, -8.506034117234991143, 9.277923463524135883 ) ) ;
#63731=DIRECTION ( 'NONE',  ( 1.000000000000000000, -0.000000000000000000, -0.000000000000000000 ) ) ;
#63741=CARTESIAN_POINT ( 'NONE',  ( 0.2872850955227749803, -9.519656861923676772, -7.715220952083337913 ) ) ;
#63743=CARTESIAN_POINT ( 'NONE',  ( 1.372161826076970792, 3.755740169579696808, -12.04315837901310893 ) ) ;
#63745=CARTESIAN_POINT ( 'NONE',  ( 2.241317068080787234, -1.235499051333821319, 7.533758201955880196 ) ) ;
#63746=DIRECTION ( 'NONE',  ( 0.3939253465568943180, 0.1691689424289825050, -0.9034404741085547696 ) ) ;
#63747=EDGE_LOOP ( 'NONE', ( #62234, #20240, #37780, #50983 ) ) ;
#63749=PRESENTATION_STYLE_ASSIGNMENT (( #2945 ) ) ;
#63757=CARTESIAN_POINT ( 'NONE',  ( 2.280717697723833037, 6.543326285614686988, -3.958470850374239181 ) ) ;
#63761=DIRECTION ( 'NONE',  ( -1.000000000000000000, -0.000000000000000000, -0.000000000000000000 ) ) ;
#63764=ORIENTED_EDGE ( 'NONE', *, *, #7329, .F. ) ;
#63770=VECTOR ( 'NONE', #14887, 1000.000000000000114 ) ;
#63776=CARTESIAN_POINT ( 'NONE',  ( 1.719304012338398246, 7.581471372739840398, 10.22720798541364395 ) ) ;
#63785=CARTESIAN_POINT ( 'NONE',  ( 1.287602823388156237, 0.5522659225156872909, -12.57487505104594128 ) ) ;
#63788=CARTESIAN_POINT ( 'NONE',  ( 0.4626703367443177339, 5.909149965571010021, 10.80124546303551902 ) ) ;
#63793=CARTESIAN_POINT ( 'NONE',  ( 3.047904605210429274, -7.270585891216597929, -3.098478597269381130 ) ) ;
#63801=CARTESIAN_POINT ( 'NONE',  ( 2.242819959140645469, -6.662619100654771032, 3.728423299584962436 ) ) ;
#63804=CARTESIAN_POINT ( 'NONE',  ( 0.4613984246114868348, 10.51786362586223156, -6.399144685811604560 ) ) ;
#63809=ADVANCED_FACE ( 'NONE', ( #60556 ), #14349, .F. ) ;
#63815=CARTESIAN_POINT ( 'NONE',  ( 1.633930747252546833, -8.702439996575384029, -9.253127167384830543 ) ) ;
#63816=CARTESIAN_POINT ( 'NONE',  ( 2.273267844204866606, -3.952852893982251814, -6.543821324256922090 ) ) ;
#63825=CARTESIAN_POINT ( 'NONE',  ( 3.152665057734104437, -3.546019893116280741, -7.102135024645891193 ) ) ;
#63828=CARTESIAN_POINT ( 'NONE',  ( 0.2872850955227778114, 9.251080475901458655, -8.035297825011268102 ) ) ;
#63833=CARTESIAN_POINT ( 'NONE',  ( 1.719304012338199517, 0.000000000000000000, 0.000000000000000000 ) ) ;
#63837=ORIENTED_EDGE ( 'NONE', *, *, #39156, .T. ) ;
#63840=CARTESIAN_POINT ( 'NONE',  ( 2.241352910868908754, -7.532448145350516988, 1.243507963608069700 ) ) ;
#63848=CARTESIAN_POINT ( 'NONE',  ( 2.177405672431364181, 3.189307221898113998, -10.73538068360681663 ) ) ;
#63849=ORIENTED_EDGE ( 'NONE', *, *, #52887, .F. ) ;
#63851=EDGE_LOOP ( 'NONE', ( #37351, #57464, #7365, #54141 ) ) ;
#63853=CARTESIAN_POINT ( 'NONE',  ( 0.2653141617321017609, -4.229807441322391171, 11.49253039221381201 ) ) ;
#63857=ADVANCED_FACE ( 'NONE', ( #29973 ), #42895, .F. ) ;
#63873=CARTESIAN_POINT ( 'NONE',  ( 3.031336079628918156, -7.694633165537201336, 1.779751109289165356 ) ) ;
#63881=( BOUNDED_SURFACE ( )  B_SPLINE_SURFACE ( 3, 1, ( 
 ( #25889, #30214 ),
 ( #65756, #10913 ),
 ( #15560, #61129 ),
 ( #38964, #28991 ) ),
 .UNSPECIFIED., .F., .F., .F. ) 
 B_SPLINE_SURFACE_WITH_KNOTS ( ( 4, 4 ),
 ( 2, 2 ),
 ( 0.000000000000000000, 1.000000000000000000 ),
 ( 0.000000000000000000, 1.000000000000000000 ),
 .UNSPECIFIED. ) 
 GEOMETRIC_REPRESENTATION_ITEM ( )  RATIONAL_B_SPLINE_SURFACE ( (
 ( 1.000000000000000000, 1.000000000000000000),
 ( 0.6933888150995267674, 0.9895912004443193632),
 ( 0.6933888150995267674, 0.9895912004443193632),
 ( 1.000000000000000000, 1.000000000000000000) ) ) 
 REPRESENTATION_ITEM ( '' )  SURFACE ( )  );
#63887=CARTESIAN_POINT ( 'NONE',  ( 0.2676618633000459879, -9.277614237849222789, -7.994628339664919814 ) ) ;
#63902=CARTESIAN_POINT ( 'NONE',  ( 0.2651627682582937129, 7.938957913267755018, 9.324228491541544983 ) ) ;
#63909=CARTESIAN_POINT ( 'NONE',  ( 0.2958664285830440721, 1.910785783655738035, -12.10650684287251977 ) ) ;
#63914=CARTESIAN_POINT ( 'NONE',  ( 2.241537034860906719, 4.910958050585514378, -5.845308934728727479 ) ) ;
#63918=ORIENTED_EDGE ( 'NONE', *, *, #54236, .T. ) ;
#63920=CARTESIAN_POINT ( 'NONE',  ( 2.256373768223413290, -7.132139410180986516, 2.737361830682297104 ) ) ;
#63937=CARTESIAN_POINT ( 'NONE',  ( 0.3040950598368152291, 3.956873563689688567, -11.60568999039890770 ) ) ;
#63942=CARTESIAN_POINT ( 'NONE',  ( 2.350038591458107007, 3.024612895785500744, 10.18214835919902050 ) ) ;
#63945=CARTESIAN_POINT ( 'NONE',  ( 0.9232058338315048962, 8.301689855530291595, -9.306586124266512883 ) ) ;
#63948=CARTESIAN_POINT ( 'NONE',  ( 0.2650492594609241692, -11.54478160586240065, 4.084774262246043008 ) ) ;
#63952=EDGE_LOOP ( 'NONE', ( #688, #37535, #63514, #225 ) ) ;
#63953=ORIENTED_EDGE ( 'NONE', *, *, #3945, .T. ) ;
#63956=ORIENTED_EDGE ( 'NONE', *, *, #23246, .T. ) ;
#63958=CARTESIAN_POINT ( 'NONE',  ( 0.3040950598368152291, 12.11647736519421059, 1.881452845810416719 ) ) ;
#63960=CARTESIAN_POINT ( 'NONE',  ( 0.2648978790185619880, -10.53870023327867855, 6.237101853238509186 ) ) ;
#63961=CARTESIAN_POINT ( 'NONE',  ( 1.452237505248555660, -11.24427360515637986, -5.807998527926010013 ) ) ;
#63963=CARTESIAN_POINT ( 'NONE',  ( 1.194176325881338263, -11.12159247766668990, -5.827386336992995908 ) ) ;
#63969=CARTESIAN_POINT ( 'NONE',  ( 1.719304012338199517, 0.000000000000000000, 0.000000000000000000 ) ) ;
#63977=EDGE_CURVE ( 'NONE', #48647, #60647, #64482, .T. ) ;
#63982=CARTESIAN_POINT ( 'NONE',  ( 0.2652384770603647413, 2.191555293694135376, -12.04846497255940818 ) ) ;
#63995=CARTESIAN_POINT ( 'NONE',  ( 0.2801149460245124789, 2.320387321174167017, 12.02936836014264088 ) ) ;
#64002=CARTESIAN_POINT ( 'NONE',  ( 0.7446945582518622597, -12.15064199164609526, -2.504154979876258569 ) ) ;
#64007=CARTESIAN_POINT ( 'NONE',  ( 5.536195898058073439, 0.004027525919832952543, -0.007485416011288117955 ) ) ;
#64010=CARTESIAN_POINT ( 'NONE',  ( 0.2638984909335716500, 9.252728947331076981, 8.023974293733212804 ) ) ;
#64016=VERTEX_POINT ( 'NONE', #60157 ) ;
#64021=LINE ( 'NONE', #8170, #25383 ) ;
#64024=ORIENTED_EDGE ( 'NONE', *, *, #31732, .T. ) ;
#64026=CARTESIAN_POINT ( 'NONE',  ( 2.266490820343226353, 5.760233951938587893, -5.023127813992145363 ) ) ;
#64029=VECTOR ( 'NONE', #7049, 1000.000000000000114 ) ;
#64034=CARTESIAN_POINT ( 'NONE',  ( 2.241317068080785013, -7.501982551779182273, 1.415707718487486000 ) ) ;
#64035=CARTESIAN_POINT ( 'NONE',  ( 1.948354844646975170, -9.982942661981358157, 6.595573209515230850 ) ) ;
#64044=CARTESIAN_POINT ( 'NONE',  ( 1.462291587748811184, 3.724645088507181789, 12.08418494300826218 ) ) ;
#64046=CARTESIAN_POINT ( 'NONE',  ( 0.2651627682582914369, -11.53745347823612910, -4.105539787731825818 ) ) ;
#64047=EDGE_CURVE ( 'NONE', #43973, #31716, #55167, .T. ) ;
#64055=EDGE_CURVE ( 'NONE', #47570, #61002, #18455, .T. ) ;
#64056=CARTESIAN_POINT ( 'NONE',  ( 2.241352910868908310, 1.407733736974867034, 7.503490710578237355 ) ) ;
#64068=CARTESIAN_POINT ( 'NONE',  ( 2.430348790457182329, -3.678671624790087247, 6.761480562106249259 ) ) ;
#64069=CARTESIAN_POINT ( 'NONE',  ( 2.247206125382827935, -5.923516414428620536, 4.819320926502617120 ) ) ;
#64070=( BOUNDED_SURFACE ( )  B_SPLINE_SURFACE ( 3, 1, ( 
 ( #50360, #15411 ),
 ( #20404, #4806 ),
 ( #20075, #60977 ),
 ( #778, #46013 ) ),
 .UNSPECIFIED., .F., .F., .F. ) 
 B_SPLINE_SURFACE_WITH_KNOTS ( ( 4, 4 ),
 ( 2, 2 ),
 ( 0.000000000000000000, 1.000000000000000000 ),
 ( 0.000000000000000000, 1.000000000000000000 ),
 .UNSPECIFIED. ) 
 GEOMETRIC_REPRESENTATION_ITEM ( )  RATIONAL_B_SPLINE_SURFACE ( (
 ( 1.000000000000000000, 1.000000000000000000),
 ( 0.9942764183789327692, 0.8450855930916585379),
 ( 0.9942764183789327692, 0.8450855930916585379),
 ( 1.000000000000000000, 1.000000000000000000) ) ) 
 REPRESENTATION_ITEM ( '' )  SURFACE ( )  );
#64072=CARTESIAN_POINT ( 'NONE',  ( 2.244591118396557672, -2.510215291309266128, 7.211060161907638211 ) ) ;
#64077=CARTESIAN_POINT ( 'NONE',  ( 0.2655924914740778187, 12.05257978623653869, 2.169924872618101297 ) ) ;
#64081=CARTESIAN_POINT ( 'NONE',  ( 0.3053067050349125289, -8.055646999028066801, 9.241336250185334222 ) ) ;
#64089=CARTESIAN_POINT ( 'NONE',  ( 0.3006302518452032002, -9.533790235540692493, -7.704827863860894688 ) ) ;
#64090=CARTESIAN_POINT ( 'NONE',  ( 2.827825597296805604, -7.250702617666013872, 5.372687261161241956 ) ) ;
#64091=( BOUNDED_SURFACE ( )  B_SPLINE_SURFACE ( 3, 1, ( 
 ( #53901, #53245 ),
 ( #59220, #7689 ),
 ( #42928, #58575 ),
 ( #22988, #17990 ) ),
 .UNSPECIFIED., .F., .F., .F. ) 
 B_SPLINE_SURFACE_WITH_KNOTS ( ( 4, 4 ),
 ( 2, 2 ),
 ( 0.000000000000000000, 1.000000000000000000 ),
 ( 0.000000000000000000, 1.000000000000000000 ),
 .UNSPECIFIED. ) 
 GEOMETRIC_REPRESENTATION_ITEM ( )  RATIONAL_B_SPLINE_SURFACE ( (
 ( 1.000000000000000000, 1.000000000000000000),
 ( 0.9942764183789327692, 0.8450855930916580938),
 ( 0.9942764183789327692, 0.8450855930916580938),
 ( 1.000000000000000000, 1.000000000000000000) ) ) 
 REPRESENTATION_ITEM ( '' )  SURFACE ( )  );
#64092=CARTESIAN_POINT ( 'NONE',  ( 2.268878695253355282, 7.551766617932588410, -1.181158368266874037 ) ) ;
#64099=CARTESIAN_POINT ( 'NONE',  ( 2.350038591458114112, -7.305692696275646547, 7.710465783963738495 ) ) ;
#64108=DIRECTION ( 'NONE',  ( 0.3865475372811021382, 0.6938894834606000872, 0.6075346789811233439 ) ) ;
#64116=ORIENTED_EDGE ( 'NONE', *, *, #7002, .F. ) ;
#64134=AXIS2_PLACEMENT_3D ( 'NONE', #50967, #26337, #46620 ) ;
#64139=EDGE_CURVE ( 'NONE', #10582, #37098, #62010, .T. ) ;
#64145=CARTESIAN_POINT ( 'NONE',  ( 2.284126774967656370, -7.503320429541872727, -1.483972655035289190 ) ) ;
#64151=CARTESIAN_POINT ( 'NONE',  ( 2.990245332647774923, 0.5125330575219455564, -8.465748356453799417 ) ) ;
#64156=EDGE_CURVE ( 'NONE', #54308, #40020, #27977, .T. ) ;
#64162=CARTESIAN_POINT ( 'NONE',  ( 2.653899356899350526, 5.782420802795862791, -5.192946150929053317 ) ) ;
#64166=B_SPLINE_CURVE_WITH_KNOTS ( 'NONE', 3,
 ( #63, #20686, #5072, #40961, #29347, #49643, #55930, #4083, #59954, #54942, #9371, #49962, #24692, #44971, #19719, #39973 ),
 .UNSPECIFIED., .F., .F.,
 ( 4, 3, 3, 3, 3, 4 ),
 ( 0.000000000000000000, 0.0002999043160757389670, 0.0005998071753051078311, 0.0008997092107374667037, 0.001204458948195704076, 0.001510329163476617368 ),
 .UNSPECIFIED. ) ;
#64171=EDGE_CURVE ( 'NONE', #12912, #54893, #18432, .T. ) ;
#64172=CARTESIAN_POINT ( 'NONE',  ( 2.276905613633471326, 5.031956778294004451, 5.757134111949740785 ) ) ;
#64173=CARTESIAN_POINT ( 'NONE',  ( 2.889800649504073782, -0.06738247734054683691, 6.121013568931506832 ) ) ;
#64175=CARTESIAN_POINT ( 'NONE',  ( 0.2915757698887319060, 9.248369946372635653, -8.040595355212850848 ) ) ;
#64176=CARTESIAN_POINT ( 'NONE',  ( 0.3675815128205912052, -10.76447900494944321, 5.910255304480407368 ) ) ;
#64186=CARTESIAN_POINT ( 'NONE',  ( 0.2648978790185610999, -2.256510822326061483, -12.03635331166814382 ) ) ;
#64187=CARTESIAN_POINT ( 'NONE',  ( 2.255723233588952770, -7.544965460065571783, 1.196143347838687143 ) ) ;
#64189=CARTESIAN_POINT ( 'NONE',  ( 2.305787727787083519, 7.135468203929983488, 2.774453000917173284 ) ) ;
#64202=CARTESIAN_POINT ( 'NONE',  ( 0.2650492433740054277, -4.084772052580676771, 11.54478237753290770 ) ) ;
#64220=CARTESIAN_POINT ( 'NONE',  ( 2.589278595513797576, -6.829211973730751950, -3.664724287895283261 ) ) ;
#64224=CARTESIAN_POINT ( 'NONE',  ( 0.2657645697724694833, -9.283243433323022487, -7.987126944299723696 ) ) ;
#64225=CARTESIAN_POINT ( 'NONE',  ( 1.014383007554951144, -9.280879504740996211, 8.367379244277097783 ) ) ;
#64233=CARTESIAN_POINT ( 'NONE',  ( 5.530133899448235191, 0.01111090067015107867, 0.01149180883054605647 ) ) ;
#64238=ORIENTED_EDGE ( 'NONE', *, *, #11053, .F. ) ;
#64245=CARTESIAN_POINT ( 'NONE',  ( 0.2653141617321040369, -12.24612535104215638, -0.04404194803643789180 ) ) ;
#64256=CARTESIAN_POINT ( 'NONE',  ( 2.889800649504073782, -6.121013568931505944, -0.06738247734056820870 ) ) ;
#64258=CARTESIAN_POINT ( 'NONE',  ( 0.2646305136544072623, -11.55263159009961704, 4.064188116014512353 ) ) ;
#64261=EDGE_CURVE ( 'NONE', #42095, #36790, #4889, .T. ) ;
#64266=CARTESIAN_POINT ( 'NONE',  ( 0.2646305136544065406, 4.064188116014703311, -11.55263159009954421 ) ) ;
#64269=B_SPLINE_CURVE_WITH_KNOTS ( 'NONE', 3,
 ( #36485, #4929, #29843, #35496, #60438, #21183, #55794, #30501, #65413, #25192 ),
 .UNSPECIFIED., .F., .F.,
 ( 4, 3, 3, 4 ),
 ( 0.000000000000000000, 6.607638129004513277E-05, 9.911389841680569692E-05, 0.0001667630577588627449 ),
 .UNSPECIFIED. ) ;
#64272=CARTESIAN_POINT ( 'NONE',  ( 0.3474126878361829540, 3.953748424960800811, -11.61929161290141721 ) ) ;
#64274=CARTESIAN_POINT ( 'NONE',  ( 5.516018279890452902, -0.002104829434641057422, -0.006440244342253404787 ) ) ;
#64275=CARTESIAN_POINT ( 'NONE',  ( 0.3341166715381352348, -3.958014133396687839, 11.61315925169693664 ) ) ;
#64276=CARTESIAN_POINT ( 'NONE',  ( 0.2652384770603681829, -11.53005438969046814, 4.126289928142361951 ) ) ;
#64280=( BOUNDED_SURFACE ( )  B_SPLINE_SURFACE ( 3, 1, ( 
 ( #60464, #53864 ),
 ( #13600, #3975 ),
 ( #44198, #59494 ),
 ( #24237, #14566 ) ),
 .UNSPECIFIED., .F., .F., .F. ) 
 B_SPLINE_SURFACE_WITH_KNOTS ( ( 4, 4 ),
 ( 2, 2 ),
 ( 0.000000000000000000, 1.000000000000000000 ),
 ( 0.000000000000000000, 1.000000000000000000 ),
 .UNSPECIFIED. ) 
 GEOMETRIC_REPRESENTATION_ITEM ( )  RATIONAL_B_SPLINE_SURFACE ( (
 ( 1.000000000000000000, 1.000000000000000000),
 ( 0.9856612449720755231, 0.9999558406602322425),
 ( 0.9856612449720755231, 0.9999558406602322425),
 ( 1.000000000000000000, 1.000000000000000000) ) ) 
 REPRESENTATION_ITEM ( '' )  SURFACE ( )  );
#64284=EDGE_CURVE ( 'NONE', #25922, #27962, #43738, .T. ) ;
#64286=CARTESIAN_POINT ( 'NONE',  ( 1.633930747253119486, 1.494486044208924946, -12.61425129500200093 ) ) ;
#64292=CARTESIAN_POINT ( 'NONE',  ( 0.3218525148189821383, 10.74192973049796151, -5.919623386703225520 ) ) ;
#64295=VERTEX_POINT ( 'NONE', #6937 ) ;
#64297=LINE ( 'NONE', #4113, #17548 ) ;
#64329=EDGE_CURVE ( 'NONE', #22231, #17057, #29181, .T. ) ;
#64331=CARTESIAN_POINT ( 'NONE',  ( 2.241536586108912488, -7.634468130435847044, 0.006292724672621609859 ) ) ;
#64336=CARTESIAN_POINT ( 'NONE',  ( 0.2653519991613824680, 10.61652626436036506, -6.104031847944908939 ) ) ;
#64349=VECTOR ( 'NONE', #5452, 1000.000000000000114 ) ;
#64353=EDGE_CURVE ( 'NONE', #36589, #6075, #17620, .T. ) ;
#64356=CARTESIAN_POINT ( 'NONE',  ( 2.259025283528087957, -7.499281868334244372, 1.461109758650534829 ) ) ;
#64359=AXIS2_PLACEMENT_3D ( 'NONE', #26406, #9797, #30082 ) ;
#64361=CARTESIAN_POINT ( 'NONE',  ( 2.827825597296802496, -8.776379025186162863, -2.100863646776143234 ) ) ;
#64365=CARTESIAN_POINT ( 'NONE',  ( 1.287602823385632034, 3.781900355162443272, 12.00540336274424646 ) ) ;
#64376=CARTESIAN_POINT ( 'NONE',  ( 0.2653519789438778531, 12.06397564829376101, 2.104833950422620337 ) ) ;
#64379=CARTESIAN_POINT ( 'NONE',  ( 2.034671305880032754, 8.476347594673310226, 8.030508024279379597 ) ) ;
#64381=CARTESIAN_POINT ( 'NONE',  ( 2.280717697723839255, -0.1564731737569588776, -7.645922213779910770 ) ) ;
#64382=CARTESIAN_POINT ( 'NONE',  ( 2.245754705088395031, -5.920355780195118989, 4.822435078157726984 ) ) ;
#64391=LINE ( 'NONE', #53468, #41296 ) ;
#64393=CARTESIAN_POINT ( 'NONE',  ( 0.2648978790185584908, -7.972372351883092456, 9.295532325666423290 ) ) ;
#64398=CARTESIAN_POINT ( 'NONE',  ( 0.2646305136544065406, 10.67138229758237955, -6.008537389229304360 ) ) ;
#64399=CARTESIAN_POINT ( 'NONE',  ( 3.100650473569440901, 7.585586315875629815, -2.280184661131237078 ) ) ;
#64400=CARTESIAN_POINT ( 'NONE',  ( 3.152665057734045373, -6.378477742800418682, 4.725420687650736085 ) ) ;
#64401=DIRECTION ( 'NONE',  ( 0.3865475372811021382, -0.4442537292684384798, -0.8082200352954632683 ) ) ;
#64404=CARTESIAN_POINT ( 'NONE',  ( 2.297017764049619437, 1.166330442180481652, -7.563558677601394997 ) ) ;
#64417=CARTESIAN_POINT ( 'NONE',  ( 0.2717059086739028184, 5.971041827598971174, -10.69429229731970743 ) ) ;
#64418=CARTESIAN_POINT ( 'NONE',  ( 2.273267844204860832, 6.543821324256936300, -3.952852893982225613 ) ) ;
#64420=ORIENTED_EDGE ( 'NONE', *, *, #42375, .F. ) ;
#64427=ORIENTED_EDGE ( 'NONE', *, *, #40752, .F. ) ;
#64437=CARTESIAN_POINT ( 'NONE',  ( 1.719304012338200849, 11.38834240361387096, 5.690355757826642602 ) ) ;
#64441=CARTESIAN_POINT ( 'NONE',  ( 1.020182472824201936, 0.4462553704991011339, -12.48987306958628274 ) ) ;
#64450=( BOUNDED_SURFACE ( )  B_SPLINE_SURFACE ( 3, 1, ( 
 ( #56887, #11312 ),
 ( #31579, #49523 ),
 ( #27920, #18921 ),
 ( #48228, #13280 ) ),
 .UNSPECIFIED., .F., .F., .F. ) 
 B_SPLINE_SURFACE_WITH_KNOTS ( ( 4, 4 ),
 ( 2, 2 ),
 ( 0.000000000000000000, 1.000000000000000000 ),
 ( 0.000000000000000000, 1.000000000000000000 ),
 .UNSPECIFIED. ) 
 GEOMETRIC_REPRESENTATION_ITEM ( )  RATIONAL_B_SPLINE_SURFACE ( (
 ( 1.000000000000000000, 1.000000000000000000),
 ( 0.6933888150995267674, 0.9895912004443193632),
 ( 0.6933888150995267674, 0.9895912004443193632),
 ( 1.000000000000000000, 1.000000000000000000) ) ) 
 REPRESENTATION_ITEM ( '' )  SURFACE ( )  );
#64455=CARTESIAN_POINT ( 'NONE',  ( 0.2650492433740059828, 9.451472485870558771, 7.786978278830003042 ) ) ;
#64456=CARTESIAN_POINT ( 'NONE',  ( 2.969415267405026704, 5.354299007565745505, 5.777543886622345859 ) ) ;
#64462=CARTESIAN_POINT ( 'NONE',  ( 0.7400311444011721251, 2.502569705372971409, 12.14938086789863370 ) ) ;
#64464=( BOUNDED_SURFACE ( )  B_SPLINE_SURFACE ( 3, 1, ( 
 ( #24992, #46264 ),
 ( #9671, #10332 ),
 ( #705, #30607 ),
 ( #15331, #55898 ) ),
 .UNSPECIFIED., .F., .F., .F. ) 
 B_SPLINE_SURFACE_WITH_KNOTS ( ( 4, 4 ),
 ( 2, 2 ),
 ( 0.000000000000000000, 1.000000000000000000 ),
 ( 0.000000000000000000, 1.000000000000000000 ),
 .UNSPECIFIED. ) 
 GEOMETRIC_REPRESENTATION_ITEM ( )  RATIONAL_B_SPLINE_SURFACE ( (
 ( 1.000000000000000000, 1.000000000000000000),
 ( 0.6933888150995267674, 0.9895912004443193632),
 ( 0.6933888150995267674, 0.9895912004443193632),
 ( 1.000000000000000000, 1.000000000000000000) ) ) 
 REPRESENTATION_ITEM ( '' )  SURFACE ( )  );
#64468=CARTESIAN_POINT ( 'NONE',  ( 2.844750968615307851, 5.783165144077117681, -5.286885609674412123 ) ) ;
#64469=CARTESIAN_POINT ( 'NONE',  ( 2.242418902651939661, -3.903399295463796825, -6.561482094363286777 ) ) ;
#64480=CARTESIAN_POINT ( 'NONE',  ( 5.516018279890452902, 0.004180585980734981624, 0.005331956019561726046 ) ) ;
#64482=LINE ( 'NONE', #14276, #58778 ) ;
#64487=ORIENTED_EDGE ( 'NONE', *, *, #65034, .F. ) ;
#64490=CARTESIAN_POINT ( 'NONE',  ( 0.2646305136544072623, -2.256625640822394807, 12.03696649559613974 ) ) ;
#64491=VERTEX_POINT ( 'NONE', #23415 ) ;
#64497=CARTESIAN_POINT ( 'NONE',  ( 3.152665057735194232, -3.161213418914472051, -7.281573230474045921 ) ) ;
#64505=VERTEX_POINT ( 'NONE', #59013 ) ;
#64515=VECTOR ( 'NONE', #43498, 1000.000000000000000 ) ;
#64520=CARTESIAN_POINT ( 'NONE',  ( 2.889800649504073782, 6.016320774579824615, -1.129261637821548980 ) ) ;
#64522=CARTESIAN_POINT ( 'NONE',  ( 2.305787727787084407, -6.711944854845797614, -3.682701754025583085 ) ) ;
#64527=CARTESIAN_POINT ( 'NONE',  ( 2.305787727787084407, -7.654065630109508689, 0.1666591538752418555 ) ) ;
#64533=CARTESIAN_POINT ( 'NONE',  ( 0.3537226245948373315, -9.233810598191725560, -8.088784578751390342 ) ) ;
#64535=ORIENTED_EDGE ( 'NONE', *, *, #35011, .F. ) ;
#64545=B_SPLINE_CURVE_WITH_KNOTS ( 'NONE', 3,
 ( #59291, #24047, #28056, #7417, #63942, #2465, #13714 ),
 .UNSPECIFIED., .F., .F.,
 ( 4, 3, 4 ),
 ( 0.000000000000000000, 0.001700533616330550564, 0.005002426799371241864 ),
 .UNSPECIFIED. ) ;
#64549=ORIENTED_EDGE ( 'NONE', *, *, #19810, .T. ) ;
#64552=CARTESIAN_POINT ( 'NONE',  ( 2.507146904658099196, -7.328382489803290767, 2.437115546363195051 ) ) ;
#64556=ORIENTED_EDGE ( 'NONE', *, *, #45767, .T. ) ;
#64559=CARTESIAN_POINT ( 'NONE',  ( 0.2911222467163562255, -7.711756541611626936, -9.524109243548050330 ) ) ;
#64564=CARTESIAN_POINT ( 'NONE',  ( 0.2657645697724707046, 10.52916014490830321, 6.253766234003959923 ) ) ;
#64567=CARTESIAN_POINT ( 'NONE',  ( 2.889800649504073782, 6.121013568931506832, 0.06738247734052546511 ) ) ;
#64572=CARTESIAN_POINT ( 'NONE',  ( 5.515539859299206427, -0.005991790098943843880, 0.0008592514567754646780 ) ) ;
#64578=CARTESIAN_POINT ( 'NONE',  ( 5.536195898058073439, -0.008071068258923586383, -0.002666509901870041388 ) ) ;
#64581=CARTESIAN_POINT ( 'NONE',  ( 0.2801149460245148104, 9.509848747524184631, 7.723514566794011493 ) ) ;
#64594=LINE ( 'NONE', #59001, #23589 ) ;
#64597=CARTESIAN_POINT ( 'NONE',  ( 0.2648978790185584908, 10.67083876753500427, -6.008231198268870976 ) ) ;
#64605=CARTESIAN_POINT ( 'NONE',  ( 2.249013661412229137, -5.772355099776643961, -5.000301708456380112 ) ) ;
#64607=EDGE_CURVE ( 'NONE', #21985, #39116, #28399, .T. ) ;
#64631=APPLICATION_CONTEXT ( 'automotive_design' ) ;
#64647=FACE_OUTER_BOUND ( 'NONE', #59878, .T. ) ;
#64655=DIRECTION ( 'NONE',  ( -1.000000000000000000, -0.000000000000000000, -0.000000000000000000 ) ) ;
#64660=ORIENTED_EDGE ( 'NONE', *, *, #52488, .T. ) ;
#64662=CARTESIAN_POINT ( 'NONE',  ( 5.530133899448235191, -0.01550764871776272834, 0.003876417824003489630 ) ) ;
#64665=CARTESIAN_POINT ( 'NONE',  ( 0.2657645697724694833, -10.52916014490826591, -6.253766234004032754 ) ) ;
#64668=CARTESIAN_POINT ( 'NONE',  ( 2.350038591458080361, -10.33030559206120813, -2.471682575235316648 ) ) ;
#64675=ORIENTED_EDGE ( 'NONE', *, *, #54136, .T. ) ;
#64678=CARTESIAN_POINT ( 'NONE',  ( 2.844750968616247544, 4.777247819183518374, -6.210802026112414609 ) ) ;
#64689=CARTESIAN_POINT ( 'NONE',  ( 2.781367136452661537, -5.255136723410572586, -5.783466416658777476 ) ) ;
#64692=CARTESIAN_POINT ( 'NONE',  ( 5.515539859299206427, -0.005618668168217172236, -0.002251761459665588272 ) ) ;
#64693=B_SPLINE_CURVE_WITH_KNOTS ( 'NONE', 3,
 ( #44260, #64533, #33311, #54900, #63547, #43948, #29305, #49598, #23016, #28322, #33953, #54598, #9324, #39604, #58606, #63887, #64224, #53614, #19338 ),
 .UNSPECIFIED., .F., .F.,
 ( 4, 3, 3, 3, 3, 3, 4 ),
 ( 1.039534490390255925E-17, 4.457896483014696203E-05, 6.639290541541784888E-05, 8.820687556478307243E-05, 0.0001100173248778876675, 0.0001545671401658054074, 0.0001830328308068552429 ),
 .UNSPECIFIED. ) ;
#64698=EDGE_CURVE ( 'NONE', #61317, #49256, #8772, .T. ) ;
#64710=CARTESIAN_POINT ( 'NONE',  ( 1.020182472820972963, 12.48987306958525068, 0.4462553704978033942 ) ) ;
#64711=CARTESIAN_POINT ( 'NONE',  ( 3.152665057736013132, 7.281573230473836311, -3.161213418915250095 ) ) ;
#64714=ORIENTED_EDGE ( 'NONE', *, *, #24260, .T. ) ;
#64715=CARTESIAN_POINT ( 'NONE',  ( 2.253265082352431836, -7.220580418434031422, 2.491579069691566062 ) ) ;
#64716=DIRECTION ( 'NONE',  ( 0.000000000000000000, 0.000000000000000000, 1.000000000000000000 ) ) ;
#64721=DIRECTION ( 'NONE',  ( 0.3865475372811021382, 0.9046932595863036441, 0.1791957239473755126 ) ) ;
#64723=CARTESIAN_POINT ( 'NONE',  ( 2.256373768221670684, 1.195444820372209227, -7.545294827889062361 ) ) ;
#64732=CARTESIAN_POINT ( 'NONE',  ( 0.3675815128205912052, -6.367184624550238148, 10.50067073900649461 ) ) ;
#64733=VERTEX_POINT ( 'NONE', #23763 ) ;
#64736=CARTESIAN_POINT ( 'NONE',  ( 2.266490820343744605, -5.023127813992656066, -5.760233951938361407 ) ) ;
#64739=CARTESIAN_POINT ( 'NONE',  ( 2.297017764050091948, -7.246120070222743514, -2.462009443075682924 ) ) ;
#64742=ORIENTED_EDGE ( 'NONE', *, *, #27782, .T. ) ;
#64743=CIRCLE ( 'NONE', #13766, 12.15774668701806149 ) ;
#64750=EDGE_CURVE ( 'NONE', #63267, #14741, #21485, .T. ) ;
#64753=CARTESIAN_POINT ( 'NONE',  ( 2.305787727787084407, 7.654065630109506913, -0.1666591538752953128 ) ) ;
#64756=EDGE_CURVE ( 'NONE', #62968, #14946, #62026, .T. ) ;
#64757=LINE ( 'NONE', #54493, #52950 ) ;
#64760=DIRECTION ( 'NONE',  ( -1.000000000000000000, -0.000000000000000000, -0.000000000000000000 ) ) ;
#64766=CARTESIAN_POINT ( 'NONE',  ( 0.2671309869109501078, 0.1620273132355689594, 12.24572650704445032 ) ) ;
#64781=CIRCLE ( 'NONE', #11681, 7.938172270156617749 ) ;
#64787=CARTESIAN_POINT ( 'NONE',  ( 2.297017764050091060, 6.543724852214733545, -3.968300849026689558 ) ) ;
#64790=CARTESIAN_POINT ( 'NONE',  ( 2.990245332647883281, 5.834301250882278467, -6.155689586375134859 ) ) ;
#64791=DIRECTION ( 'NONE',  ( 0.000000000000000000, -1.000000000000000000, -0.000000000000000000 ) ) ;
#64816=CARTESIAN_POINT ( 'NONE',  ( 3.100650473569692256, 7.276570693048406646, 3.129198107107961313 ) ) ;
#64821=CARTESIAN_POINT ( 'NONE',  ( 0.3675815128205894289, -7.689697408877210094, -9.574637318042043432 ) ) ;
#64826=VERTEX_POINT ( 'NONE', #22265 ) ;
#64829=CARTESIAN_POINT ( 'NONE',  ( 0.2653519991613835782, 11.50013121838207653, 4.209134909048784401 ) ) ;
#64833=ORIENTED_EDGE ( 'NONE', *, *, #4830, .T. ) ;
#64835=CARTESIAN_POINT ( 'NONE',  ( 2.249013661412229581, -7.134443398813858472, -2.724484898587359982 ) ) ;
#64837=( BOUNDED_SURFACE ( )  B_SPLINE_SURFACE ( 3, 1, ( 
 ( #38581, #49240 ),
 ( #42907, #58553 ),
 ( #33262, #33596 ),
 ( #39222, #17975 ) ),
 .UNSPECIFIED., .F., .F., .F. ) 
 B_SPLINE_SURFACE_WITH_KNOTS ( ( 4, 4 ),
 ( 2, 2 ),
 ( 0.000000000000000000, 1.000000000000000000 ),
 ( 0.000000000000000000, 1.000000000000000000 ),
 .UNSPECIFIED. ) 
 GEOMETRIC_REPRESENTATION_ITEM ( )  RATIONAL_B_SPLINE_SURFACE ( (
 ( 1.000000000000000000, 1.000000000000000000),
 ( 0.9942764183789327692, 0.8450855930916585379),
 ( 0.9942764183789327692, 0.8450855930916585379),
 ( 1.000000000000000000, 1.000000000000000000) ) ) 
 REPRESENTATION_ITEM ( '' )  SURFACE ( )  );
#64844=CARTESIAN_POINT ( 'NONE',  ( 5.514970785353741078, 0.004233694591582955018, 0.002093325033903826408 ) ) ;
#64846=CARTESIAN_POINT ( 'NONE',  ( 0.3675815128205894289, -2.391755495700522705, -12.04510820461661780 ) ) ;
#64847=EDGE_CURVE ( 'NONE', #58835, #17087, #46087, .T. ) ;
#64848=ORIENTED_EDGE ( 'NONE', *, *, #36104, .T. ) ;
#64850=CARTESIAN_POINT ( 'NONE',  ( 0.7400311444011672402, 6.506979270898180623, 10.56075429936769616 ) ) ;
#64856=CIRCLE ( 'NONE', #13922, 12.73084802173761787 ) ;
#64857=CARTESIAN_POINT ( 'NONE',  ( 0.5547464869798233167, -9.256151063740606588, 8.164898018378787370 ) ) ;
#64866=CARTESIAN_POINT ( 'NONE',  ( 0.2767916011545406008, -12.09541651105894822, -1.940025653808966410 ) ) ;
#64867=CARTESIAN_POINT ( 'NONE',  ( 2.899286259009687061, -5.316140236670800157, 5.780956296532494321 ) ) ;
#64873=VECTOR ( 'NONE', #28628, 1000.000000000000000 ) ;
#64875=ORIENTED_EDGE ( 'NONE', *, *, #54038, .T. ) ;
#64884=CARTESIAN_POINT ( 'NONE',  ( 2.258463476537672765, -1.192666169131278986, -7.546439757229372880 ) ) ;
#64889=CARTESIAN_POINT ( 'NONE',  ( 0.2646305136544065406, 7.972778379581675345, -9.296005949277144964 ) ) ;
#64901=CARTESIAN_POINT ( 'NONE',  ( 2.305787727787084407, -1.493241775258372872, -7.508843116234172221 ) ) ;
#64915=CARTESIAN_POINT ( 'NONE',  ( 0.3474126878361796789, -12.27082419038178784, 0.2587235634077604818 ) ) ;
#64918=CARTESIAN_POINT ( 'NONE',  ( 0.3401186441510197223, -3.955862996551428257, -11.61600526280575707 ) ) ;
#64920=VERTEX_POINT ( 'NONE', #45118 ) ;
#64925=ORIENTED_EDGE ( 'NONE', *, *, #26145, .T. ) ;
#64927=FACE_OUTER_BOUND ( 'NONE', #38695, .T. ) ;
#64929=CARTESIAN_POINT ( 'NONE',  ( 3.152665057735760445, 4.725420687649616092, -6.378477742801607953 ) ) ;
#64940=CARTESIAN_POINT ( 'NONE',  ( 0.2648978790185584908, -7.769924372105139199, -9.465406350830686932 ) ) ;
#64949=CARTESIAN_POINT ( 'NONE',  ( 0.2648978790185584908, 2.256510822326303956, -12.03635331166809941 ) ) ;
#64950=CARTESIAN_POINT ( 'NONE',  ( 0.2638984909335720941, -11.43908195192332578, 4.375449752477094556 ) ) ;
#64952=B_SPLINE_CURVE_WITH_KNOTS ( 'NONE', 3,
 ( #61596, #46645, #41977, #30679, #47321, #1767, #56287, #22025, #771, #461, #31992, #21033, #52313, #16401, #46331, #60969, #36981, #46985, #20728 ),
 .UNSPECIFIED., .F., .F.,
 ( 4, 3, 3, 3, 3, 3, 4 ),
 ( 9.550984261304515293E-18, 4.457896483014562033E-05, 6.639290541541465049E-05, 8.820687556478086337E-05, 0.0001100173248778839812, 0.0001545671401658083347, 0.0001830328308068577365 ),
 .UNSPECIFIED. ) ;
#64977=CARTESIAN_POINT ( 'NONE',  ( 0.3106921474978425746, -6.333448016104122225, 10.49891314301084044 ) ) ;
#64978=CARTESIAN_POINT ( 'NONE',  ( 0.2653519890518162283, 4.188437879978412326, -11.50766430042464883 ) ) ;
#64979=EDGE_CURVE ( 'NONE', #239, #65794, #30195, .T. ) ;
#64981=CARTESIAN_POINT ( 'NONE',  ( 0.3632410797595258534, -10.76277061791635958, -5.910360611678935783 ) ) ;
#64982=CARTESIAN_POINT ( 'NONE',  ( 2.241531873784868623, 0.01153688368842444717, 7.634454672504356054 ) ) ;
#64983=CARTESIAN_POINT ( 'NONE',  ( 2.241451721903215510, -7.634225434981129155, -0.06083185034804090840 ) ) ;
#64984=VERTEX_POINT ( 'NONE', #14187 ) ;
#64986=CARTESIAN_POINT ( 'NONE',  ( 0.2646305136544065406, 9.296005949277226676, 7.972778379581582975 ) ) ;
#64998=CARTESIAN_POINT ( 'NONE',  ( 2.244591118395373286, 5.917635828472982418, 4.825158615935962736 ) ) ;
#65005=CARTESIAN_POINT ( 'NONE',  ( 2.247112776671468470, -7.499199956302002867, 1.440655381229448029 ) ) ;
#65008=CARTESIAN_POINT ( 'NONE',  ( 0.7400311444011681283, -12.14938086789864258, 2.502569705372930109 ) ) ;
#65015=CARTESIAN_POINT ( 'NONE',  ( 2.080613030138687147, 0.000000000000000000, 0.000000000000000000 ) ) ;
#65025=CARTESIAN_POINT ( 'NONE',  ( 2.241506898688419902, 5.822995664778323643, -4.937416071751777658 ) ) ;
#65026=CARTESIAN_POINT ( 'NONE',  ( 5.530133899448235191, -0.003876417824003551213, 0.01550764871776215414 ) ) ;
#65029=APPLICATION_CONTEXT ( 'automotive_design' ) ;
#65030=CARTESIAN_POINT ( 'NONE',  ( 2.907497136249938663, -6.243048412628442456, -4.769582063554289597 ) ) ;
#65034=EDGE_CURVE ( 'NONE', #11018, #28687, #6411, .T. ) ;
#65036=CARTESIAN_POINT ( 'NONE',  ( 2.290907136833251201, -5.963935563308454313, 4.792500160339664639 ) ) ;
#65037=( BOUNDED_SURFACE ( )  B_SPLINE_SURFACE ( 3, 1, ( 
 ( #15012, #45958 ),
 ( #413, #20682 ),
 ( #35939, #51286 ),
 ( #5736, #21677 ) ),
 .UNSPECIFIED., .F., .F., .F. ) 
 B_SPLINE_SURFACE_WITH_KNOTS ( ( 4, 4 ),
 ( 2, 2 ),
 ( 0.000000000000000000, 1.000000000000000000 ),
 ( 0.000000000000000000, 1.000000000000000000 ),
 .UNSPECIFIED. ) 
 GEOMETRIC_REPRESENTATION_ITEM ( )  RATIONAL_B_SPLINE_SURFACE ( (
 ( 1.000000000000000000, 1.000000000000000000),
 ( 0.9942764183789327692, 0.8450855930916585379),
 ( 0.9942764183789327692, 0.8450855930916585379),
 ( 1.000000000000000000, 1.000000000000000000) ) ) 
 REPRESENTATION_ITEM ( '' )  SURFACE ( )  );
#65039=CARTESIAN_POINT ( 'NONE',  ( 2.260457164927185847, -2.482766715766957510, 7.226149053012477452 ) ) ;
#65040=CARTESIAN_POINT ( 'NONE',  ( 2.963017218115493012, 6.619413971958212350, 4.265970453343873814 ) ) ;
#65042=ORIENTED_EDGE ( 'NONE', *, *, #29690, .T. ) ;
#65045=FACE_OUTER_BOUND ( 'NONE', #3185, .T. ) ;
#65052=CARTESIAN_POINT ( 'NONE',  ( 1.194176325881335154, 12.26540585042612719, -2.684784923266161361 ) ) ;
#65058=CARTESIAN_POINT ( 'NONE',  ( 2.259830038565000088, 7.547174990768423797, -1.190932096469573320 ) ) ;
#65081=CARTESIAN_POINT ( 'NONE',  ( 3.047904605210431939, 0.4249306449416465070, -7.891858004695958329 ) ) ;
#65093=CARTESIAN_POINT ( 'NONE',  ( 2.247112776671467582, 7.635437439951565430, -0.1165461824817972114 ) ) ;
#65095=EDGE_CURVE ( 'NONE', #8838, #26102, #36092, .T. ) ;
#65096=CARTESIAN_POINT ( 'NONE',  ( 1.719304012340734378, -11.38834240361519612, -5.690355757825884986 ) ) ;
#65108=CARTESIAN_POINT ( 'NONE',  ( 1.937114397841935398, -10.63710405811938742, 7.182898292393728568 ) ) ;
#65110=CARTESIAN_POINT ( 'NONE',  ( 2.305787727787083519, 5.970480882365222897, 4.792270232040915623 ) ) ;
#65114=CARTESIAN_POINT ( 'NONE',  ( 0.2651627682582914924, -12.04449770099952843, 2.213224986694545038 ) ) ;
#65115=CARTESIAN_POINT ( 'NONE',  ( 0.3665391374699472626, -4.447929964102772082, -11.44911061034390976 ) ) ;
#65124=CARTESIAN_POINT ( 'NONE',  ( 0.2648978790185584908, -6.008231198268910056, -10.67083876753498117 ) ) ;
#65129=ORIENTED_EDGE ( 'NONE', *, *, #32779, .T. ) ;
#65143=CARTESIAN_POINT ( 'NONE',  ( 2.241528039335008771, 4.919377664485172552, -5.838210500619323895 ) ) ;
#65145=CARTESIAN_POINT ( 'NONE',  ( 2.368238019615410028, 6.556525400300650119, -3.992969450835625711 ) ) ;
#65173=ORIENTED_EDGE ( 'NONE', *, *, #39320, .F. ) ;
#65183=CARTESIAN_POINT ( 'NONE',  ( 2.245754705088262693, -2.506725724682980161, -7.212684575686632904 ) ) ;
#65190=CARTESIAN_POINT ( 'NONE',  ( 0.7446945582530672958, 9.728576129010571449, -7.698291984229237883 ) ) ;
#65192=CARTESIAN_POINT ( 'NONE',  ( 2.257661810676414582, -6.682681612748183397, -3.702552158175678176 ) ) ;
#65196=CARTESIAN_POINT ( 'NONE',  ( 2.256373768223416842, -7.638251659827610673, 0.1329433694244051001 ) ) ;
#65200=CARTESIAN_POINT ( 'NONE',  ( 2.507146904658099640, 6.793847219607499710, -3.672650549645595230 ) ) ;
#65206=CARTESIAN_POINT ( 'NONE',  ( 2.259025283528092842, -4.805599953367692301, 5.939720477913342123 ) ) ;
#65210=EDGE_CURVE ( 'NONE', #5409, #43973, #22287, .T. ) ;
#65212=CARTESIAN_POINT ( 'NONE',  ( 2.994568964204209038, -5.368337437440291460, 5.775954174106914252 ) ) ;
#65239=CARTESIAN_POINT ( 'NONE',  ( 5.514970785353741078, -0.001326349372336325721, 0.004532877335078709831 ) ) ;
#65271=CARTESIAN_POINT ( 'NONE',  ( 0.8320506296491583242, -12.42924193558400425, 0.3827056590416399451 ) ) ;
#65275=CARTESIAN_POINT ( 'NONE',  ( 2.273267844203311405, 7.234348261135926883, 2.472013099046034057 ) ) ;
#65282=ORIENTED_EDGE ( 'NONE', *, *, #46126, .F. ) ;
#65283=PRODUCT_DEFINITION ( 'UNKNOWN', '', #44125, #37234 ) ;
#65294=EDGE_CURVE ( 'NONE', #17087, #54467, #33, .T. ) ;
#65298=CARTESIAN_POINT ( 'NONE',  ( 2.242418902651940105, 0.09970190380433034683, 7.634109827927228586 ) ) ;
#65300=CARTESIAN_POINT ( 'NONE',  ( 1.452237505248555660, 5.807998527926049093, -11.24427360515636032 ) ) ;
#65304=ORIENTED_EDGE ( 'NONE', *, *, #21976, .T. ) ;
#65320=CARTESIAN_POINT ( 'NONE',  ( 2.241352910868908310, -2.689314586382399952, 7.145045428366567641 ) ) ;
#65330=CARTESIAN_POINT ( 'NONE',  ( 2.573738926104377267, 7.664876274722926652, -1.112690714006459247 ) ) ;
#65339=LINE ( 'NONE', #40733, #19227 ) ;
#65340=CARTESIAN_POINT ( 'NONE',  ( 1.104777566491140117, -12.24382064406180959, 2.644034362100653901 ) ) ;
#65342=CARTESIAN_POINT ( 'NONE',  ( 2.241311220309554653, 7.633829235838275551, 0.09281826062098677554 ) ) ;
#65357=CARTESIAN_POINT ( 'NONE',  ( 5.520433897694421610, -0.0005131706886600394431, 0.01505375422439068044 ) ) ;
#65361=FACE_OUTER_BOUND ( 'NONE', #7104, .T. ) ;
#65367=CARTESIAN_POINT ( 'NONE',  ( 5.514624014163232779, 0.003278974416024606296, -0.002529391395135317452 ) ) ;
#65368=CARTESIAN_POINT ( 'NONE',  ( 5.516018279890452902, 0.003580555109620875767, -0.005752102158674359499 ) ) ;
#65374=CARTESIAN_POINT ( 'NONE',  ( 0.5572780756278377101, 12.33974848088617549, 0.3055340344618433512 ) ) ;
#65384=CARTESIAN_POINT ( 'NONE',  ( 0.3278977287071223601, -11.44003061923228159, -4.427879319183004370 ) ) ;
#65389=CARTESIAN_POINT ( 'NONE',  ( 2.255723233588951437, -5.010912740808161736, 5.766109278028616281 ) ) ;
#65402=CARTESIAN_POINT ( 'NONE',  ( 1.719304012338199517, 0.000000000000000000, 0.000000000000000000 ) ) ;
#65405=CARTESIAN_POINT ( 'NONE',  ( 2.288423627607478750, 7.131972212895042240, -2.767471693622725049 ) ) ;
#65411=CARTESIAN_POINT ( 'NONE',  ( 2.262775599886257094, -1.465770593192945226, 7.499645832851606464 ) ) ;
#65412=CARTESIAN_POINT ( 'NONE',  ( 0.2652384770603698483, -9.423432754625777008, 7.820955051613289299 ) ) ;
#65413=CARTESIAN_POINT ( 'NONE',  ( 2.241451721903216399, 5.809054012306858361, 4.953785420083431035 ) ) ;
#65420=ADVANCED_FACE ( 'NONE', ( #19777 ), #58928, .T. ) ;
#65423=AXIS2_PLACEMENT_3D ( 'NONE', #52662, #1124, #47014 ) ;
#65426=( BOUNDED_SURFACE ( )  B_SPLINE_SURFACE ( 3, 1, ( 
 ( #2320, #57193 ),
 ( #58166, #12272 ),
 ( #32536, #52847 ),
 ( #22594, #42859 ) ),
 .UNSPECIFIED., .F., .F., .F. ) 
 B_SPLINE_SURFACE_WITH_KNOTS ( ( 4, 4 ),
 ( 2, 2 ),
 ( 0.000000000000000000, 1.000000000000000000 ),
 ( 0.000000000000000000, 1.000000000000000000 ),
 .UNSPECIFIED. ) 
 GEOMETRIC_REPRESENTATION_ITEM ( )  RATIONAL_B_SPLINE_SURFACE ( (
 ( 1.000000000000000000, 1.000000000000000000),
 ( 0.9856612449720755231, 0.9999558406602322425),
 ( 0.9856612449720755231, 0.9999558406602322425),
 ( 1.000000000000000000, 1.000000000000000000) ) ) 
 REPRESENTATION_ITEM ( '' )  SURFACE ( )  );
#65429=CARTESIAN_POINT ( 'NONE',  ( 0.3675815128205894289, 12.27743992903066328, -0.2638082659428851451 ) ) ;
#65431=CARTESIAN_POINT ( 'NONE',  ( 5.520433897694421610, -0.01505375422439067697, -0.0005131706886600855217 ) ) ;
#65432=CARTESIAN_POINT ( 'NONE',  ( 3.031336079629178393, -7.839300734793016368, -0.9593005538808098143 ) ) ;
#65439=CARTESIAN_POINT ( 'NONE',  ( 2.827825597296808713, 4.975864478227498111, -7.528560921609551926 ) ) ;
#65445=CARTESIAN_POINT ( 'NONE',  ( 3.152665057734040488, 0.000000000000000000, 0.000000000000000000 ) ) ;
#65447=CARTESIAN_POINT ( 'NONE',  ( 0.2653141334712581512, 12.24612529725264132, -0.04405251235385006237 ) ) ;
#65453=CARTESIAN_POINT ( 'NONE',  ( 0.2648978790185602672, 12.24533305150758089, -0.1321385342562831633 ) ) ;
#65456=CARTESIAN_POINT ( 'NONE',  ( 2.258463476536643366, -6.547539277368008115, -3.937122681832554427 ) ) ;
#65457=CARTESIAN_POINT ( 'NONE',  ( 0.3665391374699472626, -0.2638605131386310143, -12.27992639892678639 ) ) ;
#65460=CARTESIAN_POINT ( 'NONE',  ( 0.5547464869798230946, 9.256151063740663432, -8.164898018378718092 ) ) ;
#65464=CARTESIAN_POINT ( 'NONE',  ( 3.100650473569755317, -2.280184661131145596, -7.585586315875764818 ) ) ;
#65465=ORIENTED_EDGE ( 'NONE', *, *, #35702, .F. ) ;
#65468=CARTESIAN_POINT ( 'NONE',  ( 3.152665057735613008, -6.378477742801520023, -4.725420687649700469 ) ) ;
#65469=CARTESIAN_POINT ( 'NONE',  ( 3.152665057734004073, 7.102135024645805039, -3.546019893116331811 ) ) ;
#65471=AXIS2_PLACEMENT_3D ( 'NONE', #37922, #16985, #33268 ) ;
#65474=CARTESIAN_POINT ( 'NONE',  ( 1.719304012338199295, 12.64775761152512423, 1.452142814150486183 ) ) ;
#65477=CARTESIAN_POINT ( 'NONE',  ( 3.152665057734125309, -6.622010822086626725, -4.377619405892440696 ) ) ;
#65480=CARTESIAN_POINT ( 'NONE',  ( 2.705197763288543999, -6.881024880055373494, 3.649695155981489414 ) ) ;
#65482=ORIENTED_EDGE ( 'NONE', *, *, #3568, .T. ) ;
#65496=CARTESIAN_POINT ( 'NONE',  ( 1.452237505248552996, 6.833827325205466430, -10.65201107290460492 ) ) ;
#65497=CARTESIAN_POINT ( 'NONE',  ( 0.2648978790185584908, 4.063980959785046032, 11.55204314799265042 ) ) ;
#65498=CARTESIAN_POINT ( 'NONE',  ( 2.244591118396555007, -6.665613643996570303, -3.724266936773059644 ) ) ;
#65501=CARTESIAN_POINT ( 'NONE',  ( 1.014383007554940264, 6.628652139012910283, 10.59286224865783943 ) ) ;
#65502=CIRCLE ( 'NONE', #34692, 7.938172270156617749 ) ;
#65504=EDGE_CURVE ( 'NONE', #15452, #12898, #23021, .T. ) ;
#65514=CARTESIAN_POINT ( 'NONE',  ( 2.241509619876139059, 3.850348903238805409, -6.592435552901080520 ) ) ;
#65518=CARTESIAN_POINT ( 'NONE',  ( 0.3341166715381300722, -12.12403120948088464, -1.881279064087967523 ) ) ;
#65525=EDGE_CURVE ( 'NONE', #29925, #27543, #14265, .T. ) ;
#65534=CARTESIAN_POINT ( 'NONE',  ( 5.516018279890452902, -0.005752102158674371642, -0.003580555109620855384 ) ) ;
#65540=CARTESIAN_POINT ( 'NONE',  ( 2.556980015513997007, 3.668282146013217559, -6.815084337351887456 ) ) ;
#65541=ORIENTED_EDGE ( 'NONE', *, *, #1745, .T. ) ;
#65542=CARTESIAN_POINT ( 'NONE',  ( 2.655192694323576852, -0.5793947661801577276, -9.584054627288868033 ) ) ;
#65544=CARTESIAN_POINT ( 'NONE',  ( 2.653899356899988682, -2.411250235128107100, 7.388433688587405790 ) ) ;
#65546=CARTESIAN_POINT ( 'NONE',  ( 2.266490820343738832, 4.800466063945178163, -5.947069344280496495 ) ) ;
#65554=B_SPLINE_CURVE_WITH_KNOTS ( 'NONE', 3,
 ( #40244, #45566, #20302, #65200, #60532, #45913, #10317, #4716, #45251, #4039, #367, #34912, #49597, #39603, #24306, #20645 ),
 .UNSPECIFIED., .F., .F.,
 ( 4, 3, 3, 3, 3, 4 ),
 ( 4.336808689942017255E-19, 0.0002176109881720244036, 0.0004352086762394596366, 0.0006528017811446883752, 0.0007615147961451703253, 0.0009453342004945543752 ),
 .UNSPECIFIED. ) ;
#65565=CARTESIAN_POINT ( 'NONE',  ( 0.3675815128205894289, -9.574637318041910206, -7.689697408877373519 ) ) ;
#65577=CARTESIAN_POINT ( 'NONE',  ( 0.3654063281920724160, 8.093076148786037649, 9.235228056823945764 ) ) ;
#65578=CARTESIAN_POINT ( 'NONE',  ( 5.515539859299206427, -0.0008592514567755275617, -0.005991790098943834339 ) ) ;
#65587=CARTESIAN_POINT ( 'NONE',  ( 0.2653141617321003731, -7.837919552760664210, -9.409385893408590107 ) ) ;
#65594=ORIENTED_EDGE ( 'NONE', *, *, #1218, .F. ) ;
#65596=B_SPLINE_CURVE_WITH_KNOTS ( 'NONE', 3,
 ( #28174, #18848, #59402, #55394, #19164, #35084, #18546 ),
 .UNSPECIFIED., .F., .F.,
 ( 4, 3, 4 ),
 ( 7.847387629678164802E-15, 0.002398160485434857984, 0.005002426799384661685 ),
 .UNSPECIFIED. ) ;
#65612=CARTESIAN_POINT ( 'NONE',  ( 2.241449424704146320, 6.642105568284105921, 3.763973574060562655 ) ) ;
#65617=CARTESIAN_POINT ( 'NONE',  ( 3.152665057734040488, 0.000000000000000000, 0.000000000000000000 ) ) ;
#65618=CARTESIAN_POINT ( 'NONE',  ( 0.2650492433740058718, 6.027445608088999762, -10.66007796911762995 ) ) ;
#65627=CARTESIAN_POINT ( 'NONE',  ( 0.3665391374699472626, -11.62960183138724446, -3.952034409876412635 ) ) ;
#65634=EDGE_CURVE ( 'NONE', #43663, #65715, #42775, .T. ) ;
#65650=CARTESIAN_POINT ( 'NONE',  ( 0.2739690278137261181, 10.51531306167495217, -6.282352088166152981 ) ) ;
#65652=CARTESIAN_POINT ( 'NONE',  ( 2.241528039335008327, 1.310213701658589081, 7.521191296022422534 ) ) ;
#65655=CARTESIAN_POINT ( 'NONE',  ( 2.990245332647628818, -8.248134185053306311, -1.974808303407486809 ) ) ;
#65667=CARTESIAN_POINT ( 'NONE',  ( 2.241536586108914264, 5.844297002038606692, -4.912162027558427013 ) ) ;
#65668=CARTESIAN_POINT ( 'NONE',  ( 2.491965175173733282, 6.046355957630737521, 4.796682362486673235 ) ) ;
#65669=ORIENTED_EDGE ( 'NONE', *, *, #59118, .F. ) ;
#65670=CARTESIAN_POINT ( 'NONE',  ( 3.047904605210419060, -0.4249306449415868880, 7.891858004695965434 ) ) ;
#65671=CARTESIAN_POINT ( 'NONE',  ( 0.2638984909335720941, 10.50550771760528690, -6.295352574288876291 ) ) ;
#65676=CARTESIAN_POINT ( 'NONE',  ( 3.152665057734023613, 0.4801242025591827001, -7.923639299008664594 ) ) ;
#65677=CARTESIAN_POINT ( 'NONE',  ( 2.491965175174425173, -7.177226758613745261, 2.837956678388492637 ) ) ;
#65681=CARTESIAN_POINT ( 'NONE',  ( 5.536195898058073439, -0.003145317580921097589, -0.007896796515810917613 ) ) ;
#65692=ADVANCED_FACE ( 'NONE', ( #31857 ), #40275, .F. ) ;
#65693=CARTESIAN_POINT ( 'NONE',  ( 2.969415267404607928, -7.525730903320708265, -2.326350273511738287 ) ) ;
#65699=CARTESIAN_POINT ( 'NONE',  ( 0.3160775863651105189, -11.43919651388222647, -4.419114254410010822 ) ) ;
#65706=DIRECTION ( 'NONE',  ( 0.3865475372811021382, 0.7187975063895720718, -0.5778504531711020631 ) ) ;
#65712=FACE_OUTER_BOUND ( 'NONE', #57871, .T. ) ;
#65715=VERTEX_POINT ( 'NONE', #24679 ) ;
#65723=CARTESIAN_POINT ( 'NONE',  ( 2.273267844204864829, 7.130811676080313077, -2.756477528575228320 ) ) ;
#65727=CARTESIAN_POINT ( 'NONE',  ( 0.2653519789438754106, -10.59450269107738585, 6.142177718873902847 ) ) ;
#65728=CARTESIAN_POINT ( 'NONE',  ( 0.3632410797595194141, 11.62558329798851098, 3.951633449030948153 ) ) ;
#65730=CARTESIAN_POINT ( 'NONE',  ( 0.8375941296802019709, -11.81283813871866961, 3.890418817177930588 ) ) ;
#65738=B_SPLINE_CURVE_WITH_KNOTS ( 'NONE', 3,
 ( #23023, #18705, #53935, #38963, #53280, #63240, #53621, #8375, #52635, #27656, #62911, #12362, #48624, #23341, #28650, #28330 ),
 .UNSPECIFIED., .F., .F.,
 ( 4, 3, 3, 3, 3, 4 ),
 ( 0.000000000000000000, 0.0002176109881720234278, 0.0004352086762394595824, 0.0006528017811446865321, 0.0007615147961451697832, 0.0009453342004943755903 ),
 .UNSPECIFIED. ) ;
#65745=CARTESIAN_POINT ( 'NONE',  ( 0.3040950598368144520, 12.25911170648142878, 0.2511348647276071544 ) ) ;
#65746=CARTESIAN_POINT ( 'NONE',  ( 5.536195898058073439, -0.007230647766619060536, -0.004468797463753857412 ) ) ;
#65747=CARTESIAN_POINT ( 'NONE',  ( 2.907497136250466241, -7.791429554169687854, -1.009055026158189428 ) ) ;
#65748=CARTESIAN_POINT ( 'NONE',  ( 5.520433897694421610, 0.01397038704729914628, -0.005630909886753002538 ) ) ;
#65751=CARTESIAN_POINT ( 'NONE',  ( 2.589278595512906289, 2.423168677232077517, -7.361833592938230808 ) ) ;
#65753=CARTESIAN_POINT ( 'NONE',  ( 2.241526690369556096, -6.620271521148406890, -3.802233103835238825 ) ) ;
#65756=CARTESIAN_POINT ( 'NONE',  ( 5.520433897694421610, -0.002108682515300378500, 0.01491416502703865263 ) ) ;
#65774=CARTESIAN_POINT ( 'NONE',  ( 1.452237505248552996, 10.65201107290467597, 6.833827325205354519 ) ) ;
#65777=CARTESIAN_POINT ( 'NONE',  ( 1.375507693220547001, 11.20969178069697492, -5.789143338281640183 ) ) ;
#65787=ORIENTED_EDGE ( 'NONE', *, *, #37142, .T. ) ;
#65788=( BOUNDED_SURFACE ( )  B_SPLINE_SURFACE ( 3, 1, ( 
 ( #14808, #35750 ),
 ( #40422, #10172 ),
 ( #39782, #213 ),
 ( #15484, #40092 ) ),
 .UNSPECIFIED., .F., .F., .F. ) 
 B_SPLINE_SURFACE_WITH_KNOTS ( ( 4, 4 ),
 ( 2, 2 ),
 ( 0.000000000000000000, 1.000000000000000000 ),
 ( 0.000000000000000000, 1.000000000000000000 ),
 .UNSPECIFIED. ) 
 GEOMETRIC_REPRESENTATION_ITEM ( )  RATIONAL_B_SPLINE_SURFACE ( (
 ( 1.000000000000000000, 1.000000000000000000),
 ( 0.9942764183789327692, 0.8450855930916585379),
 ( 0.9942764183789327692, 0.8450855930916585379),
 ( 1.000000000000000000, 1.000000000000000000) ) ) 
 REPRESENTATION_ITEM ( '' )  SURFACE ( )  );
#65793=CARTESIAN_POINT ( 'NONE',  ( 2.491965175174054359, 7.177226758613687529, -2.837956678388308340 ) ) ;
#65794=VERTEX_POINT ( 'NONE', #45600 ) ;
#65797=EDGE_CURVE ( 'NONE', #12912, #4057, #13450, .T. ) ;
#65799=CARTESIAN_POINT ( 'NONE',  ( 0.3106921474978477926, 11.60027394202204398, -3.971572160646637872 ) ) ;
ENDSEC;
END-ISO-10303-21;
